ISO-10303-21;
HEADER;
/* Generated by software containing ST-Developer
 * from STEP Tools, Inc. (www.steptools.com) 
 */

FILE_DESCRIPTION(
/* description */ (
'Independent keyed-quill tailstock, native coupled50mm slider andM16x2
 feed screw, conical dead center, bronze sleeves/thrust washers, cross
-pinned handwheel and bolted guide key. Custom center taper; no standa
rd taper compatibility, machine-bed compatibility or load rating assig
ned.'),
/* implementation_level */ '2;1');

FILE_NAME(
/* name */ 'Socket head cap screw M4x20.step',
/* time_stamp */ '2026-11-14T07:17:36-08:00',
/* author */ (''),
/* organization */ (''),
/* preprocessor_version */ 'ST-DEVELOPER v20.2',
/* originating_system */ 'Autodesk Translation Framework v15.17.0.0',
/* authorisation */ '');

FILE_SCHEMA (('AUTOMOTIVE_DESIGN { 1 0 10303 214 3 1 1 }'));
ENDSEC;

DATA;
#10=MECHANICAL_DESIGN_GEOMETRIC_PRESENTATION_REPRESENTATION('',(#168),#289387);
#116=CONICAL_SURFACE('',#17789,1.5,0.785398163397448);
#117=CONICAL_SURFACE('',#17828,1.5,0.785398163397448);
#134=SHAPE_REPRESENTATION_RELATIONSHIP('SRR','None',#289469,#151);
#151=ADVANCED_BREP_SHAPE_REPRESENTATION('',(#185),#289385);
#168=STYLED_ITEM('',(#289553),#185);
#185=MANIFOLD_SOLID_BREP('Body1',#16856);
#269=FACE_BOUND('',#1786,.T.);
#270=FACE_BOUND('',#1789,.T.);
#299=B_SPLINE_SURFACE_WITH_KNOTS('',3,3,((#277484,#277485,#277486,#277487,
#277488,#277489,#277490,#277491,#277492,#277493,#277494,#277495,#277496,
#277497,#277498,#277499,#277500,#277501,#277502,#277503,#277504,#277505,
#277506,#277507,#277508,#277509,#277510,#277511,#277512,#277513,#277514,
#277515,#277516,#277517,#277518,#277519,#277520,#277521,#277522,#277523,
#277524,#277525,#277526,#277527,#277528,#277529,#277530,#277531,#277532,
#277533,#277534,#277535,#277536,#277537,#277538,#277539,#277540,#277541,
#277542,#277543,#277544,#277545,#277546,#277547,#277548,#277549,#277550,
#277551,#277552,#277553,#277554,#277555,#277556,#277557,#277558,#277559,
#277560,#277561,#277562,#277563,#277564,#277565,#277566,#277567,#277568,
#277569,#277570,#277571,#277572,#277573,#277574,#277575,#277576,#277577,
#277578,#277579,#277580,#277581,#277582,#277583,#277584,#277585,#277586,
#277587,#277588,#277589,#277590,#277591,#277592,#277593,#277594,#277595,
#277596,#277597,#277598,#277599,#277600,#277601,#277602,#277603,#277604,
#277605,#277606,#277607,#277608,#277609,#277610,#277611,#277612,#277613,
#277614,#277615,#277616,#277617,#277618,#277619,#277620,#277621,#277622,
#277623,#277624,#277625,#277626,#277627,#277628,#277629,#277630,#277631,
#277632,#277633,#277634,#277635,#277636,#277637,#277638,#277639,#277640,
#277641,#277642,#277643,#277644,#277645,#277646,#277647,#277648,#277649,
#277650,#277651,#277652,#277653,#277654,#277655,#277656,#277657,#277658,
#277659,#277660,#277661),(#277662,#277663,#277664,#277665,#277666,#277667,
#277668,#277669,#277670,#277671,#277672,#277673,#277674,#277675,#277676,
#277677,#277678,#277679,#277680,#277681,#277682,#277683,#277684,#277685,
#277686,#277687,#277688,#277689,#277690,#277691,#277692,#277693,#277694,
#277695,#277696,#277697,#277698,#277699,#277700,#277701,#277702,#277703,
#277704,#277705,#277706,#277707,#277708,#277709,#277710,#277711,#277712,
#277713,#277714,#277715,#277716,#277717,#277718,#277719,#277720,#277721,
#277722,#277723,#277724,#277725,#277726,#277727,#277728,#277729,#277730,
#277731,#277732,#277733,#277734,#277735,#277736,#277737,#277738,#277739,
#277740,#277741,#277742,#277743,#277744,#277745,#277746,#277747,#277748,
#277749,#277750,#277751,#277752,#277753,#277754,#277755,#277756,#277757,
#277758,#277759,#277760,#277761,#277762,#277763,#277764,#277765,#277766,
#277767,#277768,#277769,#277770,#277771,#277772,#277773,#277774,#277775,
#277776,#277777,#277778,#277779,#277780,#277781,#277782,#277783,#277784,
#277785,#277786,#277787,#277788,#277789,#277790,#277791,#277792,#277793,
#277794,#277795,#277796,#277797,#277798,#277799,#277800,#277801,#277802,
#277803,#277804,#277805,#277806,#277807,#277808,#277809,#277810,#277811,
#277812,#277813,#277814,#277815,#277816,#277817,#277818,#277819,#277820,
#277821,#277822,#277823,#277824,#277825,#277826,#277827,#277828,#277829,
#277830,#277831,#277832,#277833,#277834,#277835,#277836,#277837,#277838,
#277839),(#277840,#277841,#277842,#277843,#277844,#277845,#277846,#277847,
#277848,#277849,#277850,#277851,#277852,#277853,#277854,#277855,#277856,
#277857,#277858,#277859,#277860,#277861,#277862,#277863,#277864,#277865,
#277866,#277867,#277868,#277869,#277870,#277871,#277872,#277873,#277874,
#277875,#277876,#277877,#277878,#277879,#277880,#277881,#277882,#277883,
#277884,#277885,#277886,#277887,#277888,#277889,#277890,#277891,#277892,
#277893,#277894,#277895,#277896,#277897,#277898,#277899,#277900,#277901,
#277902,#277903,#277904,#277905,#277906,#277907,#277908,#277909,#277910,
#277911,#277912,#277913,#277914,#277915,#277916,#277917,#277918,#277919,
#277920,#277921,#277922,#277923,#277924,#277925,#277926,#277927,#277928,
#277929,#277930,#277931,#277932,#277933,#277934,#277935,#277936,#277937,
#277938,#277939,#277940,#277941,#277942,#277943,#277944,#277945,#277946,
#277947,#277948,#277949,#277950,#277951,#277952,#277953,#277954,#277955,
#277956,#277957,#277958,#277959,#277960,#277961,#277962,#277963,#277964,
#277965,#277966,#277967,#277968,#277969,#277970,#277971,#277972,#277973,
#277974,#277975,#277976,#277977,#277978,#277979,#277980,#277981,#277982,
#277983,#277984,#277985,#277986,#277987,#277988,#277989,#277990,#277991,
#277992,#277993,#277994,#277995,#277996,#277997,#277998,#277999,#278000,
#278001,#278002,#278003,#278004,#278005,#278006,#278007,#278008,#278009,
#278010,#278011,#278012,#278013,#278014,#278015,#278016,#278017),(#278018,
#278019,#278020,#278021,#278022,#278023,#278024,#278025,#278026,#278027,
#278028,#278029,#278030,#278031,#278032,#278033,#278034,#278035,#278036,
#278037,#278038,#278039,#278040,#278041,#278042,#278043,#278044,#278045,
#278046,#278047,#278048,#278049,#278050,#278051,#278052,#278053,#278054,
#278055,#278056,#278057,#278058,#278059,#278060,#278061,#278062,#278063,
#278064,#278065,#278066,#278067,#278068,#278069,#278070,#278071,#278072,
#278073,#278074,#278075,#278076,#278077,#278078,#278079,#278080,#278081,
#278082,#278083,#278084,#278085,#278086,#278087,#278088,#278089,#278090,
#278091,#278092,#278093,#278094,#278095,#278096,#278097,#278098,#278099,
#278100,#278101,#278102,#278103,#278104,#278105,#278106,#278107,#278108,
#278109,#278110,#278111,#278112,#278113,#278114,#278115,#278116,#278117,
#278118,#278119,#278120,#278121,#278122,#278123,#278124,#278125,#278126,
#278127,#278128,#278129,#278130,#278131,#278132,#278133,#278134,#278135,
#278136,#278137,#278138,#278139,#278140,#278141,#278142,#278143,#278144,
#278145,#278146,#278147,#278148,#278149,#278150,#278151,#278152,#278153,
#278154,#278155,#278156,#278157,#278158,#278159,#278160,#278161,#278162,
#278163,#278164,#278165,#278166,#278167,#278168,#278169,#278170,#278171,
#278172,#278173,#278174,#278175,#278176,#278177,#278178,#278179,#278180,
#278181,#278182,#278183,#278184,#278185,#278186,#278187,#278188,#278189,
#278190,#278191,#278192,#278193,#278194,#278195)),.UNSPECIFIED.,.F.,.F.,
 .F.,(4,4),(4,1,1,1,1,1,1,1,1,1,1,1,1,1,1,1,1,1,1,1,1,1,1,1,1,1,1,1,1,1,
1,1,1,1,1,1,1,1,1,1,1,1,1,1,1,1,1,1,1,1,1,1,1,1,1,1,1,1,1,1,1,1,1,1,1,1,
1,1,1,1,1,1,1,1,1,1,1,1,1,1,1,1,1,1,1,1,1,1,1,1,1,1,1,1,1,1,1,1,1,1,1,1,
1,1,1,1,1,1,1,1,1,1,1,1,1,1,1,1,1,1,1,1,1,1,1,1,1,1,1,1,1,1,1,1,1,1,1,1,
1,1,1,1,1,1,1,1,1,1,1,1,1,1,1,1,1,1,1,1,1,1,1,1,1,1,1,1,1,1,1,1,1,1,1,1,
1,4),(-0.000292625423985075,0.0463342147672139),(11.6151021207979,12.6127553697675,
13.6100892204243,14.607423071081,15.6047569217378,16.6020907723946,17.5994246230513,
18.5967584737081,19.5940923243649,20.5914261750216,21.5887600256784,22.5860938763352,
23.5834277269919,24.5807615776487,25.5780954283055,26.5754292789622,27.572763129619,
28.5700969802757,29.5674308309325,30.5647646815893,31.562098532246,32.5594323829028,
33.5567662335596,34.5541000842163,35.5514339348731,36.5487677855299,37.5461016361866,
38.5434354868434,39.5407693375002,40.5381031881569,41.5354370388137,42.5327708894705,
43.5301047401272,44.527438590784,45.5247724414408,46.5221062920975,47.5194401427543,
48.5167739934111,49.5141078440678,50.5114416947246,51.5087755453814,52.5061093960381,
53.5034432466949,54.5007770973516,55.4981109480084,56.4954447986652,57.4927786493219,
58.4901124999787,59.4874463506355,60.4847802012922,61.482114051949,62.4794479026058,
63.4767817532625,64.4741156039193,65.4714494545761,66.4687833052328,67.4661171558896,
68.4634510065464,69.4607848572031,70.4581187078599,71.4554525585167,72.4527864091734,
73.4501202598302,74.447454110487,75.4447879611437,76.4421218118005,77.4394556624572,
78.436789513114,79.4341233637708,80.4314572144275,81.4287910650843,82.4261249157411,
83.4234587663978,84.4207926170546,85.4181264677114,86.4154603183681,87.4127941690249,
88.4101280196817,89.4074618703384,90.4047957209952,91.402129571652,92.3994634223087,
93.3967972729655,94.3941311236223,95.391464974279,96.3887988249358,97.3861326755925,
98.3834665262493,99.3808003769061,100.378134227563,101.37546807822,102.372801928876,
103.370135779533,104.36746963019,105.364803480847,106.362137331503,107.35947118216,
108.356805032817,109.354138883474,110.35147273413,111.348806584787,112.346140435444,
113.343474286101,114.340808136758,115.338141987414,116.335475838071,117.332809688728,
118.330143539385,119.327477390041,120.324811240698,121.322145091355,122.319478942012,
123.316812792668,124.314146643325,125.311480493982,126.308814344639,127.306148195296,
128.303482045952,129.300815896609,130.298149747266,131.295483597923,132.292817448579,
133.290151299236,134.287485149893,135.28481900055,136.282152851206,137.279486701863,
138.27682055252,139.274154403177,140.271488253833,141.26882210449,142.266155955147,
143.263489805804,144.260823656461,145.258157507117,146.255491357774,147.252825208431,
148.250159059088,149.247492909744,150.244826760401,151.242160611058,152.239494461715,
153.236828312371,154.234162163028,155.231496013685,156.228829864342,157.226163714998,
158.223497565655,159.220831416312,160.218165266969,161.215499117626,162.212832968282,
163.210166818939,164.207500669596,165.204834520253,166.202168370909,167.199502221566,
168.196836072223,169.19416992288,170.191503773536,171.188837624193,172.18617147485,
173.183505325507,174.180839176163,175.17817302682,176.175506877477,177.172840728134,
178.170174578791,179.167508429447,180.164842280104,181.162176130761,182.159509981418,
183.156843832074,184.154177682731,185.151511533388,186.148902899087),
 .UNSPECIFIED.);
#300=B_SPLINE_SURFACE_WITH_KNOTS('',3,3,((#278281,#278282,#278283,#278284,
#278285,#278286,#278287,#278288,#278289,#278290,#278291,#278292,#278293,
#278294,#278295,#278296,#278297,#278298,#278299,#278300,#278301,#278302,
#278303,#278304,#278305,#278306,#278307,#278308,#278309,#278310,#278311,
#278312,#278313,#278314,#278315,#278316,#278317,#278318,#278319,#278320,
#278321,#278322,#278323,#278324,#278325,#278326,#278327,#278328,#278329,
#278330,#278331,#278332,#278333,#278334,#278335,#278336,#278337,#278338,
#278339,#278340,#278341,#278342,#278343,#278344,#278345,#278346,#278347,
#278348,#278349,#278350,#278351,#278352,#278353,#278354,#278355,#278356,
#278357,#278358,#278359,#278360,#278361,#278362,#278363,#278364,#278365,
#278366,#278367,#278368,#278369,#278370,#278371,#278372,#278373,#278374,
#278375,#278376,#278377,#278378,#278379,#278380,#278381,#278382,#278383,
#278384,#278385,#278386,#278387,#278388,#278389,#278390,#278391,#278392,
#278393,#278394,#278395,#278396,#278397,#278398,#278399,#278400,#278401,
#278402,#278403,#278404,#278405,#278406,#278407,#278408,#278409,#278410,
#278411,#278412,#278413,#278414,#278415,#278416,#278417,#278418,#278419,
#278420,#278421,#278422,#278423,#278424,#278425,#278426,#278427,#278428,
#278429,#278430,#278431,#278432,#278433,#278434,#278435,#278436,#278437,
#278438,#278439,#278440,#278441,#278442,#278443,#278444,#278445,#278446,
#278447,#278448,#278449,#278450,#278451,#278452,#278453,#278454,#278455,
#278456,#278457,#278458,#278459,#278460),(#278461,#278462,#278463,#278464,
#278465,#278466,#278467,#278468,#278469,#278470,#278471,#278472,#278473,
#278474,#278475,#278476,#278477,#278478,#278479,#278480,#278481,#278482,
#278483,#278484,#278485,#278486,#278487,#278488,#278489,#278490,#278491,
#278492,#278493,#278494,#278495,#278496,#278497,#278498,#278499,#278500,
#278501,#278502,#278503,#278504,#278505,#278506,#278507,#278508,#278509,
#278510,#278511,#278512,#278513,#278514,#278515,#278516,#278517,#278518,
#278519,#278520,#278521,#278522,#278523,#278524,#278525,#278526,#278527,
#278528,#278529,#278530,#278531,#278532,#278533,#278534,#278535,#278536,
#278537,#278538,#278539,#278540,#278541,#278542,#278543,#278544,#278545,
#278546,#278547,#278548,#278549,#278550,#278551,#278552,#278553,#278554,
#278555,#278556,#278557,#278558,#278559,#278560,#278561,#278562,#278563,
#278564,#278565,#278566,#278567,#278568,#278569,#278570,#278571,#278572,
#278573,#278574,#278575,#278576,#278577,#278578,#278579,#278580,#278581,
#278582,#278583,#278584,#278585,#278586,#278587,#278588,#278589,#278590,
#278591,#278592,#278593,#278594,#278595,#278596,#278597,#278598,#278599,
#278600,#278601,#278602,#278603,#278604,#278605,#278606,#278607,#278608,
#278609,#278610,#278611,#278612,#278613,#278614,#278615,#278616,#278617,
#278618,#278619,#278620,#278621,#278622,#278623,#278624,#278625,#278626,
#278627,#278628,#278629,#278630,#278631,#278632,#278633,#278634,#278635,
#278636,#278637,#278638,#278639,#278640),(#278641,#278642,#278643,#278644,
#278645,#278646,#278647,#278648,#278649,#278650,#278651,#278652,#278653,
#278654,#278655,#278656,#278657,#278658,#278659,#278660,#278661,#278662,
#278663,#278664,#278665,#278666,#278667,#278668,#278669,#278670,#278671,
#278672,#278673,#278674,#278675,#278676,#278677,#278678,#278679,#278680,
#278681,#278682,#278683,#278684,#278685,#278686,#278687,#278688,#278689,
#278690,#278691,#278692,#278693,#278694,#278695,#278696,#278697,#278698,
#278699,#278700,#278701,#278702,#278703,#278704,#278705,#278706,#278707,
#278708,#278709,#278710,#278711,#278712,#278713,#278714,#278715,#278716,
#278717,#278718,#278719,#278720,#278721,#278722,#278723,#278724,#278725,
#278726,#278727,#278728,#278729,#278730,#278731,#278732,#278733,#278734,
#278735,#278736,#278737,#278738,#278739,#278740,#278741,#278742,#278743,
#278744,#278745,#278746,#278747,#278748,#278749,#278750,#278751,#278752,
#278753,#278754,#278755,#278756,#278757,#278758,#278759,#278760,#278761,
#278762,#278763,#278764,#278765,#278766,#278767,#278768,#278769,#278770,
#278771,#278772,#278773,#278774,#278775,#278776,#278777,#278778,#278779,
#278780,#278781,#278782,#278783,#278784,#278785,#278786,#278787,#278788,
#278789,#278790,#278791,#278792,#278793,#278794,#278795,#278796,#278797,
#278798,#278799,#278800,#278801,#278802,#278803,#278804,#278805,#278806,
#278807,#278808,#278809,#278810,#278811,#278812,#278813,#278814,#278815,
#278816,#278817,#278818,#278819,#278820),(#278821,#278822,#278823,#278824,
#278825,#278826,#278827,#278828,#278829,#278830,#278831,#278832,#278833,
#278834,#278835,#278836,#278837,#278838,#278839,#278840,#278841,#278842,
#278843,#278844,#278845,#278846,#278847,#278848,#278849,#278850,#278851,
#278852,#278853,#278854,#278855,#278856,#278857,#278858,#278859,#278860,
#278861,#278862,#278863,#278864,#278865,#278866,#278867,#278868,#278869,
#278870,#278871,#278872,#278873,#278874,#278875,#278876,#278877,#278878,
#278879,#278880,#278881,#278882,#278883,#278884,#278885,#278886,#278887,
#278888,#278889,#278890,#278891,#278892,#278893,#278894,#278895,#278896,
#278897,#278898,#278899,#278900,#278901,#278902,#278903,#278904,#278905,
#278906,#278907,#278908,#278909,#278910,#278911,#278912,#278913,#278914,
#278915,#278916,#278917,#278918,#278919,#278920,#278921,#278922,#278923,
#278924,#278925,#278926,#278927,#278928,#278929,#278930,#278931,#278932,
#278933,#278934,#278935,#278936,#278937,#278938,#278939,#278940,#278941,
#278942,#278943,#278944,#278945,#278946,#278947,#278948,#278949,#278950,
#278951,#278952,#278953,#278954,#278955,#278956,#278957,#278958,#278959,
#278960,#278961,#278962,#278963,#278964,#278965,#278966,#278967,#278968,
#278969,#278970,#278971,#278972,#278973,#278974,#278975,#278976,#278977,
#278978,#278979,#278980,#278981,#278982,#278983,#278984,#278985,#278986,
#278987,#278988,#278989,#278990,#278991,#278992,#278993,#278994,#278995,
#278996,#278997,#278998,#278999,#279000)),.UNSPECIFIED.,.F.,.F.,.F.,(4,
4),(4,1,1,1,1,1,1,1,1,1,1,1,1,1,1,1,1,1,1,1,1,1,1,1,1,1,1,1,1,1,1,1,1,1,
1,1,1,1,1,1,1,1,1,1,1,1,1,1,1,1,1,1,1,1,1,1,1,1,1,1,1,1,1,1,1,1,1,1,1,1,
1,1,1,1,1,1,1,1,1,1,1,1,1,1,1,1,1,1,1,1,1,1,1,1,1,1,1,1,1,1,1,1,1,1,1,1,
1,1,1,1,1,1,1,1,1,1,1,1,1,1,1,1,1,1,1,1,1,1,1,1,1,1,1,1,1,1,1,1,1,1,1,1,
1,1,1,1,1,1,1,1,1,1,1,1,1,1,1,1,1,1,1,1,1,1,1,1,1,1,1,1,1,1,1,1,1,1,1,4),
(-0.000319937213065475,0.0463079691845939),(8.31044140786475,9.30831892272975,
10.3060509227196,11.3037829227095,12.3015149226994,13.2992469226893,14.2969789226792,
15.2947109226691,16.292442922659,17.2901749226489,18.2879069226388,19.2856389226287,
20.2833709226186,21.2811029226085,22.2788349225984,23.2765669225883,24.2742989225782,
25.2720309225681,26.269762922558,27.2674949225479,28.2652269225378,29.2629589225277,
30.2606909225176,31.2584229225075,32.2561549224974,33.2538869224873,34.2516189224772,
35.2493509224671,36.247082922457,37.2448149224469,38.2425469224368,39.2402789224267,
40.2380109224166,41.2357429224065,42.2334749223964,43.2312069223863,44.2289389223762,
45.2266709223661,46.224402922356,47.2221349223459,48.2198669223358,49.2175989223257,
50.2153309223156,51.2130629223055,52.2107949222954,53.2085269222853,54.2062589222752,
55.2039909222651,56.201722922255,57.1994549222449,58.1971869222348,59.1949189222247,
60.1926509222146,61.1903829222045,62.1881149221944,63.1858469221843,64.1835789221742,
65.1813109221641,66.179042922154,67.1767749221439,68.1745069221338,69.1722389221237,
70.1699709221136,71.1677029221035,72.1654349220934,73.1631669220833,74.1608989220732,
75.1586309220631,76.1563629220529,77.1540949220428,78.1518269220327,79.1495589220227,
80.1472909220126,81.1450229220025,82.1427549219923,83.1404869219822,84.1382189219721,
85.135950921962,86.1336829219519,87.1314149219419,88.1291469219317,89.1268789219216,
90.1246109219115,91.1223429219014,92.1200749218913,93.1178069218812,94.1155389218711,
95.113270921861,96.1110029218509,97.1087349218408,98.1064669218307,99.1041989218206,
100.101930921811,101.0996629218,102.09739492179,103.09512692178,104.09285892177,
105.09059092176,106.08832292175,107.08605492174,108.08378692173,109.08151892172,
110.07925092171,111.076982921699,112.074714921689,113.072446921679,114.070178921669,
115.067910921659,116.065642921649,117.063374921639,118.061106921629,119.058838921619,
120.056570921608,121.054302921598,122.052034921588,123.049766921578,124.047498921568,
125.045230921558,126.042962921548,127.040694921538,128.038426921528,129.036158921518,
130.033890921507,131.031622921497,132.029354921487,133.027086921477,134.024818921467,
135.022550921457,136.020282921447,137.018014921437,138.015746921427,139.013478921417,
140.011210921406,141.008942921396,142.006674921386,143.004406921376,144.002138921366,
144.999870921356,145.997602921346,146.995334921336,147.993066921326,148.990798921316,
149.988530921305,150.986262921295,151.983994921285,152.981726921275,153.979458921265,
154.977190921255,155.974922921245,156.972654921235,157.970386921225,158.968118921215,
159.965850921204,160.963582921194,161.961314921184,162.959046921174,163.956778921164,
164.954510921154,165.952242921144,166.949974921134,167.947706921124,168.945438921114,
169.943170921103,170.940902921093,171.938634921083,172.936366921073,173.934098921063,
174.931830921053,175.929562921043,176.927294921033,177.925026921023,178.922758921013,
179.920490921002,180.918222920992,181.915954920982,182.913686920972,183.911418920962,
184.909470858165),.UNSPECIFIED.);
#403=PLANE('',#17829);
#404=PLANE('',#17830);
#405=PLANE('',#17831);
#406=PLANE('',#17832);
#407=PLANE('',#17833);
#408=PLANE('',#17834);
#409=PLANE('',#17835);
#410=PLANE('',#17836);
#411=PLANE('',#17840);
#412=PLANE('',#17841);
#1012=FACE_OUTER_BOUND('',#1744,.T.);
#1013=FACE_OUTER_BOUND('',#1745,.T.);
#1014=FACE_OUTER_BOUND('',#1746,.T.);
#1015=FACE_OUTER_BOUND('',#1747,.T.);
#1016=FACE_OUTER_BOUND('',#1748,.T.);
#1017=FACE_OUTER_BOUND('',#1749,.T.);
#1018=FACE_OUTER_BOUND('',#1750,.T.);
#1019=FACE_OUTER_BOUND('',#1751,.T.);
#1020=FACE_OUTER_BOUND('',#1752,.T.);
#1021=FACE_OUTER_BOUND('',#1753,.T.);
#1022=FACE_OUTER_BOUND('',#1754,.T.);
#1023=FACE_OUTER_BOUND('',#1755,.T.);
#1024=FACE_OUTER_BOUND('',#1756,.T.);
#1025=FACE_OUTER_BOUND('',#1757,.T.);
#1026=FACE_OUTER_BOUND('',#1758,.T.);
#1027=FACE_OUTER_BOUND('',#1759,.T.);
#1028=FACE_OUTER_BOUND('',#1760,.T.);
#1029=FACE_OUTER_BOUND('',#1761,.T.);
#1030=FACE_OUTER_BOUND('',#1762,.T.);
#1031=FACE_OUTER_BOUND('',#1763,.T.);
#1032=FACE_OUTER_BOUND('',#1764,.T.);
#1033=FACE_OUTER_BOUND('',#1765,.T.);
#1034=FACE_OUTER_BOUND('',#1766,.T.);
#1035=FACE_OUTER_BOUND('',#1767,.T.);
#1036=FACE_OUTER_BOUND('',#1768,.T.);
#1037=FACE_OUTER_BOUND('',#1769,.T.);
#1038=FACE_OUTER_BOUND('',#1770,.T.);
#1039=FACE_OUTER_BOUND('',#1771,.T.);
#1040=FACE_OUTER_BOUND('',#1772,.T.);
#1041=FACE_OUTER_BOUND('',#1773,.T.);
#1042=FACE_OUTER_BOUND('',#1774,.T.);
#1043=FACE_OUTER_BOUND('',#1775,.T.);
#1044=FACE_OUTER_BOUND('',#1776,.T.);
#1045=FACE_OUTER_BOUND('',#1777,.T.);
#1046=FACE_OUTER_BOUND('',#1778,.T.);
#1047=FACE_OUTER_BOUND('',#1779,.T.);
#1048=FACE_OUTER_BOUND('',#1780,.T.);
#1049=FACE_OUTER_BOUND('',#1781,.T.);
#1050=FACE_OUTER_BOUND('',#1782,.T.);
#1051=FACE_OUTER_BOUND('',#1783,.T.);
#1052=FACE_OUTER_BOUND('',#1784,.T.);
#1053=FACE_OUTER_BOUND('',#1785,.T.);
#1054=FACE_OUTER_BOUND('',#1787,.T.);
#1055=FACE_OUTER_BOUND('',#1788,.T.);
#1056=FACE_OUTER_BOUND('',#1790,.T.);
#1744=EDGE_LOOP('',(#15103,#15104,#15105,#15106,#15107,#15108,#15109,#15110,
#15111));
#1745=EDGE_LOOP('',(#15112,#15113,#15114,#15115));
#1746=EDGE_LOOP('',(#15116,#15117,#15118,#15119,#15120,#15121));
#1747=EDGE_LOOP('',(#15122,#15123,#15124,#15125));
#1748=EDGE_LOOP('',(#15126,#15127,#15128,#15129,#15130,#15131));
#1749=EDGE_LOOP('',(#15132,#15133,#15134,#15135));
#1750=EDGE_LOOP('',(#15136,#15137,#15138,#15139,#15140,#15141));
#1751=EDGE_LOOP('',(#15142,#15143,#15144,#15145));
#1752=EDGE_LOOP('',(#15146,#15147,#15148,#15149,#15150,#15151));
#1753=EDGE_LOOP('',(#15152,#15153,#15154,#15155,#15156));
#1754=EDGE_LOOP('',(#15157,#15158,#15159,#15160,#15161));
#1755=EDGE_LOOP('',(#15162,#15163,#15164,#15165,#15166,#15167));
#1756=EDGE_LOOP('',(#15168,#15169,#15170,#15171));
#1757=EDGE_LOOP('',(#15172,#15173,#15174,#15175,#15176,#15177));
#1758=EDGE_LOOP('',(#15178,#15179,#15180,#15181,#15182));
#1759=EDGE_LOOP('',(#15183,#15184,#15185,#15186,#15187));
#1760=EDGE_LOOP('',(#15188,#15189,#15190,#15191,#15192));
#1761=EDGE_LOOP('',(#15193,#15194,#15195,#15196,#15197));
#1762=EDGE_LOOP('',(#15198,#15199,#15200,#15201,#15202,#15203));
#1763=EDGE_LOOP('',(#15204,#15205,#15206,#15207,#15208));
#1764=EDGE_LOOP('',(#15209,#15210,#15211,#15212,#15213));
#1765=EDGE_LOOP('',(#15214,#15215,#15216,#15217,#15218));
#1766=EDGE_LOOP('',(#15219,#15220,#15221,#15222,#15223));
#1767=EDGE_LOOP('',(#15224,#15225,#15226,#15227,#15228));
#1768=EDGE_LOOP('',(#15229,#15230,#15231,#15232,#15233));
#1769=EDGE_LOOP('',(#15234,#15235,#15236,#15237,#15238));
#1770=EDGE_LOOP('',(#15239,#15240,#15241,#15242,#15243));
#1771=EDGE_LOOP('',(#15244,#15245,#15246,#15247,#15248));
#1772=EDGE_LOOP('',(#15249,#15250,#15251,#15252,#15253,#15254));
#1773=EDGE_LOOP('',(#15255,#15256,#15257,#15258,#15259,#15260,#15261,#15262,
#15263,#15264,#15265,#15266,#15267,#15268,#15269,#15270,#15271,#15272,#15273,
#15274,#15275,#15276,#15277,#15278,#15279,#15280,#15281,#15282,#15283,#15284,
#15285,#15286,#15287,#15288,#15289,#15290,#15291,#15292,#15293,#15294,#15295,
#15296,#15297,#15298,#15299,#15300,#15301,#15302,#15303,#15304,#15305,#15306,
#15307,#15308,#15309,#15310,#15311,#15312,#15313,#15314));
#1774=EDGE_LOOP('',(#15315,#15316,#15317,#15318,#15319,#15320));
#1775=EDGE_LOOP('',(#15321,#15322,#15323));
#1776=EDGE_LOOP('',(#15324,#15325,#15326,#15327,#15328,#15329,#15330,#15331,
#15332,#15333,#15334,#15335,#15336,#15337,#15338,#15339,#15340,#15341,#15342,
#15343,#15344,#15345,#15346,#15347,#15348,#15349,#15350,#15351,#15352,#15353,
#15354,#15355,#15356,#15357,#15358,#15359,#15360,#15361,#15362,#15363,#15364,
#15365,#15366,#15367,#15368,#15369,#15370,#15371,#15372,#15373,#15374,#15375,
#15376,#15377,#15378,#15379,#15380,#15381,#15382,#15383,#15384,#15385,#15386,
#15387,#15388,#15389,#15390,#15391,#15392,#15393,#15394,#15395,#15396,#15397,
#15398,#15399,#15400));
#1777=EDGE_LOOP('',(#15401,#15402,#15403,#15404,#15405,#15406,#15407,#15408,
#15409,#15410,#15411,#15412,#15413,#15414,#15415,#15416,#15417,#15418,#15419,
#15420,#15421,#15422,#15423,#15424,#15425,#15426,#15427,#15428,#15429,#15430,
#15431,#15432,#15433,#15434,#15435,#15436,#15437,#15438,#15439,#15440,#15441,
#15442,#15443,#15444,#15445,#15446,#15447,#15448,#15449,#15450,#15451,#15452,
#15453,#15454,#15455,#15456,#15457,#15458,#15459,#15460,#15461,#15462,#15463,
#15464,#15465,#15466,#15467,#15468,#15469,#15470,#15471,#15472,#15473,#15474,
#15475));
#1778=EDGE_LOOP('',(#15476,#15477,#15478,#15479));
#1779=EDGE_LOOP('',(#15480,#15481,#15482,#15483));
#1780=EDGE_LOOP('',(#15484,#15485,#15486,#15487));
#1781=EDGE_LOOP('',(#15488,#15489,#15490,#15491));
#1782=EDGE_LOOP('',(#15492,#15493,#15494,#15495));
#1783=EDGE_LOOP('',(#15496,#15497,#15498,#15499));
#1784=EDGE_LOOP('',(#15500,#15501,#15502,#15503,#15504,#15505));
#1785=EDGE_LOOP('',(#15506));
#1786=EDGE_LOOP('',(#15507,#15508,#15509,#15510));
#1787=EDGE_LOOP('',(#15511,#15512,#15513,#15514));
#1788=EDGE_LOOP('',(#15515));
#1789=EDGE_LOOP('',(#15516,#15517,#15518,#15519,#15520,#15521));
#1790=EDGE_LOOP('',(#15522));
#1972=CIRCLE('',#17790,1.954);
#1973=CIRCLE('',#17791,1.5555);
#1974=CIRCLE('',#17792,1.);
#1975=CIRCLE('',#17793,1.5555);
#1976=CIRCLE('',#17795,1.5555);
#1977=CIRCLE('',#17824,1.954);
#1978=CIRCLE('',#17825,1.96035170728095);
#1979=CIRCLE('',#17826,1.954);
#1980=CIRCLE('',#17837,3.5);
#1981=CIRCLE('',#17839,3.5);
#3729=B_SPLINE_CURVE_WITH_KNOTS('',3,(#260681,#260682,#260683,#260684,#260685,
#260686,#260687,#260688,#260689,#260690,#260691,#260692,#260693,#260694,
#260695,#260696,#260697,#260698,#260699,#260700,#260701,#260702,#260703,
#260704,#260705,#260706,#260707,#260708,#260709,#260710,#260711,#260712,
#260713,#260714,#260715,#260716,#260717,#260718,#260719,#260720,#260721,
#260722,#260723,#260724,#260725,#260726,#260727,#260728,#260729,#260730,
#260731,#260732,#260733,#260734,#260735,#260736,#260737,#260738,#260739,
#260740,#260741,#260742,#260743,#260744,#260745,#260746,#260747,#260748,
#260749,#260750,#260751,#260752,#260753,#260754,#260755,#260756,#260757,
#260758,#260759,#260760,#260761,#260762,#260763,#260764,#260765,#260766,
#260767,#260768,#260769,#260770,#260771,#260772,#260773,#260774,#260775,
#260776,#260777,#260778,#260779,#260780,#260781,#260782,#260783,#260784,
#260785,#260786,#260787,#260788,#260789,#260790,#260791,#260792,#260793,
#260794,#260795,#260796,#260797,#260798,#260799,#260800,#260801,#260802,
#260803,#260804,#260805,#260806,#260807,#260808,#260809,#260810,#260811,
#260812,#260813,#260814,#260815,#260816,#260817,#260818,#260819,#260820,
#260821,#260822,#260823,#260824,#260825,#260826,#260827,#260828,#260829,
#260830,#260831,#260832,#260833,#260834,#260835,#260836,#260837,#260838,
#260839,#260840,#260841,#260842,#260843,#260844,#260845,#260846,#260847,
#260848,#260849,#260850,#260851,#260852,#260853,#260854,#260855,#260856,
#260857,#260858,#260859,#260860,#260861,#260862,#260863,#260864,#260865,
#260866,#260867,#260868,#260869,#260870,#260871,#260872,#260873,#260874,
#260875,#260876,#260877,#260878,#260879,#260880,#260881,#260882,#260883,
#260884,#260885,#260886,#260887,#260888,#260889,#260890,#260891,#260892,
#260893,#260894,#260895,#260896,#260897,#260898,#260899,#260900,#260901,
#260902,#260903,#260904,#260905,#260906,#260907,#260908,#260909,#260910,
#260911,#260912,#260913,#260914,#260915,#260916,#260917,#260918),
 .UNSPECIFIED.,.F.,.F.,(4,3,3,3,3,3,3,3,3,3,3,3,3,3,3,3,3,3,3,3,3,3,3,3,
3,3,3,3,3,3,3,3,3,3,3,3,3,3,3,3,3,3,3,3,3,3,3,3,3,3,3,3,3,3,3,3,3,3,3,3,
3,3,3,3,3,3,3,3,3,3,3,3,3,3,3,3,3,3,3,4),(-0.996917990983662,-0.97987983316105,
-0.978871413435325,-0.961116856180621,-0.951587145757447,-0.947910386874838,
-0.928982261184871,-0.90990005817218,-0.905014559890978,-0.901598586961351,
-0.882292182793549,-0.863107350127392,-0.849971152762544,-0.842038908785025,
-0.838710948675444,-0.836834955397696,-0.818300729608859,-0.798949153300391,
-0.782788097020223,-0.778225005840288,-0.774303315136981,-0.754735795630886,
-0.734928220216909,-0.718611340927443,-0.712743439168397,-0.709092797998921,
-0.689172521999581,-0.669660703059046,-0.64998645040343,-0.645862963244773,
-0.642554076823802,-0.622791476319913,-0.60262246477522,-0.589248643053048,
-0.580502223935803,-0.577010713467821,-0.556520757801954,-0.536095573597444,
-0.515863732297644,-0.510831775808524,-0.506523713187674,-0.495631890997843,
-0.476757208574652,-0.475757192304605,-0.455615109588419,-0.446506125233596,
-0.440748198417535,-0.437135126114829,-0.416450924878763,-0.395477580104861,
-0.375263317722426,-0.368809689737484,-0.365367048241743,-0.34417333376397,
-0.323355482063595,-0.314620530575122,-0.30288119489851,-0.297338412534419,
-0.29378483272482,-0.272901128535689,-0.251582427725212,-0.235983519228227,
-0.228246846789718,-0.224656212168728,-0.221044939969769,-0.1994931133928,
-0.177920926015553,-0.15673512369944,-0.15170307566897,-0.148203038640002,
-0.12679115974933,-0.106630188425335,-0.105503598453981,-0.0837818265101803,
-0.0759343988619359,-0.0724446243915576,-0.0506399122259315,-0.028541324462408,
-0.00653824277564539,0.),.UNSPECIFIED.);
#3730=B_SPLINE_CURVE_WITH_KNOTS('',3,(#260926,#260927,#260928,#260929,#260930,
#260931,#260932,#260933,#260934,#260935,#260936,#260937,#260938,#260939,
#260940,#260941,#260942,#260943,#260944,#260945,#260946,#260947,#260948,
#260949,#260950,#260951,#260952,#260953,#260954,#260955,#260956,#260957,
#260958,#260959),.UNSPECIFIED.,.F.,.F.,(4,3,3,3,3,3,3,3,3,3,3,4),(-0.135495685711106,
-0.130764870569518,-0.110890150910476,-0.0911021965626242,-0.0717094166696496,
-0.0636025318400057,-0.0603549952613959,-0.0416129334602128,-0.0231970346481039,
-0.00669672064089262,-0.00531383823267436,0.),.UNSPECIFIED.);
#3731=B_SPLINE_CURVE_WITH_KNOTS('',3,(#260965,#260966,#260967,#260968,#260969,
#260970,#260971,#260972,#260973,#260974,#260975,#260976,#260977,#260978,
#260979,#260980,#260981,#260982,#260983,#260984,#260985,#260986,#260987,
#260988,#260989,#260990,#260991,#260992,#260993,#260994,#260995,#260996,
#260997,#260998,#260999,#261000,#261001,#261002,#261003,#261004,#261005,
#261006,#261007,#261008,#261009,#261010,#261011,#261012,#261013,#261014,
#261015,#261016,#261017,#261018,#261019,#261020,#261021,#261022,#261023,
#261024,#261025,#261026,#261027,#261028,#261029,#261030,#261031,#261032,
#261033,#261034,#261035,#261036,#261037),.UNSPECIFIED.,.F.,.F.,(4,3,3,3,
3,3,3,3,3,3,3,3,3,3,3,3,3,3,3,3,3,3,3,3,4),(10.3761005036881,10.4920608060658,
10.6025246039385,10.7128890189401,10.8231984893798,10.9334973658563,11.0439020613945,
11.154368831279,11.2650249188774,11.3037829227095,11.4156702736963,11.527365113134,
11.6389525957845,11.7504752987031,11.8619757060865,11.973579669562,12.0852315334915,
12.1971014732273,12.3015149226994,12.4130322909134,12.5243820781322,12.6356109379018,
12.746764643097,12.8579360623938,12.962846328138),.UNSPECIFIED.);
#3732=B_SPLINE_CURVE_WITH_KNOTS('',3,(#261040,#261041,#261042,#261043,#261044,
#261045,#261046,#261047,#261048,#261049,#261050,#261051,#261052,#261053,
#261054,#261055,#261056,#261057,#261058,#261059,#261060,#261061,#261062,
#261063,#261064,#261065,#261066,#261067,#261068,#261069,#261070,#261071,
#261072,#261073,#261074,#261075,#261076,#261077,#261078,#261079),
 .UNSPECIFIED.,.F.,.F.,(4,3,3,3,3,3,3,3,3,3,3,3,3,4),(11.6154215191107,
11.7297387352054,11.8440009194378,11.9582350805506,12.072475803645,12.1867576725813,
12.3012123412273,12.4157557152712,12.5305425716753,12.6127553697675,12.7232745471891,
12.8336234769681,12.9438241005833,12.9641212388815),.UNSPECIFIED.);
#3733=B_SPLINE_CURVE_WITH_KNOTS('',3,(#261085,#261086,#261087,#261088,#261089,
#261090,#261091,#261092,#261093,#261094,#261095,#261096,#261097,#261098,
#261099,#261100,#261101,#261102,#261103,#261104,#261105,#261106,#261107,
#261108,#261109,#261110,#261111,#261112,#261113,#261114,#261115,#261116,
#261117,#261118,#261119,#261120,#261121,#261122,#261123,#261124,#261125,
#261126,#261127,#261128,#261129,#261130,#261131,#261132,#261133,#261134,
#261135,#261136,#261137,#261138,#261139,#261140,#261141,#261142,#261143,
#261144,#261145,#261146,#261147,#261148,#261149,#261150,#261151,#261152,
#261153,#261154,#261155,#261156,#261157,#261158,#261159,#261160,#261161,
#261162,#261163,#261164,#261165,#261166,#261167,#261168,#261169,#261170,
#261171,#261172,#261173,#261174,#261175,#261176,#261177,#261178,#261179,
#261180,#261181,#261182,#261183,#261184,#261185,#261186,#261187,#261188,
#261189,#261190,#261191,#261192,#261193,#261194,#261195,#261196,#261197,
#261198,#261199,#261200,#261201,#261202,#261203,#261204,#261205,#261206,
#261207,#261208),.UNSPECIFIED.,.F.,.F.,(4,2,2,2,2,2,2,2,2,2,2,2,2,2,2,2,
2,2,2,2,2,2,2,2,2,2,2,2,2,2,2,2,2,2,2,2,2,2,2,2,2,2,2,2,2,2,2,2,2,2,2,2,
2,2,2,2,2,2,2,2,2,4),(-0.552947915177876,-0.544185360780231,-0.51218218436496,
-0.488189034423349,-0.484648122800509,-0.482446896583355,-0.480732351908997,
-0.47883597676679,-0.475714314137584,-0.464114614355967,-0.419003879019557,
-0.40715830506582,-0.405160537844409,-0.403927534603725,-0.402969700281705,
-0.401860730166516,-0.399880616425001,-0.390353475498068,-0.346512915273737,
-0.331676450249068,-0.328199494079562,-0.326204152709283,-0.324517345195867,
-0.322466289877511,-0.318632060010591,-0.29260268614785,-0.266934087854077,
-0.262655616377667,-0.251362376908043,-0.249392698891025,-0.248167981037694,
-0.247210488374884,-0.246094706241731,-0.244085508640898,-0.234068401248511,
-0.183577356834065,-0.182068791615472,-0.17451174617764,-0.171740812681764,
-0.17010252972066,-0.16841328938821,-0.166217870318622,-0.163797452958358,
-0.159779510990715,-0.15150417860358,-0.106352984611612,-0.095541494497319,
-0.0935956104315449,-0.0923781161284116,-0.0914219328422961,-0.0903032256914169,
-0.088274674515791,-0.0778537337230705,-0.0308276129186543,-0.0202923165647704,
-0.0170438453819075,-0.0149325205532303,-0.013328725997535,-0.0117302233231597,
-0.00985101753289302,-0.00596234470578328,-0.000462250202742447),
 .UNSPECIFIED.);
#3734=B_SPLINE_CURVE_WITH_KNOTS('',3,(#261209,#261210,#261211,#261212,#261213,
#261214,#261215,#261216,#261217,#261218,#261219,#261220,#261221,#261222,
#261223,#261224,#261225,#261226,#261227,#261228,#261229,#261230,#261231,
#261232,#261233,#261234,#261235,#261236,#261237,#261238,#261239,#261240,
#261241,#261242,#261243,#261244,#261245,#261246,#261247,#261248,#261249,
#261250,#261251,#261252,#261253,#261254,#261255,#261256,#261257,#261258,
#261259,#261260,#261261,#261262,#261263,#261264,#261265,#261266,#261267,
#261268,#261269,#261270,#261271,#261272,#261273,#261274,#261275,#261276,
#261277,#261278,#261279,#261280,#261281,#261282,#261283,#261284),
 .UNSPECIFIED.,.F.,.F.,(4,3,3,3,3,3,3,3,3,3,3,3,3,3,3,3,3,3,3,3,3,3,3,3,
3,4),(12.962846328138,13.0741156623616,13.1866812925254,13.2992469226893,
13.4109725593946,13.5224995862497,13.6339156712123,13.7452636982314,13.8565864540708,
13.9680095127458,14.0794784018147,14.1911642428179,14.2969789226792,14.4086941947502,
14.5202114955061,14.6316182494718,14.7429573571259,14.8542716222304,14.9656869401723,
15.0771484850974,15.18882776068,15.2947109226691,15.4175521494668,15.5400015244941,
15.6618361688977,15.7079632676234),.UNSPECIFIED.);
#3735=B_SPLINE_CURVE_WITH_KNOTS('',3,(#261286,#261287,#261288,#261289,#261290,
#261291,#261292,#261293,#261294,#261295,#261296,#261297,#261298,#261299,
#261300,#261301,#261302,#261303,#261304,#261305,#261306,#261307,#261308,
#261309,#261310,#261311,#261312,#261313,#261314,#261315,#261316,#261317,
#261318,#261319,#261320,#261321,#261322,#261323,#261324,#261325,#261326,
#261327,#261328,#261329,#261330,#261331,#261332,#261333,#261334,#261335,
#261336,#261337,#261338,#261339,#261340,#261341,#261342,#261343,#261344,
#261345,#261346,#261347,#261348,#261349,#261350,#261351,#261352,#261353,
#261354,#261355,#261356,#261357,#261358,#261359,#261360,#261361),
 .UNSPECIFIED.,.F.,.F.,(4,3,3,3,3,3,3,3,3,3,3,3,3,3,3,3,3,3,3,3,3,3,3,3,
3,4),(12.9641212388815,13.074229711549,13.1843101652664,13.2944889695355,
13.4047143343461,13.5151543602736,13.6100892204243,13.7219600539943,13.8336321466415,
13.9451931128889,14.0566855716135,14.1681520443355,14.2797163578875,14.3913254608342,
14.5031474993986,14.607423071081,14.7193156410109,14.8310158640507,14.9426088321047,
15.0541371117456,15.1656431768019,15.2772527477869,15.3889102779343,15.5007855451298,
15.6047569217378,15.707963267949),.UNSPECIFIED.);
#3736=B_SPLINE_CURVE_WITH_KNOTS('',3,(#261362,#261363,#261364,#261365,#261366,
#261367,#261368,#261369,#261370,#261371,#261372,#261373,#261374,#261375,
#261376,#261377,#261378,#261379,#261380,#261381,#261382,#261383,#261384,
#261385,#261386,#261387,#261388,#261389,#261390,#261391,#261392,#261393,
#261394,#261395,#261396,#261397,#261398,#261399,#261400,#261401,#261402,
#261403,#261404,#261405,#261406,#261407,#261408,#261409,#261410,#261411,
#261412,#261413,#261414,#261415,#261416,#261417,#261418,#261419,#261420,
#261421,#261422,#261423,#261424,#261425,#261426,#261427,#261428,#261429,
#261430,#261431,#261432,#261433,#261434,#261435,#261436,#261437,#261438,
#261439,#261440,#261441,#261442,#261443,#261444,#261445,#261446,#261447,
#261448,#261449,#261450,#261451,#261452,#261453,#261454,#261455,#261456,
#261457,#261458,#261459,#261460,#261461,#261462,#261463,#261464,#261465,
#261466,#261467,#261468,#261469,#261470,#261471,#261472,#261473,#261474,
#261475,#261476,#261477,#261478,#261479,#261480,#261481),.UNSPECIFIED.,
 .F.,.F.,(4,2,2,2,2,2,2,2,2,2,2,2,2,2,2,2,2,2,2,2,2,2,2,2,2,2,2,2,2,2,2,
2,2,2,2,2,2,2,2,2,2,2,2,2,2,2,2,2,2,2,2,2,2,2,2,2,2,2,2,4),(-1.96129963604252,
-1.93322459695046,-1.9090261506906,-1.90355760708412,-1.90118796758417,
-1.89944226607523,-1.89782450274418,-1.8956133373866,-1.89003323316185,
-1.85580303280489,-1.83565344211002,-1.82866187122417,-1.82566758490452,
-1.82402199023137,-1.82259561103283,-1.8216157956448,-1.82071142512442,
-1.81924560135888,-1.81562210787264,-1.78588026363565,-1.75093023406771,
-1.74691431796691,-1.7448073864601,-1.74307878105252,-1.74107020406526,
-1.73761082759208,-1.72345599400789,-1.67867418663412,-1.66971364432886,
-1.66774729959421,-1.66663025038523,-1.66565665950387,-1.66441033784986,
-1.66235120010726,-1.64943925171088,-1.61610925304974,-1.59705654272514,
-1.59220344036914,-1.58993377696539,-1.58819243396338,-1.58652684445777,
-1.5836832771723,-1.57576054590822,-1.52429907328513,-1.514215372696,-1.5121873348502,
-1.51106001936016,-1.51009182085771,-1.50885150676948,-1.50685253641527,
-1.4952331432125,-1.45022036797864,-1.44246532139049,-1.43684770883712,
-1.43444311549047,-1.43268245335169,-1.43105831068808,-1.4288498238886,
-1.42333489991376,-1.40933590033974),.UNSPECIFIED.);
#3737=B_SPLINE_CURVE_WITH_KNOTS('',3,(#261486,#261487,#261488,#261489,#261490,
#261491,#261492,#261493,#261494,#261495,#261496,#261497,#261498,#261499,
#261500,#261501,#261502,#261503,#261504,#261505,#261506,#261507,#261508,
#261509,#261510,#261511,#261512,#261513,#261514,#261515,#261516,#261517,
#261518,#261519,#261520,#261521,#261522,#261523,#261524,#261525,#261526,
#261527,#261528,#261529,#261530,#261531,#261532,#261533,#261534,#261535,
#261536,#261537,#261538,#261539,#261540,#261541,#261542,#261543,#261544,
#261545,#261546,#261547,#261548,#261549,#261550,#261551,#261552,#261553,
#261554,#261555,#261556,#261557,#261558,#261559,#261560,#261561,#261562,
#261563,#261564,#261565,#261566,#261567,#261568,#261569,#261570,#261571,
#261572,#261573,#261574,#261575,#261576,#261577,#261578,#261579,#261580,
#261581,#261582,#261583,#261584,#261585,#261586,#261587,#261588,#261589,
#261590,#261591,#261592,#261593,#261594,#261595,#261596,#261597,#261598,
#261599,#261600,#261601,#261602,#261603,#261604,#261605,#261606,#261607,
#261608,#261609,#261610,#261611,#261612,#261613,#261614,#261615,#261616,
#261617,#261618,#261619,#261620,#261621,#261622,#261623,#261624,#261625,
#261626,#261627,#261628,#261629,#261630,#261631,#261632,#261633,#261634,
#261635,#261636,#261637,#261638,#261639,#261640,#261641,#261642,#261643,
#261644,#261645,#261646,#261647,#261648,#261649,#261650,#261651,#261652,
#261653,#261654,#261655,#261656,#261657,#261658,#261659,#261660,#261661,
#261662,#261663,#261664,#261665,#261666,#261667,#261668,#261669,#261670,
#261671,#261672,#261673,#261674,#261675,#261676,#261677,#261678,#261679,
#261680,#261681,#261682,#261683,#261684,#261685,#261686,#261687,#261688,
#261689,#261690,#261691,#261692,#261693,#261694,#261695,#261696,#261697),
 .UNSPECIFIED.,.F.,.F.,(4,2,2,2,2,2,2,2,2,2,2,2,2,2,2,2,2,2,2,2,2,2,2,2,
2,2,2,2,2,2,2,2,2,2,2,2,2,2,2,2,2,2,2,2,2,2,2,2,2,2,2,2,2,2,2,2,2,2,2,2,
2,2,2,2,2,2,2,2,2,2,2,2,2,2,2,2,2,2,2,2,2,2,2,2,2,2,2,2,2,2,2,2,2,2,2,2,
2,2,2,2,2,2,2,2,2,4),(-1.53345529214133,-1.50623797145372,-1.49666778590912,
-1.49468562835921,-1.49357646710803,-1.49261903591414,-1.4913873033109,
-1.48939310752656,-1.47761518201257,-1.43260330554539,-1.42091188985495,
-1.41778283896294,-1.41588518144206,-1.41417153561813,-1.41197432624087,
-1.40844567634991,-1.38490781828261,-1.35248790390611,-1.34114977072669,
-1.33907451947209,-1.33794525606482,-1.33698998554753,-1.33578586152309,
-1.33334993757023,-1.310344853583,-1.2899061599334,-1.27425450561612,-1.26484871808546,
-1.26194327849021,-1.26009471117923,-1.25836601744075,-1.2561016813172,
-1.2510516762149,-1.20924808508801,-1.18805524002374,-1.18425774448664,
-1.1828177920521,-1.18182724679977,-1.18092974525103,-1.17945981077153,
-1.17575153961848,-1.15139721764207,-1.12753783981288,-1.11032587436593,
-1.10681802966037,-1.10483714246409,-1.10330500467478,-1.10130388675173,
-1.09779983399027,-1.08256045074441,-1.03823381155214,-1.02954926661654,
-1.02762227042416,-1.02652502296403,-1.02556549711038,-1.0243354515801,
-1.0223030501286,-1.00962660013027,-0.981465851632982,-0.955418973806751,
-0.951842505099802,-0.949630618795421,-0.947914730907127,-0.946023910479201,
-0.942927525326686,-0.931611011768376,-0.886308352535297,-0.874340306264157,
-0.872337154902847,-0.871102528501961,-0.870144544065615,-0.869036673994313,
-0.867061502217166,-0.857616191642048,-0.813726209767829,-0.798870236314403,
-0.795392311394328,-0.793396912446735,-0.791710345148474,-0.789659934860234,
-0.785827972708482,-0.759878407236498,-0.73573378499714,-0.718895547609784,
-0.71653190729292,-0.715326293140029,-0.714370589664715,-0.713241663294021,
-0.711169372215316,-0.699906461945282,-0.672596371774356,-0.644013921137628,
-0.640417241078222,-0.638222962205271,-0.636504372237274,-0.634622911961739,
-0.631569693993843,-0.620721821254798,-0.579982296388231,-0.563188511800519,
-0.560825839195544,-0.559620372967933,-0.558664709612266,-0.557535803543035,
-0.555463048841534,-0.552947915177876),.UNSPECIFIED.);
#3738=B_SPLINE_CURVE_WITH_KNOTS('',3,(#261698,#261699,#261700,#261701,#261702,
#261703,#261704,#261705,#261706,#261707,#261708,#261709,#261710,#261711,
#261712,#261713,#261714,#261715,#261716,#261717,#261718,#261719,#261720,
#261721,#261722,#261723,#261724,#261725,#261726,#261727,#261728,#261729,
#261730,#261731,#261732,#261733,#261734,#261735,#261736,#261737,#261738,
#261739,#261740,#261741,#261742,#261743,#261744,#261745,#261746,#261747,
#261748,#261749,#261750,#261751,#261752,#261753,#261754,#261755,#261756,
#261757,#261758,#261759,#261760,#261761,#261762,#261763,#261764,#261765,
#261766,#261767,#261768,#261769,#261770,#261771,#261772,#261773,#261774,
#261775,#261776,#261777,#261778,#261779,#261780,#261781,#261782,#261783,
#261784,#261785,#261786,#261787,#261788,#261789,#261790,#261791,#261792,
#261793,#261794,#261795,#261796,#261797,#261798,#261799,#261800,#261801,
#261802,#261803,#261804,#261805,#261806,#261807,#261808,#261809,#261810,
#261811,#261812,#261813,#261814,#261815,#261816,#261817,#261818,#261819,
#261820,#261821,#261822,#261823,#261824,#261825,#261826,#261827,#261828,
#261829,#261830,#261831,#261832,#261833,#261834,#261835,#261836,#261837,
#261838,#261839,#261840,#261841,#261842,#261843,#261844,#261845,#261846,
#261847,#261848,#261849,#261850,#261851,#261852,#261853,#261854,#261855,
#261856,#261857,#261858,#261859,#261860,#261861,#261862,#261863,#261864,
#261865,#261866,#261867,#261868,#261869,#261870,#261871,#261872,#261873,
#261874,#261875,#261876,#261877,#261878,#261879,#261880,#261881,#261882,
#261883,#261884,#261885,#261886,#261887,#261888,#261889,#261890,#261891,
#261892,#261893,#261894,#261895,#261896,#261897,#261898,#261899,#261900,
#261901,#261902,#261903,#261904,#261905,#261906,#261907,#261908,#261909,
#261910,#261911,#261912,#261913,#261914,#261915),.UNSPECIFIED.,.F.,.F.,
(4,2,2,2,2,2,2,2,2,2,2,2,2,2,2,2,2,2,2,2,2,2,2,2,2,2,2,2,2,2,2,2,2,2,2,
2,2,2,2,2,2,2,2,2,2,2,2,2,2,2,2,2,2,2,2,2,2,2,2,2,2,2,2,2,2,2,2,2,2,2,2,
2,2,2,2,2,2,2,2,2,2,2,2,2,2,2,2,2,2,2,2,2,2,2,2,2,2,2,2,2,2,2,2,2,2,2,2,
2,4),(-1.40933590033974,-1.36873680763542,-1.3585295663257,-1.35649568484385,
-1.35536757973072,-1.35439904341142,-1.35315934536828,-1.35116510804622,
-1.33967674844955,-1.29469961770618,-1.28279432784207,-1.27962074009993,
-1.27769750463332,-1.27596146396164,-1.27373625854639,-1.27016336466128,
-1.23814508520663,-1.21331869966716,-1.20297950979278,-1.20093602729277,
-1.19980462011342,-1.19883556977395,-1.19759752506688,-1.19560874410812,
-1.18423292999466,-1.18143777472054,-1.15591591349934,-1.12859383792929,
-1.12469958595851,-1.12262087979613,-1.12091336561011,-1.1188957129464,
-1.11538472380333,-1.10043203257075,-1.05614521136344,-1.04723743539541,
-1.04527987709019,-1.04416765471278,-1.04319635058693,-1.04195196528199,
-1.03989695713317,-1.027056953605,-0.997880176508862,-0.98116705413691,
-0.979464544434689,-0.978252858937561,-0.970864183644352,-0.968098869278444,
-0.96644850888878,-0.964700600244288,-0.962384545392156,-0.957279726806057,
-0.936270927248185,-0.905454299305012,-0.900909676879024,-0.891865102368475,
-0.889826008433882,-0.888683586653056,-0.887715908698133,-0.886493631815395,
-0.884012394801899,-0.880756124771468,-0.872893772212155,-0.837816007122391,
-0.817338165789125,-0.813869629521449,-0.811676058826272,-0.809943841679992,
-0.808003155477414,-0.804749381881429,-0.791870709350594,-0.742990370048334,
-0.741753466290543,-0.735729813996039,-0.733936205198346,-0.732859931922798,
-0.731879021678569,-0.73054422929792,-0.727462079000046,-0.723160923480397,
-0.711303092606892,-0.669432121913061,-0.667619483096744,-0.667341765710061,
-0.659690660752527,-0.65688615538079,-0.65522793283421,-0.653483037121117,
-0.651190020334603,-0.646212990405797,-0.62621695233956,-0.598047697932467,
-0.581185010605895,-0.578800751394741,-0.57758203601285,-0.57661443217304,
-0.575468823864746,-0.573358192769217,-0.561655372267942,-0.526779453384891,
-0.506098934002557,-0.502612077937401,-0.500412920864941,-0.498680053227548,
-0.496742563048483,-0.493503517609593,-0.480810991169626,-0.434198512552718,
-0.428921571146853),.UNSPECIFIED.);
#3739=B_SPLINE_CURVE_WITH_KNOTS('',3,(#261921,#261922,#261923,#261924,#261925,
#261926,#261927,#261928,#261929,#261930,#261931,#261932,#261933,#261934,
#261935,#261936,#261937,#261938,#261939,#261940,#261941,#261942,#261943,
#261944,#261945,#261946,#261947,#261948,#261949,#261950,#261951,#261952,
#261953,#261954,#261955,#261956,#261957,#261958,#261959,#261960,#261961,
#261962,#261963,#261964,#261965,#261966,#261967,#261968,#261969,#261970,
#261971,#261972,#261973,#261974,#261975,#261976,#261977,#261978,#261979,
#261980,#261981,#261982,#261983,#261984,#261985,#261986,#261987,#261988,
#261989,#261990,#261991,#261992,#261993,#261994,#261995,#261996,#261997,
#261998,#261999,#262000,#262001,#262002,#262003,#262004,#262005,#262006,
#262007,#262008,#262009,#262010,#262011,#262012,#262013,#262014,#262015,
#262016,#262017,#262018,#262019,#262020,#262021,#262022,#262023,#262024,
#262025,#262026,#262027,#262028,#262029,#262030,#262031,#262032,#262033,
#262034,#262035,#262036,#262037,#262038,#262039,#262040,#262041,#262042,
#262043,#262044),.UNSPECIFIED.,.F.,.F.,(4,2,2,2,2,2,2,2,2,2,2,2,2,2,2,2,
2,2,2,2,2,2,2,2,2,2,2,2,2,2,2,2,2,2,2,2,2,2,2,2,2,2,2,2,2,2,2,2,2,2,2,2,
2,2,2,2,2,2,2,2,2,4),(-0.552653709409288,-0.550934822503833,-0.547405028794108,
-0.545207258145108,-0.543493280814131,-0.541595364287432,-0.53846613981931,
-0.5267775329029,-0.481729369420564,-0.46994011210014,-0.467945010901042,
-0.46671287206948,-0.465755219283742,-0.464645900598761,-0.46266371335701,
-0.453097591169776,-0.409269788252985,-0.394488477298573,-0.391016139527422,
-0.389022179702472,-0.387335801025847,-0.385284363563794,-0.381446703137949,
-0.35523561174603,-0.32750681026561,-0.322387971467438,-0.313884898605568,
-0.311901196140213,-0.310779640832601,-0.309919239757913,-0.308752313056401,
-0.30649950447498,-0.290122486717528,-0.249388147950734,-0.238242756816616,
-0.235034173950901,-0.233118764753075,-0.231579335112055,-0.229495875623519,
-0.225504468525894,-0.190546244543438,-0.160699123481394,-0.157097786116065,
-0.155669865901035,-0.15469034019135,-0.153796305928183,-0.152489736773474,
-0.149128735066113,-0.132602820240614,-0.101780357939939,-0.083511942147516,
-0.0801495186860906,-0.0780022809874654,-0.076293676827951,-0.0743659086835844,
-0.0711015120187754,-0.0577423953078272,-0.0321019381278825,-0.00452335382496099,
-0.00166022821521149,-0.000744519849027736,-0.00046009660915402),
 .UNSPECIFIED.);
#3740=B_SPLINE_CURVE_WITH_KNOTS('',3,(#262045,#262046,#262047,#262048,#262049,
#262050,#262051,#262052,#262053,#262054,#262055,#262056,#262057,#262058,
#262059,#262060,#262061,#262062,#262063,#262064,#262065,#262066,#262067,
#262068,#262069,#262070,#262071,#262072,#262073,#262074,#262075,#262076,
#262077,#262078,#262079,#262080,#262081,#262082,#262083,#262084,#262085,
#262086,#262087,#262088,#262089,#262090,#262091,#262092,#262093,#262094,
#262095,#262096,#262097,#262098,#262099,#262100,#262101,#262102,#262103,
#262104,#262105,#262106,#262107,#262108,#262109,#262110,#262111,#262112,
#262113,#262114,#262115,#262116,#262117,#262118,#262119,#262120,#262121,
#262122,#262123,#262124,#262125,#262126,#262127,#262128,#262129,#262130,
#262131,#262132,#262133,#262134,#262135,#262136,#262137,#262138,#262139,
#262140,#262141,#262142,#262143,#262144,#262145,#262146),.UNSPECIFIED.,
 .F.,.F.,(4,2,2,2,2,2,2,2,2,2,2,2,2,2,2,2,2,2,2,2,2,2,2,2,2,2,2,2,2,2,2,
2,2,2,2,2,2,2,2,2,2,2,2,2,2,2,2,2,2,2,4),(-1.96165355527632,-1.96128010600046,
-1.96037377007412,-1.95941733540217,-1.95810332857501,-1.95512425600224,
-1.95207954611179,-1.94444725734518,-1.89921232004835,-1.88786245187576,
-1.88476387934134,-1.88287303892651,-1.88115798633747,-1.87894837628733,
-1.87537802452049,-1.84431116858309,-1.82192140543595,-1.81275543589084,
-1.80737027036756,-1.80614556930356,-1.80501857608304,-1.8040825641375,
-1.80291378371364,-1.80076355688354,-1.78931212618323,-1.74470211981379,
-1.73237102260667,-1.72918815072057,-1.7272788288345,-1.72556793572463,
-1.7233925084727,-1.71993557794375,-1.69897949826961,-1.65657637973759,
-1.65322925066462,-1.65070000241082,-1.64947745120312,-1.64852093440975,
-1.64740564732197,-1.64544856528959,-1.63729569772236,-1.63183731221877,
-1.60409508856384,-1.57789712492263,-1.57406089061736,-1.57201009130559,
-1.57032417114524,-1.5683306767659,-1.56485895134277,-1.55007789823857,
-1.53345529214133),.UNSPECIFIED.);
#3741=B_SPLINE_CURVE_WITH_KNOTS('',3,(#262148,#262149,#262150,#262151,#262152,
#262153,#262154,#262155,#262156,#262157,#262158,#262159,#262160,#262161,
#262162,#262163,#262164,#262165,#262166,#262167,#262168,#262169,#262170,
#262171,#262172,#262173,#262174,#262175,#262176,#262177,#262178,#262179,
#262180,#262181,#262182,#262183,#262184,#262185,#262186,#262187,#262188,
#262189,#262190,#262191,#262192,#262193,#262194,#262195,#262196,#262197,
#262198,#262199,#262200,#262201,#262202,#262203,#262204,#262205,#262206,
#262207,#262208,#262209,#262210,#262211,#262212,#262213,#262214,#262215,
#262216,#262217,#262218,#262219,#262220,#262221,#262222,#262223,#262224,
#262225,#262226,#262227,#262228,#262229,#262230,#262231,#262232,#262233,
#262234,#262235,#262236,#262237,#262238,#262239,#262240,#262241,#262242,
#262243,#262244,#262245,#262246,#262247,#262248,#262249,#262250,#262251,
#262252,#262253),.UNSPECIFIED.,.F.,.F.,(4,2,2,2,2,2,2,2,2,2,2,2,2,2,2,2,
2,2,2,2,2,2,2,2,2,2,2,2,2,2,2,2,2,2,2,2,2,2,2,2,2,2,2,2,2,2,2,2,2,2,2,2,
4),(-0.428921571146853,-0.424968544272072,-0.423096680319819,-0.421893996806391,
-0.420927011708669,-0.419767688591699,-0.417593267307482,-0.404361768701686,
-0.381549437142564,-0.35064637422367,-0.347048400612306,-0.344815597620563,
-0.343078564875199,-0.341159259207509,-0.338003792436699,-0.32630806445896,
-0.281150145284207,-0.269550144429268,-0.267549813665198,-0.266308018734925,
-0.265338489465567,-0.264209536185,-0.262177053892415,-0.25210323750283,
-0.200666519410322,-0.200289359103597,-0.192673510277237,-0.189874020243945,
-0.188216647291982,-0.18647110261026,-0.184220426432803,-0.179424127296979,
-0.173032303496688,-0.15690065245941,-0.133259132557622,-0.114222170209687,
-0.111813215884357,-0.110589165303511,-0.109621141039482,-0.108479501081243,
-0.106387686775185,-0.0952531048343403,-0.0779269994880584,-0.0597811234362074,
-0.0391189537714606,-0.0356304489188435,-0.0334306158212738,-0.0316974428853265,
-0.0300771657471151,-0.0281751615843451,-0.025434668570542,-0.0175897605599473,
-0.000459285835135901),.UNSPECIFIED.);
#3742=B_SPLINE_CURVE_WITH_KNOTS('',3,(#262254,#262255,#262256,#262257,#262258,
#262259,#262260,#262261,#262262,#262263,#262264,#262265,#262266,#262267,
#262268,#262269,#262270,#262271,#262272,#262273,#262274,#262275,#262276,
#262277,#262278,#262279,#262280,#262281,#262282,#262283,#262284,#262285,
#262286,#262287,#262288,#262289,#262290,#262291,#262292,#262293,#262294,
#262295,#262296,#262297,#262298,#262299,#262300,#262301,#262302,#262303,
#262304,#262305,#262306,#262307,#262308,#262309,#262310,#262311,#262312,
#262313,#262314,#262315,#262316,#262317,#262318,#262319,#262320,#262321,
#262322,#262323,#262324,#262325,#262326,#262327,#262328,#262329,#262330,
#262331,#262332,#262333,#262334,#262335,#262336,#262337,#262338,#262339,
#262340,#262341,#262342,#262343,#262344,#262345,#262346,#262347,#262348,
#262349,#262350,#262351,#262352,#262353,#262354,#262355,#262356,#262357,
#262358,#262359,#262360,#262361,#262362,#262363,#262364,#262365,#262366,
#262367,#262368,#262369,#262370,#262371,#262372,#262373),.UNSPECIFIED.,
 .F.,.F.,(4,2,2,2,2,2,2,2,2,2,2,2,2,2,2,2,2,2,2,2,2,2,2,2,2,2,2,2,2,2,2,
2,2,2,2,2,2,2,2,2,2,2,2,2,2,2,2,2,2,2,2,2,2,2,2,2,2,2,2,4),(-1.96149836071343,
-1.92271697299584,-1.91960104043406,-1.91790458130877,-1.91642579372871,
-1.91541861373057,-1.91451326294395,-1.91304322816939,-1.90939552210831,
-1.88016061636188,-1.86415767440557,-1.85094536952365,-1.84260982058666,
-1.83988874093019,-1.8382689185902,-1.83653642994018,-1.83433868182765,
-1.8308558747775,-1.81005008463793,-1.7752563031124,-1.76356935314919,-1.76145590270137,
-1.76030977540865,-1.75934233407634,-1.75812458796808,-1.75574446675404,
-1.73909577528902,-1.69825012629792,-1.69113945576909,-1.68588603616201,
-1.68354306811159,-1.68179083098752,-1.68014800712977,-1.67787238156269,
-1.67196005164735,-1.61792822148563,-1.60773957345381,-1.60570468501316,
-1.60457535979885,-1.60360611873077,-1.60236548545786,-1.60036855329615,
-1.58883024159793,-1.54377745127124,-1.5319719637818,-1.52880727803495,
-1.52688616304685,-1.52514993877195,-1.52292158830651,-1.51933774374819,
-1.48744873071576,-1.46248216436062,-1.45211120408237,-1.45006648609837,
-1.44893507689342,-1.44796615095104,-1.44672863406259,-1.44474190912332,
-1.43341386242247,-1.40942950879856),.UNSPECIFIED.);
#3743=B_SPLINE_CURVE_WITH_KNOTS('',3,(#262378,#262379,#262380,#262381,#262382,
#262383,#262384,#262385,#262386,#262387,#262388,#262389,#262390,#262391,
#262392,#262393,#262394,#262395,#262396,#262397,#262398,#262399,#262400,
#262401,#262402,#262403,#262404,#262405,#262406,#262407,#262408,#262409,
#262410,#262411,#262412,#262413,#262414,#262415,#262416,#262417,#262418,
#262419,#262420,#262421,#262422,#262423,#262424,#262425,#262426,#262427,
#262428,#262429,#262430,#262431,#262432,#262433,#262434,#262435,#262436,
#262437,#262438,#262439,#262440,#262441,#262442,#262443,#262444,#262445,
#262446,#262447,#262448,#262449,#262450,#262451,#262452,#262453,#262454,
#262455,#262456,#262457,#262458,#262459,#262460,#262461,#262462,#262463,
#262464,#262465,#262466,#262467,#262468,#262469,#262470,#262471,#262472,
#262473,#262474,#262475,#262476,#262477,#262478,#262479,#262480,#262481,
#262482,#262483,#262484,#262485,#262486,#262487,#262488,#262489,#262490,
#262491,#262492,#262493,#262494,#262495,#262496,#262497,#262498,#262499,
#262500,#262501,#262502,#262503,#262504,#262505,#262506,#262507,#262508,
#262509,#262510,#262511,#262512,#262513,#262514,#262515,#262516,#262517,
#262518,#262519,#262520,#262521,#262522,#262523,#262524,#262525,#262526,
#262527,#262528,#262529,#262530,#262531,#262532,#262533,#262534,#262535,
#262536,#262537,#262538,#262539,#262540,#262541,#262542,#262543,#262544,
#262545,#262546,#262547,#262548,#262549,#262550,#262551,#262552,#262553,
#262554,#262555,#262556,#262557,#262558,#262559,#262560,#262561,#262562,
#262563,#262564,#262565,#262566,#262567,#262568,#262569,#262570,#262571,
#262572,#262573,#262574,#262575,#262576,#262577,#262578,#262579,#262580,
#262581,#262582,#262583),.UNSPECIFIED.,.F.,.F.,(4,2,2,2,2,2,2,2,2,2,2,2,
2,2,2,2,2,2,2,2,2,2,2,2,2,2,2,2,2,2,2,2,2,2,2,2,2,2,2,2,2,2,2,2,2,2,2,2,
2,2,2,2,2,2,2,2,2,2,2,2,2,2,2,2,2,2,2,2,2,2,2,2,2,2,2,2,2,2,2,2,2,2,2,2,
2,2,2,2,2,2,2,2,2,2,2,2,2,2,2,2,2,2,4),(-1.53294839269393,-1.50715734523062,
-1.48668724489829,-1.4816758773482,-1.47939465594995,-1.47767027686247,
-1.47604022894185,-1.47330474693597,-1.46597263665537,-1.41374072859881,
-1.40364410062386,-1.4016324867234,-1.40051717230878,-1.39956091068862,
-1.39833905531885,-1.39637695301433,-1.38521249522548,-1.38244504690862,
-1.34959390755089,-1.33072532617322,-1.32592095734334,-1.32367773379579,
-1.32195852775607,-1.32031565367334,-1.31751509766915,-1.30974277351457,
-1.30797781676012,-1.25797364547037,-1.24798058889317,-1.24597441216338,
-1.24486013750876,-1.24390353070443,-1.24267963587142,-1.24071119407982,
-1.2294215704208,-1.22668281973664,-1.19962855385,-1.17351002101486,-1.16967568867581,
-1.16762531210876,-1.1659394357966,-1.16394563596818,-1.16047247386088,
-1.14567057439514,-1.10181325983102,-1.09228109449825,-1.09030120905274,
-1.08919255459757,-1.08823507183336,-1.08700263701566,-1.08500606819549,
-1.07325956921364,-1.02828099408303,-1.01653906455637,-1.01340564261391,
-1.0115070372706,-1.00979362891146,-1.00759824343698,-1.00407561873939,
-0.980768739722173,-0.954884476788388,-0.950053569025437,-0.937105811619782,
-0.935063438540616,-0.933830675246918,-0.932871113526241,-0.931776216740182,
-0.92985886788984,-0.921310620840032,-0.876942796516238,-0.861653696028039,
-0.858146845057731,-0.856145448493659,-0.854613791152804,-0.852634339012002,
-0.849131446379631,-0.83199966912809,-0.783915984485502,-0.779978693174232,
-0.778471939679158,-0.777567489192838,-0.776583615037072,-0.775177396041581,
-0.771600516677463,-0.752865078406153,-0.73333833051738,-0.706706901799627,
-0.703126505516105,-0.700913659570756,-0.699197918855124,-0.697308159985908,
-0.694215565435119,-0.682936551839584,-0.642532950543339,-0.625927156810066,
-0.62356833656366,-0.622363885242111,-0.621408456664485,-0.620279119339662,
-0.618204034303994,-0.606873328468868,-0.574502497876915,-0.552653709409288),
 .UNSPECIFIED.);
#3744=B_SPLINE_CURVE_WITH_KNOTS('',3,(#262584,#262585,#262586,#262587,#262588,
#262589,#262590,#262591,#262592,#262593,#262594,#262595,#262596,#262597,
#262598,#262599,#262600,#262601,#262602,#262603,#262604,#262605,#262606,
#262607,#262608,#262609,#262610,#262611,#262612,#262613,#262614,#262615,
#262616,#262617,#262618,#262619,#262620,#262621,#262622,#262623,#262624,
#262625,#262626,#262627,#262628,#262629,#262630,#262631,#262632,#262633,
#262634,#262635,#262636,#262637,#262638,#262639,#262640,#262641,#262642,
#262643,#262644,#262645,#262646,#262647,#262648,#262649,#262650,#262651,
#262652,#262653,#262654,#262655,#262656,#262657,#262658,#262659,#262660,
#262661,#262662,#262663,#262664,#262665,#262666,#262667,#262668,#262669,
#262670,#262671,#262672,#262673,#262674,#262675,#262676,#262677,#262678,
#262679,#262680,#262681,#262682,#262683,#262684,#262685,#262686,#262687,
#262688,#262689,#262690,#262691,#262692,#262693,#262694,#262695,#262696,
#262697,#262698,#262699,#262700,#262701,#262702,#262703,#262704,#262705,
#262706,#262707,#262708,#262709,#262710,#262711,#262712,#262713,#262714,
#262715,#262716,#262717,#262718,#262719,#262720,#262721,#262722,#262723,
#262724,#262725,#262726,#262727,#262728,#262729,#262730,#262731,#262732,
#262733,#262734,#262735,#262736,#262737,#262738,#262739,#262740,#262741,
#262742,#262743,#262744,#262745,#262746,#262747,#262748,#262749,#262750,
#262751,#262752,#262753,#262754,#262755,#262756,#262757,#262758,#262759,
#262760,#262761,#262762,#262763,#262764,#262765,#262766,#262767,#262768,
#262769,#262770,#262771,#262772,#262773,#262774,#262775,#262776,#262777,
#262778,#262779,#262780,#262781,#262782,#262783,#262784,#262785,#262786,
#262787,#262788,#262789,#262790,#262791,#262792,#262793,#262794,#262795,
#262796,#262797,#262798,#262799),.UNSPECIFIED.,.F.,.F.,(4,2,2,2,2,2,2,2,
2,2,2,2,2,2,2,2,2,2,2,2,2,2,2,2,2,2,2,2,2,2,2,2,2,2,2,2,2,2,2,2,2,2,2,2,
2,2,2,2,2,2,2,2,2,2,2,2,2,2,2,2,2,2,2,2,2,2,2,2,2,2,2,2,2,2,2,2,2,2,2,2,
2,2,2,2,2,2,2,2,2,2,2,2,2,2,2,2,2,2,2,2,2,2,2,2,2,2,2,4),(-1.40942950879856,
-1.38861304144377,-1.3805496856759,-1.3747588546159,-1.37232289813186,-1.37055470453129,
-1.36893428696517,-1.36674707004159,-1.36136802938653,-1.32359918641245,
-1.307615493727,-1.29653270004572,-1.29445141793771,-1.29331214353993,-1.29234406177558,
-1.29111731126272,-1.28916612026667,-1.27854639235415,-1.27547356077125,
-1.24707539963117,-1.22428477842012,-1.21896208020509,-1.21660657626528,
-1.21485211020589,-1.21321235319538,-1.21050430842141,-1.20348138814874,
-1.1509089609167,-1.14077693624782,-1.1387449826738,-1.13761620192476,-1.13664674754946,
-1.13540496053058,-1.13340447718157,-1.12179763315987,-1.07665166829597,
-1.06498116947726,-1.06182806854527,-1.05990934406415,-1.05817228176482,
-1.05593866417192,-1.0523377462319,-1.02128847038156,-0.99921439171761,
-0.985397129056081,-0.983201275189535,-0.982037445569841,-0.981070650166951,
-0.979873115810151,-0.977515138225075,-0.956979575243179,-0.938135400528358,
-0.910909014803633,-0.90729617743362,-0.905058954014673,-0.903321407828912,
-0.901404498864463,-0.898259780108079,-0.886684572504042,-0.841450435640829,
-0.829790584165557,-0.827787253034824,-0.826544573236164,-0.825574986912447,
-0.824446694325688,-0.822417213456583,-0.812330511145004,-0.760740033014283,
-0.752959322364347,-0.750135735503812,-0.748473717906294,-0.746730245202018,
-0.744448107644155,-0.739530395502785,-0.719993577785478,-0.700304479201148,
-0.692744829615634,-0.674444666114828,-0.672045364984539,-0.67082338417009,
-0.669855511404987,-0.668712308239237,-0.666613144512317,-0.655160907085027,
-0.622128985326625,-0.599423901356696,-0.595888446229588,-0.593674532367159,
-0.591939897877407,-0.590010619389462,-0.586809317585552,-0.574578533715085,
-0.529755859061051,-0.518434217679464,-0.51644361040841,-0.515204813006902,
-0.514235625642115,-0.51310475904775,-0.511063140776853,-0.500753665586637,
-0.47607771616976,-0.443850004213923,-0.440268275712005,-0.438040324966765,
-0.436303864748369,-0.434381930471452,-0.431214606924753,-0.428814745063029),
 .UNSPECIFIED.);
#3745=B_SPLINE_CURVE_WITH_KNOTS('',3,(#262805,#262806,#262807,#262808,#262809,
#262810,#262811,#262812,#262813,#262814,#262815,#262816,#262817,#262818,
#262819,#262820,#262821,#262822,#262823,#262824,#262825,#262826,#262827,
#262828,#262829,#262830,#262831,#262832,#262833,#262834,#262835,#262836,
#262837,#262838,#262839,#262840,#262841,#262842,#262843,#262844,#262845,
#262846,#262847,#262848,#262849,#262850,#262851,#262852,#262853,#262854,
#262855,#262856,#262857,#262858,#262859,#262860,#262861,#262862,#262863,
#262864,#262865,#262866,#262867,#262868,#262869,#262870,#262871,#262872,
#262873,#262874,#262875,#262876,#262877,#262878,#262879,#262880,#262881,
#262882,#262883,#262884,#262885,#262886,#262887,#262888,#262889,#262890,
#262891,#262892,#262893,#262894,#262895,#262896,#262897,#262898,#262899,
#262900,#262901,#262902,#262903,#262904,#262905,#262906,#262907,#262908,
#262909,#262910,#262911,#262912,#262913,#262914,#262915,#262916,#262917,
#262918,#262919,#262920,#262921,#262922,#262923,#262924,#262925,#262926),
 .UNSPECIFIED.,.F.,.F.,(4,2,2,2,2,2,2,2,2,2,2,2,2,2,2,2,2,2,2,2,2,2,2,2,
2,2,2,2,2,2,2,2,2,2,2,2,2,2,2,2,2,2,2,2,2,2,2,2,2,2,2,2,2,2,2,2,2,2,2,2,
4),(-0.552689914471559,-0.53888975115974,-0.532400108143506,-0.53057076666574,
-0.529495072958845,-0.528530748836056,-0.527241537949452,-0.524360496763293,
-0.500036481612907,-0.46049347862675,-0.455179566002614,-0.453076441484597,
-0.451331350094738,-0.449544166024695,-0.446927402124816,-0.439839691691527,
-0.393568916420078,-0.3875384594585,-0.377187470630721,-0.375265767096169,
-0.374055704787414,-0.373099738071941,-0.371974335989141,-0.369918198958697,
-0.35898666783065,-0.331102666900535,-0.302707803616355,-0.299120914999867,
-0.296929560985358,-0.29521142880357,-0.293328599113484,-0.290268957309992,
-0.279352349096004,-0.238664867078956,-0.22189840475082,-0.219536406979483,
-0.21833108152658,-0.217375353232618,-0.216246123470924,-0.214172428977807,
-0.2028803267417,-0.170783060116345,-0.146910877916098,-0.143364167456997,
-0.141161004349836,-0.139508402273642,-0.137696628212653,-0.134811841798616,
-0.131396197404177,-0.124813631756402,-0.107873719505434,-0.0796227569997071,
-0.0767218008853527,-0.0658347608184948,-0.0638852368526337,-0.0626667194880947,
-0.0617100942006382,-0.0605908994118284,-0.0585636874731907,-0.0481976612391398,
-0.000460427453030607),.UNSPECIFIED.);
#3746=B_SPLINE_CURVE_WITH_KNOTS('',3,(#262927,#262928,#262929,#262930,#262931,
#262932,#262933,#262934,#262935,#262936,#262937,#262938,#262939,#262940,
#262941,#262942,#262943,#262944,#262945,#262946,#262947,#262948,#262949,
#262950,#262951,#262952,#262953,#262954,#262955,#262956,#262957,#262958,
#262959,#262960,#262961,#262962,#262963,#262964,#262965,#262966,#262967,
#262968,#262969,#262970,#262971,#262972,#262973,#262974,#262975,#262976,
#262977,#262978,#262979,#262980,#262981,#262982,#262983,#262984,#262985,
#262986,#262987,#262988,#262989,#262990,#262991,#262992,#262993,#262994,
#262995,#262996,#262997,#262998,#262999,#263000,#263001,#263002,#263003,
#263004,#263005,#263006,#263007,#263008,#263009,#263010,#263011,#263012,
#263013,#263014,#263015,#263016,#263017,#263018,#263019,#263020,#263021,
#263022,#263023,#263024,#263025,#263026,#263027,#263028,#263029,#263030,
#263031,#263032,#263033,#263034,#263035,#263036,#263037,#263038,#263039,
#263040,#263041,#263042,#263043,#263044,#263045,#263046,#263047,#263048,
#263049,#263050,#263051,#263052,#263053,#263054,#263055,#263056,#263057,
#263058,#263059,#263060,#263061,#263062),.UNSPECIFIED.,.F.,.F.,(4,2,2,2,
2,2,2,2,2,2,2,2,2,2,2,2,2,2,2,2,2,2,2,2,2,2,2,2,2,2,2,2,2,2,2,2,2,2,2,2,
2,2,2,2,2,2,2,2,2,2,2,2,2,2,2,2,2,2,2,2,2,2,2,2,2,2,2,4),(-1.96089412384933,
-1.95111155903107,-1.94850265213132,-1.94666474488551,-1.94507028877428,
-1.9433521571946,-1.94114768953157,-1.93641752020172,-1.92503904424038,
-1.88056367329849,-1.87034626162354,-1.86832878004811,-1.86721252977914,
-1.8662569084715,-1.86503773012088,-1.86308347264384,-1.85206509827071,
-1.83770757676361,-1.80870865413596,-1.79963963372712,-1.79535436650305,
-1.79187633694713,-1.78992194540447,-1.78990221780106,-1.78988203700657,
-1.7898677157285,-1.78985186170132,-1.78983431069918,-1.78981488097315,
-1.78979337143355,-1.78976955968104,-1.78974319987673,-1.78971402044014,
-1.78968172115807,-1.78964597111424,-1.78960640794046,-1.78956446585443,
-1.78791900619621,-1.78572815867446,-1.78221788674665,-1.75932877422693,
-1.72636109176316,-1.71494864461973,-1.71287105704267,-1.71174179620534,
-1.71078729155849,-1.70958510123825,-1.7071562035258,-1.68692282854521,
-1.65794663861193,-1.64602253305327,-1.64083169258486,-1.63674192889211,
-1.63463932995941,-1.63293582499214,-1.63098058859212,-1.62767255291511,
-1.61509178296851,-1.56899740250181,-1.55923719541135,-1.55724485420481,
-1.55613389366973,-1.55517737605739,-1.55395002106763,-1.5519691191632,
-1.5404106693462,-1.53736271093113,-1.53294839269393),.UNSPECIFIED.);
#3747=B_SPLINE_CURVE_WITH_KNOTS('',3,(#263064,#263065,#263066,#263067,#263068,
#263069,#263070,#263071,#263072,#263073,#263074,#263075,#263076,#263077,
#263078,#263079,#263080,#263081,#263082,#263083,#263084,#263085,#263086,
#263087,#263088,#263089,#263090,#263091,#263092,#263093,#263094,#263095,
#263096,#263097,#263098,#263099,#263100,#263101,#263102,#263103,#263104,
#263105,#263106,#263107,#263108,#263109,#263110,#263111,#263112,#263113,
#263114,#263115,#263116,#263117,#263118,#263119,#263120,#263121,#263122,
#263123,#263124,#263125,#263126,#263127,#263128,#263129,#263130,#263131,
#263132,#263133,#263134,#263135,#263136,#263137,#263138,#263139,#263140,
#263141,#263142,#263143,#263144,#263145,#263146,#263147,#263148,#263149,
#263150,#263151,#263152,#263153),.UNSPECIFIED.,.F.,.F.,(4,2,2,2,2,2,2,2,
2,2,2,2,2,2,2,2,2,2,2,2,2,2,2,2,2,2,2,2,2,2,2,2,2,2,2,2,2,2,2,2,2,2,2,2,
4),(-0.428814745063029,-0.419384051194465,-0.374312020670882,-0.362775961472799,
-0.36077873576139,-0.359537869855122,-0.358568407715106,-0.35743877054547,
-0.355403202231188,-0.345207637561813,-0.290954712936072,-0.285204544328501,
-0.282954478113407,-0.281317974791492,-0.279561106527703,-0.277192082929494,
-0.271793780344759,-0.264429701809189,-0.223841863174784,-0.207338123235077,
-0.204962172166002,-0.20374509890667,-0.20277741881434,-0.201630092163345,
-0.19951204909479,-0.187724636868222,-0.152155857672964,-0.132184242199741,
-0.128732946806886,-0.126544347386178,-0.124812314167515,-0.123191179605364,
-0.120452161792452,-0.111970009384296,-0.098435349243074,-0.0827281159732794,
-0.0536547568499099,-0.0499956923219941,-0.0485234403619077,-0.0476174481053444,
-0.0466102462583693,-0.0451326359295614,-0.0434381365216323,-0.0403279468249156,
-0.000459537648819321),.UNSPECIFIED.);
#3748=B_SPLINE_CURVE_WITH_KNOTS('',3,(#263154,#263155,#263156,#263157,#263158,
#263159,#263160,#263161,#263162,#263163,#263164,#263165,#263166,#263167,
#263168,#263169,#263170,#263171,#263172,#263173,#263174,#263175,#263176,
#263177,#263178,#263179,#263180,#263181,#263182,#263183,#263184,#263185,
#263186,#263187,#263188,#263189,#263190,#263191,#263192,#263193,#263194,
#263195,#263196,#263197,#263198,#263199,#263200,#263201,#263202,#263203,
#263204,#263205,#263206,#263207,#263208,#263209,#263210,#263211,#263212,
#263213,#263214,#263215,#263216,#263217,#263218,#263219,#263220,#263221,
#263222,#263223,#263224,#263225,#263226,#263227,#263228,#263229,#263230,
#263231,#263232,#263233,#263234,#263235,#263236,#263237,#263238,#263239,
#263240,#263241,#263242,#263243,#263244,#263245,#263246,#263247,#263248,
#263249,#263250,#263251,#263252,#263253,#263254,#263255,#263256,#263257,
#263258,#263259,#263260,#263261,#263262,#263263,#263264,#263265,#263266,
#263267,#263268,#263269,#263270,#263271,#263272,#263273,#263274,#263275,
#263276,#263277,#263278,#263279,#263280,#263281,#263282,#263283,#263284,
#263285,#263286,#263287,#263288,#263289,#263290,#263291,#263292,#263293,
#263294,#263295,#263296,#263297,#263298,#263299,#263300,#263301,#263302,
#263303,#263304,#263305,#263306,#263307,#263308,#263309,#263310,#263311),
 .UNSPECIFIED.,.F.,.F.,(4,2,2,2,2,2,2,2,2,2,2,2,2,2,2,2,2,2,2,2,2,2,2,2,
2,2,2,2,2,2,2,2,2,2,2,2,2,2,2,2,2,2,2,2,2,2,2,2,2,2,2,2,2,2,2,2,2,2,2,2,
2,2,2,2,2,2,2,2,2,2,2,2,2,2,2,2,2,2,4),(-1.96138640067636,-1.93753988811331,
-1.9347858843805,-1.93287862975556,-1.93125818038573,-1.92952663419017,
-1.92733775711206,-1.9238842242701,-1.90383011118708,-1.88467208175021,
-1.86572224418153,-1.85636031406122,-1.85436653906471,-1.85324635290098,
-1.85227621783515,-1.85102302911827,-1.84898360871115,-1.83653863245051,
-1.82420793444266,-1.79657328911591,-1.78645659687477,-1.78181289121297,
-1.77810059683376,-1.77606922209948,-1.77605156459095,-1.77603352605037,
-1.77601509612071,-1.77599626412166,-1.77597701903074,-1.77595734947769,
-1.77593724373396,-1.77591668969965,-1.7759017153278,-1.77588518123298,
-1.77586692113158,-1.77584675032292,-1.77582446354924,-1.77579983260114,
-1.77577260364895,-1.77574249427717,-1.7740117003386,-1.77183040437884,
-1.76840188487783,-1.74903144906365,-1.71113565698982,-1.70087873320262,
-1.69883710164232,-1.69770643395865,-1.6967375404316,-1.69549928731661,
-1.69350989305837,-1.68220373273009,-1.63742324512692,-1.62518482147105,
-1.62198345743502,-1.62005446898891,-1.61832030215597,-1.61610727052186,
-1.61257376540291,-1.58992043060127,-1.55553128405715,-1.54525395501303,
-1.54321451878416,-1.54208435228591,-1.54111544178994,-1.53987659062665,
-1.53788513192151,-1.52645427305035,-1.48153987435252,-1.46952895738865,
-1.46634695382225,-1.46442227887355,-1.46268729179309,-1.46046671294052,
-1.45690796299239,-1.43330769607406,-1.42727426603096,-1.41101453606077,
-1.40924613825003),.UNSPECIFIED.);
#3749=B_SPLINE_CURVE_WITH_KNOTS('',3,(#263316,#263317,#263318,#263319,#263320,
#263321,#263322,#263323,#263324,#263325,#263326,#263327,#263328,#263329,
#263330,#263331,#263332,#263333,#263334,#263335,#263336,#263337,#263338,
#263339,#263340,#263341,#263342,#263343,#263344,#263345,#263346,#263347,
#263348,#263349,#263350,#263351,#263352,#263353,#263354,#263355,#263356,
#263357,#263358,#263359,#263360,#263361,#263362,#263363,#263364,#263365,
#263366,#263367,#263368,#263369,#263370,#263371,#263372,#263373,#263374,
#263375,#263376,#263377,#263378,#263379,#263380,#263381,#263382,#263383,
#263384,#263385,#263386,#263387,#263388,#263389,#263390,#263391,#263392,
#263393,#263394,#263395,#263396,#263397,#263398,#263399,#263400,#263401,
#263402,#263403,#263404,#263405,#263406,#263407,#263408,#263409,#263410,
#263411,#263412,#263413,#263414,#263415,#263416,#263417,#263418,#263419,
#263420,#263421,#263422,#263423,#263424,#263425,#263426,#263427,#263428,
#263429,#263430,#263431,#263432,#263433,#263434,#263435,#263436,#263437,
#263438,#263439,#263440,#263441,#263442,#263443,#263444,#263445,#263446,
#263447,#263448,#263449,#263450,#263451,#263452,#263453,#263454,#263455,
#263456,#263457,#263458,#263459,#263460,#263461,#263462,#263463,#263464,
#263465,#263466,#263467,#263468,#263469,#263470,#263471,#263472,#263473,
#263474,#263475,#263476,#263477,#263478,#263479,#263480,#263481,#263482,
#263483,#263484,#263485,#263486,#263487,#263488,#263489,#263490,#263491,
#263492,#263493,#263494,#263495,#263496,#263497,#263498,#263499,#263500,
#263501,#263502,#263503,#263504,#263505,#263506,#263507,#263508,#263509,
#263510,#263511,#263512,#263513,#263514,#263515,#263516,#263517),
 .UNSPECIFIED.,.F.,.F.,(4,2,2,2,2,2,2,2,2,2,2,2,2,2,2,2,2,2,2,2,2,2,2,2,
2,2,2,2,2,2,2,2,2,2,2,2,2,2,2,2,2,2,2,2,2,2,2,2,2,2,2,2,2,2,2,2,2,2,2,2,
2,2,2,2,2,2,2,2,2,2,2,2,2,2,2,2,2,2,2,2,2,2,2,2,2,2,2,2,2,2,2,2,2,2,2,2,
2,2,2,2,4),(-1.53330080949059,-1.52159254796867,-1.47664759525897,-1.4669630218542,
-1.46497434560148,-1.46386384845335,-1.46290672904625,-1.46167730197349,
-1.4596905378569,-1.44804080654177,-1.44471429391727,-1.41574532421974,
-1.40017750437384,-1.39080676414814,-1.38790533353725,-1.38605774495952,
-1.38432886735644,-1.38206270143341,-1.37700185085542,-1.33528682306582,
-1.31403474741313,-1.31023234032745,-1.30879173320487,-1.30780111966584,
-1.30690386113888,-1.30543488734828,-1.30173165240809,-1.27768428593851,
-1.25371552928813,-1.2363216655335,-1.23280447697778,-1.23082168397464,
-1.22928963914096,-1.22729087249176,-1.22379664311068,-1.20869496133257,
-1.16453689073453,-1.15855892954612,-1.15461100738752,-1.15314889990963,
-1.15215380755164,-1.1512603274393,-1.14981228436362,-1.1462338597832,-1.11577257964686,
-1.08149420049871,-1.07745978983135,-1.0753674568826,-1.07382704747102,
-1.07191754302616,-1.06873575493666,-1.0578531235264,-1.00981463279724,
-0.99992678517416,-0.997925889411925,-0.996812466399093,-0.995855282278934,
-0.994628954763936,-0.992653341323871,-0.981227440979096,-0.946924784723346,
-0.925459695953636,-0.921987297428701,-0.919806601518821,-0.91809435768501,
-0.916186419610415,-0.913012682921902,-0.900806197381744,-0.856070903685685,
-0.844534686097814,-0.842553463558889,-0.841325382231954,-0.840367949075674,
-0.839255514548768,-0.837259541701091,-0.827460382585157,-0.78084310729135,
-0.768701190182902,-0.765396626744238,-0.763459880392136,-0.761923056867151,
-0.759868528409631,-0.756016999864159,-0.729207174076636,-0.700292104491353,
-0.688787835841003,-0.686808335251893,-0.685580834533151,-0.684623536883799,
-0.683510895240562,-0.681513658280727,-0.671689866488207,-0.624673574142428,
-0.612899164290838,-0.60962899683885,-0.607699933617078,-0.606162336667133,
-0.604097941730268,-0.600198706252296,-0.570807023845745,-0.552689914471559),
 .UNSPECIFIED.);
#3750=B_SPLINE_CURVE_WITH_KNOTS('',3,(#263518,#263519,#263520,#263521,#263522,
#263523,#263524,#263525,#263526,#263527,#263528,#263529,#263530,#263531,
#263532,#263533,#263534,#263535,#263536,#263537,#263538,#263539,#263540,
#263541,#263542,#263543,#263544,#263545,#263546,#263547,#263548,#263549,
#263550,#263551,#263552,#263553,#263554,#263555,#263556,#263557,#263558,
#263559,#263560,#263561,#263562,#263563,#263564,#263565,#263566,#263567,
#263568,#263569,#263570,#263571,#263572,#263573,#263574,#263575,#263576,
#263577,#263578,#263579,#263580,#263581,#263582,#263583,#263584,#263585,
#263586,#263587,#263588,#263589,#263590,#263591,#263592,#263593,#263594,
#263595,#263596,#263597,#263598,#263599,#263600,#263601,#263602,#263603,
#263604,#263605,#263606,#263607,#263608,#263609,#263610,#263611,#263612,
#263613,#263614,#263615,#263616,#263617,#263618,#263619,#263620,#263621,
#263622,#263623,#263624,#263625,#263626,#263627,#263628,#263629,#263630,
#263631,#263632,#263633,#263634,#263635,#263636,#263637,#263638,#263639,
#263640,#263641,#263642,#263643,#263644,#263645,#263646,#263647,#263648,
#263649,#263650,#263651,#263652,#263653,#263654,#263655,#263656,#263657,
#263658,#263659,#263660,#263661,#263662,#263663,#263664,#263665,#263666,
#263667,#263668,#263669,#263670,#263671,#263672,#263673,#263674,#263675,
#263676,#263677,#263678,#263679,#263680,#263681,#263682,#263683,#263684,
#263685,#263686,#263687,#263688,#263689,#263690,#263691,#263692,#263693,
#263694,#263695,#263696,#263697,#263698,#263699,#263700,#263701,#263702,
#263703,#263704,#263705,#263706,#263707,#263708,#263709,#263710,#263711,
#263712,#263713,#263714,#263715,#263716,#263717,#263718,#263719,#263720,
#263721,#263722,#263723,#263724,#263725,#263726,#263727,#263728,#263729,
#263730,#263731,#263732,#263733),.UNSPECIFIED.,.F.,.F.,(4,2,2,2,2,2,2,2,
2,2,2,2,2,2,2,2,2,2,2,2,2,2,2,2,2,2,2,2,2,2,2,2,2,2,2,2,2,2,2,2,2,2,2,2,
2,2,2,2,2,2,2,2,2,2,2,2,2,2,2,2,2,2,2,2,2,2,2,2,2,2,2,2,2,2,2,2,2,2,2,2,
2,2,2,2,2,2,2,2,2,2,2,2,2,2,2,2,2,2,2,2,2,2,2,2,2,2,2,4),(-1.40924613825003,
-1.3920519537756,-1.38843713478053,-1.38701450222455,-1.38601851466477,
-1.38510192842546,-1.38357216125138,-1.3795570674253,-1.32716665632577,
-1.31407280283506,-1.31080304653491,-1.30885928918695,-1.307128350303,-1.30494182932298,
-1.30149515233824,-1.28161275254803,-1.24596038299465,-1.23415948757676,
-1.23204493244415,-1.23089873850769,-1.22993155796098,-1.22871454209766,
-1.22625859743881,-1.2051057878793,-1.18747202730614,-1.15966435339812,
-1.15576054441803,-1.15367991458202,-1.1521241311294,-1.15016405427495,
-1.14682046847236,-1.13451740043587,-1.0972976844991,-1.08057210432518,
-1.07717501840345,-1.07578724475558,-1.07479775747969,-1.07387271879958,
-1.07256349998838,-1.06901431789296,-1.03779864425538,-1.00524303283522,
-1.00062654142338,-0.998402163997258,-0.996666889796871,-0.994744635944326,
-0.991573002092818,-0.981007710048585,-0.940162399629186,-0.923516464322548,
-0.92113669995226,-0.919919121268088,-0.918951805775388,-0.917805813678165,
-0.915692585290634,-0.903923752986713,-0.868518484606315,-0.848398529313525,
-0.84494310570162,-0.842753753679539,-0.841022301404241,-0.839079781735084,
-0.835816477618869,-0.822810515648565,-0.772058943781637,-0.766665744623544,
-0.764945847752992,-0.76388611663593,-0.76289884973839,-0.761524780739271,
-0.758212033382876,-0.742310720546279,-0.699906247952902,-0.698203275920053,
-0.690719006976775,-0.687939431922229,-0.686286135536854,-0.684539220746047,
-0.682231421352475,-0.677173187131354,-0.656538054041314,-0.629690228413494,
-0.62621626397745,-0.62340110628864,-0.611950210810646,-0.609957693600707,
-0.608718516635916,-0.607749563257127,-0.606619582794039,-0.604581082044936,
-0.594320577604801,-0.55698117440526,-0.537123528475259,-0.533677204871732,
-0.531490465100231,-0.529759086400023,-0.527814554446985,-0.524542821988681,
-0.511432114884855,-0.458825837099145,-0.454946198874758,-0.453437467580887,
-0.452524675142581,-0.451524617678329,-0.450082421968034,-0.446342958476149,
-0.440801141483845,-0.428888128758527),.UNSPECIFIED.);
#3751=B_SPLINE_CURVE_WITH_KNOTS('',3,(#263739,#263740,#263741,#263742,#263743,
#263744,#263745,#263746,#263747,#263748,#263749,#263750,#263751,#263752,
#263753,#263754,#263755,#263756,#263757,#263758,#263759,#263760,#263761,
#263762,#263763,#263764,#263765,#263766,#263767,#263768,#263769,#263770,
#263771,#263772,#263773,#263774,#263775,#263776,#263777,#263778,#263779,
#263780,#263781,#263782,#263783,#263784,#263785,#263786,#263787,#263788,
#263789,#263790,#263791,#263792,#263793,#263794,#263795,#263796,#263797,
#263798,#263799,#263800,#263801,#263802,#263803,#263804,#263805,#263806,
#263807,#263808,#263809,#263810,#263811,#263812,#263813,#263814,#263815,
#263816,#263817,#263818,#263819,#263820,#263821,#263822,#263823,#263824,
#263825,#263826,#263827,#263828,#263829,#263830,#263831,#263832,#263833,
#263834,#263835,#263836,#263837,#263838,#263839,#263840,#263841,#263842,
#263843,#263844,#263845,#263846,#263847,#263848,#263849,#263850,#263851,
#263852,#263853,#263854,#263855,#263856,#263857,#263858,#263859,#263860,
#263861,#263862,#263863,#263864),.UNSPECIFIED.,.F.,.F.,(4,2,2,2,2,2,2,2,
2,2,2,2,2,2,2,2,2,2,2,2,2,2,2,2,2,2,2,2,2,2,2,2,2,2,2,2,2,2,2,2,2,2,2,2,
2,2,2,2,2,2,2,2,2,2,2,2,2,2,2,2,2,2,4),(-0.552732293014681,-0.544526721663612,
-0.521443127730424,-0.517925922747745,-0.5157319163145,-0.514018367597968,
-0.512118361653583,-0.508979738586424,-0.497183324147925,-0.452203697215895,
-0.440469805914575,-0.43847540222017,-0.437243463969527,-0.436285818214354,
-0.435176337211476,-0.433193446836002,-0.423615724010117,-0.379792803641223,
-0.365017697019254,-0.361545767081861,-0.359551883937695,-0.357865478456037,
-0.355813896294542,-0.351975627845191,-0.325740108391654,-0.30091888290929,
-0.295160809780153,-0.284650279422643,-0.282720365838429,-0.281507920630911,
-0.280551937044157,-0.279428689091944,-0.277382012164753,-0.26663441544752,
-0.23971069293146,-0.233652170519376,-0.21007357601036,-0.206543318400608,
-0.204345337128094,-0.202631243555407,-0.200733247313348,-0.197866419508975,
-0.187762297764411,-0.170302907495981,-0.139921321040147,-0.12903834759887,
-0.127089311294619,-0.125871068529074,-0.12491463882738,-0.124010201867978,
-0.122297285983923,-0.116174002758719,-0.105061876475186,-0.0866783339072084,
-0.0544456451986642,-0.0509002231849731,-0.0486976846775913,-0.0469830271232924,
-0.0450874495901178,-0.043132183430273,-0.0402378723461658,-0.0350321380960057,
-0.000460216426560407),.UNSPECIFIED.);
#3752=B_SPLINE_CURVE_WITH_KNOTS('',3,(#263865,#263866,#263867,#263868,#263869,
#263870,#263871,#263872,#263873,#263874,#263875,#263876,#263877,#263878,
#263879,#263880,#263881,#263882,#263883,#263884,#263885,#263886,#263887,
#263888,#263889,#263890,#263891,#263892,#263893,#263894,#263895,#263896,
#263897,#263898,#263899,#263900,#263901,#263902,#263903,#263904,#263905,
#263906,#263907,#263908,#263909,#263910,#263911,#263912,#263913,#263914,
#263915,#263916,#263917,#263918,#263919,#263920,#263921,#263922,#263923,
#263924,#263925,#263926,#263927,#263928,#263929,#263930,#263931,#263932,
#263933,#263934,#263935,#263936,#263937,#263938,#263939,#263940,#263941,
#263942,#263943,#263944,#263945,#263946,#263947,#263948,#263949,#263950,
#263951,#263952,#263953,#263954,#263955,#263956,#263957,#263958,#263959,
#263960,#263961,#263962,#263963,#263964,#263965,#263966,#263967,#263968,
#263969,#263970),.UNSPECIFIED.,.F.,.F.,(4,2,2,2,2,2,2,2,2,2,2,2,2,2,2,2,
2,2,2,2,2,2,2,2,2,2,2,2,2,2,2,2,2,2,2,2,2,2,2,2,2,2,2,2,2,2,2,2,2,2,2,2,
4),(-1.9612255480559,-1.9405886767412,-1.93449603501467,-1.9328157050967,
-1.93169950834601,-1.93079315603296,-1.9298381208837,-1.9286341750782,-1.92619823164976,
-1.90289450440463,-1.88481491118963,-1.86346440347446,-1.85697678295479,
-1.85502137317573,-1.853125879729,-1.85141214521489,-1.84921197455577,-1.84567274751162,
-1.82169278466138,-1.79359873747615,-1.78347439452138,-1.77772095940746,
-1.77607827153416,-1.77517551457198,-1.77421878708292,-1.77299240711089,
-1.77101548031275,-1.75954648192973,-1.7568303040546,-1.71866896826405,
-1.70838918172379,-1.70152094424652,-1.69889082756806,-1.69710149112821,
-1.69535964781507,-1.69326688571293,-1.68801440987397,-1.64790795331707,
-1.62548139028703,-1.62158071654605,-1.62012579467928,-1.61913242424126,
-1.61823807761331,-1.6167840945605,-1.61316835477589,-1.58349695362429,
-1.54839982601569,-1.54442996702593,-1.54235142620455,-1.5406485568595,
-1.53867290759651,-1.53527858671223,-1.53330080949059),.UNSPECIFIED.);
#3753=B_SPLINE_CURVE_WITH_KNOTS('',3,(#263972,#263973,#263974,#263975,#263976,
#263977,#263978,#263979,#263980,#263981,#263982,#263983,#263984,#263985,
#263986,#263987,#263988,#263989,#263990,#263991,#263992,#263993,#263994,
#263995,#263996,#263997,#263998,#263999,#264000,#264001,#264002,#264003,
#264004,#264005,#264006,#264007,#264008,#264009,#264010,#264011,#264012,
#264013,#264014,#264015,#264016,#264017,#264018,#264019,#264020,#264021,
#264022,#264023,#264024,#264025,#264026,#264027,#264028,#264029,#264030,
#264031,#264032,#264033,#264034,#264035,#264036,#264037,#264038,#264039,
#264040,#264041,#264042,#264043,#264044,#264045,#264046,#264047,#264048,
#264049,#264050,#264051,#264052,#264053,#264054,#264055,#264056,#264057,
#264058,#264059,#264060,#264061),.UNSPECIFIED.,.F.,.F.,(4,2,2,2,2,2,2,2,
2,2,2,2,2,2,2,2,2,2,2,2,2,2,2,2,2,2,2,2,2,2,2,2,2,2,2,2,2,2,2,2,2,2,2,2,
4),(-0.428888128758527,-0.396149256973793,-0.380951640173066,-0.377423098483843,
-0.375401050325071,-0.37369311932673,-0.371617937666183,-0.367742421211991,
-0.341347888932855,-0.312612316858321,-0.300671760432889,-0.298653579684501,
-0.297406587066225,-0.296436814460417,-0.295311952691367,-0.293297545098321,
-0.283470482356494,-0.236637361538213,-0.22480588070762,-0.221505587000739,
-0.219554666063805,-0.217997194006659,-0.215902750986338,-0.211934654893356,
-0.179779493763917,-0.170684231586507,-0.145326264716195,-0.142930477393819,
-0.141709332279537,-0.14079593250481,-0.139696882183857,-0.137819208491731,
-0.135464995242747,-0.13051150020455,-0.115748856860529,-0.109306850298441,
-0.0728741192258072,-0.0714380750948244,-0.0668166219952595,-0.0645909335809879,
-0.0628551140711278,-0.0609327435162668,-0.0577620471575559,-0.0458865390397537,
-0.000459688585513052),.UNSPECIFIED.);
#3754=B_SPLINE_CURVE_WITH_KNOTS('',3,(#264062,#264063,#264064,#264065,#264066,
#264067,#264068,#264069),.UNSPECIFIED.,.F.,.F.,(4,1,1,1,1,4),(53.4070751110266,
53.5034432466949,54.5007770973516,55.4981109480084,56.4954447986652,56.945832495276),
 .UNSPECIFIED.);
#3755=B_SPLINE_CURVE_WITH_KNOTS('',3,(#264074,#264075,#264076,#264077,#264078,
#264079,#264080,#264081,#264082,#264083,#264084,#264085,#264086,#264087,
#264088,#264089,#264090,#264091,#264092,#264093,#264094,#264095,#264096,
#264097,#264098,#264099,#264100,#264101,#264102,#264103,#264104,#264105,
#264106,#264107,#264108,#264109,#264110,#264111,#264112,#264113,#264114,
#264115,#264116,#264117,#264118,#264119,#264120,#264121,#264122,#264123,
#264124,#264125,#264126,#264127,#264128,#264129,#264130,#264131,#264132,
#264133,#264134,#264135,#264136,#264137,#264138,#264139,#264140,#264141,
#264142,#264143,#264144,#264145,#264146,#264147,#264148,#264149,#264150,
#264151,#264152,#264153,#264154,#264155,#264156,#264157,#264158,#264159,
#264160,#264161,#264162,#264163,#264164,#264165,#264166,#264167,#264168,
#264169,#264170,#264171,#264172,#264173,#264174,#264175,#264176,#264177,
#264178,#264179,#264180,#264181,#264182,#264183,#264184,#264185,#264186,
#264187,#264188,#264189,#264190,#264191,#264192,#264193,#264194,#264195,
#264196,#264197,#264198,#264199,#264200,#264201,#264202,#264203,#264204,
#264205,#264206,#264207,#264208,#264209,#264210,#264211,#264212,#264213,
#264214,#264215,#264216,#264217,#264218,#264219,#264220,#264221,#264222,
#264223,#264224,#264225,#264226,#264227,#264228,#264229,#264230,#264231,
#264232,#264233,#264234,#264235,#264236,#264237,#264238,#264239,#264240,
#264241,#264242,#264243,#264244,#264245,#264246,#264247,#264248,#264249,
#264250,#264251,#264252,#264253,#264254,#264255,#264256,#264257,#264258,
#264259,#264260,#264261,#264262,#264263,#264264,#264265,#264266,#264267,
#264268,#264269,#264270,#264271,#264272,#264273,#264274,#264275,#264276,
#264277,#264278,#264279,#264280,#264281,#264282,#264283,#264284,#264285,
#264286,#264287,#264288,#264289,#264290,#264291),.UNSPECIFIED.,.F.,.F.,
(4,2,2,2,2,2,2,2,2,2,2,2,2,2,2,2,2,2,2,2,2,2,2,2,2,2,2,2,2,2,2,2,2,2,2,
2,2,2,2,2,2,2,2,2,2,2,2,2,2,2,2,2,2,2,2,2,2,2,2,2,2,2,2,2,2,2,2,2,2,2,2,
2,2,2,2,2,2,2,2,2,2,2,2,2,2,2,2,2,2,2,2,2,2,2,2,2,2,2,2,2,2,2,2,2,2,2,2,
2,4),(-1.53316853732264,-1.53081551367157,-1.52829084480876,-1.52706928721019,
-1.52611296467185,-1.52499723132008,-1.52303781081447,-1.51485342291321,
-1.50942856401873,-1.48169382206184,-1.45794391741066,-1.45253568003227,
-1.4501832563714,-1.44844698515222,-1.44683569283706,-1.44462990550193,
-1.43904574362156,-1.39817851464175,-1.37701390324708,-1.37321933466248,
-1.37178004054277,-1.37078980634098,-1.36989248801421,-1.36842264584295,
-1.36471364553914,-1.34045277188475,-1.32019267977353,-1.3014102281572,
-1.29661684162022,-1.29437540733383,-1.29265616233146,-1.29101218394169,
-1.28820709096339,-1.28040554207598,-1.27861539451046,-1.22865904745447,
-1.21866694912144,-1.2166605332583,-1.21554606960949,-1.21458926533872,
-1.21336507234076,-1.21139606362848,-1.20010063816694,-1.15985315760856,
-1.149062141103,-1.1418599509632,-1.13922739024492,-1.13743718283085,-1.1356950984785,
-1.13360277770248,-1.12835537222977,-1.08817759759204,-1.0657892218717,
-1.06189109040472,-1.06043627986703,-1.05944272759548,-1.05854802071693,
-1.05709308175168,-1.05347312168424,-1.02392044270956,-0.988691601922453,
-0.984719498058419,-0.982640123242514,-0.98110121389413,-0.979183245198251,
-0.975962675272834,-0.963171081926161,-0.915239598309298,-0.907183750346714,
-0.905233996930918,-0.904120160524173,-0.903163093038548,-0.901937525843802,
-0.899394161783937,-0.896023821664812,-0.887723613756562,-0.846745637911942,
-0.832137863816986,-0.82867739227419,-0.826686111034553,-0.824999584999771,
-0.822945011256146,-0.819092559077852,-0.792221837291364,-0.763433265202599,
-0.751878661977455,-0.749896820952441,-0.748668693002376,-0.747711442688195,
-0.746599472408422,-0.744604948270223,-0.73482556557149,-0.688490548923068,
-0.676113404013373,-0.672820556945495,-0.670867815562935,-0.669162483627626,
-0.667052468962199,-0.662931603590999,-0.630222737197789,-0.598212380874071,
-0.594697593893947,-0.5932601949988,-0.592279972204606,-0.591262586112446,
-0.589696083200367,-0.584970014082902,-0.577337491191725,-0.552732293014681),
 .UNSPECIFIED.);
#3756=B_SPLINE_CURVE_WITH_KNOTS('',3,(#264293,#264294,#264295,#264296,#264297,
#264298,#264299),.UNSPECIFIED.,.F.,.F.,(4,1,1,1,4),(56.945832495276,57.4927786493219,
58.4901124999787,59.4874463506355,59.6902604182062),.UNSPECIFIED.);
#3757=B_SPLINE_CURVE_WITH_KNOTS('',3,(#264300,#264301,#264302,#264303,#264304,
#264305,#264306,#264307,#264308,#264309,#264310,#264311,#264312,#264313,
#264314,#264315,#264316,#264317,#264318,#264319,#264320,#264321,#264322,
#264323,#264324,#264325,#264326,#264327,#264328,#264329,#264330,#264331,
#264332,#264333,#264334,#264335,#264336,#264337,#264338,#264339,#264340,
#264341,#264342,#264343,#264344,#264345,#264346,#264347,#264348,#264349,
#264350,#264351,#264352,#264353,#264354,#264355,#264356,#264357,#264358,
#264359,#264360,#264361,#264362,#264363,#264364,#264365,#264366,#264367,
#264368,#264369,#264370,#264371,#264372,#264373,#264374,#264375,#264376,
#264377,#264378,#264379,#264380,#264381,#264382,#264383,#264384,#264385,
#264386,#264387,#264388,#264389,#264390,#264391,#264392,#264393,#264394,
#264395,#264396,#264397,#264398,#264399,#264400,#264401,#264402,#264403,
#264404,#264405,#264406,#264407,#264408,#264409,#264410,#264411,#264412,
#264413,#264414,#264415,#264416,#264417,#264418,#264419,#264420,#264421),
 .UNSPECIFIED.,.F.,.F.,(4,2,2,2,2,2,2,2,2,2,2,2,2,2,2,2,2,2,2,2,2,2,2,2,
2,2,2,2,2,2,2,2,2,2,2,2,2,2,2,2,2,2,2,2,2,2,2,2,2,2,2,2,2,2,2,2,2,2,2,2,
4),(-1.96243636638787,-1.92873122880033,-1.92345762837139,-1.92052619707091,
-1.91854583558166,-1.9166258280168,-1.91488875034608,-1.91265671532101,
-1.90906163714298,-1.87746944506871,-1.85890238795916,-1.84755329411216,
-1.84132627277157,-1.83959618940266,-1.83867922969657,-1.83771059374843,
-1.83647975383564,-1.83451568587979,-1.82365391048351,-1.79366833211531,
-1.77602800307227,-1.76582801244604,-1.76291983695349,-1.761000548976,-1.75926327589006,
-1.75702980606436,-1.75342998659544,-1.72231437695619,-1.6967274153731,
-1.68622469363991,-1.684172509338,-1.68303928435714,-1.68207024185141,-1.68083442756679,
-1.67885396290855,-1.66766359560826,-1.62300014774661,-1.61476393451037,
-1.60887748613216,-1.60642521992754,-1.60465369139878,-1.60303605252178,
-1.60086137152891,-1.5955571477268,-1.55689061586263,-1.53341901218345,
-1.52941447228155,-1.52793282012685,-1.52692472107987,-1.52601933081797,
-1.52455070023411,-1.52091379352729,-1.4914888424095,-1.45724411427105,
-1.45261175712674,-1.45038355295896,-1.44864697895625,-1.44672500409201,
-1.44355781116524,-1.43304437783208,-1.41001614483363),.UNSPECIFIED.);
#3758=B_SPLINE_CURVE_WITH_KNOTS('',3,(#264427,#264428,#264429,#264430,#264431,
#264432,#264433,#264434),.UNSPECIFIED.,.F.,.F.,(4,1,1,1,1,4),(65.9734457253858,
66.179042922154,67.1767749221439,68.1745069221338,69.1722389221237,69.5126852782938),
 .UNSPECIFIED.);
#3759=B_SPLINE_CURVE_WITH_KNOTS('',3,(#264435,#264436,#264437,#264438,#264439,
#264440,#264441,#264442,#264443,#264444,#264445,#264446,#264447,#264448,
#264449,#264450,#264451,#264452,#264453,#264454,#264455,#264456,#264457,
#264458,#264459,#264460,#264461,#264462,#264463,#264464,#264465,#264466,
#264467,#264468,#264469,#264470,#264471,#264472,#264473,#264474,#264475,
#264476,#264477,#264478,#264479,#264480,#264481,#264482,#264483,#264484,
#264485,#264486,#264487,#264488,#264489,#264490,#264491,#264492,#264493,
#264494,#264495,#264496,#264497,#264498,#264499,#264500,#264501,#264502,
#264503,#264504,#264505,#264506,#264507,#264508,#264509,#264510,#264511,
#264512,#264513,#264514,#264515,#264516,#264517,#264518,#264519,#264520,
#264521,#264522,#264523,#264524,#264525,#264526),.UNSPECIFIED.,.F.,.F.,
(4,2,2,2,2,2,2,2,2,2,2,2,2,2,2,2,2,2,2,2,2,2,2,2,2,2,2,2,2,2,2,2,2,2,2,
2,2,2,2,2,2,2,2,2,2,4),(-1.961444596389,-1.92797148288741,-1.92278945608443,
-1.91990484640394,-1.91795405212732,-1.91606186451412,-1.91434777267141,
-1.91214246088824,-1.90858535102273,-1.8767036812167,-1.85739092388925,
-1.84669630513855,-1.84073661592871,-1.83902964573844,-1.838127458231,-1.83717068021997,
-1.83594181942472,-1.83395621803567,-1.8223179290392,-1.81894017432273,
-1.7832616839657,-1.76686003893351,-1.76305502428428,-1.76097758804903,
-1.75943954900616,-1.75752193746662,-1.75430021824994,-1.74301168724916,
-1.69546421731742,-1.68560972645131,-1.68361155175159,-1.68249911130248,
-1.68154243712619,-1.68031632930557,-1.67834023413792,-1.66688733707865,
-1.62228310176853,-1.60995361789867,-1.60677116269319,-1.60486209074503,
-1.60315142157672,-1.60097627903177,-1.59751980084343,-1.57656646232454,
-1.53415504157875,-1.53316853732264),.UNSPECIFIED.);
#3760=B_SPLINE_CURVE_WITH_KNOTS('',3,(#264527,#264528,#264529,#264530,#264531,
#264532,#264533,#264534,#264535,#264536,#264537,#264538,#264539,#264540,
#264541,#264542,#264543,#264544,#264545,#264546,#264547,#264548,#264549,
#264550,#264551,#264552,#264553,#264554,#264555,#264556,#264557,#264558,
#264559,#264560,#264561,#264562,#264563,#264564,#264565,#264566,#264567,
#264568,#264569,#264570,#264571,#264572,#264573,#264574,#264575,#264576,
#264577,#264578,#264579,#264580,#264581,#264582,#264583,#264584,#264585,
#264586,#264587,#264588,#264589,#264590,#264591,#264592,#264593,#264594,
#264595,#264596,#264597,#264598,#264599,#264600,#264601,#264602,#264603,
#264604,#264605,#264606,#264607,#264608,#264609,#264610,#264611,#264612,
#264613,#264614,#264615,#264616,#264617,#264618,#264619,#264620,#264621,
#264622,#264623,#264624,#264625,#264626,#264627,#264628,#264629,#264630,
#264631,#264632,#264633,#264634,#264635,#264636,#264637,#264638,#264639,
#264640,#264641,#264642,#264643,#264644,#264645,#264646,#264647,#264648,
#264649,#264650,#264651,#264652,#264653,#264654,#264655,#264656,#264657,
#264658,#264659,#264660,#264661,#264662,#264663,#264664,#264665,#264666,
#264667,#264668,#264669,#264670,#264671,#264672,#264673,#264674,#264675,
#264676,#264677,#264678,#264679,#264680,#264681,#264682,#264683,#264684,
#264685,#264686,#264687,#264688,#264689,#264690,#264691,#264692,#264693,
#264694,#264695,#264696,#264697,#264698,#264699,#264700,#264701,#264702,
#264703,#264704,#264705,#264706,#264707,#264708,#264709,#264710,#264711,
#264712,#264713,#264714,#264715,#264716,#264717,#264718,#264719,#264720,
#264721,#264722,#264723,#264724,#264725,#264726,#264727,#264728,#264729,
#264730,#264731,#264732,#264733,#264734,#264735,#264736,#264737,#264738,
#264739,#264740),.UNSPECIFIED.,.F.,.F.,(4,2,2,2,2,2,2,2,2,2,2,2,2,2,2,2,
2,2,2,2,2,2,2,2,2,2,2,2,2,2,2,2,2,2,2,2,2,2,2,2,2,2,2,2,2,2,2,2,2,2,2,2,
2,2,2,2,2,2,2,2,2,2,2,2,2,2,2,2,2,2,2,2,2,2,2,2,2,2,2,2,2,2,2,2,2,2,2,2,
2,2,2,2,2,2,2,2,2,2,2,2,2,2,2,2,2,2,4),(-1.41001614483363,-1.39225513613191,
-1.38065973984924,-1.376421476499,-1.37337426020363,-1.37204543874264,-1.37106530782206,
-1.36998605563137,-1.36817943629454,-1.36203867008771,-1.31665184071068,
-1.30546121509686,-1.29804410829108,-1.29536097604857,-1.29354398226279,
-1.29178143809269,-1.28967105923585,-1.28441160664946,-1.24422366100781,
-1.22191465916282,-1.21800451467768,-1.21653661861258,-1.21553132303034,
-1.21462342845557,-1.21314125408657,-1.2094237054695,-1.18299421871368,
-1.15699808566829,-1.14362689665319,-1.14033431707254,-1.13838466794598,
-1.13665322620501,-1.13447244007195,-1.1310473254096,-1.11180204486799,
-1.0829950071077,-1.06567440482489,-1.06221660516705,-1.0608184682476,-1.05982666920218,
-1.05890354238529,-1.05760267469567,-1.05411253706449,-1.0215481111743,
-0.990108237000798,-0.985560031238105,-0.983348127396927,-0.981613437844249,
-0.979682416626492,-0.976474271423693,-0.964166657090143,-0.919378789263433,
-0.908088046324516,-0.906102513316289,-0.904865121885621,-0.903895881267495,
-0.902763618270317,-0.900716164076702,-0.890303726744272,-0.865149581939166,
-0.833523248932328,-0.82992857594515,-0.827696523580716,-0.825959282040161,
-0.824038940180786,-0.82087991374156,-0.809148784368028,-0.764003561856856,
-0.752415027705897,-0.750414971150481,-0.749173129940184,-0.748203418330058,
-0.74707408132241,-0.745040510205677,-0.734886271452398,-0.681757543573821,
-0.675163483334289,-0.672521483364338,-0.670893665926067,-0.669130160021742,
-0.666723713955244,-0.661110981536136,-0.65336761074115,-0.608218489812041,
-0.596625602948298,-0.594625417977323,-0.593383576453568,-0.592413916530432,
-0.591284699580605,-0.58925149209545,-0.579102229562427,-0.526085175969397,
-0.519410126806953,-0.516754505253086,-0.51512423603572,-0.513362699944944,
-0.510967210879639,-0.505417874058922,-0.497787274338213,-0.452528348348435,
-0.440852928976274,-0.438848619395513,-0.437605575058572,-0.436635862464329,
-0.435507605037135,-0.433478634774835,-0.429017715179976),.UNSPECIFIED.);
#3761=B_SPLINE_CURVE_WITH_KNOTS('',3,(#264746,#264747,#264748,#264749,#264750,
#264751,#264752,#264753,#264754,#264755,#264756,#264757,#264758,#264759,
#264760,#264761,#264762,#264763,#264764,#264765,#264766,#264767,#264768,
#264769,#264770,#264771,#264772,#264773,#264774,#264775,#264776,#264777,
#264778,#264779,#264780,#264781,#264782,#264783,#264784,#264785,#264786,
#264787,#264788,#264789,#264790,#264791,#264792,#264793,#264794,#264795,
#264796,#264797,#264798,#264799,#264800,#264801,#264802,#264803,#264804,
#264805,#264806,#264807,#264808,#264809,#264810,#264811,#264812,#264813,
#264814,#264815,#264816,#264817,#264818,#264819,#264820,#264821,#264822,
#264823,#264824,#264825,#264826,#264827,#264828,#264829,#264830,#264831,
#264832,#264833,#264834,#264835,#264836,#264837,#264838,#264839,#264840,
#264841,#264842,#264843,#264844,#264845,#264846,#264847,#264848,#264849,
#264850,#264851,#264852,#264853,#264854,#264855,#264856,#264857,#264858,
#264859,#264860,#264861,#264862,#264863,#264864,#264865,#264866,#264867,
#264868,#264869,#264870,#264871),.UNSPECIFIED.,.F.,.F.,(4,2,2,2,2,2,2,2,
2,2,2,2,2,2,2,2,2,2,2,2,2,2,2,2,2,2,2,2,2,2,2,2,2,2,2,2,2,2,2,2,2,2,2,2,
2,2,2,2,2,2,2,2,2,2,2,2,2,2,2,2,2,2,4),(-0.552641378009195,-0.540781647137896,
-0.535233133886294,-0.533032912503839,-0.531422649836385,-0.52968460282655,
-0.527324657016637,-0.521876101476598,-0.497779811663714,-0.46874954818786,
-0.457145285080451,-0.455160901218344,-0.453932041216431,-0.452974768855968,
-0.451863402712269,-0.449871499929522,-0.440136434336113,-0.394461432118698,
-0.381469688671962,-0.378130061027684,-0.376166611317052,-0.37446233434963,
-0.372366938580967,-0.36831721201437,-0.363190775635023,-0.351482642274451,
-0.32729370208429,-0.301784826599703,-0.299412922280656,-0.298205739899813,
-0.297250214851437,-0.296123186985811,-0.294058582447317,-0.282944942472228,
-0.266795587014716,-0.229180882302226,-0.226243562427763,-0.222989964282724,
-0.220876195390768,-0.219170702282629,-0.217220919246893,-0.213855274221538,
-0.199045190378691,-0.165314507066046,-0.146155579505983,-0.143765941310845,
-0.14255499193553,-0.141650281186909,-0.14056871296215,-0.138730277521751,
-0.136430803410411,-0.131616844833293,-0.117441525137364,-0.0975863550034039,
-0.071226326335163,-0.0676477925026255,-0.0654354924249702,-0.0637198074745481,
-0.0618297391996461,-0.0587357918562178,-0.0474420888279364,-0.00213289938031032,
-0.000460482320649901),.UNSPECIFIED.);
#3762=B_SPLINE_CURVE_WITH_KNOTS('',3,(#264872,#264873,#264874,#264875,#264876,
#264877,#264878),.UNSPECIFIED.,.F.,.F.,(4,1,1,1,4),(69.5126852782938,70.1699709221136,
71.1677029221035,72.1654349220934,72.2566310325654),.UNSPECIFIED.);
#3763=B_SPLINE_CURVE_WITH_KNOTS('',3,(#264880,#264881,#264882,#264883,#264884,
#264885,#264886,#264887,#264888,#264889,#264890,#264891,#264892,#264893,
#264894,#264895,#264896,#264897,#264898,#264899,#264900,#264901,#264902,
#264903,#264904,#264905,#264906,#264907,#264908,#264909,#264910,#264911,
#264912,#264913,#264914,#264915,#264916,#264917,#264918,#264919,#264920,
#264921,#264922,#264923,#264924,#264925,#264926,#264927,#264928,#264929,
#264930,#264931,#264932,#264933,#264934,#264935,#264936,#264937,#264938,
#264939,#264940,#264941,#264942,#264943,#264944,#264945,#264946,#264947,
#264948,#264949,#264950,#264951,#264952,#264953,#264954,#264955,#264956,
#264957,#264958,#264959,#264960,#264961,#264962,#264963,#264964,#264965,
#264966,#264967,#264968,#264969,#264970,#264971,#264972,#264973,#264974,
#264975),.UNSPECIFIED.,.F.,.F.,(4,2,2,2,2,2,2,2,2,2,2,2,2,2,2,2,2,2,2,2,
2,2,2,2,2,2,2,2,2,2,2,2,2,2,2,2,2,2,2,2,2,2,2,2,2,2,2,4),(-0.429017715179976,
-0.423403954564558,-0.372093636464055,-0.371467916069141,-0.363935600074779,
-0.36114832096306,-0.35949318514206,-0.357746339610022,-0.355442024540115,
-0.350405215805828,-0.329945432012915,-0.299875940613244,-0.296777314673502,
-0.285136710570285,-0.283134449509169,-0.281892124955387,-0.280922614338927,
-0.279794177764365,-0.27776386747213,-0.267660917996547,-0.215698368926963,
-0.208215183171208,-0.205435522846508,-0.203782043248226,-0.2020348374104,
-0.199726488907313,-0.194849116939424,-0.188279414534909,-0.171459642434667,
-0.139926095878457,-0.129347031904572,-0.127397757769541,-0.126171526198963,
-0.12520338666699,-0.124285898634109,-0.122556375741725,-0.116271228017277,
-0.104772083128549,-0.0867835856361286,-0.054851439527974,-0.0512731530003628,
-0.0490463646925665,-0.0473102104214056,-0.0453880027651295,-0.0434042427038484,
-0.0404641866046306,-0.0351677589407834,-0.000459409169756657),
 .UNSPECIFIED.);
#3764=B_SPLINE_CURVE_WITH_KNOTS('',3,(#264976,#264977,#264978,#264979,#264980,
#264981,#264982,#264983,#264984,#264985,#264986,#264987,#264988,#264989,
#264990,#264991,#264992,#264993,#264994,#264995,#264996,#264997,#264998,
#264999,#265000,#265001,#265002,#265003,#265004,#265005,#265006,#265007,
#265008,#265009,#265010,#265011,#265012,#265013,#265014,#265015,#265016,
#265017,#265018,#265019,#265020,#265021,#265022,#265023,#265024,#265025,
#265026,#265027,#265028,#265029,#265030,#265031,#265032,#265033,#265034,
#265035,#265036,#265037,#265038,#265039,#265040,#265041,#265042,#265043,
#265044,#265045,#265046,#265047,#265048,#265049,#265050,#265051,#265052,
#265053,#265054,#265055,#265056,#265057,#265058,#265059,#265060,#265061,
#265062,#265063,#265064,#265065,#265066,#265067,#265068,#265069,#265070,
#265071,#265072,#265073,#265074,#265075,#265076,#265077,#265078,#265079,
#265080,#265081,#265082,#265083,#265084,#265085,#265086,#265087,#265088,
#265089,#265090,#265091,#265092,#265093,#265094,#265095,#265096,#265097,
#265098,#265099,#265100,#265101,#265102,#265103),.UNSPECIFIED.,.F.,.F.,
(4,2,2,2,2,2,2,2,2,2,2,2,2,2,2,2,2,2,2,2,2,2,2,2,2,2,2,2,2,2,2,2,2,2,2,
2,2,2,2,2,2,2,2,2,2,2,2,2,2,2,2,2,2,2,2,2,2,2,2,2,2,2,2,4),(-1.9613855033268,
-1.93508066903094,-1.93337100487253,-1.93223724462457,-1.93131827400647,
-1.93035078653872,-1.92913344926569,-1.92667706329812,-1.90390393165469,
-1.88653238443498,-1.86423273947521,-1.85757798830135,-1.85558998602215,
-1.85366482028954,-1.8519294907388,-1.84970861207128,-1.84614966324438,
-1.82256534237624,-1.79473233025188,-1.78421876084219,-1.77829710629275,
-1.77662505331695,-1.77570968411641,-1.77474065236175,-1.77350165179664,
-1.77150996373025,-1.76007810444082,-1.75727703441271,-1.71286707877054,
-1.70283977167619,-1.69995003840863,-1.69802883628234,-1.69629280596669,
-1.69406508448902,-1.69048302890886,-1.65857609141762,-1.6336258765276,
-1.62325880519486,-1.62121441620711,-1.62008313366752,-1.61911428191488,
-1.61787681546689,-1.61589008651907,-1.60455953972686,-1.55975854910694,
-1.55170004044053,-1.54591199706385,-1.54347662521593,-1.54170864427399,
-1.54008827538572,-1.53790090273535,-1.53252035872154,-1.49477884010259,
-1.4787812579919,-1.46769367164578,-1.46561227852245,-1.46447303630186,
-1.4635050383444,-1.46227846622805,-1.46032769443297,-1.4497138330154,-1.44423865138944,
-1.4283803357202,-1.40944749342716),.UNSPECIFIED.);
#3765=B_SPLINE_CURVE_WITH_KNOTS('',3,(#265108,#265109,#265110,#265111,#265112,
#265113,#265114,#265115,#265116,#265117,#265118,#265119,#265120,#265121,
#265122,#265123,#265124,#265125,#265126,#265127,#265128,#265129,#265130,
#265131,#265132,#265133,#265134,#265135,#265136,#265137,#265138,#265139,
#265140,#265141,#265142,#265143,#265144,#265145,#265146,#265147,#265148,
#265149,#265150,#265151,#265152,#265153,#265154,#265155,#265156,#265157,
#265158,#265159,#265160,#265161,#265162,#265163,#265164,#265165,#265166,
#265167,#265168,#265169,#265170,#265171,#265172,#265173,#265174,#265175,
#265176,#265177,#265178,#265179,#265180,#265181,#265182,#265183,#265184,
#265185,#265186,#265187,#265188,#265189,#265190,#265191,#265192,#265193,
#265194,#265195,#265196,#265197,#265198,#265199,#265200,#265201,#265202,
#265203,#265204,#265205,#265206,#265207,#265208,#265209,#265210,#265211,
#265212,#265213,#265214,#265215,#265216,#265217,#265218,#265219,#265220,
#265221,#265222,#265223,#265224,#265225,#265226,#265227,#265228,#265229,
#265230,#265231,#265232,#265233,#265234,#265235,#265236,#265237,#265238,
#265239,#265240,#265241,#265242,#265243,#265244,#265245,#265246,#265247,
#265248,#265249,#265250,#265251,#265252,#265253,#265254,#265255,#265256,
#265257,#265258,#265259,#265260,#265261,#265262,#265263,#265264,#265265,
#265266,#265267,#265268,#265269,#265270,#265271,#265272,#265273,#265274,
#265275,#265276,#265277,#265278,#265279,#265280,#265281,#265282,#265283,
#265284,#265285,#265286,#265287,#265288,#265289,#265290,#265291,#265292,
#265293,#265294,#265295,#265296,#265297,#265298,#265299,#265300,#265301,
#265302,#265303,#265304,#265305),.UNSPECIFIED.,.F.,.F.,(4,2,2,2,2,2,2,2,
2,2,2,2,2,2,2,2,2,2,2,2,2,2,2,2,2,2,2,2,2,2,2,2,2,2,2,2,2,2,2,2,2,2,2,2,
2,2,2,2,2,2,2,2,2,2,2,2,2,2,2,2,2,2,2,2,2,2,2,2,2,2,2,2,2,2,2,2,2,2,2,2,
2,2,2,2,2,2,2,2,2,2,2,2,2,2,2,2,2,2,4),(-1.53325260190294,-1.52242625781252,
-1.48177886514756,-1.47086017453636,-1.46780092593041,-1.46591851637425,
-1.46420088380173,-1.46201032461387,-1.45842504024837,-1.43095190227417,
-1.41237905773923,-1.39351591331953,-1.38992727548277,-1.3885192097765,
-1.38753497521275,-1.38663092516517,-1.38537376267351,-1.38212302487428,
-1.34719406708861,-1.31674100278451,-1.31282744470658,-1.3107603111279,
-1.30922271351678,-1.30729631638362,-1.30403717291467,-1.29237441448629,
-1.24521662778124,-1.23538294069485,-1.23338530251937,-1.23227267368181,
-1.23131553050119,-1.23008842373757,-1.22810995124981,-1.21662131896378,
-1.17196319845482,-1.16386055173013,-1.15806179030878,-1.15564266123855,
-1.15389423402223,-1.152297255681,-1.15014990003729,-1.14491154101944,-1.10012040650216,
-1.08196253870356,-1.07844036785622,-1.07704260017154,-1.07606021935041,
-1.07515363447275,-1.0738872246539,-1.07057422673835,-1.03620841936487,
-1.00527831725009,-1.00135811733981,-0.999289405848374,-0.997751447789123,
-0.995825657793389,-0.992570120563453,-0.980948402575276,-0.935993394489741,
-0.924277015074869,-0.922284629007087,-0.921053281444805,-0.920095670542737,
-0.918985743835248,-0.917000877428164,-0.907390088228778,-0.863464588742385,
-0.848811456111164,-0.845347801952433,-0.843355779121299,-0.841669260767104,
-0.839615475745699,-0.835766856509783,-0.809074557497812,-0.780038311021655,
-0.768540107948506,-0.766561054460697,-0.765333755002252,-0.764376564786102,
-0.763263991075153,-0.761266736608362,-0.751439973374302,-0.704364513561757,
-0.692649275263066,-0.689384952530542,-0.687457303238192,-0.685919709229434,
-0.68385386778967,-0.679947071754868,-0.650029385346784,-0.616943745121949,
-0.612101152449112,-0.610305936431538,-0.609237880818621,-0.608271458095834,
-0.606967092242401,-0.604001370873981,-0.575274682149757,-0.552641378009195),
 .UNSPECIFIED.);
#3766=B_SPLINE_CURVE_WITH_KNOTS('',3,(#265306,#265307,#265308,#265309,#265310,
#265311,#265312,#265313,#265314,#265315,#265316,#265317,#265318,#265319,
#265320,#265321,#265322,#265323,#265324,#265325,#265326,#265327,#265328,
#265329,#265330,#265331,#265332,#265333,#265334,#265335,#265336,#265337,
#265338,#265339,#265340,#265341,#265342,#265343,#265344,#265345,#265346,
#265347,#265348,#265349,#265350,#265351,#265352,#265353,#265354,#265355,
#265356,#265357,#265358,#265359,#265360,#265361,#265362,#265363,#265364,
#265365,#265366,#265367,#265368,#265369,#265370,#265371,#265372,#265373,
#265374,#265375,#265376,#265377,#265378,#265379,#265380,#265381,#265382,
#265383,#265384,#265385,#265386,#265387,#265388,#265389,#265390,#265391,
#265392,#265393,#265394,#265395,#265396,#265397,#265398,#265399,#265400,
#265401,#265402,#265403,#265404,#265405,#265406,#265407,#265408,#265409,
#265410,#265411,#265412,#265413,#265414,#265415,#265416,#265417,#265418,
#265419,#265420,#265421,#265422,#265423,#265424,#265425,#265426,#265427,
#265428,#265429,#265430,#265431,#265432,#265433,#265434,#265435,#265436,
#265437,#265438,#265439,#265440,#265441,#265442,#265443,#265444,#265445,
#265446,#265447,#265448,#265449,#265450,#265451,#265452,#265453,#265454,
#265455,#265456,#265457,#265458,#265459,#265460,#265461,#265462,#265463,
#265464,#265465,#265466,#265467,#265468,#265469,#265470,#265471,#265472,
#265473,#265474,#265475,#265476,#265477,#265478,#265479,#265480,#265481,
#265482,#265483,#265484,#265485,#265486,#265487,#265488,#265489,#265490,
#265491,#265492,#265493,#265494,#265495,#265496,#265497,#265498,#265499,
#265500,#265501,#265502,#265503,#265504,#265505,#265506,#265507,#265508,
#265509,#265510,#265511,#265512,#265513,#265514,#265515,#265516,#265517,
#265518,#265519,#265520,#265521,#265522,#265523,#265524,#265525,#265526,
#265527,#265528,#265529,#265530,#265531),.UNSPECIFIED.,.F.,.F.,(4,2,2,2,
2,2,2,2,2,2,2,2,2,2,2,2,2,2,2,2,2,2,2,2,2,2,2,2,2,2,2,2,2,2,2,2,2,2,2,2,
2,2,2,2,2,2,2,2,2,2,2,2,2,2,2,2,2,2,2,2,2,2,2,2,2,2,2,2,2,2,2,2,2,2,2,2,
2,2,2,2,2,2,2,2,2,2,2,2,2,2,2,2,2,2,2,2,2,2,2,2,2,2,2,2,2,2,2,2,2,2,2,2,
4),(-1.40944749342716,-1.39341217372204,-1.38939766731936,-1.38729366204968,
-1.38556862571454,-1.38356557824273,-1.38011938465242,-1.36609943832109,
-1.32538159487734,-1.3122440987815,-1.31007350367566,-1.30891513195081,
-1.30794829523266,-1.30674499624919,-1.30487078438903,-1.29559965722073,
-1.29127871094758,-1.26053787408271,-1.23952164303054,-1.23441501349005,
-1.23209829312566,-1.23034993719488,-1.22869918768659,-1.22593331459503,
-1.21854390903335,-1.21704073759394,-1.21538752143635,-1.1693810998379,
-1.15658942778471,-1.15443209770918,-1.15327643803154,-1.15230932218284,
-1.15110248956195,-1.14921704640649,-1.13976994424371,-1.11041363984206,
-1.08199531445636,-1.07807853968733,-1.07599461170209,-1.07443790241986,
-1.07247868709675,-1.06914158920952,-1.05691984351894,-1.05133094855607,
-1.01302705981138,-1.00091160154793,-0.998782282123513,-0.997632546935002,
-0.996665028114012,-0.995450931621492,-0.993541842385773,-0.983699521102618,
-0.98124865528132,-0.941498567575853,-0.925828771845722,-0.922572260369002,
-0.920443216336071,-0.918716304428376,-0.916731810120721,-0.913279383494423,
-0.897556901347341,-0.858707869884544,-0.853930048011537,-0.845115480821931,
-0.843092397721518,-0.841953294967731,-0.840984927385365,-0.839757263246613,
-0.837250028538095,-0.833950546160351,-0.825938029607814,-0.78911792581559,
-0.770464119929121,-0.767061437680973,-0.764887579109853,-0.763156956403062,
-0.761203256613833,-0.757891696030379,-0.744263910891211,-0.717368451479347,
-0.706878905392441,-0.690104605546518,-0.687722266993808,-0.686503839252694,
-0.685536096684031,-0.684389889831171,-0.682277023130487,-0.670530922458198,
-0.635328285677444,-0.631298277055792,-0.616016094628711,-0.611528431110734,
-0.609328508283789,-0.60759529638834,-0.605657690912757,-0.60241909369536,
-0.589736925929533,-0.543252636462868,-0.533888644662619,-0.532008087521358,
-0.530802633179374,-0.529835395091906,-0.528678123796034,-0.526513859732013,
-0.513552848733347,-0.464748666546273,-0.45722288305549,-0.454436655911459,
-0.452781775497855,-0.451034928629009,-0.448730155429978,-0.44369049343699,
-0.428866937278303),.UNSPECIFIED.);
#3767=B_SPLINE_CURVE_WITH_KNOTS('',3,(#265537,#265538,#265539,#265540,#265541,
#265542,#265543,#265544),.UNSPECIFIED.,.F.,.F.,(4,1,1,1,1,4),(84.8230078218033,
85.135950921962,86.1336829219519,87.1314149219419,88.1291469219317,88.3624145086695),
 .UNSPECIFIED.);
#3768=B_SPLINE_CURVE_WITH_KNOTS('',3,(#265545,#265546,#265547,#265548,#265549,
#265550,#265551,#265552,#265553,#265554,#265555,#265556,#265557,#265558,
#265559,#265560,#265561,#265562,#265563,#265564,#265565,#265566,#265567,
#265568,#265569,#265570,#265571,#265572,#265573,#265574,#265575,#265576,
#265577,#265578,#265579,#265580,#265581,#265582,#265583,#265584,#265585,
#265586,#265587,#265588,#265589,#265590,#265591,#265592,#265593,#265594,
#265595,#265596,#265597,#265598,#265599,#265600,#265601,#265602,#265603,
#265604,#265605,#265606,#265607,#265608,#265609,#265610,#265611,#265612,
#265613,#265614,#265615,#265616,#265617,#265618,#265619,#265620,#265621,
#265622,#265623,#265624,#265625,#265626,#265627,#265628,#265629,#265630,
#265631,#265632,#265633,#265634,#265635,#265636,#265637,#265638,#265639,
#265640,#265641,#265642,#265643,#265644,#265645,#265646,#265647,#265648,
#265649,#265650,#265651,#265652,#265653,#265654),.UNSPECIFIED.,.F.,.F.,
(4,2,2,2,2,2,2,2,2,2,2,2,2,2,2,2,2,2,2,2,2,2,2,2,2,2,2,2,2,2,2,2,2,2,2,
2,2,2,2,2,2,2,2,2,2,2,2,2,2,2,2,2,2,2,4),(-1.96159473691807,-1.93952011890684,
-1.93669937117787,-1.93477445021545,-1.93316774712418,-1.93146325880569,
-1.92936606932586,-1.92616665351387,-1.91082409396615,-1.89905984713847,
-1.8674817293113,-1.8580727791185,-1.85609269705463,-1.85498391836113,-1.85402631928996,
-1.85279372303083,-1.85079686979542,-1.8389624032588,-1.82584346183981,
-1.80018120789963,-1.7888770727583,-1.78387374741379,-1.77993815215203,
-1.77787545239181,-1.77617037939151,-1.77421343351222,-1.77090272207376,
-1.75831472800199,-1.75338403115019,-1.72272699557335,-1.70463561341793,
-1.70131815135195,-1.69989926638815,-1.69891283746,-1.69801097724501,-1.6965182063791,
-1.69266984937646,-1.69125473828562,-1.68334346359076,-1.63827022124228,
-1.62666187963963,-1.62353982285794,-1.62164354216759,-1.61992929429808,
-1.61772874126219,-1.61418946509796,-1.5903040320498,-1.55819333146133,
-1.5468999912072,-1.5448266421068,-1.5436976940666,-1.54274225646772,-1.54153737067804,
-1.53917644967491,-1.53325260190294),.UNSPECIFIED.);
#3769=B_SPLINE_CURVE_WITH_KNOTS('',3,(#265656,#265657,#265658,#265659,#265660,
#265661,#265662,#265663,#265664,#265665,#265666,#265667,#265668,#265669,
#265670,#265671,#265672,#265673,#265674,#265675,#265676,#265677,#265678,
#265679,#265680,#265681,#265682,#265683,#265684,#265685,#265686,#265687,
#265688,#265689,#265690,#265691,#265692,#265693,#265694,#265695,#265696,
#265697,#265698,#265699,#265700,#265701,#265702,#265703,#265704,#265705,
#265706,#265707,#265708,#265709,#265710,#265711,#265712,#265713,#265714,
#265715,#265716,#265717,#265718,#265719,#265720,#265721,#265722,#265723,
#265724,#265725,#265726,#265727,#265728,#265729,#265730,#265731,#265732,
#265733,#265734,#265735,#265736,#265737,#265738,#265739,#265740,#265741,
#265742,#265743,#265744,#265745,#265746,#265747,#265748,#265749,#265750,
#265751,#265752,#265753),.UNSPECIFIED.,.F.,.F.,(4,2,2,2,2,2,2,2,2,2,2,2,
2,2,2,2,2,2,2,2,2,2,2,2,2,2,2,2,2,2,2,2,2,2,2,2,2,2,2,2,2,2,2,2,2,2,2,2,
4),(-0.428866937278303,-0.42320732256552,-0.393569772979738,-0.39004470234996,
-0.378428445471691,-0.376427486662957,-0.37518558566945,-0.374216154435437,
-0.373087520844399,-0.371056144111157,-0.360932709214475,-0.308487302947778,
-0.307042580648101,-0.300995483957519,-0.298444783013751,-0.29683383005651,
-0.295056685101948,-0.292572473219648,-0.286488250833324,-0.277887406244554,
-0.226685948116768,-0.222177314863061,-0.220255388560647,-0.219139444607701,
-0.218265494335097,-0.217056418430856,-0.214642103968728,-0.188419145878424,
-0.150319415248422,-0.1449704987427,-0.142788118420279,-0.141168598663867,
-0.139462964355577,-0.137282324520504,-0.134745664090128,-0.130465186969945,
-0.121454504365611,-0.0929685813714968,-0.0802272210570355,-0.0748265394073259,
-0.0666376690446946,-0.0646614887242369,-0.0635331093220079,-0.0625636295368711,
-0.0613213308404195,-0.0587396392407635,-0.0553147526601607,-0.0130298331063881,
-0.000459572696942942),.UNSPECIFIED.);
#3770=B_SPLINE_CURVE_WITH_KNOTS('',3,(#265754,#265755,#265756,#265757,#265758,
#265759,#265760,#265761,#265762,#265763,#265764,#265765,#265766,#265767,
#265768,#265769,#265770,#265771,#265772,#265773,#265774,#265775,#265776,
#265777,#265778,#265779,#265780,#265781,#265782,#265783,#265784,#265785,
#265786,#265787,#265788,#265789,#265790,#265791,#265792,#265793,#265794,
#265795,#265796,#265797,#265798,#265799,#265800,#265801,#265802,#265803,
#265804,#265805,#265806,#265807,#265808,#265809,#265810,#265811,#265812,
#265813,#265814,#265815,#265816,#265817,#265818,#265819,#265820,#265821,
#265822,#265823,#265824,#265825,#265826,#265827,#265828,#265829,#265830,
#265831,#265832,#265833,#265834,#265835,#265836,#265837,#265838,#265839,
#265840,#265841,#265842,#265843,#265844,#265845,#265846,#265847,#265848,
#265849,#265850,#265851,#265852,#265853,#265854,#265855,#265856,#265857,
#265858,#265859,#265860,#265861,#265862,#265863,#265864,#265865,#265866,
#265867,#265868,#265869,#265870,#265871,#265872,#265873),.UNSPECIFIED.,
 .F.,.F.,(4,2,2,2,2,2,2,2,2,2,2,2,2,2,2,2,2,2,2,2,2,2,2,2,2,2,2,2,2,2,2,
2,2,2,2,2,2,2,2,2,2,2,2,2,2,2,2,2,2,2,2,2,2,2,2,2,2,2,2,4),(-1.96219528177021,
-1.95370052296186,-1.95103360796627,-1.94916151951121,-1.94754439225189,
-1.94587978338466,-1.94366525906557,-1.94012731532003,-1.92844967070181,
-1.88451417505534,-1.87289382871881,-1.87078677855098,-1.86964188147441,
-1.86867413363559,-1.86745429605936,-1.8650650684701,-1.84799858690288,
-1.81631719942177,-1.80410433588762,-1.79880954429901,-1.79587002244979,
-1.793299657197,-1.79152463932424,-1.7897579642343,-1.78763081253416,-1.78226529849946,
-1.74309513282626,-1.7200193782832,-1.71604681797504,-1.71456991018287,
-1.71356287136283,-1.71265678169625,-1.71118391709184,-1.70752106346708,
-1.67873805535211,-1.64390249333053,-1.63926596891892,-1.63703712684833,
-1.63530065824877,-1.63337941390567,-1.63021484440797,-1.61972326742647,
-1.57893502942534,-1.56340571911286,-1.56013208784729,-1.55876437831452,
-1.55777804298384,-1.55671550896419,-1.55498369372193,-1.54949434249468,
-1.50338177345386,-1.49215146453805,-1.48471520369557,-1.48202964566041,
-1.48021230505982,-1.47845040914041,-1.47634198436901,-1.47109369720167,
-1.43081744864416,-1.40984887783672),.UNSPECIFIED.);
#3771=B_SPLINE_CURVE_WITH_KNOTS('',3,(#265879,#265880,#265881,#265882,#265883,
#265884,#265885,#265886,#265887,#265888,#265889,#265890,#265891,#265892,
#265893,#265894,#265895,#265896,#265897,#265898,#265899,#265900,#265901,
#265902,#265903,#265904,#265905,#265906,#265907,#265908,#265909,#265910,
#265911,#265912,#265913,#265914,#265915,#265916,#265917,#265918,#265919,
#265920,#265921,#265922,#265923,#265924,#265925,#265926,#265927,#265928,
#265929,#265930,#265931,#265932,#265933,#265934,#265935,#265936,#265937,
#265938,#265939,#265940,#265941,#265942,#265943,#265944,#265945,#265946,
#265947,#265948,#265949,#265950,#265951,#265952,#265953,#265954,#265955,
#265956,#265957,#265958,#265959,#265960,#265961,#265962,#265963,#265964,
#265965,#265966,#265967,#265968,#265969,#265970,#265971,#265972,#265973,
#265974,#265975,#265976,#265977,#265978,#265979,#265980,#265981,#265982,
#265983,#265984,#265985,#265986,#265987,#265988,#265989,#265990,#265991,
#265992,#265993,#265994,#265995,#265996,#265997,#265998,#265999,#266000,
#266001,#266002,#266003,#266004,#266005,#266006,#266007,#266008,#266009,
#266010),.UNSPECIFIED.,.F.,.F.,(4,2,2,2,2,2,2,2,2,2,2,2,2,2,2,2,2,2,2,2,
2,2,2,2,2,2,2,2,2,2,2,2,2,2,2,2,2,2,2,2,2,2,2,2,2,2,2,2,2,2,2,2,2,2,2,2,
2,2,2,2,2,2,2,2,2,4),(-0.552515408999662,-0.550562583847312,-0.5485691073841,
-0.546883270987737,-0.544832656399416,-0.540997026342526,-0.514829200587625,
-0.487392633236008,-0.484148625212631,-0.47368318569461,-0.471756079770518,
-0.470544685020202,-0.469589052214475,-0.468465659835004,-0.466417306951006,
-0.455627025855104,-0.428473796370327,-0.399235265646561,-0.395645839730378,
-0.393454291221716,-0.391736822411601,-0.389855552778546,-0.386800318915267,
-0.375919967445849,-0.335228676595158,-0.318443097765979,-0.316090930433491,
-0.314888045426701,-0.313932893317432,-0.312802747807837,-0.310723237087268,
-0.299291011094534,-0.26620728990669,-0.243436705492283,-0.239928481705376,
-0.237737428683071,-0.236024553178534,-0.234123619485329,-0.230979565084765,
-0.219114615318666,-0.174190110811827,-0.162490105068495,-0.160326700915107,
-0.159154776059503,-0.158218456666738,-0.157094050736013,-0.155872990397383,
-0.153938599055296,-0.150166470411612,-0.140378836319171,-0.11862545123976,
-0.0878648919629591,-0.084302197542259,-0.0820946500710547,-0.0803795818287885,
-0.0784870873031429,-0.0753820560426363,-0.063965122043383,-0.018740854008447,
-0.0103186347474948,-0.00570293104685778,-0.00409665056792943,-0.00317259876107923,
-0.0022540795145313,-0.00121835079695155,-0.000484202096339386),
 .UNSPECIFIED.);
#3772=B_SPLINE_CURVE_WITH_KNOTS('',3,(#266011,#266012,#266013,#266014,#266015,
#266016),.UNSPECIFIED.,.F.,.F.,(4,1,1,4),(88.3624145086695,89.1268789219216,
90.1246109219115,91.1061847853801),.UNSPECIFIED.);
#3773=B_SPLINE_CURVE_WITH_KNOTS('',3,(#266017,#266018,#266019,#266020,#266021,
#266022,#266023,#266024,#266025,#266026,#266027,#266028,#266029,#266030,
#266031,#266032,#266033,#266034,#266035,#266036,#266037,#266038,#266039,
#266040,#266041,#266042,#266043,#266044,#266045,#266046,#266047,#266048,
#266049,#266050,#266051,#266052,#266053,#266054,#266055,#266056,#266057,
#266058,#266059,#266060,#266061,#266062,#266063,#266064,#266065,#266066,
#266067,#266068,#266069,#266070,#266071,#266072,#266073,#266074,#266075,
#266076,#266077,#266078,#266079,#266080,#266081,#266082,#266083,#266084,
#266085,#266086,#266087,#266088,#266089,#266090,#266091,#266092,#266093,
#266094,#266095,#266096,#266097,#266098,#266099,#266100,#266101,#266102,
#266103,#266104,#266105,#266106,#266107,#266108,#266109,#266110,#266111,
#266112,#266113,#266114,#266115,#266116,#266117,#266118,#266119,#266120,
#266121,#266122,#266123,#266124,#266125,#266126,#266127,#266128,#266129,
#266130,#266131,#266132,#266133,#266134,#266135,#266136,#266137,#266138,
#266139,#266140,#266141,#266142,#266143,#266144,#266145,#266146,#266147,
#266148,#266149,#266150,#266151,#266152,#266153,#266154,#266155,#266156,
#266157,#266158,#266159,#266160,#266161,#266162,#266163,#266164,#266165,
#266166,#266167,#266168,#266169,#266170,#266171,#266172,#266173,#266174,
#266175,#266176,#266177,#266178,#266179,#266180,#266181,#266182,#266183,
#266184,#266185,#266186,#266187,#266188,#266189,#266190,#266191,#266192,
#266193,#266194,#266195,#266196,#266197,#266198,#266199,#266200,#266201,
#266202,#266203,#266204,#266205,#266206,#266207,#266208,#266209,#266210,
#266211,#266212,#266213,#266214,#266215,#266216,#266217,#266218,#266219,
#266220,#266221,#266222,#266223,#266224,#266225,#266226,#266227,#266228,
#266229,#266230,#266231,#266232,#266233,#266234,#266235,#266236),
 .UNSPECIFIED.,.F.,.F.,(4,2,2,2,2,2,2,2,2,2,2,2,2,2,2,2,2,2,2,2,2,2,2,2,
2,2,2,2,2,2,2,2,2,2,2,2,2,2,2,2,2,2,2,2,2,2,2,2,2,2,2,2,2,2,2,2,2,2,2,2,
2,2,2,2,2,2,2,2,2,2,2,2,2,2,2,2,2,2,2,2,2,2,2,2,2,2,2,2,2,2,2,2,2,2,2,2,
2,2,2,2,2,2,2,2,2,2,2,2,2,4),(-1.40984887783672,-1.40858109118894,-1.40467723020394,
-1.40321037085499,-1.40220537363299,-1.40129743253415,-1.39981458330455,
-1.39609243885983,-1.37140866560196,-1.35938817646871,-1.33140447122275,
-1.32749555056619,-1.32541320021292,-1.32370482132622,-1.32168864233041,
-1.3181865089127,-1.30337769985326,-1.25918302244788,-1.25308002825821,
-1.24906041727865,-1.24757656543176,-1.24656799307939,-1.24566295435361,
-1.24419634518802,-1.24057167695035,-1.23902061351389,-1.18756430399654,
-1.17895522340259,-1.17286572874282,-1.17038045160242,-1.16860291337359,
-1.16699184729797,-1.16444150190383,-1.15839819515696,-1.10452286728443,
-1.0943374464735,-1.09230226256678,-1.09117265214809,-1.09020309048535,
-1.08896194864078,-1.08696400886707,-1.07541443221742,-1.03033748959946,
-1.0185435398649,-1.01537917837385,-1.01345774225161,-1.01172089414015,
-1.0094912778187,-1.00590444524125,-0.981178689891814,-0.951672077919365,
-0.939050690930436,-0.937003207722224,-0.935747283609764,-0.934776443434211,
-0.933657041478681,-0.931668500146943,-0.922282647414454,-0.900404865010337,
-0.867019850412069,-0.861414850269682,-0.859188866237729,-0.857558310418939,
-0.855796839911998,-0.853402109270118,-0.847857574366884,-0.84023561093515,
-0.794965376147343,-0.783282863548261,-0.781278104852778,-0.780034894991323,
-0.779065126994091,-0.777936889987388,-0.775908164871343,-0.765839114169796,
-0.714657205693773,-0.713806141586569,-0.706340538677844,-0.703563146092031,
-0.701909854653766,-0.700161992931681,-0.697851332971283,-0.692780254111559,
-0.672050503091122,-0.653164454804631,-0.638802024601857,-0.627540546591587,
-0.625556646775046,-0.624319843656763,-0.623350780780778,-0.622218397756811,
-0.620169910903498,-0.609733973074542,-0.584464527244917,-0.552991288534467,
-0.549396262463241,-0.547164277760831,-0.54542726420331,-0.54350735255492,
-0.540349444682187,-0.52862739641612,-0.483484264259973,-0.471893886236024,
-0.469893953694271,-0.468652245850116,-0.467682675238836,-0.466553544927272,
-0.464520450656246,-0.454370836409654,-0.428910700075966),.UNSPECIFIED.);
#3774=B_SPLINE_CURVE_WITH_KNOTS('',3,(#266241,#266242,#266243,#266244,#266245,
#266246,#266247,#266248,#266249,#266250,#266251,#266252,#266253,#266254,
#266255,#266256,#266257,#266258,#266259,#266260,#266261,#266262,#266263,
#266264,#266265,#266266,#266267,#266268,#266269,#266270,#266271,#266272,
#266273,#266274,#266275,#266276,#266277,#266278,#266279,#266280,#266281,
#266282,#266283,#266284,#266285,#266286,#266287,#266288,#266289,#266290,
#266291,#266292,#266293,#266294,#266295,#266296,#266297,#266298,#266299,
#266300,#266301,#266302,#266303,#266304,#266305,#266306,#266307,#266308,
#266309,#266310,#266311,#266312,#266313,#266314,#266315,#266316,#266317,
#266318,#266319,#266320,#266321,#266322,#266323,#266324,#266325,#266326,
#266327,#266328,#266329,#266330,#266331,#266332,#266333,#266334,#266335,
#266336,#266337,#266338,#266339,#266340,#266341,#266342,#266343,#266344,
#266345,#266346,#266347,#266348,#266349,#266350,#266351,#266352,#266353,
#266354,#266355,#266356,#266357,#266358,#266359,#266360,#266361,#266362,
#266363,#266364,#266365,#266366,#266367,#266368,#266369,#266370,#266371,
#266372,#266373,#266374,#266375,#266376,#266377,#266378,#266379,#266380,
#266381,#266382,#266383,#266384,#266385,#266386,#266387,#266388,#266389,
#266390,#266391,#266392,#266393,#266394,#266395,#266396,#266397,#266398,
#266399,#266400,#266401,#266402,#266403,#266404,#266405,#266406,#266407,
#266408,#266409,#266410,#266411,#266412,#266413,#266414,#266415,#266416,
#266417,#266418,#266419,#266420,#266421,#266422,#266423,#266424,#266425,
#266426,#266427,#266428,#266429,#266430,#266431,#266432,#266433,#266434,
#266435,#266436,#266437,#266438,#266439,#266440,#266441,#266442,#266443,
#266444,#266445,#266446),.UNSPECIFIED.,.F.,.F.,(4,2,2,2,2,2,2,2,2,2,2,2,
2,2,2,2,2,2,2,2,2,2,2,2,2,2,2,2,2,2,2,2,2,2,2,2,2,2,2,2,2,2,2,2,2,2,2,2,
2,2,2,2,2,2,2,2,2,2,2,2,2,2,2,2,2,2,2,2,2,2,2,2,2,2,2,2,2,2,2,2,2,2,2,2,
2,2,2,2,2,2,2,2,2,2,2,2,2,2,2,2,2,2,4),(-1.53266505380209,-1.49849600946528,
-1.48710556072061,-1.48400384552523,-1.48211260898317,-1.48039818453306,
-1.47819076986197,-1.47462682072641,-1.44310439031065,-1.41776663031675,
-1.40734159687292,-1.40531233398729,-1.40419321469861,-1.40323739549041,
-1.40202086612147,-1.40007635986551,-1.38926663946939,-1.38631959813282,
-1.35898967925782,-1.33284789840875,-1.32901378318673,-1.3269637447182,
-1.32527825990125,-1.32328505662668,-1.31981327193128,-1.30502274815647,
-1.26118259451269,-1.25163844020031,-1.24965817781261,-1.24854960049733,
-1.24759236799536,-1.2463604944228,-1.24436530067272,-1.23255653475088,
-1.18751008388276,-1.17589193455821,-1.17276982708576,-1.17087400197217,
-1.1691604792869,-1.16696129398885,-1.16342511082118,-1.13956092599805,
-1.10744951032914,-1.09615858182613,-1.09408594157186,-1.09295740992581,
-1.09200234303678,-1.09079794799921,-1.08843805730691,-1.07169894648921,
-1.03107582275221,-1.02015010044846,-1.01709097560005,-1.01520906006167,
-1.01349215354584,-1.01130289670794,-1.00772054554375,-0.980581083968393,
-0.954060344302462,-0.949032867604237,-0.940444816007854,-0.938455393840801,
-0.937332869243849,-0.936377337611118,-0.935165264038896,-0.932688358816214,
-0.929429284737236,-0.921520707418623,-0.885700290016859,-0.865897153891311,
-0.862480793973977,-0.860317759163765,-0.858608361647581,-0.856692083254173,
-0.853477020028921,-0.840744123011053,-0.793470065872141,-0.784804104307314,
-0.782808672427906,-0.781684673243543,-0.780729109699587,-0.779518558209755,
-0.777049896147459,-0.749724337367329,-0.712925618763617,-0.707494981872777,
-0.705315060930709,-0.703710292484619,-0.701969196985548,-0.699588995927991,
-0.694019611656257,-0.686328468736558,-0.641267920883151,-0.6294629149485,
-0.627467387413243,-0.626235322541208,-0.625277945165936,-0.62416919491249,
-0.622188627486733,-0.612642294534342,-0.568820414856862,-0.554034479445235,
-0.552515408999662),.UNSPECIFIED.);
#3775=B_SPLINE_CURVE_WITH_KNOTS('',3,(#266448,#266449,#266450,#266451,#266452,
#266453,#266454,#266455,#266456,#266457,#266458,#266459,#266460,#266461,
#266462,#266463,#266464,#266465,#266466,#266467,#266468,#266469,#266470,
#266471,#266472,#266473,#266474,#266475,#266476,#266477,#266478,#266479,
#266480,#266481,#266482,#266483,#266484,#266485,#266486,#266487,#266488,
#266489,#266490,#266491,#266492,#266493,#266494,#266495,#266496,#266497,
#266498,#266499,#266500,#266501,#266502,#266503,#266504,#266505,#266506,
#266507,#266508,#266509,#266510,#266511,#266512,#266513,#266514,#266515,
#266516,#266517,#266518,#266519,#266520,#266521,#266522,#266523,#266524,
#266525,#266526,#266527,#266528,#266529,#266530,#266531,#266532,#266533,
#266534,#266535,#266536,#266537,#266538,#266539,#266540,#266541,#266542,
#266543,#266544,#266545),.UNSPECIFIED.,.F.,.F.,(4,2,2,2,2,2,2,2,2,2,2,2,
2,2,2,2,2,2,2,2,2,2,2,2,2,2,2,2,2,2,2,2,2,2,2,2,2,2,2,2,2,2,2,2,2,2,2,2,
4),(-0.428910700075966,-0.401327195880147,-0.394676408531252,-0.392024963494874,
-0.390395571031352,-0.388633668509475,-0.386235334247601,-0.380668695047072,
-0.373007130517893,-0.32778432842315,-0.316133126173067,-0.31413021888457,
-0.312887654141444,-0.311918061048298,-0.310789649379656,-0.308759681097413,
-0.298664753279152,-0.246895264192716,-0.239255997029793,-0.236453046160825,
-0.234794999368418,-0.233049746963605,-0.23075535519183,-0.225771710496655,
-0.205726179648854,-0.179684164004229,-0.160806562752999,-0.158408697854989,
-0.157199625455021,-0.156248431113482,-0.155335549346347,-0.153591087697067,
-0.147364149919041,-0.136098558475487,-0.09566174766719,-0.0845010069003123,
-0.0812663184104489,-0.0793296905778867,-0.0777698332817407,-0.0756540875679837,
-0.0715839632477447,-0.0372611061454265,-0.0151554489785241,-0.0104177429443904,
-0.00409972392282309,-0.00231064211441393,-0.00123989900939373,-0.000618795737507542,
-0.000459177337394708),.UNSPECIFIED.);
#3776=B_SPLINE_CURVE_WITH_KNOTS('',3,(#266546,#266547,#266548,#266549,#266550,
#266551,#266552,#266553,#266554,#266555,#266556,#266557,#266558,#266559,
#266560,#266561,#266562,#266563,#266564,#266565,#266566,#266567,#266568,
#266569,#266570,#266571,#266572,#266573,#266574,#266575,#266576,#266577,
#266578,#266579,#266580,#266581,#266582,#266583,#266584,#266585,#266586,
#266587,#266588,#266589,#266590,#266591,#266592,#266593,#266594,#266595,
#266596,#266597,#266598,#266599,#266600,#266601,#266602,#266603,#266604,
#266605,#266606,#266607,#266608,#266609,#266610,#266611,#266612,#266613,
#266614,#266615,#266616,#266617,#266618,#266619,#266620,#266621,#266622,
#266623,#266624,#266625,#266626,#266627,#266628,#266629,#266630,#266631,
#266632,#266633,#266634,#266635,#266636,#266637,#266638,#266639,#266640,
#266641,#266642,#266643,#266644,#266645,#266646,#266647,#266648,#266649,
#266650,#266651,#266652,#266653,#266654,#266655,#266656,#266657,#266658,
#266659,#266660,#266661,#266662,#266663,#266664,#266665,#266666,#266667,
#266668,#266669,#266670,#266671),.UNSPECIFIED.,.F.,.F.,(4,2,2,2,2,2,2,2,
2,2,2,2,2,2,2,2,2,2,2,2,2,2,2,2,2,2,2,2,2,2,2,2,2,2,2,2,2,2,2,2,2,2,2,2,
2,2,2,2,2,2,2,2,2,2,2,2,2,2,2,2,2,2,4),(-1.96154488249404,-1.96129893185349,
-1.96025239001222,-1.9579087962454,-1.94319819707872,-1.91410580065968,
-1.89310558206934,-1.88800192046861,-1.8856862811165,-1.8839386339106,-1.88228847468457,
-1.87952340142396,-1.87213479768615,-1.87094141939202,-1.82795747142864,
-1.81600109233696,-1.80952153450638,-1.80775354808749,-1.80683937008797,
-1.80593025890328,-1.80475301194569,-1.802498762158,-1.78919770031518,-1.76313605075455,
-1.7356378806577,-1.73174007341828,-1.72966065945942,-1.72795317045841,
-1.72593625957732,-1.72242835716419,-1.70751796603955,-1.66322895052082,
-1.65429374669277,-1.65233429275933,-1.65122159332096,-1.65025023090843,
-1.64900623071248,-1.64695283179287,-1.63415931018071,-1.60492299736787,
-1.58224770233286,-1.57693905252869,-1.5745862218616,-1.57283236788994,
-1.57119218814615,-1.56848112614209,-1.5614399657562,-1.50899688680722,
-1.49877950519643,-1.49674303261131,-1.49561336209561,-1.49464415928807,
-1.49340400723117,-1.49140867905184,-1.47990365604023,-1.43489257299263,
-1.42302041755802,-1.41984992196797,-1.4179275235888,-1.41619158153964,
-1.41396560084263,-1.41038966913363,-1.40945693535865),.UNSPECIFIED.);
#3777=B_SPLINE_CURVE_WITH_KNOTS('',3,(#266677,#266678,#266679,#266680,#266681,
#266682,#266683,#266684,#266685,#266686,#266687,#266688,#266689,#266690,
#266691,#266692,#266693,#266694,#266695,#266696,#266697,#266698,#266699,
#266700,#266701,#266702,#266703,#266704,#266705,#266706,#266707,#266708,
#266709,#266710,#266711,#266712,#266713,#266714,#266715,#266716,#266717,
#266718,#266719,#266720,#266721,#266722,#266723,#266724,#266725,#266726,
#266727,#266728,#266729,#266730,#266731,#266732,#266733,#266734,#266735,
#266736,#266737,#266738,#266739,#266740,#266741,#266742,#266743,#266744,
#266745,#266746,#266747,#266748,#266749,#266750,#266751,#266752,#266753,
#266754,#266755,#266756,#266757,#266758,#266759,#266760,#266761,#266762,
#266763,#266764,#266765,#266766,#266767,#266768,#266769,#266770,#266771,
#266772,#266773,#266774,#266775,#266776,#266777,#266778,#266779,#266780,
#266781,#266782,#266783,#266784,#266785,#266786,#266787,#266788,#266789,
#266790,#266791,#266792,#266793,#266794,#266795,#266796,#266797,#266798,
#266799,#266800,#266801,#266802,#266803,#266804,#266805,#266806,#266807,
#266808,#266809,#266810,#266811,#266812,#266813,#266814,#266815,#266816,
#266817,#266818,#266819,#266820,#266821,#266822,#266823,#266824),
 .UNSPECIFIED.,.F.,.F.,(4,2,2,2,2,2,2,2,2,2,2,2,2,2,2,2,2,2,2,2,2,2,2,2,
2,2,2,2,2,2,2,2,2,2,2,2,2,2,2,2,2,2,2,2,2,2,2,2,2,2,2,2,2,2,2,2,2,2,2,2,
2,2,2,2,2,2,2,2,2,2,2,2,2,4),(-0.552785672327454,-0.537478823530765,-0.535041105726873,
-0.533836357281231,-0.532880724479598,-0.53175118269923,-0.529675817416682,
-0.518346069941391,-0.485991210353301,-0.46239336053074,-0.458862174919824,
-0.456663746250476,-0.454949383812827,-0.453051171528342,-0.449921762038409,
-0.438236129923043,-0.393174928575462,-0.381380546581408,-0.37938490740365,
-0.378152473444212,-0.377194615256916,-0.376085086079105,-0.374102589276208,
-0.364536293915182,-0.320698355109572,-0.305912891806877,-0.302439747567133,
-0.300445349993075,-0.298758615846738,-0.296706764005296,-0.292868382674435,
-0.266655622928351,-0.238950353662178,-0.234067936368551,-0.225323902570269,
-0.223321968350755,-0.222196118729412,-0.221240135041514,-0.220030521840422,
-0.217568582065273,-0.19101014965597,-0.153296724498725,-0.15041593525838,
-0.147138819700689,-0.145017460068174,-0.143352928632042,-0.143315551472416,
-0.143286868528517,-0.143264725003336,-0.143226694481738,-0.143190628643951,
-0.143156370934165,-0.143123781088961,-0.143092733072147,-0.143063113317469,
-0.143034819221448,-0.143007757850762,-0.142981844827678,-0.142957003365903,
-0.142933163430683,-0.142910261012062,-0.140840952239203,-0.138600365909729,
-0.135018779518392,-0.127980672657713,-0.087073879279006,-0.0701942544411946,
-0.0678293639304637,-0.0666234069992897,-0.065667621763324,-0.0645388450072447,
-0.0624673244303813,-0.0512217167953855,-0.000460369818743296),
 .UNSPECIFIED.);
#3778=B_SPLINE_CURVE_WITH_KNOTS('',3,(#266825,#266826,#266827,#266828,#266829,
#266830,#266831,#266832,#266833,#266834,#266835,#266836,#266837,#266838,
#266839,#266840,#266841,#266842,#266843,#266844,#266845,#266846,#266847,
#266848,#266849,#266850,#266851,#266852,#266853,#266854,#266855,#266856,
#266857,#266858,#266859,#266860,#266861,#266862,#266863,#266864,#266865,
#266866,#266867,#266868,#266869,#266870,#266871,#266872,#266873,#266874,
#266875,#266876,#266877,#266878,#266879,#266880,#266881,#266882,#266883,
#266884,#266885,#266886,#266887,#266888,#266889,#266890,#266891,#266892,
#266893,#266894,#266895,#266896,#266897,#266898,#266899,#266900,#266901,
#266902,#266903,#266904,#266905,#266906,#266907,#266908,#266909,#266910,
#266911,#266912,#266913,#266914,#266915,#266916,#266917,#266918,#266919,
#266920,#266921,#266922,#266923,#266924,#266925,#266926),.UNSPECIFIED.,
 .F.,.F.,(4,2,2,2,2,2,2,2,2,2,2,2,2,2,2,2,2,2,2,2,2,2,2,2,2,2,2,2,2,2,2,
2,2,2,2,2,2,2,2,2,2,2,2,2,2,2,2,2,2,2,4),(-1.96079981085505,-1.95342043335075,
-1.95131157403659,-1.94965857635379,-1.94799529337163,-1.9460955291017,
-1.94295263153211,-1.93241406535318,-1.88522823021898,-1.87425087267518,
-1.87219395948775,-1.87106908459013,-1.87011413961342,-1.86890610977445,
-1.86652782879441,-1.84815840603686,-1.81254155119779,-1.80345640271211,
-1.79916560383019,-1.79663528584534,-1.79436126316174,-1.79266137729354,
-1.79104947431068,-1.78840903253175,-1.78169311163644,-1.72867487316804,
-1.7185462305063,-1.71653301758151,-1.7154174301808,-1.71446131737511,-1.71324014607761,
-1.71128008636296,-1.70015445102028,-1.69555049687401,-1.6700740172427,
-1.64408383727216,-1.64025351746894,-1.63820437096798,-1.63651903758875,
-1.63452532834209,-1.63105092637364,-1.61622102525889,-1.57234855170949,
-1.56287849928834,-1.56090274729691,-1.55979520366588,-1.55883791170082,
-1.55760472060856,-1.55560497128255,-1.54369028547836,-1.53266505380209),
 .UNSPECIFIED.);
#3779=B_SPLINE_CURVE_WITH_KNOTS('',3,(#266927,#266928,#266929,#266930,#266931,
#266932,#266933,#266934,#266935,#266936,#266937,#266938,#266939,#266940,
#266941,#266942,#266943,#266944,#266945,#266946,#266947,#266948,#266949,
#266950,#266951,#266952,#266953,#266954,#266955,#266956,#266957,#266958,
#266959,#266960,#266961,#266962,#266963,#266964,#266965,#266966,#266967,
#266968,#266969,#266970,#266971,#266972,#266973,#266974,#266975,#266976,
#266977,#266978,#266979,#266980,#266981,#266982,#266983,#266984,#266985,
#266986,#266987,#266988,#266989,#266990,#266991,#266992,#266993,#266994,
#266995,#266996,#266997,#266998,#266999,#267000,#267001,#267002,#267003,
#267004,#267005,#267006,#267007,#267008,#267009,#267010,#267011,#267012,
#267013,#267014,#267015,#267016,#267017,#267018,#267019,#267020,#267021,
#267022,#267023,#267024,#267025,#267026,#267027,#267028,#267029,#267030,
#267031,#267032,#267033,#267034,#267035,#267036,#267037,#267038,#267039,
#267040,#267041,#267042,#267043,#267044,#267045,#267046,#267047,#267048,
#267049,#267050,#267051,#267052,#267053,#267054,#267055,#267056,#267057,
#267058,#267059,#267060,#267061,#267062,#267063,#267064,#267065,#267066,
#267067,#267068,#267069,#267070,#267071,#267072,#267073,#267074,#267075,
#267076,#267077,#267078,#267079,#267080,#267081,#267082,#267083,#267084,
#267085,#267086,#267087,#267088,#267089,#267090,#267091,#267092,#267093,
#267094,#267095,#267096,#267097,#267098,#267099,#267100,#267101,#267102,
#267103,#267104,#267105,#267106,#267107,#267108,#267109,#267110,#267111,
#267112,#267113,#267114,#267115,#267116,#267117,#267118,#267119,#267120,
#267121,#267122,#267123,#267124,#267125,#267126,#267127,#267128),
 .UNSPECIFIED.,.F.,.F.,(4,2,2,2,2,2,2,2,2,2,2,2,2,2,2,2,2,2,2,2,2,2,2,2,
2,2,2,2,2,2,2,2,2,2,2,2,2,2,2,2,2,2,2,2,2,2,2,2,2,2,2,2,2,2,2,2,2,2,2,2,
2,2,2,2,2,2,2,2,2,2,2,2,2,2,2,2,2,2,2,2,2,2,2,2,2,2,2,2,2,2,2,2,2,2,2,2,
2,2,2,2,4),(-1.40945693535865,-1.37838947460745,-1.35350089257598,-1.34314655046212,
-1.34110272464701,-1.33997150714698,-1.33900255738699,-1.33776476753182,
-1.33577714057381,-1.32443042040914,-1.27960865926656,-1.27156830356978,
-1.26579019131671,-1.2633563589074,-1.26158854394664,-1.25996766950727,
-1.25777861763317,-1.25238889280262,-1.21475513144017,-1.1892136361745,
-1.18607180540606,-1.18472672675155,-1.18374430946283,-1.18267285418179,
-1.18090028874194,-1.17506163266528,-1.12484563434287,-1.11187552262099,
-1.1086148391072,-1.10667277217922,-1.10494103203791,-1.10275038125122,
-1.09929102276075,-1.07907376490314,-1.04372319126061,-1.03195855793559,
-1.02984524507958,-1.02869914521696,-1.0277316977101,-1.02651390722933,
-1.02413359502781,-1.0074127280503,-0.981260395843197,-0.957535941138206,
-0.953973782830811,-0.951752033499747,-0.950016734268253,-0.948092329504277,
-0.944912211015954,-0.932926685416591,-0.88796576599348,-0.876512901613823,
-0.874520089272509,-0.873280734560196,-0.872311645999344,-0.87118151228185,
-0.869142745928059,-0.858881141785129,-0.821460108992222,-0.801670676264679,
-0.79822646347277,-0.796040205828108,-0.794308666794342,-0.792363384214712,
-0.789089011803875,-0.775948177113348,-0.729180522752018,-0.720544459338339,
-0.718534711110628,-0.717398679476688,-0.716439316217247,-0.715212574978455,
-0.712709810187156,-0.709417770130657,-0.701431202850471,-0.664923375561086,
-0.645944085854017,-0.642529522144502,-0.640352102250721,-0.638621212366825,
-0.636669936587437,-0.633369138805949,-0.619884768039655,-0.593493089583819,
-0.567564600634969,-0.563843988058514,-0.562361399865462,-0.561453505618237,
-0.560448450082026,-0.558981322531756,-0.555075623720123,-0.532819587383517,
-0.492605477471602,-0.487353244556039,-0.485244175143252,-0.483482094361268,
-0.481664935570213,-0.478980351516481,-0.47155145660358,-0.460334590086816,
-0.428878856138385),.UNSPECIFIED.);
#3780=B_SPLINE_CURVE_WITH_KNOTS('',3,(#267133,#267134,#267135,#267136,#267137,
#267138,#267139,#267140,#267141,#267142,#267143,#267144,#267145,#267146,
#267147,#267148,#267149,#267150,#267151,#267152,#267153,#267154,#267155,
#267156,#267157,#267158,#267159,#267160,#267161,#267162,#267163,#267164,
#267165,#267166,#267167,#267168,#267169,#267170,#267171,#267172,#267173,
#267174,#267175,#267176,#267177,#267178,#267179,#267180,#267181,#267182,
#267183,#267184,#267185,#267186,#267187,#267188,#267189,#267190,#267191,
#267192,#267193,#267194,#267195,#267196,#267197,#267198,#267199,#267200,
#267201,#267202,#267203,#267204,#267205,#267206,#267207,#267208,#267209,
#267210,#267211,#267212,#267213,#267214,#267215,#267216,#267217,#267218,
#267219,#267220,#267221,#267222,#267223,#267224,#267225,#267226,#267227,
#267228,#267229,#267230,#267231,#267232,#267233,#267234,#267235,#267236,
#267237,#267238,#267239,#267240,#267241,#267242,#267243,#267244,#267245,
#267246,#267247,#267248,#267249,#267250,#267251,#267252,#267253,#267254,
#267255,#267256,#267257,#267258,#267259,#267260,#267261,#267262,#267263,
#267264,#267265,#267266,#267267,#267268,#267269,#267270,#267271,#267272,
#267273,#267274,#267275,#267276,#267277,#267278,#267279,#267280,#267281,
#267282,#267283,#267284,#267285,#267286,#267287,#267288,#267289,#267290,
#267291,#267292,#267293,#267294,#267295,#267296,#267297,#267298,#267299,
#267300,#267301,#267302,#267303,#267304,#267305,#267306,#267307,#267308,
#267309,#267310,#267311,#267312,#267313,#267314,#267315,#267316,#267317,
#267318,#267319,#267320,#267321,#267322,#267323,#267324,#267325,#267326,
#267327,#267328,#267329,#267330,#267331,#267332,#267333,#267334,#267335,
#267336,#267337,#267338,#267339,#267340,#267341,#267342,#267343,#267344,
#267345,#267346,#267347,#267348),.UNSPECIFIED.,.F.,.F.,(4,2,2,2,2,2,2,2,
2,2,2,2,2,2,2,2,2,2,2,2,2,2,2,2,2,2,2,2,2,2,2,2,2,2,2,2,2,2,2,2,2,2,2,2,
2,2,2,2,2,2,2,2,2,2,2,2,2,2,2,2,2,2,2,2,2,2,2,2,2,2,2,2,2,2,2,2,2,2,2,2,
2,2,2,2,2,2,2,2,2,2,2,2,2,2,2,2,2,2,2,2,2,2,2,2,2,2,2,4),(-1.53329438485854,
-1.5259062052296,-1.480603133297,-1.47089302354938,-1.46890278666044,-1.46779191186589,
-1.4668347797346,-1.46560574246885,-1.46362039520212,-1.45199453136208,
-1.44888351571002,-1.41965858942628,-1.40409704144739,-1.39472874895801,
-1.39182748500431,-1.38997986613554,-1.38825086476795,-1.38598439861036,
-1.38092228936624,-1.33921241411468,-1.31795382282117,-1.31415074823298,
-1.31270999364298,-1.3117193119623,-1.31082201732667,-1.30935303329966,
-1.30565000066324,-1.28163689618677,-1.2617921957469,-1.24243706497407,
-1.23756759700035,-1.23531164353587,-1.23359005635413,-1.23195044922239,
-1.22916913987559,-1.22153457805077,-1.22056396702445,-1.21883268540074,
-1.17714976079237,-1.16547971816755,-1.1612364069134,-1.15819387794447,
-1.15687594263843,-1.15590746511566,-1.15484567458574,-1.15307864441314,
-1.14717069880328,-1.1141705894017,-1.08519128108787,-1.08129925294514,
-1.07923645695844,-1.07769910610654,-1.07576912342217,-1.07249437895039,
-1.0606701652163,-1.01368349094619,-1.00385963691052,-1.00186237793883,
-1.00074974592119,-0.999792464813292,-0.998565005983239,-0.996585627703639,
-0.985082169055234,-0.981243770102034,-0.94648392980948,-0.940296456308359,
-0.928388678935088,-0.925105771095938,-0.923173795571481,-0.921636409691605,
-0.91957555372042,-0.915693786515719,-0.887357715187065,-0.857848729190882,
-0.848317177892823,-0.846441697426153,-0.845245714726122,-0.844290582937609,
-0.843154004247797,-0.841045701945348,-0.828983198969002,-0.790910921974196,
-0.784352392714729,-0.77265137104738,-0.769387997807632,-0.767460329471485,
-0.765922399620724,-0.763855692893597,-0.759945880358528,-0.729863261114264,
-0.696369525917018,-0.691725220676978,-0.690114729029839,-0.689189743577349,
-0.688219123186576,-0.686888641328333,-0.683774807169631,-0.658243791503835,
-0.62048296779988,-0.617607930943817,-0.61432870249477,-0.61220672882242,
-0.61050012928326,-0.608555078341277,-0.60521272881707,-0.590762969089393,
-0.558786816909496,-0.552785672327454),.UNSPECIFIED.);
#3781=B_SPLINE_CURVE_WITH_KNOTS('',3,(#267350,#267351,#267352,#267353,#267354,
#267355,#267356,#267357,#267358,#267359,#267360,#267361,#267362,#267363,
#267364,#267365,#267366,#267367,#267368,#267369,#267370,#267371,#267372,
#267373,#267374,#267375,#267376,#267377,#267378,#267379,#267380,#267381,
#267382,#267383,#267384,#267385,#267386,#267387,#267388,#267389,#267390,
#267391,#267392,#267393,#267394,#267395,#267396,#267397,#267398,#267399,
#267400,#267401,#267402,#267403,#267404,#267405,#267406,#267407,#267408,
#267409,#267410,#267411,#267412,#267413,#267414,#267415,#267416,#267417,
#267418,#267419,#267420,#267421,#267422,#267423,#267424,#267425,#267426,
#267427,#267428,#267429,#267430,#267431,#267432,#267433,#267434,#267435,
#267436,#267437,#267438,#267439,#267440,#267441,#267442,#267443,#267444,
#267445,#267446,#267447,#267448,#267449,#267450,#267451,#267452,#267453,
#267454,#267455,#267456,#267457),.UNSPECIFIED.,.F.,.F.,(4,2,2,2,2,2,2,2,
2,2,2,2,2,2,2,2,2,2,2,2,2,2,2,2,2,2,2,2,2,2,2,2,2,2,2,2,2,2,2,2,2,2,2,2,
2,2,2,2,2,2,2,2,2,4),(-0.428878856138385,-0.414539067174868,-0.408745235198775,
-0.406977463123421,-0.405906873567645,-0.404923712968806,-0.403575456785685,
-0.400416589639969,-0.385946393982195,-0.347982234667841,-0.334070851631951,
-0.330631589446018,-0.32862967323089,-0.326903876317232,-0.324796765404635,
-0.32076958170194,-0.315694366763854,-0.304206035376409,-0.280181266764184,
-0.274913526395652,-0.254306251572381,-0.251881356743021,-0.250653831437889,
-0.249685462227338,-0.248546220611693,-0.246465956318455,-0.235410961878035,
-0.219504911377629,-0.181627390737452,-0.176260141162723,-0.174074615602289,
-0.172454327115028,-0.170720520256211,-0.168358957171198,-0.16571277973357,
-0.161160663846559,-0.151327650494007,-0.117249102053957,-0.0986305884952339,
-0.0962266732314018,-0.0950036062527597,-0.0940355351680851,-0.0928928735374122,
-0.0907967011352938,-0.0794126896682031,-0.0360801441414657,-0.0244912492889776,
-0.0199920016666521,-0.0177898190531764,-0.0161315529739948,-0.01451368040225,
-0.0126359538946524,-0.00995542805505722,-0.000458834895657056),
 .UNSPECIFIED.);
#3782=B_SPLINE_CURVE_WITH_KNOTS('',3,(#267458,#267459,#267460,#267461,#267462,
#267463,#267464,#267465,#267466,#267467,#267468,#267469,#267470,#267471,
#267472,#267473,#267474,#267475,#267476,#267477,#267478,#267479,#267480,
#267481,#267482,#267483,#267484,#267485,#267486,#267487,#267488,#267489,
#267490,#267491,#267492,#267493,#267494,#267495,#267496,#267497,#267498,
#267499,#267500,#267501,#267502,#267503,#267504,#267505,#267506,#267507,
#267508,#267509,#267510,#267511,#267512,#267513,#267514,#267515,#267516,
#267517,#267518,#267519,#267520,#267521,#267522,#267523,#267524,#267525,
#267526,#267527,#267528,#267529,#267530,#267531,#267532,#267533,#267534,
#267535,#267536,#267537,#267538,#267539,#267540,#267541,#267542,#267543,
#267544,#267545,#267546,#267547,#267548,#267549,#267550,#267551,#267552,
#267553,#267554,#267555,#267556,#267557),.UNSPECIFIED.,.F.,.F.,(4,3,3,3,
3,3,3,3,3,3,3,3,3,3,3,3,3,3,3,3,3,3,3,3,3,3,3,3,3,3,3,3,3,4),(109.955742876003,
110.079083637333,110.202919711225,110.327367828986,110.35147273413,110.463170399599,
110.574669461548,110.686057610363,110.797377778424,110.90867280093,111.020068420613,
111.131510063134,111.243168982288,111.348806584787,111.460504250256,111.572003312205,
111.68339146102,111.794711629081,111.906006651587,112.017402271271,112.128843913791,
112.240502832945,112.346140435444,112.457838100913,112.569337162862,112.680725311677,
112.792045479738,112.903340502244,113.014736121928,113.126177764448,113.237836683603,
113.343474286101,113.45515745485,113.494796146192),.UNSPECIFIED.);
#3783=B_SPLINE_CURVE_WITH_KNOTS('',3,(#267563,#267564,#267565,#267566,#267567,
#267568,#267569,#267570,#267571,#267572,#267573,#267574,#267575,#267576,
#267577,#267578,#267579,#267580,#267581,#267582,#267583,#267584,#267585,
#267586,#267587,#267588,#267589,#267590,#267591,#267592,#267593,#267594,
#267595,#267596,#267597,#267598,#267599,#267600,#267601,#267602,#267603,
#267604,#267605,#267606,#267607,#267608,#267609,#267610,#267611,#267612,
#267613,#267614,#267615,#267616,#267617,#267618,#267619,#267620,#267621,
#267622,#267623,#267624,#267625,#267626,#267627,#267628,#267629,#267630,
#267631,#267632,#267633,#267634,#267635,#267636,#267637,#267638,#267639,
#267640,#267641,#267642,#267643,#267644,#267645,#267646,#267647,#267648,
#267649,#267650,#267651,#267652,#267653,#267654,#267655,#267656,#267657,
#267658,#267659,#267660,#267661,#267662,#267663,#267664,#267665,#267666,
#267667,#267668,#267669,#267670,#267671,#267672,#267673,#267674,#267675,
#267676,#267677,#267678,#267679,#267680,#267681,#267682,#267683,#267684),
 .UNSPECIFIED.,.F.,.F.,(4,2,2,2,2,2,2,2,2,2,2,2,2,2,2,2,2,2,2,2,2,2,2,2,
2,2,2,2,2,2,2,2,2,2,2,2,2,2,2,2,2,2,2,2,2,2,2,2,2,2,2,2,2,2,2,2,2,2,2,2,
4),(-0.552744682324884,-0.539491799904537,-0.524713764816097,-0.52124195532014,
-0.519248262641362,-0.517562088831951,-0.515510874819621,-0.511673554868996,
-0.485460133163769,-0.457693480591708,-0.452233774608359,-0.444074270314207,
-0.442116424640607,-0.441000858687102,-0.440044196854515,-0.438821591884561,
-0.436292667323589,-0.407658195450849,-0.372370765588914,-0.366856423207403,
-0.364662113907197,-0.363053470609611,-0.361314590389507,-0.358948910088451,
-0.353466211478536,-0.345929895836228,-0.300698588616303,-0.288776636779942,
-0.286775816551164,-0.285542020707468,-0.284584289440006,-0.283476262385566,
-0.281499724480592,-0.272026633724511,-0.228158122524084,-0.213327162248706,
-0.209851511001255,-0.207856903484334,-0.206170706652158,-0.204120382005885,
-0.200287483806872,-0.182154629221436,-0.142678681496718,-0.13285990295235,
-0.130967715539691,-0.129766735717618,-0.128811483606482,-0.127904117109684,
-0.126191168710766,-0.119835656448654,-0.108114842245078,-0.0913752337551362,
-0.0611227125542174,-0.0555039882382235,-0.0532918923060263,-0.0516785676441627,
-0.049942542441728,-0.0475947669337017,-0.0450050725458054,-0.0369382998639502,
-0.000460337843206879),.UNSPECIFIED.);
#3784=B_SPLINE_CURVE_WITH_KNOTS('',3,(#267685,#267686,#267687,#267688,#267689,
#267690,#267691,#267692,#267693,#267694,#267695,#267696,#267697,#267698,
#267699,#267700,#267701,#267702,#267703,#267704,#267705,#267706,#267707,
#267708,#267709,#267710,#267711,#267712,#267713,#267714,#267715,#267716,
#267717,#267718,#267719,#267720,#267721,#267722,#267723,#267724,#267725,
#267726,#267727,#267728,#267729,#267730,#267731,#267732,#267733,#267734,
#267735,#267736,#267737,#267738,#267739,#267740,#267741,#267742,#267743,
#267744,#267745,#267746,#267747,#267748,#267749,#267750,#267751,#267752,
#267753,#267754,#267755,#267756,#267757,#267758,#267759,#267760,#267761,
#267762,#267763,#267764,#267765,#267766,#267767,#267768,#267769,#267770,
#267771,#267772,#267773,#267774,#267775,#267776,#267777,#267778,#267779,
#267780,#267781,#267782,#267783,#267784,#267785,#267786,#267787,#267788,
#267789,#267790,#267791,#267792,#267793,#267794,#267795,#267796),
 .UNSPECIFIED.,.F.,.F.,(4,2,2,2,2,2,2,2,2,2,2,2,2,2,2,2,2,2,2,2,2,2,2,2,
2,2,2,2,2,2,2,2,2,2,2,2,2,2,2,2,2,2,2,2,2,2,2,2,2,2,2,2,2,2,2,4),(-1.96112117373986,
-1.93832776576274,-1.93664462059022,-1.9355272830046,-1.93462067799193,
-1.93366577556876,-1.93246347086777,-1.9300355826801,-1.91002528253084,
-1.89268236084572,-1.87306924994882,-1.86192616881238,-1.85883101451738,
-1.85694109581914,-1.8552261222988,-1.85301554977393,-1.8494414463733,-1.82349909405135,
-1.79766957712133,-1.78738618786051,-1.78156964225285,-1.7799209000981,
-1.77901772498458,-1.77806129524977,-1.77683803196797,-1.77487138272681,
-1.76361468733173,-1.7608577783962,-1.73413386995263,-1.71639119420624,
-1.70637685635215,-1.7032699767239,-1.70137743634478,-1.69966302540739,
-1.69745730374043,-1.69389953409202,-1.66153650195464,-1.63686321154794,
-1.62657845779151,-1.62455645673067,-1.62343881571737,-1.62248269292914,
-1.62126376183288,-1.61931158864701,-1.60835262753931,-1.6034358978591,
-1.59290928585705,-1.56894388580332,-1.55745512800824,-1.55239565032577,
-1.54838798531646,-1.54630155539103,-1.54459818355804,-1.54262863849183,
-1.53926122404421,-1.53329438485854),.UNSPECIFIED.);
#3785=B_SPLINE_CURVE_WITH_KNOTS('',3,(#267798,#267799,#267800,#267801,#267802,
#267803,#267804,#267805,#267806,#267807,#267808,#267809,#267810,#267811,
#267812,#267813,#267814,#267815,#267816,#267817,#267818,#267819,#267820,
#267821,#267822,#267823,#267824,#267825,#267826,#267827,#267828,#267829,
#267830,#267831,#267832,#267833,#267834,#267835,#267836,#267837,#267838,
#267839,#267840,#267841,#267842,#267843,#267844,#267845,#267846,#267847,
#267848,#267849,#267850,#267851,#267852,#267853,#267854,#267855,#267856,
#267857,#267858,#267859,#267860,#267861,#267862,#267863,#267864,#267865,
#267866,#267867,#267868,#267869,#267870,#267871,#267872,#267873,#267874,
#267875,#267876),.UNSPECIFIED.,.F.,.F.,(4,3,3,3,3,3,3,3,3,3,3,3,3,3,3,3,
3,3,3,3,3,3,3,3,3,3,4),(113.494796146192,113.606250882577,113.717609971385,
113.828916304694,113.940212695218,114.051620250569,114.163087476167,114.274758952439,
114.340808136758,114.452505802227,114.564004864176,114.675393012991,114.786713181052,
114.898008203558,115.009403823241,115.120845465761,115.232504384916,115.338141987414,
115.450740226908,115.560871664889,115.670896225704,115.780858808389,115.895376082134,
116.005413941336,116.115510914744,116.225774396111,116.238927903367),
 .UNSPECIFIED.);
#3786=B_SPLINE_CURVE_WITH_KNOTS('',3,(#267877,#267878,#267879,#267880,#267881,
#267882,#267883,#267884),.UNSPECIFIED.,.F.,.F.,(4,1,1,1,1,4),(116.238928182822,
116.335475838071,117.332809688728,118.330143539385,119.327477390041,119.777686492919),
 .UNSPECIFIED.);
#3787=B_SPLINE_CURVE_WITH_KNOTS('',3,(#267889,#267890,#267891,#267892,#267893,
#267894,#267895,#267896,#267897,#267898,#267899,#267900,#267901,#267902,
#267903,#267904,#267905,#267906,#267907,#267908,#267909,#267910,#267911,
#267912,#267913,#267914,#267915,#267916,#267917,#267918,#267919,#267920,
#267921,#267922,#267923,#267924,#267925,#267926,#267927,#267928,#267929,
#267930,#267931,#267932,#267933,#267934,#267935,#267936,#267937,#267938,
#267939,#267940,#267941,#267942,#267943,#267944,#267945,#267946,#267947,
#267948,#267949,#267950,#267951,#267952,#267953,#267954,#267955,#267956,
#267957,#267958,#267959,#267960,#267961,#267962,#267963,#267964,#267965,
#267966,#267967,#267968,#267969,#267970,#267971,#267972,#267973,#267974,
#267975,#267976,#267977,#267978,#267979,#267980,#267981,#267982,#267983,
#267984,#267985,#267986,#267987,#267988,#267989,#267990,#267991,#267992,
#267993,#267994,#267995,#267996,#267997,#267998,#267999,#268000,#268001,
#268002,#268003,#268004,#268005,#268006,#268007,#268008,#268009,#268010,
#268011,#268012,#268013,#268014,#268015,#268016,#268017,#268018,#268019,
#268020,#268021,#268022,#268023,#268024,#268025,#268026,#268027,#268028,
#268029,#268030,#268031,#268032,#268033,#268034,#268035,#268036,#268037,
#268038,#268039,#268040,#268041,#268042,#268043,#268044,#268045,#268046,
#268047,#268048,#268049,#268050,#268051,#268052,#268053,#268054,#268055,
#268056,#268057,#268058,#268059,#268060,#268061,#268062,#268063,#268064,
#268065,#268066,#268067,#268068,#268069,#268070,#268071,#268072,#268073,
#268074,#268075,#268076,#268077,#268078,#268079,#268080,#268081,#268082,
#268083,#268084,#268085,#268086,#268087,#268088,#268089,#268090,#268091,
#268092,#268093,#268094,#268095,#268096,#268097,#268098,#268099,#268100,
#268101,#268102,#268103,#268104,#268105,#268106,#268107,#268108,#268109,
#268110,#268111,#268112,#268113,#268114),.UNSPECIFIED.,.F.,.F.,(4,2,2,2,
2,2,2,2,2,2,2,2,2,2,2,2,2,2,2,2,2,2,2,2,2,2,2,2,2,2,2,2,2,2,2,2,2,2,2,2,
2,2,2,2,2,2,2,2,2,2,2,2,2,2,2,2,2,2,2,2,2,2,2,2,2,2,2,2,2,2,2,2,2,2,2,2,
2,2,2,2,2,2,2,2,2,2,2,2,2,2,2,2,2,2,2,2,2,2,2,2,2,2,2,2,2,2,2,2,2,2,2,2,
4),(-1.53304027296573,-1.5316933786242,-1.53059862789435,-1.52963896918988,
-1.52840580818723,-1.52636222400816,-1.51338180602523,-1.47986731226285,
-1.46086274598092,-1.4560396602581,-1.45379252083902,-1.45207234176464,
-1.45043006830222,-1.44763433141302,-1.4398990132202,-1.43929879688,-1.43752180201361,
-1.39577611690525,-1.38402074778217,-1.37975715595556,-1.37670349300103,
-1.37538370234128,-1.37441502483976,-1.37335425565733,-1.37159146258138,
-1.36572016526932,-1.35896876808938,-1.31389858892671,-1.30229649506668,
-1.29917527390024,-1.29727934172938,-1.29556530642887,-1.29336488331976,
-1.28982552372144,-1.26586265434036,-1.23382676724874,-1.22254546405914,
-1.22047289424212,-1.21934420677549,-1.2183888911161,-1.21718403388192,
-1.21482279880908,-1.19804997227739,-1.15736136842732,-1.14650532861651,
-1.14345227090486,-1.14157139083122,-1.13985364898079,-1.13766088945787,
-1.13406760616426,-1.10560515707813,-1.07777913052247,-1.06686010611868,
-1.06480513336529,-1.06368025450795,-1.06272465843784,-1.06151497854141,
-1.05913097837272,-1.04042587742878,-1.01815170145439,-0.994699467949108,
-0.989325134502199,-0.98697833711723,-0.985242748269195,-0.983629619613522,
-0.980986566553452,-0.973708527986447,-0.962762024740855,-0.920722289454511,
-0.911250337706766,-0.909378708109777,-0.908184054914625,-0.907229207742768,
-0.906092047332384,-0.903980229380461,-0.891826343980013,-0.852888345556283,
-0.845385051251205,-0.84373823557601,-0.842233750249596,-0.834638357150912,
-0.831862859584372,-0.830224435130571,-0.828502454189615,-0.826243269710176,
-0.821356080551775,-0.801861767721198,-0.782102464277489,-0.777319312506229,
-0.756202074192142,-0.753765687659272,-0.752561444260335,-0.75160613589723,
-0.750476888193142,-0.748401832073659,-0.737067741766625,-0.704668370777625,
-0.681139457402112,-0.677611017844322,-0.675413792572174,-0.673700057731437,
-0.671802223105242,-0.668672701392535,-0.65697774269502,-0.611940116441193,
-0.600156065133991,-0.598161374450457,-0.596929436096105,-0.595971904814009,
-0.594862687580587,-0.592880586472537,-0.583312991155123,-0.552744682324884),
 .UNSPECIFIED.);
#3788=B_SPLINE_CURVE_WITH_KNOTS('',3,(#268116,#268117,#268118,#268119,#268120,
#268121,#268122),.UNSPECIFIED.,.F.,.F.,(4,1,1,1,4),(119.777686492919,120.324811240698,
121.322145091355,122.319478942012,122.522113490002),.UNSPECIFIED.);
#3789=B_SPLINE_CURVE_WITH_KNOTS('',3,(#268123,#268124,#268125,#268126,#268127,
#268128,#268129,#268130,#268131,#268132,#268133,#268134,#268135,#268136,
#268137,#268138,#268139,#268140,#268141,#268142,#268143,#268144,#268145,
#268146,#268147,#268148,#268149,#268150,#268151,#268152,#268153,#268154,
#268155,#268156,#268157,#268158,#268159,#268160,#268161,#268162,#268163,
#268164,#268165,#268166,#268167,#268168,#268169,#268170,#268171,#268172,
#268173,#268174,#268175,#268176,#268177,#268178,#268179,#268180,#268181,
#268182,#268183,#268184,#268185,#268186,#268187,#268188,#268189,#268190,
#268191,#268192,#268193,#268194,#268195,#268196,#268197,#268198,#268199,
#268200,#268201,#268202,#268203,#268204,#268205,#268206,#268207,#268208,
#268209,#268210,#268211,#268212,#268213,#268214,#268215,#268216,#268217,
#268218,#268219,#268220,#268221,#268222,#268223,#268224,#268225,#268226,
#268227,#268228,#268229,#268230,#268231,#268232,#268233,#268234,#268235,
#268236,#268237,#268238,#268239,#268240,#268241,#268242,#268243,#268244,
#268245,#268246,#268247,#268248),.UNSPECIFIED.,.F.,.F.,(4,2,2,2,2,2,2,2,
2,2,2,2,2,2,2,2,2,2,2,2,2,2,2,2,2,2,2,2,2,2,2,2,2,2,2,2,2,2,2,2,2,2,2,2,
2,2,2,2,2,2,2,2,2,2,2,2,2,2,2,2,2,2,4),(-1.96140461786641,-1.92769353217711,
-1.92242452363725,-1.91949550116251,-1.917516678651,-1.91559812502333,-1.91386225364756,
-1.91163161614589,-1.9080384760744,-1.87663664301394,-1.85851588646038,
-1.84675774764076,-1.84037984140565,-1.83865240462828,-1.83773363402596,
-1.83676658476978,-1.83555063814005,-1.83317786167412,-1.81673692710697,
-1.77627338487616,-1.76884859787116,-1.76347393746544,-1.76107717808805,
-1.75931644559865,-1.75768813906028,-1.75546764655194,-1.74988923849613,
-1.71577810669206,-1.69445703659498,-1.68828776594107,-1.68423648905864,
-1.68274880054525,-1.68173998293721,-1.68083651144448,-1.67937576947549,
-1.67578217545974,-1.64539413071381,-1.61124242736164,-1.6071523018085,
-1.60503317305514,-1.60347369342269,-1.60154119982685,-1.59832209192733,
-1.58730232424351,-1.54262385269019,-1.52993135105201,-1.52777882011535,
-1.52662452863726,-1.52565785508531,-1.52445069291963,-1.52256314522001,
-1.51307058074189,-1.50896831995664,-1.47827904743643,-1.45726463825833,
-1.45215909875675,-1.44984305905339,-1.44809529186693,-1.44644515352447,
-1.44368043706037,-1.43629505540247,-1.4348004361727,-1.40935215081212),
 .UNSPECIFIED.);
#3790=B_SPLINE_CURVE_WITH_KNOTS('',3,(#268254,#268255,#268256,#268257,#268258,
#268259,#268260,#268261,#268262,#268263,#268264,#268265,#268266,#268267,
#268268,#268269,#268270,#268271,#268272,#268273,#268274,#268275,#268276,
#268277,#268278,#268279,#268280,#268281,#268282,#268283,#268284,#268285,
#268286,#268287,#268288,#268289,#268290,#268291,#268292,#268293,#268294,
#268295,#268296,#268297,#268298,#268299,#268300,#268301,#268302,#268303,
#268304,#268305,#268306,#268307,#268308,#268309,#268310,#268311,#268312,
#268313,#268314,#268315,#268316,#268317,#268318,#268319,#268320,#268321,
#268322,#268323,#268324,#268325,#268326,#268327,#268328,#268329,#268330,
#268331,#268332,#268333,#268334,#268335,#268336,#268337,#268338,#268339,
#268340,#268341,#268342,#268343,#268344,#268345,#268346,#268347,#268348,
#268349,#268350,#268351,#268352,#268353,#268354,#268355,#268356,#268357,
#268358,#268359,#268360,#268361,#268362,#268363,#268364,#268365,#268366,
#268367,#268368,#268369,#268370,#268371,#268372,#268373,#268374,#268375,
#268376,#268377),.UNSPECIFIED.,.F.,.F.,(4,2,2,2,2,2,2,2,2,2,2,2,2,2,2,2,
2,2,2,2,2,2,2,2,2,2,2,2,2,2,2,2,2,2,2,2,2,2,2,2,2,2,2,2,2,2,2,2,2,2,2,2,
2,2,2,2,2,2,2,2,2,4),(-0.552568402974919,-0.533818180356304,-0.507622669869086,
-0.505256919662991,-0.504050916278603,-0.503095299981104,-0.501966963901806,
-0.499896873499081,-0.488674999504696,-0.457037227726781,-0.432649183897734,
-0.429099133080411,-0.426895166903973,-0.42518028300109,-0.423285354599918,
-0.420170265507477,-0.408644754825207,-0.363483860427586,-0.351614781241579,
-0.349615994897949,-0.348382683517896,-0.347424831720345,-0.346316097278136,
-0.344336925297352,-0.334824288074235,-0.29096552735152,-0.276152377318475,
-0.272677516954602,-0.270682853061345,-0.268996311892583,-0.266945205998973,
-0.263250925411805,-0.258592090828962,-0.248384144912683,-0.210959912866051,
-0.207521692546721,-0.195863125043467,-0.193875294090291,-0.192645289816032,
-0.191687768998619,-0.190576851902533,-0.188703989824544,-0.180177952027278,
-0.135783508398606,-0.120482117208579,-0.116973378157439,-0.114971053133357,
-0.113438763106351,-0.111458585460992,-0.109382951858319,-0.101398647248031,
-0.0834201594127288,-0.0671972741633204,-0.0424792406047148,-0.0387704868789293,
-0.0373003746695206,-0.0364027637722067,-0.0354120835546178,-0.0344121372081074,
-0.0330206229605259,-0.030668307090341,-0.00046003148883276),
 .UNSPECIFIED.);
#3791=B_SPLINE_CURVE_WITH_KNOTS('',3,(#268378,#268379,#268380,#268381,#268382,
#268383,#268384,#268385,#268386,#268387,#268388,#268389,#268390,#268391,
#268392,#268393,#268394,#268395,#268396,#268397,#268398,#268399,#268400,
#268401,#268402,#268403,#268404,#268405,#268406,#268407,#268408,#268409,
#268410,#268411,#268412,#268413,#268414,#268415,#268416,#268417,#268418,
#268419,#268420,#268421,#268422,#268423,#268424,#268425,#268426,#268427,
#268428,#268429,#268430,#268431,#268432,#268433,#268434,#268435,#268436,
#268437,#268438,#268439,#268440,#268441,#268442,#268443,#268444,#268445,
#268446,#268447,#268448,#268449,#268450,#268451,#268452,#268453,#268454,
#268455,#268456,#268457,#268458,#268459,#268460,#268461,#268462,#268463,
#268464,#268465,#268466,#268467,#268468,#268469,#268470,#268471,#268472,
#268473),.UNSPECIFIED.,.F.,.F.,(4,2,2,2,2,2,2,2,2,2,2,2,2,2,2,2,2,2,2,2,
2,2,2,2,2,2,2,2,2,2,2,2,2,2,2,2,2,2,2,2,2,2,2,2,2,2,2,4),(-1.96142034783854,
-1.92657433847609,-1.9237305089718,-1.92179629247507,-1.91991542049242,
-1.91819781746739,-1.91600541523768,-1.91241310186858,-1.88400082421549,
-1.86688259523144,-1.84849765698183,-1.84425682866014,-1.84308977961811,
-1.84198620836535,-1.84102817572916,-1.83978856185613,-1.83776763320117,
-1.82536289064326,-1.81967137528589,-1.78720718752015,-1.77590103164971,
-1.77089756026477,-1.76698950040469,-1.76529091825504,-1.76356041014398,
-1.76193964650569,-1.75969748433022,-1.75389165525563,-1.71044307049571,
-1.69634448260789,-1.69154745589561,-1.68822697878564,-1.68686525333391,
-1.68588458545841,-1.68497638807889,-1.68344997396578,-1.67938196851299,
-1.63148736639158,-1.61437281373885,-1.61087093117825,-1.60889169858573,
-1.60736004230269,-1.60535841479486,-1.60185054790136,-1.58654807324172,
-1.54214427265775,-1.53360989706048,-1.53304027296573),.UNSPECIFIED.);
#3792=B_SPLINE_CURVE_WITH_KNOTS('',3,(#268474,#268475,#268476,#268477,#268478,
#268479,#268480,#268481,#268482,#268483,#268484,#268485,#268486,#268487,
#268488,#268489,#268490,#268491,#268492,#268493,#268494,#268495,#268496,
#268497,#268498,#268499,#268500,#268501,#268502,#268503,#268504,#268505,
#268506,#268507,#268508,#268509,#268510,#268511,#268512,#268513,#268514,
#268515,#268516,#268517,#268518,#268519,#268520,#268521,#268522,#268523,
#268524,#268525,#268526,#268527,#268528,#268529,#268530,#268531,#268532,
#268533,#268534,#268535,#268536,#268537,#268538,#268539,#268540,#268541,
#268542,#268543,#268544,#268545,#268546,#268547,#268548,#268549,#268550,
#268551,#268552,#268553,#268554,#268555,#268556,#268557,#268558,#268559,
#268560,#268561,#268562,#268563,#268564,#268565,#268566,#268567,#268568,
#268569,#268570,#268571,#268572,#268573,#268574,#268575,#268576,#268577,
#268578,#268579,#268580,#268581,#268582,#268583,#268584,#268585,#268586,
#268587,#268588,#268589,#268590,#268591,#268592,#268593,#268594,#268595,
#268596,#268597,#268598,#268599,#268600,#268601,#268602,#268603,#268604,
#268605,#268606,#268607,#268608,#268609,#268610,#268611,#268612,#268613,
#268614,#268615,#268616,#268617,#268618,#268619,#268620,#268621,#268622,
#268623,#268624,#268625,#268626,#268627,#268628,#268629,#268630,#268631,
#268632,#268633,#268634,#268635,#268636,#268637,#268638,#268639,#268640,
#268641,#268642,#268643,#268644,#268645,#268646,#268647,#268648,#268649,
#268650,#268651,#268652,#268653,#268654,#268655,#268656,#268657,#268658,
#268659,#268660,#268661,#268662,#268663,#268664,#268665,#268666,#268667,
#268668,#268669,#268670,#268671,#268672,#268673,#268674,#268675,#268676,
#268677,#268678,#268679,#268680,#268681,#268682,#268683,#268684,#268685,
#268686,#268687,#268688,#268689,#268690,#268691),.UNSPECIFIED.,.F.,.F.,
(4,2,2,2,2,2,2,2,2,2,2,2,2,2,2,2,2,2,2,2,2,2,2,2,2,2,2,2,2,2,2,2,2,2,2,
2,2,2,2,2,2,2,2,2,2,2,2,2,2,2,2,2,2,2,2,2,2,2,2,2,2,2,2,2,2,2,2,2,2,2,2,
2,2,2,2,2,2,2,2,2,2,2,2,2,2,2,2,2,2,2,2,2,2,2,2,2,2,2,2,2,2,2,2,2,2,2,2,
2,4),(-1.40935215081212,-1.38414989925974,-1.37410809746072,-1.37208173083532,
-1.37095442059732,-1.36998520113837,-1.36874238321402,-1.36673767131879,
-1.35504115585052,-1.30978221365538,-1.30220290135856,-1.29668258589555,
-1.29429284107092,-1.29253297750705,-1.29090244741502,-1.28867423216686,
-1.2830519423058,-1.25055533505058,-1.22799182673477,-1.21845016586842,
-1.21645292499742,-1.21533200443641,-1.21436201195971,-1.21311002446733,
-1.21107455580077,-1.19872273665609,-1.1862735220927,-1.17208011983953,
-1.14416073401425,-1.14025428303527,-1.13817291554743,-1.1364651738715,
-1.13444954872091,-1.13094787793857,-1.11613256457903,-1.07194199297956,
-1.06585673302858,-1.06184620912954,-1.06036399985209,-1.05935602466236,
-1.05845112754953,-1.05698401103913,-1.05335441378921,-1.02373542580131,
-0.989695697719933,-0.985066449059518,-0.982839296809448,-0.981103346970758,
-0.979181863440628,-0.976015018520641,-0.964183039325222,-0.919126716211047,
-0.907596283741008,-0.905599736084144,-0.904359254730039,-0.903390068986468,
-0.902260726139816,-0.900225619746422,-0.890030890920978,-0.83573685320341,
-0.830028623694332,-0.82778586894948,-0.826151543804733,-0.824394053757696,
-0.822018979273781,-0.816583799664372,-0.792825521239947,-0.76475642353124,
-0.752022149523379,-0.749970973510691,-0.748714266748787,-0.747743766598975,
-0.746625831644567,-0.744642456688066,-0.735329257281941,-0.713750728228456,
-0.680001111787145,-0.674410135254135,-0.672187147202926,-0.670557879620062,
-0.668796936710608,-0.666401381299168,-0.6608479123896,-0.653208970243973,
-0.607982229638827,-0.596320609503819,-0.594317654331137,-0.593075303875223,
-0.592106037241798,-0.590978188895139,-0.588949684600726,-0.578871601881753,
-0.527412785990045,-0.527114457262083,-0.519473040575407,-0.516670366071667,
-0.515012767033611,-0.513268192970907,-0.510975039364734,-0.505995471067384,
-0.485975035601746,-0.457584989845919,-0.440982529391697,-0.438604143742915,
-0.437386840864667,-0.436419517083748,-0.435273247420906,-0.433158809815512,
-0.428879403561289),.UNSPECIFIED.);
#3793=B_SPLINE_CURVE_WITH_KNOTS('',3,(#268696,#268697,#268698,#268699,#268700,
#268701,#268702,#268703,#268704,#268705,#268706,#268707,#268708,#268709,
#268710,#268711,#268712,#268713,#268714,#268715,#268716,#268717,#268718,
#268719,#268720,#268721,#268722,#268723,#268724,#268725,#268726,#268727,
#268728,#268729,#268730,#268731,#268732,#268733,#268734,#268735,#268736,
#268737,#268738,#268739,#268740,#268741,#268742,#268743,#268744,#268745,
#268746,#268747,#268748,#268749,#268750,#268751,#268752,#268753,#268754,
#268755,#268756,#268757,#268758,#268759,#268760,#268761,#268762,#268763,
#268764,#268765,#268766,#268767,#268768,#268769,#268770,#268771,#268772,
#268773,#268774,#268775,#268776,#268777,#268778,#268779,#268780,#268781,
#268782,#268783,#268784,#268785,#268786,#268787,#268788,#268789,#268790,
#268791,#268792,#268793,#268794,#268795,#268796,#268797,#268798,#268799,
#268800,#268801,#268802,#268803,#268804,#268805,#268806,#268807,#268808,
#268809,#268810,#268811,#268812,#268813,#268814,#268815,#268816,#268817,
#268818,#268819,#268820,#268821,#268822,#268823,#268824,#268825,#268826,
#268827,#268828,#268829,#268830,#268831,#268832,#268833,#268834,#268835,
#268836,#268837,#268838,#268839,#268840,#268841,#268842,#268843,#268844,
#268845,#268846,#268847,#268848,#268849,#268850,#268851,#268852,#268853,
#268854,#268855,#268856,#268857,#268858,#268859,#268860,#268861,#268862,
#268863,#268864,#268865,#268866,#268867,#268868,#268869,#268870,#268871,
#268872,#268873,#268874,#268875,#268876,#268877,#268878,#268879,#268880,
#268881,#268882,#268883,#268884,#268885,#268886,#268887,#268888,#268889,
#268890,#268891,#268892,#268893,#268894,#268895,#268896,#268897,#268898,
#268899,#268900,#268901,#268902,#268903,#268904,#268905,#268906,#268907,
#268908,#268909,#268910,#268911,#268912,#268913,#268914,#268915,#268916,
#268917,#268918,#268919,#268920,#268921),.UNSPECIFIED.,.F.,.F.,(4,2,2,2,
2,2,2,2,2,2,2,2,2,2,2,2,2,2,2,2,2,2,2,2,2,2,2,2,2,2,2,2,2,2,2,2,2,2,2,2,
2,2,2,2,2,2,2,2,2,2,2,2,2,2,2,2,2,2,2,2,2,2,2,2,2,2,2,2,2,2,2,2,2,2,2,2,
2,2,2,2,2,2,2,2,2,2,2,2,2,2,2,2,2,2,2,2,2,2,2,2,2,2,2,2,2,2,2,2,2,2,2,2,
4),(-1.5331279783234,-1.53271589118596,-1.52111789403578,-1.51799642383371,
-1.51610008588491,-1.5143855196618,-1.51218418609851,-1.50864289377132,
-1.48463609144734,-1.4526241978639,-1.4413445932304,-1.4392716571504,-1.43814269253739,
-1.43718709552344,-1.43598182401986,-1.43361960144915,-1.4168300184983,
-1.37610702308954,-1.3652772091061,-1.3622260505927,-1.36034523842165,-1.35862683020804,
-1.35643222131933,-1.35283377350258,-1.32413965328508,-1.29649732795497,
-1.28561115841552,-1.28355737840486,-1.28243255879028,-1.28147665156574,
-1.28026611635389,-1.27834265326804,-1.26795482906466,-1.26203793115821,
-1.23701082985724,-1.21102973580487,-1.20719744698848,-1.20514704176437,
-1.20346056805247,-1.20146538606876,-1.19798810386291,-1.18314082087345,
-1.13923198649287,-1.12976885972014,-1.12779256423819,-1.1266844423764,
-1.12572647579001,-1.12449218766785,-1.12249021402569,-1.11054768388819,
-1.06529352412716,-1.05393821388452,-1.05083825192968,-1.04894658215367,
-1.04723078932416,-1.04502024245374,-1.04144841172715,-1.01586287342043,
-0.994672189925102,-0.980853099889869,-0.97975604224162,-0.973696314806764,
-0.971912352629215,-0.970846704259775,-0.96987933225583,-0.968569345428101,
-0.965572581068912,-0.961412307370486,-0.950087128778832,-0.908778383745338,
-0.89831637088435,-0.895178792901896,-0.893278881702288,-0.891565072327742,
-0.889370252256426,-0.884823897038116,-0.878892175463459,-0.864405935058884,
-0.837580781683793,-0.819089142892016,-0.816707007870551,-0.815497514928769,
-0.814541671486112,-0.813416033055249,-0.811358490163329,-0.800395497002437,
-0.784650502322319,-0.746375266762727,-0.74105246047064,-0.738890412685334,
-0.737289687068503,-0.735544144605578,-0.733141806451617,-0.72744483594904,
-0.719525662951737,-0.674666678946049,-0.663024487505438,-0.661037680365348,
-0.659807978217846,-0.658850477478963,-0.657739336871963,-0.655749034626371,
-0.64604611982115,-0.600854674791085,-0.587399705166519,-0.584023784346807,
-0.582051782342297,-0.580347805026822,-0.578262552611402,-0.574263167384463,
-0.569216919330978,-0.55777248985308,-0.552568402974919),.UNSPECIFIED.);
#3794=B_SPLINE_CURVE_WITH_KNOTS('',3,(#268923,#268924,#268925,#268926,#268927,
#268928,#268929,#268930,#268931,#268932,#268933,#268934,#268935,#268936,
#268937,#268938,#268939,#268940,#268941,#268942,#268943,#268944,#268945,
#268946,#268947,#268948,#268949,#268950,#268951,#268952,#268953,#268954,
#268955,#268956,#268957,#268958,#268959,#268960,#268961,#268962,#268963,
#268964,#268965,#268966,#268967,#268968,#268969,#268970,#268971,#268972,
#268973,#268974,#268975,#268976,#268977,#268978,#268979,#268980,#268981,
#268982,#268983,#268984,#268985,#268986,#268987,#268988,#268989,#268990,
#268991,#268992,#268993,#268994,#268995,#268996,#268997,#268998,#268999,
#269000,#269001,#269002,#269003,#269004,#269005,#269006,#269007,#269008,
#269009,#269010,#269011,#269012,#269013,#269014),.UNSPECIFIED.,.F.,.F.,
(4,2,2,2,2,2,2,2,2,2,2,2,2,2,2,2,2,2,2,2,2,2,2,2,2,2,2,2,2,2,2,2,2,2,2,
2,2,2,2,2,2,2,2,2,2,4),(-0.428879403561289,-0.421364094033311,-0.385754873086396,
-0.365849832369992,-0.362402067404484,-0.360215007910518,-0.358483751897869,
-0.356539753005891,-0.353269870485476,-0.340180064009024,-0.287963614543592,
-0.283781542226331,-0.282226414648722,-0.281304742182555,-0.280312317570708,
-0.278909715129471,-0.27542277601127,-0.257804230793803,-0.227003868244697,
-0.221662202366041,-0.209333654053757,-0.205986862866056,-0.204025617038048,
-0.202469295745647,-0.200388436593215,-0.196648026409956,-0.17964520351943,
-0.142694772135559,-0.137779546365032,-0.129105222595565,-0.127092701594866,
-0.125956086034931,-0.124987614167213,-0.124046481782052,-0.12213353534955,
-0.112926261379201,-0.0917552362925678,-0.0574438196528032,-0.0518705422515606,
-0.0496501698847528,-0.0480212753648273,-0.0462592613616052,-0.04385961296452,
-0.041205972415941,-0.0325220769531143,-0.000459406881434288),
 .UNSPECIFIED.);
#3795=B_SPLINE_CURVE_WITH_KNOTS('',3,(#269015,#269016,#269017,#269018,#269019,
#269020,#269021,#269022,#269023,#269024,#269025,#269026,#269027,#269028,
#269029,#269030,#269031,#269032,#269033,#269034,#269035,#269036,#269037,
#269038,#269039,#269040,#269041,#269042,#269043,#269044,#269045,#269046,
#269047,#269048,#269049,#269050,#269051,#269052,#269053,#269054,#269055,
#269056,#269057,#269058,#269059,#269060,#269061,#269062,#269063,#269064,
#269065,#269066,#269067,#269068,#269069,#269070,#269071,#269072,#269073,
#269074,#269075,#269076,#269077,#269078,#269079,#269080,#269081,#269082,
#269083,#269084,#269085,#269086,#269087,#269088,#269089,#269090,#269091,
#269092,#269093,#269094,#269095,#269096,#269097,#269098,#269099,#269100,
#269101,#269102,#269103,#269104,#269105,#269106,#269107,#269108,#269109,
#269110,#269111,#269112,#269113,#269114,#269115,#269116,#269117,#269118,
#269119,#269120,#269121,#269122,#269123,#269124,#269125,#269126,#269127,
#269128,#269129,#269130,#269131,#269132,#269133,#269134,#269135,#269136,
#269137,#269138,#269139,#269140,#269141,#269142),.UNSPECIFIED.,.F.,.F.,
(4,2,2,2,2,2,2,2,2,2,2,2,2,2,2,2,2,2,2,2,2,2,2,2,2,2,2,2,2,2,2,2,2,2,2,
2,2,2,2,2,2,2,2,2,2,2,2,2,2,2,2,2,2,2,2,2,2,2,2,2,2,2,2,4),(-1.9614931804776,
-1.93516794709654,-1.9334587770767,-1.93232534427062,-1.93140663883529,
-1.93043943041673,-1.92922244376262,-1.92676676370697,-1.90399138611458,
-1.88670608386381,-1.86428115288063,-1.85767263726173,-1.85568900239295,
-1.85376702989839,-1.8520316262414,-1.84980654990319,-1.8462325078789,-1.82200846571697,
-1.79316961507947,-1.7837971646141,-1.7783323738917,-1.77670826805569,-1.77579658994973,
-1.77482541841812,-1.77358224975683,-1.77153142055365,-1.7587991666777,
-1.72843832271109,-1.71244643307727,-1.7060917776087,-1.7013937542631,-1.69909085977923,
-1.69734491765831,-1.69569050353671,-1.6929041329534,-1.68537242144985,
-1.63346867767306,-1.62336752496367,-1.62133765813044,-1.62020950333927,
-1.61924025141759,-1.61799828986165,-1.61599668986076,-1.60436072238026,
-1.55918294844772,-1.54758193223459,-1.54443553308857,-1.54251859416192,
-1.54078166379389,-1.53854613542431,-1.53493785602654,-1.5084345314858,
-1.50559570587053,-1.47859588600493,-1.46781188556754,-1.46574570280693,
-1.46460974021478,-1.46364143356187,-1.46241050357844,-1.4604453324152,
-1.44955107374389,-1.44669929990243,-1.41634025137202,-1.40961854510899),
 .UNSPECIFIED.);
#3796=B_SPLINE_CURVE_WITH_KNOTS('',3,(#269148,#269149,#269150,#269151,#269152,
#269153,#269154,#269155,#269156,#269157,#269158,#269159,#269160,#269161,
#269162,#269163,#269164,#269165,#269166,#269167,#269168,#269169,#269170,
#269171,#269172,#269173,#269174,#269175,#269176,#269177,#269178,#269179,
#269180,#269181,#269182,#269183,#269184,#269185,#269186,#269187,#269188,
#269189,#269190,#269191,#269192,#269193,#269194,#269195,#269196,#269197,
#269198,#269199,#269200,#269201,#269202,#269203,#269204,#269205,#269206,
#269207,#269208,#269209,#269210,#269211,#269212,#269213,#269214,#269215,
#269216,#269217,#269218,#269219,#269220,#269221,#269222,#269223,#269224,
#269225,#269226,#269227,#269228,#269229,#269230,#269231,#269232,#269233,
#269234,#269235,#269236,#269237,#269238,#269239,#269240,#269241,#269242,
#269243,#269244,#269245,#269246,#269247,#269248,#269249,#269250,#269251,
#269252,#269253,#269254,#269255,#269256,#269257,#269258,#269259,#269260,
#269261,#269262,#269263,#269264,#269265,#269266,#269267,#269268,#269269,
#269270,#269271),.UNSPECIFIED.,.F.,.F.,(4,2,2,2,2,2,2,2,2,2,2,2,2,2,2,2,
2,2,2,2,2,2,2,2,2,2,2,2,2,2,2,2,2,2,2,2,2,2,2,2,2,2,2,2,2,2,2,2,2,2,2,2,
2,2,2,2,2,2,2,2,2,4),(-0.5528747849223,-0.505972514084536,-0.494698071882762,
-0.491476707206178,-0.489558558314461,-0.488019671249651,-0.485940536591137,
-0.481969629183095,-0.476968241094244,-0.465668887209196,-0.417969358499917,
-0.413713084292922,-0.412157879710706,-0.411243867733457,-0.410266881391685,
-0.408898695399195,-0.40556044419842,-0.389258079754503,-0.361022161447314,
-0.340088374844942,-0.336630908837478,-0.334454738744394,-0.332743021372802,
-0.330832530186886,-0.327647121824573,-0.315298960178662,-0.270647749782887,
-0.259186239951686,-0.257208703812095,-0.255981740869574,-0.255024418865194,
-0.253911238535114,-0.251911783486144,-0.242051121162004,-0.194444720042155,
-0.183195873274035,-0.17997659029724,-0.178058631302659,-0.176384903087572,
-0.174282719399547,-0.170146328789071,-0.164829598806549,-0.152489423670334,
-0.120160489571626,-0.103752845699109,-0.10139992704657,-0.100196618860188,
-0.0992411101530231,-0.098110518539815,-0.09603012426652,-0.0845913795460045,
-0.0462731008833756,-0.0351023996990404,-0.0343319119317644,-0.0266469561360505,
-0.0238580113325214,-0.022216730159335,-0.0205673550014028,-0.0188994884150446,
-0.0167475610645804,-0.0109046728631205,-0.000459621179054175),
 .UNSPECIFIED.);
#3797=B_SPLINE_CURVE_WITH_KNOTS('',3,(#269272,#269273,#269274,#269275,#269276,
#269277,#269278,#269279,#269280,#269281,#269282,#269283,#269284,#269285,
#269286,#269287,#269288,#269289,#269290,#269291,#269292,#269293,#269294,
#269295,#269296,#269297,#269298,#269299,#269300,#269301,#269302,#269303,
#269304,#269305,#269306,#269307,#269308,#269309,#269310,#269311,#269312,
#269313,#269314,#269315,#269316,#269317,#269318,#269319,#269320,#269321,
#269322,#269323,#269324,#269325,#269326,#269327,#269328,#269329,#269330,
#269331,#269332,#269333,#269334,#269335,#269336,#269337,#269338,#269339,
#269340,#269341,#269342,#269343,#269344,#269345,#269346,#269347,#269348,
#269349,#269350,#269351,#269352,#269353,#269354,#269355,#269356,#269357,
#269358,#269359,#269360,#269361,#269362,#269363,#269364,#269365,#269366,
#269367,#269368,#269369),.UNSPECIFIED.,.F.,.F.,(4,2,2,2,2,2,2,2,2,2,2,2,
2,2,2,2,2,2,2,2,2,2,2,2,2,2,2,2,2,2,2,2,2,2,2,2,2,2,2,2,2,2,2,2,2,2,2,2,
4),(-1.96147649178031,-1.95505603054594,-1.91261356055287,-1.90927872759127,
-1.90675660111791,-1.9055352170814,-1.90457852385727,-1.90346177263504,
-1.90149921167885,-1.89328266276818,-1.88788401525447,-1.88312367071695,
-1.85178988632294,-1.83967312297814,-1.83442284339744,-1.83033637858477,
-1.82823993528566,-1.82656396391706,-1.82464162969244,-1.82140212171954,
-1.80994719655176,-1.7625454514864,-1.75269521114947,-1.75069632097682,
-1.74958327379444,-1.74862594653794,-1.74739883157897,-1.74484810183656,
-1.74218249656584,-1.69465504147881,-1.67755850821457,-1.67405638270499,
-1.67207652639146,-1.67054416048773,-1.66854128168764,-1.66503038967535,
-1.64970198077823,-1.61293671029031,-1.60234662102942,-1.59836861182143,
-1.59547424316152,-1.5941825577858,-1.59321783559815,-1.59214326763231,
-1.59031923805818,-1.58388204478182,-1.58258691369429,-1.57780407359389,
-1.5331279783234),.UNSPECIFIED.);
#3798=B_SPLINE_CURVE_WITH_KNOTS('',3,(#269370,#269371,#269372,#269373,#269374,
#269375,#269376,#269377,#269378,#269379,#269380,#269381,#269382,#269383,
#269384,#269385,#269386,#269387,#269388,#269389,#269390,#269391,#269392,
#269393,#269394,#269395,#269396,#269397,#269398,#269399,#269400,#269401,
#269402,#269403,#269404,#269405,#269406,#269407,#269408,#269409,#269410,
#269411,#269412,#269413,#269414,#269415,#269416,#269417,#269418,#269419,
#269420,#269421,#269422,#269423,#269424,#269425,#269426,#269427,#269428,
#269429,#269430,#269431,#269432,#269433,#269434,#269435,#269436,#269437,
#269438,#269439,#269440,#269441,#269442,#269443,#269444,#269445,#269446,
#269447,#269448,#269449,#269450,#269451,#269452,#269453,#269454,#269455,
#269456,#269457,#269458,#269459,#269460,#269461,#269462,#269463,#269464,
#269465,#269466,#269467,#269468,#269469,#269470,#269471,#269472,#269473,
#269474,#269475,#269476,#269477,#269478,#269479,#269480,#269481,#269482,
#269483,#269484,#269485,#269486,#269487,#269488,#269489,#269490,#269491,
#269492,#269493,#269494,#269495,#269496,#269497,#269498,#269499,#269500,
#269501,#269502,#269503,#269504,#269505,#269506,#269507,#269508,#269509,
#269510,#269511,#269512,#269513,#269514,#269515,#269516,#269517,#269518,
#269519,#269520,#269521,#269522,#269523,#269524,#269525,#269526,#269527,
#269528,#269529,#269530,#269531,#269532,#269533,#269534,#269535,#269536,
#269537,#269538,#269539,#269540,#269541,#269542,#269543,#269544,#269545,
#269546,#269547,#269548,#269549,#269550,#269551,#269552,#269553,#269554,
#269555,#269556,#269557,#269558,#269559,#269560,#269561,#269562,#269563,
#269564,#269565,#269566,#269567,#269568,#269569,#269570,#269571,#269572,
#269573,#269574,#269575,#269576,#269577,#269578,#269579,#269580,#269581,
#269582,#269583,#269584,#269585,#269586,#269587,#269588,#269589,#269590,
#269591),.UNSPECIFIED.,.F.,.F.,(4,2,2,2,2,2,2,2,2,2,2,2,2,2,2,2,2,2,2,2,
2,2,2,2,2,2,2,2,2,2,2,2,2,2,2,2,2,2,2,2,2,2,2,2,2,2,2,2,2,2,2,2,2,2,2,2,
2,2,2,2,2,2,2,2,2,2,2,2,2,2,2,2,2,2,2,2,2,2,2,2,2,2,2,2,2,2,2,2,2,2,2,2,
2,2,2,2,2,2,2,2,2,2,2,2,2,2,2,2,2,2,4),(-1.40961854510899,-1.39528294752712,
-1.39017139497674,-1.3878538939912,-1.38610553445163,-1.38445521258963,
-1.38169108938066,-1.374313591404,-1.37295651014169,-1.32214863493301,-1.31209716250216,
-1.31006986263412,-1.30894216626392,-1.30797269862926,-1.30672967104351,
-1.30472483042209,-1.29303224721824,-1.26444189492711,-1.24017879626115,
-1.23468458906443,-1.23229883308597,-1.23053914845212,-1.22890682937387,
-1.22667313122772,-1.22102121091431,-1.19040756074199,-1.17640423192621,
-1.15873667530518,-1.155244998724,-1.15384156224724,-1.15284892398987,-1.15192735161789,
-1.15063188715384,-1.14717953470537,-1.11430535747474,-1.08246888652409,
-1.07833775426367,-1.07620946237199,-1.07448271019517,-1.07249790158377,
-1.06913227728624,-1.05616688612967,-1.01054138771595,-1.0007907099465,
-0.998780450192614,-0.997656378600019,-0.996686310446103,-0.995437677224671,
-0.993414402107754,-0.981361496558986,-0.941866242160225,-0.934664375897499,
-0.932978414167962,-0.931644281371084,-0.924265768022248,-0.921501009307394,
-0.919850234863414,-0.918101333597226,-0.915783018571538,-0.910669295189133,
-0.889597698923813,-0.859066066059149,-0.855768714567986,-0.84539736677841,
-0.843458940229042,-0.842235915740885,-0.841267869940053,-0.84012522837066,
-0.838029067607473,-0.826644468316749,-0.79408798834002,-0.770853310184806,
-0.767303165456966,-0.765084692062664,-0.763349350066088,-0.761422228776398,
-0.758231393722498,-0.746127709496577,-0.701223263575436,-0.689826177359938,
-0.687835622731793,-0.686596762660636,-0.68562746357042,-0.684496394167292,
-0.682454230180951,-0.672138050511524,-0.6474338252567,-0.61522673578255,
-0.611648149251927,-0.609420998816315,-0.607684454608237,-0.605761705458147,
-0.602591367110766,-0.590729192897329,-0.545670540509494,-0.534148129184848,
-0.532151385112578,-0.53091058553053,-0.529941022658586,-0.528811092112484,
-0.526774560735353,-0.516564783518236,-0.461941779148298,-0.456441813864775,
-0.454237171363959,-0.452612087598778,-0.450846762892103,-0.448429210024572,
-0.442750413105181,-0.434888605918536,-0.428888253392887),.UNSPECIFIED.);
#3799=B_SPLINE_CURVE_WITH_KNOTS('',3,(#269596,#269597,#269598,#269599,#269600,
#269601,#269602,#269603,#269604,#269605,#269606,#269607,#269608,#269609,
#269610,#269611,#269612,#269613,#269614,#269615,#269616,#269617,#269618,
#269619,#269620,#269621,#269622,#269623,#269624,#269625,#269626,#269627,
#269628,#269629,#269630,#269631,#269632,#269633,#269634,#269635,#269636,
#269637,#269638,#269639,#269640,#269641,#269642,#269643,#269644,#269645,
#269646,#269647,#269648,#269649,#269650,#269651,#269652,#269653,#269654,
#269655,#269656,#269657,#269658,#269659,#269660,#269661,#269662,#269663,
#269664,#269665,#269666,#269667,#269668,#269669,#269670,#269671,#269672,
#269673,#269674,#269675,#269676,#269677,#269678,#269679,#269680,#269681,
#269682,#269683,#269684,#269685,#269686,#269687,#269688,#269689,#269690,
#269691,#269692,#269693,#269694,#269695,#269696,#269697,#269698,#269699,
#269700,#269701,#269702,#269703,#269704,#269705,#269706,#269707,#269708,
#269709,#269710,#269711,#269712,#269713,#269714,#269715,#269716,#269717,
#269718,#269719,#269720,#269721,#269722,#269723,#269724,#269725,#269726,
#269727,#269728,#269729,#269730,#269731,#269732,#269733,#269734,#269735,
#269736,#269737,#269738,#269739,#269740,#269741,#269742,#269743,#269744,
#269745,#269746,#269747,#269748,#269749,#269750,#269751,#269752,#269753,
#269754,#269755,#269756,#269757,#269758,#269759,#269760,#269761,#269762,
#269763,#269764,#269765,#269766,#269767,#269768,#269769,#269770,#269771,
#269772,#269773,#269774,#269775,#269776,#269777,#269778,#269779,#269780,
#269781,#269782,#269783,#269784,#269785,#269786,#269787,#269788,#269789,
#269790,#269791,#269792,#269793,#269794,#269795,#269796,#269797,#269798,
#269799,#269800,#269801,#269802,#269803,#269804,#269805,#269806,#269807,
#269808,#269809,#269810,#269811,#269812,#269813,#269814,#269815,#269816,
#269817),.UNSPECIFIED.,.F.,.F.,(4,2,2,2,2,2,2,2,2,2,2,2,2,2,2,2,2,2,2,2,
2,2,2,2,2,2,2,2,2,2,2,2,2,2,2,2,2,2,2,2,2,2,2,2,2,2,2,2,2,2,2,2,2,2,2,2,
2,2,2,2,2,2,2,2,2,2,2,2,2,2,2,2,2,2,2,2,2,2,2,2,2,2,2,2,2,2,2,2,2,2,2,2,
2,2,2,2,2,2,2,2,2,2,2,2,2,2,2,2,2,2,4),(-1.53326539915105,-1.51441118805452,
-1.50442152866779,-1.50241556872611,-1.50130135391595,-1.50034476052139,
-1.49912083376292,-1.49715224642753,-1.48593582258234,-1.48151042352721,
-1.47103627180541,-1.44697698015568,-1.42943032460901,-1.42590555000756,
-1.42392127980359,-1.42238939199795,-1.42039267377729,-1.41690672944437,
-1.40192052397052,-1.35788981919104,-1.34870013988331,-1.34674101181716,
-1.34563688203472,-1.34467873715503,-1.34343946629258,-1.34142006050601,
-1.3290587111249,-1.32336292323251,-1.30212865474607,-1.27436578335335,
-1.27049585840478,-1.26843779703937,-1.26675136364444,-1.264763649211,-1.26131806003861,
-1.24691984310531,-1.2027061993289,-1.19307288707911,-1.19108680234397,
-1.18997668091952,-1.18901920530666,-1.18778843656621,-1.18579778813956,
-1.17410060856547,-1.12918928949458,-1.11732745774197,-1.11418331156562,
-1.11228213331211,-1.11056891524556,-1.10837725518905,-1.10486768162515,
-1.08207392558648,-1.04896968790573,-1.03753175203287,-1.03545158593828,
-1.03432115612216,-1.03336580283884,-1.03216272045711,-1.02981033159238,
-1.01340945963597,-0.981274539999996,-0.9627547858971,-0.95938354256407,
-0.957233670347246,-0.955524880743624,-0.953598930446261,-0.950342553298724,
-0.937088868806597,-0.911404253094006,-0.884398092641331,-0.880698095120589,
-0.879229561800291,-0.878332290473879,-0.877341393486364,-0.875899919081191,
-0.872092555550014,-0.850788627647346,-0.80917082336085,-0.804099054868068,
-0.801830713192611,-0.800101253661772,-0.798254087388607,-0.795355513878867,
-0.786013685648173,-0.770513916619972,-0.739648525884712,-0.734212395838738,
-0.726028723380377,-0.724068880410922,-0.722952821123224,-0.72199615681779,
-0.720774091379117,-0.718248118217946,-0.714907003993386,-0.672504457360703,
-0.651551069633753,-0.648093923271872,-0.645918101521556,-0.64420675000539,
-0.642296762512592,-0.639112419773774,-0.626771353458799,-0.582127552134743,
-0.570666282615444,-0.568689074562597,-0.567462350944377,-0.566505238999584,
-0.565392329761455,-0.563393427445758,-0.553536859778722,-0.5528747849223),
 .UNSPECIFIED.);
#3800=B_SPLINE_CURVE_WITH_KNOTS('',3,(#269819,#269820,#269821,#269822,#269823,
#269824,#269825,#269826,#269827,#269828,#269829,#269830,#269831,#269832,
#269833,#269834,#269835,#269836,#269837,#269838,#269839,#269840,#269841,
#269842,#269843,#269844,#269845,#269846,#269847,#269848,#269849,#269850,
#269851,#269852,#269853,#269854,#269855,#269856,#269857,#269858,#269859,
#269860,#269861,#269862,#269863,#269864,#269865,#269866,#269867,#269868,
#269869,#269870,#269871,#269872,#269873,#269874,#269875,#269876,#269877,
#269878,#269879,#269880,#269881,#269882,#269883,#269884,#269885,#269886,
#269887,#269888,#269889,#269890,#269891,#269892,#269893,#269894,#269895,
#269896,#269897,#269898,#269899,#269900,#269901,#269902,#269903,#269904,
#269905,#269906,#269907,#269908,#269909,#269910),.UNSPECIFIED.,.F.,.F.,
(4,2,2,2,2,2,2,2,2,2,2,2,2,2,2,2,2,2,2,2,2,2,2,2,2,2,2,2,2,2,2,2,2,2,2,
2,2,2,2,2,2,2,2,2,2,4),(-0.428888253392887,-0.389859328426633,-0.378358579402351,
-0.376362995077369,-0.375122596429184,-0.374153137331245,-0.373023085937846,
-0.37098573958892,-0.360758938600924,-0.312513641509815,-0.302206485955008,
-0.299061935482404,-0.297144969449245,-0.295407266708984,-0.293169695000154,
-0.288488566380338,-0.282351425145204,-0.267177735747699,-0.248292068467238,
-0.233933531333192,-0.222666299052573,-0.220682195170878,-0.219445363767497,
-0.218476343939001,-0.217344086694236,-0.215296015285216,-0.204866403493975,
-0.17962580300663,-0.148114346621445,-0.144522715737607,-0.142291808018878,
-0.140618395217809,-0.138782505179035,-0.13585809218805,-0.132394692094371,
-0.125713363036948,-0.0812843597065226,-0.0784753794816904,-0.0670193387557556,
-0.0650259986512003,-0.0637863187575954,-0.062816977922961,-0.0616865523121097,
-0.0596472650809289,-0.049383163613779,-0.000459594697538254),
 .UNSPECIFIED.);
#3801=B_SPLINE_CURVE_WITH_KNOTS('',3,(#269911,#269912,#269913,#269914,#269915,
#269916,#269917,#269918,#269919,#269920,#269921,#269922,#269923,#269924,
#269925,#269926,#269927,#269928,#269929,#269930,#269931,#269932,#269933,
#269934,#269935,#269936,#269937,#269938,#269939,#269940,#269941,#269942,
#269943,#269944,#269945,#269946,#269947,#269948,#269949,#269950,#269951,
#269952,#269953,#269954,#269955,#269956,#269957,#269958,#269959,#269960,
#269961,#269962,#269963,#269964,#269965,#269966,#269967,#269968,#269969,
#269970,#269971,#269972,#269973,#269974,#269975,#269976,#269977,#269978,
#269979,#269980,#269981,#269982,#269983,#269984,#269985,#269986,#269987,
#269988,#269989,#269990,#269991,#269992,#269993,#269994,#269995,#269996,
#269997,#269998,#269999,#270000,#270001,#270002,#270003,#270004,#270005,
#270006,#270007,#270008,#270009,#270010,#270011,#270012,#270013,#270014,
#270015,#270016,#270017,#270018,#270019,#270020,#270021,#270022,#270023,
#270024,#270025,#270026,#270027,#270028,#270029,#270030,#270031,#270032,
#270033,#270034,#270035,#270036,#270037,#270038,#270039,#270040,#270041,
#270042,#270043,#270044,#270045,#270046,#270047,#270048,#270049,#270050,
#270051,#270052,#270053,#270054),.UNSPECIFIED.,.F.,.F.,(4,2,2,2,2,2,2,2,
2,2,2,2,2,2,2,2,2,2,2,2,2,2,2,2,2,2,2,2,2,2,2,2,2,2,2,2,2,2,2,2,2,2,2,2,
2,2,2,2,2,2,2,2,2,2,2,2,2,2,2,2,2,2,2,2,2,2,2,2,2,2,2,4),(-1.9612040881325,
-1.95267147311146,-1.95000996591669,-1.94814032560028,-1.94652386883341,
-1.94485741353218,-1.94263906333431,-1.93908709900391,-1.92741625365267,
-1.9020119584714,-1.87333145357916,-1.8703437883954,-1.86902607541887,-1.86804813146784,
-1.86696478730102,-1.86513767045306,-1.85879857374555,-1.80916727161314,
-1.8006379616494,-1.79652104137334,-1.79314566437734,-1.79119814565534,
-1.7911768135465,-1.79115325186968,-1.79112722923263,-1.79109849092645,
-1.79106675684813,-1.79103171896284,-1.79099303961576,-1.79096067491587,
-1.79090817464123,-1.78923435367413,-1.78700190512724,-1.78340241064852,
-1.75228854452968,-1.726744721237,-1.71625509555708,-1.71420480047387,-1.71307253508992,
-1.71210426125592,-1.71086936045761,-1.7088902325968,-1.69770376826815,
-1.68335191620711,-1.6645840776608,-1.64375477107296,-1.63867262077675,
-1.63636095688298,-1.63461396905529,-1.63296270493977,-1.63019162778334,
-1.6227600190247,-1.62112671757867,-1.61950104589317,-1.57088919005932,
-1.5606661046734,-1.55862983859817,-1.55750045506403,-1.55653160643218,
-1.55529204705724,-1.5532979401195,-1.54180774819406,-1.49682586185373,
-1.48493644378235,-1.48176520483031,-1.47984307320173,-1.47810783280695,
-1.47588339267295,-1.47231124375276,-1.44013963781075,-1.41540376682114,
-1.40915133348001),.UNSPECIFIED.);
#3802=B_SPLINE_CURVE_WITH_KNOTS('',3,(#270060,#270061,#270062,#270063,#270064,
#270065,#270066,#270067,#270068,#270069,#270070,#270071,#270072,#270073,
#270074,#270075,#270076,#270077,#270078,#270079,#270080,#270081,#270082,
#270083,#270084,#270085,#270086,#270087,#270088,#270089,#270090,#270091,
#270092,#270093,#270094,#270095,#270096,#270097,#270098,#270099,#270100,
#270101,#270102,#270103,#270104,#270105,#270106,#270107,#270108,#270109,
#270110,#270111,#270112,#270113,#270114,#270115,#270116,#270117,#270118,
#270119,#270120,#270121,#270122,#270123,#270124,#270125,#270126,#270127,
#270128,#270129,#270130,#270131,#270132,#270133,#270134,#270135,#270136,
#270137,#270138,#270139,#270140,#270141,#270142,#270143,#270144,#270145,
#270146,#270147,#270148,#270149,#270150,#270151,#270152,#270153,#270154,
#270155,#270156,#270157,#270158,#270159,#270160,#270161,#270162,#270163,
#270164,#270165,#270166,#270167,#270168,#270169,#270170,#270171,#270172,
#270173,#270174,#270175,#270176,#270177,#270178,#270179,#270180,#270181,
#270182,#270183,#270184,#270185),.UNSPECIFIED.,.F.,.F.,(4,2,2,2,2,2,2,2,
2,2,2,2,2,2,2,2,2,2,2,2,2,2,2,2,2,2,2,2,2,2,2,2,2,2,2,2,2,2,2,2,2,2,2,2,
2,2,2,2,2,2,2,2,2,2,2,2,2,2,2,2,2,2,4),(-0.552743087208093,-0.551463645223767,
-0.54956658067619,-0.546441746206178,-0.534805577518398,-0.489718220054633,
-0.477907302734968,-0.475907990292114,-0.474674528531903,-0.473716672362747,
-0.47260806142404,-0.470629420631127,-0.461125444579548,-0.417263029537525,
-0.40244533081584,-0.398970174627786,-0.396975457052239,-0.395288938015448,
-0.393237941555454,-0.389402945754804,-0.36331953863117,-0.336885520914959,
-0.333312049932213,-0.322126859121565,-0.320162836966673,-0.318940032333077,
-0.317983183346863,-0.316867355037947,-0.314855253148225,-0.304764717116578,
-0.252713864175805,-0.245224834697202,-0.242464933780685,-0.240829468877453,
-0.239106039714361,-0.236837322006661,-0.231898959191383,-0.212010395067879,
-0.192531745458719,-0.16674435868709,-0.164379520992794,-0.163173825213962,
-0.162253392146647,-0.161164847488075,-0.159993433562783,-0.158179503489128,
-0.154735457764327,-0.111109549853214,-0.091488356897101,-0.0880776462791279,
-0.0859159384254847,-0.0842061701697754,-0.0822879868149217,-0.0790661507355597,
-0.0662569692942145,-0.0181025773545897,-0.0101837221765631,-0.0082936873134663,
-0.00719361884037062,-0.00625128730748574,-0.00531577404306149,-0.00410080215318163,
-0.000459732030733911),.UNSPECIFIED.);
#3803=B_SPLINE_CURVE_WITH_KNOTS('',3,(#270186,#270187,#270188,#270189,#270190,
#270191,#270192,#270193,#270194,#270195,#270196,#270197,#270198,#270199,
#270200,#270201,#270202,#270203,#270204,#270205,#270206,#270207,#270208,
#270209,#270210,#270211,#270212,#270213,#270214,#270215,#270216,#270217,
#270218,#270219,#270220,#270221,#270222,#270223,#270224,#270225,#270226,
#270227,#270228,#270229,#270230,#270231,#270232,#270233,#270234,#270235,
#270236,#270237,#270238,#270239,#270240,#270241,#270242,#270243,#270244,
#270245,#270246,#270247,#270248,#270249,#270250,#270251,#270252,#270253,
#270254,#270255,#270256,#270257,#270258,#270259,#270260,#270261,#270262,
#270263,#270264,#270265,#270266,#270267,#270268,#270269,#270270,#270271,
#270272,#270273),.UNSPECIFIED.,.F.,.F.,(4,2,2,2,2,2,2,2,2,2,2,2,2,2,2,2,
2,2,2,2,2,2,2,2,2,2,2,2,2,2,2,2,2,2,2,2,2,2,2,2,2,2,2,4),(-1.96139969443972,
-1.92301052490004,-1.89925554019589,-1.89384741182589,-1.89149537379875,
-1.88975951524084,-1.88814869674685,-1.88594369946097,-1.88036227700312,
-1.84695703292058,-1.81904336943247,-1.81612992243739,-1.81451734056035,
-1.81311666723818,-1.81214786267482,-1.811252362167,-1.8097913082852,-1.80616043606158,
-1.77714903053835,-1.74166021980585,-1.73755815576316,-1.73545271362787,
-1.73374860676013,-1.73179455239831,-1.72849300056985,-1.71599753866194,
-1.67282555784453,-1.66027663288336,-1.65814906351459,-1.65700885265265,
-1.65605461456404,-1.65486470156417,-1.65257193362423,-1.63815217947121,
-1.60968290628084,-1.58714493845121,-1.58235366487131,-1.5801129234317,
-1.57839408509754,-1.57675040113243,-1.57394557541505,-1.56614329381475,
-1.56435197886824,-1.53326539915105),.UNSPECIFIED.);
#3804=B_SPLINE_CURVE_WITH_KNOTS('',3,(#270274,#270275,#270276,#270277,#270278,
#270279,#270280,#270281,#270282,#270283,#270284,#270285,#270286,#270287,
#270288,#270289,#270290,#270291,#270292,#270293,#270294,#270295,#270296,
#270297,#270298,#270299,#270300,#270301,#270302,#270303,#270304,#270305,
#270306,#270307,#270308,#270309,#270310,#270311,#270312,#270313,#270314,
#270315,#270316,#270317,#270318,#270319,#270320,#270321,#270322,#270323,
#270324,#270325,#270326,#270327,#270328,#270329,#270330,#270331,#270332,
#270333,#270334,#270335,#270336,#270337,#270338,#270339,#270340,#270341,
#270342,#270343,#270344,#270345,#270346,#270347,#270348,#270349,#270350,
#270351,#270352,#270353,#270354,#270355,#270356,#270357,#270358,#270359,
#270360,#270361,#270362,#270363,#270364,#270365,#270366,#270367,#270368,
#270369,#270370,#270371,#270372,#270373,#270374,#270375,#270376,#270377,
#270378,#270379,#270380,#270381,#270382,#270383,#270384,#270385,#270386,
#270387,#270388,#270389,#270390,#270391,#270392,#270393,#270394,#270395,
#270396,#270397,#270398,#270399,#270400,#270401,#270402,#270403,#270404,
#270405,#270406,#270407,#270408,#270409,#270410,#270411,#270412,#270413,
#270414,#270415,#270416,#270417,#270418,#270419,#270420,#270421,#270422,
#270423,#270424,#270425,#270426,#270427,#270428,#270429,#270430,#270431,
#270432,#270433,#270434,#270435,#270436,#270437,#270438,#270439,#270440,
#270441,#270442,#270443,#270444,#270445,#270446,#270447,#270448,#270449,
#270450,#270451,#270452,#270453,#270454,#270455,#270456,#270457,#270458,
#270459,#270460,#270461,#270462,#270463,#270464,#270465,#270466,#270467,
#270468,#270469,#270470,#270471,#270472,#270473,#270474,#270475,#270476,
#270477,#270478,#270479,#270480,#270481,#270482,#270483,#270484,#270485,
#270486,#270487,#270488,#270489,#270490,#270491),.UNSPECIFIED.,.F.,.F.,
(4,2,2,2,2,2,2,2,2,2,2,2,2,2,2,2,2,2,2,2,2,2,2,2,2,2,2,2,2,2,2,2,2,2,2,
2,2,2,2,2,2,2,2,2,2,2,2,2,2,2,2,2,2,2,2,2,2,2,2,2,2,2,2,2,2,2,2,2,2,2,2,
2,2,2,2,2,2,2,2,2,2,2,2,2,2,2,2,2,2,2,2,2,2,2,2,2,2,2,2,2,2,2,2,2,2,2,2,
2,4),(-1.40915133348001,-1.40508391580612,-1.40304247644158,-1.40191201817527,
-1.40094336836695,-1.39970550964281,-1.39771690763566,-1.38642025125725,
-1.34165807170974,-1.33357200026451,-1.32776908471959,-1.32533162461402,
-1.32356362576985,-1.32194427395641,-1.31975983801312,-1.31439441689396,
-1.2764937377024,-1.26060596855579,-1.24956099127174,-1.24748210837433,
-1.24634359165815,-1.24537581468994,-1.24414901738171,-1.24172549003802,
-1.22107003869045,-1.19877478969409,-1.17714195444833,-1.17195981384783,
-1.16962988190986,-1.16787994837469,-1.16623385157811,-1.16394499399293,
-1.15794324797883,-1.10404343407514,-1.09386118370683,-1.09182691288998,
-1.09069784531232,-1.08972877217392,-1.08848828490619,-1.08649145496779,
-1.07494990806998,-1.02989841241624,-1.0181058444109,-1.01494267235182,
-1.01302211160873,-1.01128615341194,-1.00905781702317,-1.00547332501254,
-0.980787031307708,-0.951134452614773,-0.938642636192832,-0.936601167110025,
-0.935347360372408,-0.93437715148745,-0.933257331183337,-0.931265305263494,
-0.921810652711195,-0.899628081344103,-0.866672630831311,-0.861060233852381,
-0.858833625999757,-0.857203442402559,-0.855443163307646,-0.853051458713777,
-0.847520316822411,-0.839921023637918,-0.794654092326299,-0.782963769433192,
-0.780959255895347,-0.779716439020281,-0.778747134714152,-0.777619618058664,
-0.775592632211924,-0.765541598132576,-0.714659292613148,-0.713417722644121,
-0.706035451980788,-0.703270911545356,-0.701620638403293,-0.699872542827766,
-0.697555762445799,-0.692447350445574,-0.671410162002382,-0.640663568817988,
-0.636288019694443,-0.627069496456753,-0.625018079042758,-0.623872824648781,
-0.622905403773551,-0.62168677583708,-0.619223377029523,-0.591245170842583,
-0.555229149517558,-0.549729320648476,-0.547525296878297,-0.545900859531574,
-0.544136420412792,-0.541720411809742,-0.53604679344736,-0.528193210498726,
-0.483180142221446,-0.471681079668852,-0.469686237288107,-0.468446355058509,
-0.46747733578158,-0.466347838844873,-0.464311595314957,-0.454092568234796,
-0.428759893737338),.UNSPECIFIED.);
#3805=B_SPLINE_CURVE_WITH_KNOTS('',3,(#270496,#270497,#270498,#270499,#270500,
#270501,#270502,#270503,#270504,#270505,#270506,#270507,#270508,#270509,
#270510,#270511,#270512,#270513,#270514,#270515,#270516,#270517,#270518,
#270519,#270520,#270521,#270522,#270523,#270524,#270525,#270526,#270527,
#270528,#270529,#270530,#270531,#270532,#270533,#270534,#270535,#270536,
#270537,#270538,#270539,#270540,#270541,#270542,#270543,#270544,#270545,
#270546,#270547,#270548,#270549,#270550,#270551,#270552,#270553,#270554,
#270555,#270556,#270557,#270558,#270559,#270560,#270561,#270562,#270563,
#270564,#270565,#270566,#270567,#270568,#270569,#270570,#270571,#270572,
#270573,#270574,#270575,#270576,#270577,#270578,#270579,#270580,#270581,
#270582,#270583,#270584,#270585,#270586,#270587,#270588,#270589,#270590,
#270591,#270592,#270593,#270594,#270595,#270596,#270597,#270598,#270599,
#270600,#270601,#270602,#270603,#270604,#270605,#270606,#270607,#270608,
#270609,#270610,#270611,#270612,#270613,#270614,#270615,#270616,#270617,
#270618,#270619,#270620,#270621,#270622,#270623,#270624,#270625,#270626,
#270627,#270628,#270629,#270630,#270631,#270632,#270633,#270634,#270635,
#270636,#270637,#270638,#270639,#270640,#270641,#270642,#270643,#270644,
#270645,#270646,#270647,#270648,#270649,#270650,#270651,#270652,#270653,
#270654,#270655,#270656,#270657,#270658,#270659,#270660,#270661,#270662,
#270663,#270664,#270665,#270666,#270667,#270668,#270669,#270670,#270671,
#270672,#270673,#270674,#270675,#270676,#270677,#270678,#270679,#270680,
#270681,#270682,#270683,#270684,#270685,#270686,#270687,#270688,#270689,
#270690,#270691,#270692,#270693,#270694,#270695,#270696,#270697,#270698,
#270699,#270700,#270701,#270702,#270703,#270704,#270705,#270706,#270707),
 .UNSPECIFIED.,.F.,.F.,(4,2,2,2,2,2,2,2,2,2,2,2,2,2,2,2,2,2,2,2,2,2,2,2,
2,2,2,2,2,2,2,2,2,2,2,2,2,2,2,2,2,2,2,2,2,2,2,2,2,2,2,2,2,2,2,2,2,2,2,2,
2,2,2,2,2,2,2,2,2,2,2,2,2,2,2,2,2,2,2,2,2,2,2,2,2,2,2,2,2,2,2,2,2,2,2,2,
2,2,2,2,2,2,2,2,2,4),(-1.53320397388816,-1.50966452836832,-1.49825110038352,
-1.49321455786972,-1.48922128158519,-1.4871376996192,-1.48543432547076,
-1.48346216608212,-1.48008387280973,-1.46658825100414,-1.42142867176523,
-1.41172794184418,-1.40973810785624,-1.40862725409157,-1.40767001092434,
-1.40644066337572,-1.40445449003373,-1.39281706209862,-1.34798716857844,
-1.34007667138447,-1.33438426795304,-1.33198303019519,-1.33023798413126,
-1.32863749889512,-1.32647545006743,-1.32115101882626,-1.2828863095878,
-1.26712053617903,-1.25615084092342,-1.25409325214859,-1.25296775866684,
-1.25201213719766,-1.25080305859326,-1.2488839537844,-1.23857224866304,
-1.23253287675237,-1.20755141444254,-1.18157807497612,-1.17774666119621,
-1.17569670743855,-1.17401059650931,-1.17201583364374,-1.16853925635632,
-1.15369456906268,-1.10979462708462,-1.10033463391937,-1.0983588289562,
-1.09725095957179,-1.09629319685762,-1.09505915262615,-1.09305753781793,
-1.0811159432783,-1.03586908104928,-1.02451976735837,-1.02142079257929,
-1.01952960018098,-1.01781415911997,-1.01560395131832,-1.01203243310314,
-0.980907882763103,-0.946830801909978,-0.943483755075174,-0.942212709226042,
-0.941304915827275,-0.9403235659916,-0.938931134578296,-0.935442390472182,
-0.91763245860374,-0.900352503326017,-0.896770338363765,-0.870418658840243,
-0.866839776186978,-0.864627232052068,-0.862911340577742,-0.861021027375978,
-0.857926639347896,-0.84663086917273,-0.80131660920427,-0.789341843407383,
-0.787338480226561,-0.786103823990707,-0.785145880622481,-0.784038128866323,
-0.782063337520096,-0.772623089109898,-0.728730834308382,-0.713878799273427,
-0.710401280485735,-0.708406060008061,-0.706719611575979,-0.704669306603929,
-0.700837423278388,-0.674881780103308,-0.650575343825527,-0.63390512614952,
-0.631544054771103,-0.630339055991904,-0.629383509899128,-0.628254405290249,
-0.626180707877962,-0.614882552306129,-0.582736475080812,-0.558914453882635,
-0.555377920765701,-0.553178018698002,-0.552743087208093),.UNSPECIFIED.);
#3806=B_SPLINE_CURVE_WITH_KNOTS('',3,(#270709,#270710,#270711,#270712,#270713,
#270714,#270715,#270716,#270717,#270718,#270719,#270720,#270721,#270722,
#270723,#270724,#270725,#270726,#270727,#270728,#270729,#270730,#270731,
#270732,#270733,#270734,#270735,#270736,#270737,#270738,#270739,#270740,
#270741,#270742,#270743,#270744,#270745,#270746,#270747,#270748,#270749,
#270750,#270751,#270752,#270753,#270754,#270755,#270756,#270757,#270758,
#270759,#270760,#270761,#270762,#270763,#270764,#270765,#270766,#270767,
#270768,#270769,#270770,#270771,#270772,#270773,#270774,#270775,#270776,
#270777,#270778,#270779,#270780,#270781,#270782,#270783,#270784,#270785,
#270786,#270787,#270788,#270789,#270790,#270791,#270792,#270793,#270794,
#270795,#270796,#270797,#270798,#270799,#270800,#270801,#270802,#270803,
#270804,#270805,#270806,#270807,#270808,#270809,#270810,#270811,#270812),
 .UNSPECIFIED.,.F.,.F.,(4,2,2,2,2,2,2,2,2,2,2,2,2,2,2,2,2,2,2,2,2,2,2,2,
2,2,2,2,2,2,2,2,2,2,2,2,2,2,2,2,2,2,2,2,2,2,2,2,2,2,2,4),(-0.428759893737338,
-0.404716844331025,-0.402919395679492,-0.402408249614197,-0.394841801419629,
-0.392050232866161,-0.39039479631456,-0.388649277793538,-0.386349478287384,
-0.381333723302357,-0.36103039735791,-0.331095385157423,-0.325989608056533,
-0.315918560676669,-0.313997320101226,-0.312779797279136,-0.31181247564759,
-0.310666416809,-0.308552910511493,-0.296778285593322,-0.261327808611337,
-0.241255280164544,-0.237801522724213,-0.235612664094383,-0.233881247312594,
-0.231938395040218,-0.228673636288372,-0.215649318905773,-0.164598499888124,
-0.159460609943299,-0.15780545524939,-0.156766136034789,-0.155801514783849,
-0.154826061450868,-0.152413124874335,-0.126344560462695,-0.0880879544475471,
-0.0827520735253491,-0.0805722629789152,-0.0789536535959236,-0.0771838431522886,
-0.0747390824995394,-0.0688956125479379,-0.0607358789217155,-0.0159944835945941,
-0.015518045971129,-0.010656706174842,-0.0041155350938151,-0.0023037002132017,
-0.00122762359849491,-0.00061199511029617,-0.000459178790791266),
 .UNSPECIFIED.);
#3807=B_SPLINE_CURVE_WITH_KNOTS('',3,(#270813,#270814,#270815,#270816,#270817,
#270818,#270819,#270820,#270821,#270822,#270823,#270824,#270825,#270826,
#270827,#270828,#270829,#270830,#270831,#270832,#270833,#270834,#270835,
#270836,#270837,#270838,#270839,#270840,#270841,#270842,#270843,#270844,
#270845,#270846,#270847,#270848,#270849,#270850,#270851,#270852,#270853,
#270854,#270855,#270856,#270857,#270858,#270859,#270860,#270861,#270862,
#270863,#270864,#270865,#270866,#270867,#270868,#270869,#270870,#270871,
#270872,#270873,#270874,#270875,#270876,#270877,#270878,#270879,#270880,
#270881,#270882,#270883,#270884,#270885,#270886,#270887,#270888,#270889,
#270890,#270891,#270892,#270893,#270894,#270895,#270896,#270897,#270898,
#270899,#270900,#270901,#270902,#270903,#270904,#270905,#270906,#270907,
#270908,#270909,#270910,#270911,#270912,#270913,#270914,#270915,#270916,
#270917,#270918,#270919,#270920,#270921,#270922,#270923,#270924,#270925,
#270926,#270927,#270928,#270929,#270930,#270931,#270932,#270933,#270934,
#270935,#270936,#270937,#270938,#270939,#270940),.UNSPECIFIED.,.F.,.F.,
(4,2,2,2,2,2,2,2,2,2,2,2,2,2,2,2,2,2,2,2,2,2,2,2,2,2,2,2,2,2,2,2,2,2,2,
2,2,2,2,2,2,2,2,2,2,2,2,2,2,2,2,2,2,2,2,2,2,2,2,2,2,2,2,4),(-1.96190064593619,
-1.96168461615125,-1.96069057510085,-1.95851065627135,-1.94695118128126,
-1.90185828864699,-1.89011645277352,-1.8869573556812,-1.88503747934445,
-1.88330098565153,-1.8810703508325,-1.87747886034453,-1.84675338089164,
-1.82493177473323,-1.81522115627856,-1.8114579369434,-1.80867935265324,
-1.80766583705941,-1.80676125973021,-1.80579995639157,-1.80439810913233,
-1.80101313141463,-1.76765410610869,-1.73697929888347,-1.73237611593018,
-1.73015392100707,-1.72841847335981,-1.72649410831799,-1.72331453080973,
-1.71947620868156,-1.68241249019077,-1.66598120316435,-1.65473243597924,
-1.65264302178801,-1.65150197386825,-1.65053401105883,-1.64930948394577,
-1.64689793854691,-1.62792858789181,-1.60165984739963,-1.58191077107704,
-1.5769653289044,-1.57467816605182,-1.57293411133833,-1.57127397604316,
-1.56845960225752,-1.56074116168329,-1.5589297775629,-1.50897503072888,
-1.49896526855668,-1.4969401446375,-1.49581284074294,-1.49484319481182,
-1.4935992701191,-1.49159169167385,-1.47985694710387,-1.43657274798547,
-1.42342288937204,-1.42014751417196,-1.41820181962376,-1.41647002649766,
-1.41428360004047,-1.41083938795882,-1.40968633380918),.UNSPECIFIED.);
#3808=B_SPLINE_CURVE_WITH_KNOTS('',3,(#270946,#270947,#270948,#270949,#270950,
#270951,#270952,#270953,#270954,#270955,#270956,#270957,#270958,#270959,
#270960,#270961,#270962,#270963,#270964,#270965,#270966,#270967,#270968,
#270969,#270970,#270971,#270972,#270973,#270974,#270975,#270976,#270977,
#270978,#270979,#270980,#270981,#270982,#270983,#270984,#270985,#270986,
#270987,#270988,#270989,#270990,#270991,#270992,#270993,#270994,#270995,
#270996,#270997,#270998,#270999,#271000,#271001,#271002,#271003,#271004,
#271005,#271006,#271007,#271008,#271009,#271010,#271011,#271012,#271013,
#271014,#271015,#271016,#271017,#271018,#271019,#271020,#271021,#271022,
#271023,#271024,#271025,#271026,#271027,#271028,#271029,#271030,#271031,
#271032,#271033,#271034,#271035,#271036,#271037,#271038,#271039,#271040,
#271041,#271042,#271043,#271044,#271045,#271046,#271047,#271048,#271049,
#271050,#271051,#271052,#271053,#271054,#271055,#271056,#271057,#271058,
#271059,#271060,#271061,#271062,#271063,#271064,#271065,#271066,#271067,
#271068,#271069,#271070,#271071,#271072,#271073),.UNSPECIFIED.,.F.,.F.,
(4,2,2,2,2,2,2,2,2,2,2,2,2,2,2,2,2,2,2,2,2,2,2,2,2,2,2,2,2,2,2,2,2,2,2,
2,2,2,2,2,2,2,2,2,2,2,2,2,2,2,2,2,2,2,2,2,2,2,2,2,2,2,2,4),(-0.552688099404481,
-0.543080226182336,-0.539504565796958,-0.53805672524758,-0.537163091160699,
-0.53616756700887,-0.534704357243157,-0.53075057234971,-0.524762066248855,
-0.480623365040984,-0.465530749174478,-0.46203637809736,-0.460037169602566,
-0.458504601294272,-0.456520903585182,-0.453001459098836,-0.435583191356921,
-0.411571052616499,-0.387531819257294,-0.383826846181367,-0.382357280665463,
-0.381459688388236,-0.380468729446536,-0.379027667458325,-0.375224286509052,
-0.353971633733431,-0.312267525017181,-0.307204858889346,-0.304937865628943,
-0.303208346031917,-0.301360061970108,-0.298457521813873,-0.289083220949639,
-0.273506856760414,-0.244079602444988,-0.241038350357246,-0.229495587397251,
-0.227514205300479,-0.226286152109095,-0.22532882254352,-0.224216601356228,
-0.222221243885509,-0.212429893262151,-0.165921347573548,-0.153686727866053,
-0.150373988210981,-0.148435586993842,-0.146793369908302,-0.146767685125553,
-0.146742833085923,-0.144661257863149,-0.142403430462657,-0.138779885480295,
-0.131624826081075,-0.0908669722810824,-0.0740628942811457,-0.0717002075430645,
-0.0704948320728319,-0.0695392234323915,-0.068410322160803,-0.0663377102429647,
-0.0550639112307698,-0.031404766771521,-0.000460633390386513),
 .UNSPECIFIED.);
#3809=B_SPLINE_CURVE_WITH_KNOTS('',3,(#271074,#271075,#271076,#271077,#271078,
#271079,#271080,#271081,#271082,#271083,#271084,#271085,#271086,#271087,
#271088,#271089,#271090,#271091,#271092,#271093,#271094,#271095,#271096,
#271097,#271098,#271099,#271100,#271101,#271102,#271103,#271104,#271105,
#271106,#271107,#271108,#271109,#271110,#271111,#271112,#271113,#271114,
#271115,#271116,#271117,#271118,#271119,#271120,#271121,#271122,#271123,
#271124,#271125,#271126,#271127,#271128,#271129,#271130,#271131,#271132,
#271133,#271134,#271135,#271136,#271137,#271138,#271139,#271140,#271141,
#271142,#271143,#271144,#271145,#271146,#271147,#271148,#271149,#271150,
#271151,#271152,#271153,#271154,#271155,#271156,#271157,#271158,#271159,
#271160,#271161,#271162,#271163,#271164,#271165,#271166,#271167,#271168,
#271169,#271170,#271171,#271172,#271173,#271174,#271175,#271176,#271177,
#271178,#271179,#271180,#271181),.UNSPECIFIED.,.F.,.F.,(4,2,2,2,2,2,2,2,
2,2,2,2,2,2,2,2,2,2,2,2,2,2,2,2,2,2,2,2,2,2,2,2,2,2,2,2,2,2,2,2,2,2,2,2,
2,2,2,2,2,2,2,2,2,4),(-1.96139844108125,-1.95862844136409,-1.95608434317704,
-1.95439993741817,-1.95276752843083,-1.95092989768122,-1.94807308310635,
-1.93987637397639,-1.89570893868502,-1.884398659602,-1.88024286206601,-1.87724914064632,
-1.87594005117869,-1.87497317614033,-1.87390788235311,-1.87212413415349,
-1.86606151973467,-1.86492223942551,-1.8207625547489,-1.80942705350922,
-1.80441469803589,-1.8015963265701,-1.79967265328359,-1.79783116935074,
-1.79616510496926,-1.79396837401651,-1.79044062736615,-1.76688913963448,
-1.73449036700842,-1.72315654338757,-1.72108177490944,-1.71995273922696,
-1.71899763931417,-1.71779370226622,-1.71535806835029,-1.69422066415637,
-1.67435303256067,-1.65096231054999,-1.64559551229352,-1.64325023494624,
-1.64151509538318,-1.6399019034764,-1.63768891105677,-1.63206220928154,
-1.59124091749299,-1.57008729720638,-1.56629357047034,-1.56485435598024,
-1.56386410079659,-1.5629667052867,-1.56149662505678,-1.55778650913308,
-1.53356319905232,-1.53320397388816),.UNSPECIFIED.);
#3810=B_SPLINE_CURVE_WITH_KNOTS('',3,(#271182,#271183,#271184,#271185,#271186,
#271187,#271188,#271189,#271190,#271191,#271192,#271193,#271194,#271195,
#271196,#271197,#271198,#271199,#271200,#271201,#271202,#271203,#271204,
#271205,#271206,#271207,#271208,#271209,#271210,#271211,#271212,#271213,
#271214,#271215,#271216,#271217,#271218,#271219,#271220,#271221,#271222,
#271223,#271224,#271225,#271226,#271227,#271228,#271229,#271230,#271231,
#271232,#271233,#271234,#271235,#271236,#271237,#271238,#271239,#271240,
#271241,#271242,#271243,#271244,#271245,#271246,#271247,#271248,#271249,
#271250,#271251,#271252,#271253,#271254,#271255,#271256,#271257,#271258,
#271259,#271260,#271261,#271262,#271263,#271264,#271265,#271266,#271267,
#271268,#271269,#271270,#271271,#271272,#271273,#271274,#271275,#271276,
#271277,#271278,#271279,#271280,#271281,#271282,#271283,#271284,#271285,
#271286,#271287,#271288,#271289,#271290,#271291,#271292,#271293,#271294,
#271295,#271296,#271297,#271298,#271299,#271300,#271301,#271302,#271303,
#271304,#271305,#271306,#271307,#271308,#271309,#271310,#271311,#271312,
#271313,#271314,#271315,#271316,#271317,#271318,#271319,#271320,#271321,
#271322,#271323,#271324,#271325,#271326,#271327,#271328,#271329,#271330,
#271331,#271332,#271333,#271334,#271335,#271336,#271337,#271338,#271339,
#271340,#271341,#271342,#271343,#271344,#271345,#271346,#271347,#271348,
#271349,#271350,#271351,#271352,#271353,#271354,#271355,#271356,#271357,
#271358,#271359,#271360,#271361,#271362,#271363,#271364,#271365,#271366,
#271367,#271368,#271369,#271370,#271371,#271372,#271373,#271374,#271375,
#271376,#271377,#271378,#271379,#271380,#271381,#271382,#271383,#271384,
#271385,#271386,#271387,#271388,#271389,#271390,#271391),.UNSPECIFIED.,
 .F.,.F.,(4,2,2,2,2,2,2,2,2,2,2,2,2,2,2,2,2,2,2,2,2,2,2,2,2,2,2,2,2,2,2,
2,2,2,2,2,2,2,2,2,2,2,2,2,2,2,2,2,2,2,2,2,2,2,2,2,2,2,2,2,2,2,2,2,2,2,2,
2,2,2,2,2,2,2,2,2,2,2,2,2,2,2,2,2,2,2,2,2,2,2,2,2,2,2,2,2,2,2,2,2,2,2,2,
2,4),(-1.40968633380918,-1.39106742680057,-1.36246948304688,-1.34546881464893,
-1.342043193426,-1.34065039062903,-1.33965966527309,-1.33873535778086,-1.33742980206677,
-1.33390723691068,-1.3019074788918,-1.2693883787101,-1.26519682504602,-1.26305614603808,
-1.26132845087531,-1.25935254724624,-1.25602586501169,-1.24356350758808,
-1.2384553738643,-1.19998398357561,-1.18785030399311,-1.18572019061832,
-1.18457028338014,-1.18360277167804,-1.18238887581029,-1.18048045237261,
-1.17068118034152,-1.1668665169803,-1.16248498682396,-1.12612554559954,
-1.11225673600861,-1.10892768503792,-1.10697017086597,-1.10524013965216,
-1.10307229749897,-1.09968924715811,-1.08158250230395,-1.0442113848527,
-1.03219990575911,-1.03007503991455,-1.02892622238753,-1.0279585928189,
-1.02674324189647,-1.02437549468282,-1.00813738135619,-0.981492838669131,
-0.957733247361841,-0.954169152711609,-0.951946417928362,-0.950210485774761,
-0.948285519111915,-0.945104797814909,-0.93312103475791,-0.888140708118944,
-0.8766807426488,-0.874687083627747,-0.873447249883194,-0.872477818071752,
-0.871347320386012,-0.869307986752799,-0.859045478216756,-0.820972519713406,
-0.801768519518855,-0.798345051951284,-0.79616469837017,-0.794433221641158,
-0.792483132420461,-0.789188839512947,-0.775797154433583,-0.749729962387388,
-0.723355306327301,-0.719635660403577,-0.718153066161175,-0.717245044169105,
-0.716239726994622,-0.714772013826291,-0.710863562826411,-0.688579344666991,
-0.648389014961514,-0.643132163968524,-0.641022096777244,-0.639259515637705,
-0.637442184553477,-0.634757993576022,-0.627334395658667,-0.616129170063791,
-0.570568931545942,-0.56455542585171,-0.562762609822515,-0.561686316369379,
-0.560704960716779,-0.559369037015774,-0.556282116718981,-0.551972810877206,
-0.540083179658493,-0.497911694747334,-0.496119454022882,-0.488481427233226,
-0.485678182890874,-0.484019762626761,-0.482273971516346,-0.479978627920426,
-0.474991940057305,-0.454928055038549,-0.428975714778273),.UNSPECIFIED.);
#3811=B_SPLINE_CURVE_WITH_KNOTS('',3,(#271396,#271397,#271398,#271399,#271400,
#271401,#271402,#271403,#271404,#271405,#271406,#271407,#271408,#271409,
#271410,#271411,#271412,#271413,#271414,#271415,#271416,#271417,#271418,
#271419,#271420,#271421,#271422,#271423,#271424,#271425,#271426,#271427,
#271428,#271429,#271430,#271431,#271432,#271433,#271434,#271435,#271436,
#271437,#271438,#271439,#271440,#271441,#271442,#271443,#271444,#271445,
#271446,#271447,#271448,#271449,#271450,#271451,#271452,#271453,#271454,
#271455,#271456,#271457,#271458,#271459,#271460,#271461,#271462,#271463,
#271464,#271465,#271466,#271467,#271468,#271469,#271470,#271471,#271472,
#271473,#271474,#271475,#271476,#271477,#271478,#271479,#271480,#271481,
#271482,#271483,#271484,#271485,#271486,#271487,#271488,#271489,#271490,
#271491,#271492,#271493,#271494,#271495,#271496,#271497,#271498,#271499,
#271500,#271501,#271502,#271503,#271504,#271505,#271506,#271507,#271508,
#271509,#271510,#271511,#271512,#271513,#271514,#271515,#271516,#271517,
#271518,#271519,#271520,#271521,#271522,#271523,#271524,#271525,#271526,
#271527,#271528,#271529,#271530,#271531,#271532,#271533,#271534,#271535,
#271536,#271537,#271538,#271539,#271540,#271541,#271542,#271543,#271544,
#271545,#271546,#271547,#271548,#271549,#271550,#271551,#271552,#271553,
#271554,#271555,#271556,#271557,#271558,#271559,#271560,#271561,#271562,
#271563,#271564,#271565,#271566,#271567,#271568,#271569,#271570,#271571,
#271572,#271573,#271574,#271575,#271576,#271577,#271578,#271579,#271580,
#271581,#271582,#271583,#271584,#271585,#271586,#271587,#271588,#271589,
#271590,#271591,#271592,#271593,#271594,#271595,#271596,#271597,#271598,
#271599,#271600,#271601),.UNSPECIFIED.,.F.,.F.,(4,2,2,2,2,2,2,2,2,2,2,2,
2,2,2,2,2,2,2,2,2,2,2,2,2,2,2,2,2,2,2,2,2,2,2,2,2,2,2,2,2,2,2,2,2,2,2,2,
2,2,2,2,2,2,2,2,2,2,2,2,2,2,2,2,2,2,2,2,2,2,2,2,2,2,2,2,2,2,2,2,2,2,2,2,
2,2,2,2,2,2,2,2,2,2,2,2,2,2,2,2,2,2,4),(-1.53336547467346,-1.52837184435063,
-1.48442974513329,-1.47488253058741,-1.47290042235175,-1.47179060832695,
-1.47083248247449,-1.46959945575158,-1.46760190496144,-1.45579765986533,
-1.41069975383796,-1.39909887260053,-1.39597714931827,-1.39408075118677,
-1.39236619062233,-1.3901649484176,-1.38662398159865,-1.36263550520391,
-1.33059653134075,-1.31931253196297,-1.31723954400461,-1.31611064800646,
-1.31515519933782,-1.3139502338751,-1.31158889882908,-1.2948235307505,-1.25416706748176,
-1.2432600914759,-1.24020195105538,-1.23831979853081,-1.23660212294275,
-1.23441113223264,-1.23082434819327,-1.2030964015189,-1.17488958685796,
-1.16361238461625,-1.16153985383053,-1.16041111321517,-1.15945561192927,
-1.15825038498334,-1.15588828341261,-1.13910090731295,-1.09838164875309,
-1.08754909498645,-1.08449765020777,-1.08261675501951,-1.08089833135568,
-1.07870378371674,-1.07510560230137,-1.04642140931866,-1.01877849766069,
-1.00789258149254,-1.00583875196146,-1.00471388690404,-1.00375797635223,
-1.00254745440242,-1.00016033571524,-0.981248841793334,-0.952221101471087,
-0.933198710977822,-0.929809318983887,-0.927653875782813,-0.925944469073865,
-0.924021850089608,-0.920780872771078,-0.907730783989583,-0.856076908028822,
-0.851340763316662,-0.849717652431206,-0.848790116696345,-0.847820675793825,
-0.846497917426387,-0.84342895725636,-0.839138593121752,-0.827274251109634,
-0.785085431849636,-0.783334438478305,-0.775580662580146,-0.772781592659653,
-0.771138236896277,-0.769417546175213,-0.767170775937671,-0.762352554144694,
-0.743389309903729,-0.71011417866222,-0.706029152146253,-0.696466763316421,
-0.694589367860108,-0.693392754735033,-0.692437516822451,-0.691301278696193,
-0.689194880672401,-0.67718006591844,-0.639541317287688,-0.631531720317251,
-0.620640317735664,-0.61745708906259,-0.615546939879591,-0.614006137608468,
-0.611913430961883,-0.607878876761342,-0.57369546293598,-0.552688099404481),
 .UNSPECIFIED.);
#3812=B_SPLINE_CURVE_WITH_KNOTS('',3,(#271603,#271604,#271605,#271606,#271607,
#271608,#271609,#271610,#271611,#271612,#271613,#271614,#271615,#271616,
#271617,#271618,#271619,#271620,#271621,#271622,#271623,#271624,#271625,
#271626,#271627,#271628,#271629,#271630,#271631,#271632,#271633,#271634,
#271635,#271636,#271637,#271638,#271639,#271640,#271641,#271642,#271643,
#271644,#271645,#271646,#271647,#271648,#271649,#271650,#271651,#271652,
#271653,#271654,#271655,#271656,#271657,#271658,#271659,#271660,#271661,
#271662,#271663,#271664,#271665,#271666,#271667,#271668,#271669,#271670,
#271671,#271672,#271673,#271674,#271675,#271676,#271677,#271678,#271679,
#271680,#271681,#271682,#271683,#271684,#271685,#271686,#271687,#271688,
#271689,#271690,#271691,#271692,#271693,#271694,#271695,#271696,#271697,
#271698,#271699,#271700,#271701,#271702,#271703,#271704,#271705,#271706,
#271707,#271708,#271709,#271710),.UNSPECIFIED.,.F.,.F.,(4,2,2,2,2,2,2,2,
2,2,2,2,2,2,2,2,2,2,2,2,2,2,2,2,2,2,2,2,2,2,2,2,2,2,2,2,2,2,2,2,2,2,2,2,
2,2,2,2,2,2,2,2,2,4),(-0.428975714778273,-0.426294289416057,-0.40993005346988,
-0.407558066930467,-0.406341681853969,-0.405373836461037,-0.404225474340388,
-0.402103323387923,-0.390158402561099,-0.353353699220583,-0.334672070253794,
-0.331267833299295,-0.329093278878789,-0.327362292265962,-0.325408383853849,
-0.322096964581708,-0.308477197377358,-0.281614425310441,-0.268637902858494,
-0.265586062554237,-0.253981995449396,-0.251981381344263,-0.250739465741727,
-0.249769868660508,-0.248640859213042,-0.246608378460792,-0.236470268848025,
-0.183707896345193,-0.176840259344229,-0.174155621690342,-0.172520029576801,
-0.170797472072009,-0.168499366602091,-0.165941834277573,-0.161609776557055,
-0.152444782583097,-0.115749441376234,-0.115301071137147,-0.098564513831558,
-0.096183043635308,-0.0949647617296688,-0.0939969867365006,-0.0928505717771237,
-0.0907368404218699,-0.0789728306255426,-0.0360263231000887,-0.0244352099508055,
-0.0199538763255009,-0.0177552350180094,-0.0160988411211704,-0.0144808829084192,
-0.0126017398449633,-0.00991766704936141,-0.000458885783622974),
 .UNSPECIFIED.);
#3813=B_SPLINE_CURVE_WITH_KNOTS('',3,(#271711,#271712,#271713,#271714,#271715,
#271716,#271717,#271718,#271719,#271720,#271721,#271722,#271723,#271724,
#271725,#271726,#271727,#271728,#271729,#271730,#271731,#271732,#271733,
#271734,#271735,#271736,#271737,#271738,#271739,#271740,#271741,#271742,
#271743,#271744,#271745,#271746,#271747,#271748,#271749,#271750,#271751,
#271752,#271753,#271754,#271755,#271756,#271757,#271758,#271759,#271760,
#271761,#271762,#271763,#271764,#271765,#271766,#271767,#271768,#271769,
#271770,#271771,#271772,#271773,#271774,#271775,#271776,#271777,#271778,
#271779,#271780,#271781,#271782,#271783,#271784,#271785,#271786,#271787,
#271788,#271789,#271790,#271791,#271792,#271793,#271794,#271795,#271796,
#271797,#271798,#271799,#271800,#271801,#271802,#271803,#271804,#271805,
#271806,#271807,#271808,#271809,#271810),.UNSPECIFIED.,.F.,.F.,(4,3,3,3,
3,3,3,3,3,3,3,3,3,3,3,3,3,3,3,3,3,3,3,3,3,3,3,3,3,3,3,3,3,4),(172.787595947799,
172.910921322851,173.034741091045,173.159172349731,173.183505325507,173.29520328459,
173.406702633491,173.51809106504,173.629411511197,173.740706806736,173.852102689415,
173.963544589889,174.075203755146,174.180839176163,174.292537996151,174.4040382227,
174.515427541451,174.62674888277,174.738045079852,174.849441866703,174.960884674288,
175.072544739568,175.17817302682,175.289867246144,175.401362865262,175.5127475755,
175.624064314911,175.735355924369,175.846748182612,175.958186486273,176.069842148544,
176.175506877477,176.287193067858,176.326648334931),.UNSPECIFIED.);
#3814=B_SPLINE_CURVE_WITH_KNOTS('',3,(#271816,#271817,#271818,#271819,#271820,
#271821,#271822,#271823,#271824,#271825,#271826,#271827,#271828,#271829,
#271830,#271831,#271832,#271833,#271834,#271835,#271836,#271837,#271838,
#271839,#271840,#271841,#271842,#271843,#271844,#271845,#271846,#271847,
#271848,#271849,#271850,#271851,#271852,#271853,#271854,#271855,#271856,
#271857,#271858,#271859,#271860,#271861,#271862,#271863,#271864,#271865,
#271866,#271867,#271868,#271869,#271870,#271871,#271872,#271873,#271874,
#271875,#271876,#271877,#271878,#271879,#271880,#271881,#271882,#271883,
#271884,#271885,#271886,#271887,#271888,#271889,#271890,#271891,#271892,
#271893,#271894,#271895,#271896,#271897,#271898,#271899,#271900,#271901,
#271902,#271903,#271904,#271905,#271906,#271907,#271908,#271909,#271910,
#271911,#271912,#271913,#271914,#271915),.UNSPECIFIED.,.F.,.F.,(4,3,3,3,
3,3,3,3,3,3,3,3,3,3,3,3,3,3,3,3,3,3,3,3,3,3,3,3,3,3,3,3,3,4),(179.070781255062,
179.180731622204,179.29056170515,179.400316708238,179.51004171136,179.619858971895,
179.729722080855,179.839787565431,179.920490921002,180.032021520138,180.143353165283,
180.254573782191,180.365726576664,180.476854656937,180.588085464791,180.699363098701,
180.810861893943,180.918222920992,181.030131969172,181.141840515982,181.25343684756,
181.364963554317,181.476463128009,181.588058687758,181.69969799648,181.811548524454,
181.915954920982,182.027784331895,182.139452203846,182.256796239415,182.368281431854,
182.479735307744,182.591228863916,182.608828346121),.UNSPECIFIED.);
#3815=B_SPLINE_CURVE_WITH_KNOTS('',3,(#271916,#271917,#271918,#271919,#271920,
#271921,#271922,#271923,#271924,#271925,#271926,#271927,#271928,#271929,
#271930,#271931,#271932,#271933,#271934,#271935,#271936,#271937,#271938,
#271939,#271940,#271941,#271942,#271943,#271944,#271945,#271946,#271947,
#271948,#271949,#271950,#271951,#271952,#271953,#271954,#271955,#271956,
#271957,#271958,#271959,#271960,#271961,#271962,#271963,#271964,#271965,
#271966,#271967,#271968,#271969,#271970,#271971,#271972,#271973,#271974,
#271975,#271976,#271977,#271978,#271979,#271980,#271981,#271982,#271983,
#271984,#271985,#271986,#271987,#271988,#271989,#271990,#271991,#271992,
#271993,#271994,#271995,#271996,#271997,#271998,#271999,#272000,#272001,
#272002,#272003,#272004,#272005,#272006,#272007,#272008,#272009,#272010,
#272011,#272012,#272013,#272014,#272015,#272016,#272017,#272018,#272019,
#272020,#272021,#272022,#272023,#272024,#272025,#272026,#272027,#272028,
#272029,#272030,#272031,#272032,#272033,#272034,#272035,#272036,#272037,
#272038,#272039,#272040,#272041,#272042,#272043,#272044,#272045,#272046,
#272047,#272048,#272049,#272050,#272051,#272052,#272053,#272054,#272055,
#272056,#272057,#272058,#272059,#272060,#272061,#272062,#272063,#272064,
#272065,#272066,#272067,#272068,#272069,#272070,#272071,#272072,#272073,
#272074,#272075,#272076,#272077,#272078,#272079,#272080,#272081,#272082,
#272083,#272084,#272085,#272086,#272087,#272088,#272089,#272090,#272091,
#272092,#272093,#272094,#272095,#272096,#272097,#272098,#272099,#272100,
#272101,#272102,#272103,#272104,#272105),.UNSPECIFIED.,.F.,.F.,(4,2,2,2,
2,2,2,2,2,2,2,2,2,2,2,2,2,2,2,2,2,2,2,2,2,2,2,2,2,2,2,2,2,2,2,2,2,2,2,2,
2,2,2,2,2,2,2,2,2,2,2,2,2,2,2,2,2,2,2,2,2,2,2,2,2,2,2,2,2,2,2,2,2,2,2,2,
2,2,2,2,2,2,2,2,2,2,2,2,2,2,2,2,2,2,4),(-1.9614308235416,-1.94268900312366,
-1.94097478816021,-1.93984265879353,-1.93892930799748,-1.93797196576572,
-1.93677921220793,-1.93491631367841,-1.92560864232203,-1.91834408018366,
-1.90452575359003,-1.89212755721821,-1.86756302972069,-1.8637402797583,
-1.86169175717883,-1.86000517100933,-1.85800789120636,-1.85452196051238,
-1.83955418950439,-1.79576306360682,-1.78942937129978,-1.78663823525168,
-1.78447142584376,-1.78332570005554,-1.78332282173635,-1.78331993323669,
-1.78331703450265,-1.78331412545015,-1.78331120601872,-1.78330827614636,
-1.78330533579758,-1.78330238489228,-1.7832994233645,-1.78329645114521,
-1.78329346816853,-1.78329047438485,-1.78328746972599,-1.78328445411386,
-1.78328142748082,-1.78327838976972,-1.78327534091679,-1.78327228084261,
-1.78326920947643,-1.78326612674772,-1.78326303259987,-1.783259926961,-1.78325680975979,
-1.78325368093163,-1.78325054039445,-1.78324738808096,-1.78324422391465,
-1.78324104783337,-1.78323785974327,-1.78323456594562,-1.78323121572594,
-1.78322780802806,-1.7832243417827,-1.78322081588857,-1.78321722922791,
-1.78321358067877,-1.78320986907769,-1.78320609322951,-1.78320225191204,
-1.78319834390456,-1.78319436794346,-1.78319032273446,-1.78223382367081,
-1.78100584010655,-1.77902206808031,-1.76740288404476,-1.76463201604894,
-1.73216599774,-1.71227154692013,-1.70817406294939,-1.70607025292478,-1.70436713886138,
-1.70241388061299,-1.69911291230588,-1.68661227720452,-1.64035330500017,
-1.63057691350791,-1.62858409354707,-1.62747329241742,-1.62651642311937,
-1.62528847978424,-1.6233074629858,-1.61177054201696,-1.58272870650308,
-1.55611307498688,-1.55226524108138,-1.55021110886266,-1.54852390237823,
-1.54653058526767,-1.54306342431935,-1.53336547467346),.UNSPECIFIED.);
#3816=B_SPLINE_CURVE_WITH_KNOTS('',3,(#272107,#272108,#272109,#272110,#272111,
#272112,#272113,#272114,#272115,#272116,#272117,#272118,#272119,#272120,
#272121,#272122,#272123,#272124,#272125,#272126,#272127,#272128,#272129,
#272130,#272131,#272132,#272133,#272134,#272135,#272136,#272137,#272138,
#272139,#272140,#272141,#272142,#272143,#272144,#272145,#272146,#272147,
#272148,#272149,#272150,#272151,#272152,#272153,#272154,#272155,#272156,
#272157,#272158,#272159,#272160,#272161,#272162,#272163,#272164,#272165,
#272166,#272167,#272168,#272169,#272170,#272171,#272172,#272173,#272174,
#272175,#272176,#272177,#272178,#272179,#272180,#272181,#272182,#272183,
#272184,#272185),.UNSPECIFIED.,.F.,.F.,(4,3,3,3,3,3,3,3,3,3,3,3,3,3,3,3,
3,3,3,3,3,3,3,3,3,3,4),(176.326648334931,176.43810614833,176.549468213479,
176.660777418181,176.772076570763,176.883486761318,176.994956518131,177.106630489581,
177.172840728134,177.284544809411,177.396050364686,177.507445049464,177.618771784714,
177.730073394283,177.841475578811,177.952923784954,178.064589178818,178.170174578791,
178.282750413203,178.392857900582,178.502858512952,178.61279717524,178.727293194952,
178.837307342147,178.947380692747,179.057620733242,179.070781254086),
 .UNSPECIFIED.);
#3817=B_SPLINE_CURVE_WITH_KNOTS('',3,(#272186,#272187,#272188,#272189,#272190,
#272191,#272192,#272193,#272194,#272195,#272196,#272197,#272198,#272199,
#272200,#272201,#272202,#272203,#272204,#272205,#272206,#272207,#272208,
#272209,#272210,#272211,#272212,#272213,#272214,#272215,#272216,#272217,
#272218,#272219,#272220,#272221,#272222,#272223,#272224,#272225,#272226,
#272227,#272228,#272229,#272230,#272231,#272232,#272233,#272234,#272235,
#272236,#272237,#272238,#272239,#272240,#272241,#272242,#272243,#272244,
#272245,#272246,#272247,#272248,#272249,#272250,#272251,#272252,#272253,
#272254,#272255,#272256,#272257,#272258,#272259,#272260,#272261,#272262,
#272263,#272264,#272265,#272266,#272267,#272268,#272269,#272270,#272271,
#272272,#272273,#272274,#272275,#272276,#272277,#272278,#272279,#272280,
#272281,#272282),.UNSPECIFIED.,.F.,.F.,(4,3,3,3,3,3,3,3,3,3,3,3,3,3,3,3,
3,3,3,3,3,3,3,3,3,3,3,3,3,3,3,3,4),(179.070781254618,179.167508429447,179.279232171007,
179.390757034655,179.502170802123,179.613516365171,179.72483651818,179.836256656482,
179.947722524142,180.059404856864,180.164842280104,180.276572613084,180.388104921402,
180.499526644752,180.610880655354,180.722209728673,180.833639447233,180.945115271315,
181.056808057843,181.162176130761,181.273712396525,181.385049880979,181.496276444199,
181.607435281783,181.718569491901,181.829806385347,181.941090169468,182.052594773618,
182.159509981418,182.272001570259,182.383719822213,182.496598079497,182.609476336781),
 .UNSPECIFIED.);
#3818=B_SPLINE_CURVE_WITH_KNOTS('',3,(#272286,#272287,#272288,#272289,#272290,
#272291,#272292,#272293,#272294,#272295,#272296,#272297,#272298,#272299,
#272300,#272301,#272302,#272303,#272304,#272305,#272306,#272307,#272308,
#272309,#272310,#272311,#272312,#272313,#272314,#272315,#272316,#272317,
#272318,#272319,#272320,#272321,#272322,#272323,#272324,#272325,#272326,
#272327,#272328,#272329,#272330,#272331,#272332,#272333,#272334,#272335,
#272336,#272337,#272338,#272339,#272340,#272341,#272342,#272343,#272344,
#272345,#272346),.UNSPECIFIED.,.F.,.F.,(4,3,3,3,3,3,3,3,3,3,3,3,3,3,3,3,
3,3,3,3,4),(-4.09254174883831,-3.98933540262706,-3.88362403077663,-3.77807219570531,
-3.67264620016847,-3.56728749237124,-3.46196026146344,-3.35662874243922,
-3.25118948387453,-3.14568938024508,-3.04001271921558,-2.9920015519703,
-2.88746494371954,-2.78310353644332,-2.6788397915561,-2.57463623079532,
-2.47045545788326,-2.36619046068214,-2.26188581379375,-2.15739845815038,
-2.06549250598675),.UNSPECIFIED.);
#3819=B_SPLINE_CURVE_WITH_KNOTS('',3,(#272350,#272351,#272352,#272353,#272354,
#272355,#272356,#272357,#272358,#272359,#272360,#272361,#272362,#272363,
#272364,#272365,#272366,#272367,#272368,#272369,#272370,#272371,#272372,
#272373,#272374,#272375,#272376,#272377,#272378,#272379,#272380,#272381,
#272382,#272383),.UNSPECIFIED.,.F.,.F.,(4,3,3,3,3,3,3,3,3,3,3,4),(0.,0.107977626581242,
0.219196923257323,0.327096938677548,0.434999393044677,0.542933442426255,
0.650928272809477,0.75909084708409,0.867351523472262,0.975811259859153,
0.997731999989892,1.11419103802964),.UNSPECIFIED.);
#3820=B_SPLINE_CURVE_WITH_KNOTS('',3,(#272385,#272386,#272387,#272388,#272389,
#272390,#272391,#272392,#272393,#272394,#272395,#272396,#272397,#272398,
#272399,#272400,#272401,#272402,#272403,#272404,#272405,#272406,#272407,
#272408,#272409,#272410,#272411,#272412,#272413,#272414,#272415,#272416,
#272417,#272418,#272419,#272420,#272421,#272422,#272423,#272424,#272425,
#272426,#272427,#272428,#272429,#272430,#272431,#272432,#272433,#272434,
#272435,#272436,#272437,#272438,#272439,#272440,#272441,#272442,#272443,
#272444,#272445,#272446,#272447,#272448,#272449,#272450,#272451,#272452,
#272453,#272454,#272455,#272456,#272457,#272458,#272459,#272460,#272461,
#272462,#272463,#272464,#272465,#272466,#272467,#272468,#272469,#272470,
#272471,#272472,#272473,#272474,#272475,#272476,#272477,#272478,#272479,
#272480,#272481,#272482,#272483,#272484,#272485,#272486,#272487,#272488,
#272489,#272490,#272491,#272492,#272493,#272494,#272495,#272496,#272497,
#272498,#272499,#272500,#272501,#272502,#272503,#272504,#272505,#272506,
#272507,#272508,#272509,#272510,#272511,#272512,#272513,#272514,#272515,
#272516,#272517,#272518,#272519,#272520,#272521,#272522,#272523,#272524,
#272525,#272526,#272527,#272528,#272529,#272530,#272531,#272532,#272533,
#272534,#272535,#272536,#272537,#272538,#272539,#272540,#272541,#272542,
#272543,#272544,#272545,#272546,#272547,#272548,#272549,#272550,#272551,
#272552,#272553,#272554,#272555,#272556,#272557,#272558,#272559,#272560,
#272561,#272562,#272563,#272564,#272565,#272566,#272567,#272568,#272569,
#272570,#272571,#272572,#272573,#272574),.UNSPECIFIED.,.F.,.F.,(4,3,3,3,
3,3,3,3,3,3,3,3,3,3,3,3,3,3,3,3,3,3,3,3,3,3,3,3,3,3,3,3,3,3,3,3,3,3,3,3,
3,3,3,3,3,3,3,3,3,3,3,3,3,3,3,3,3,3,3,3,3,3,3,4),(1.11419103844213,1.21719280051008,
1.32003416186357,1.42278762303634,1.52549195609498,1.62818584556488,1.73097732788672,
1.83382151759089,1.93684671784687,1.99546399997979,2.10112854781365,2.20663431253005,
2.31201552937527,2.4173302707785,2.52261439146672,2.62790370121181,2.73330245386298,
2.83876289331518,2.9444018424341,2.99319599996969,3.09888197434551,3.20441296474065,
3.30982494020846,3.41517386477733,3.52049555101897,3.62582577011254,3.73127024136871,
3.83677921532455,3.94247055732954,3.99092799995959,4.09628474419618,4.20148036114117,
4.30654951999312,4.41155120731135,4.51652176472632,4.62149748813044,4.72658479154611,
4.83173454902658,4.93706728469541,4.98865999994949,5.09419322308703,5.19956760510387,
5.30481804223367,5.41000246650403,5.51515694593056,5.62031750420636,5.72558976703579,
5.83092483105164,5.93644146087887,5.98639199993938,6.09191543290443,6.19728038085416,
6.30252196221905,6.40769789584472,6.51284426401526,6.6179971050861,6.72326230422794,
6.8285906675891,6.93410123136067,6.98412399992928,7.10015672991934,7.21584063271221,
7.33095558898145,7.39737594217472),.UNSPECIFIED.);
#3821=B_SPLINE_CURVE_WITH_KNOTS('',3,(#272576,#272577,#272578,#272579,#272580,
#272581,#272582,#272583,#272584,#272585),.UNSPECIFIED.,.F.,.F.,(4,1,1,1,
1,1,1,4),(7.39737634520923,7.98185599991918,8.97958799990908,9.97731999989899,
10.9750519998889,11.9727839998788,12.9705159998687,13.6805616523888),
 .UNSPECIFIED.);
#3822=B_SPLINE_CURVE_WITH_KNOTS('',3,(#272587,#272588,#272589,#272590,#272591,
#272592,#272593,#272594,#272595,#272596,#272597),.UNSPECIFIED.,.F.,.F.,
(4,1,1,1,1,1,1,1,4),(13.6805616523888,13.9682479998586,14.9659799998485,
15.9637119998384,16.9614439998283,17.9591759998182,18.9569079998081,19.954639999798,
19.9637469595684),.UNSPECIFIED.);
#3823=B_SPLINE_CURVE_WITH_KNOTS('',3,(#272599,#272600,#272601,#272602,#272603,
#272604,#272605,#272606,#272607,#272608,#272609,#272610,#272611,#272612,
#272613,#272614,#272615,#272616,#272617,#272618,#272619,#272620,#272621,
#272622,#272623,#272624,#272625,#272626,#272627,#272628,#272629,#272630,
#272631,#272632,#272633,#272634,#272635,#272636,#272637,#272638,#272639,
#272640,#272641,#272642,#272643,#272644,#272645,#272646,#272647,#272648,
#272649,#272650,#272651,#272652,#272653,#272654,#272655,#272656,#272657,
#272658,#272659,#272660,#272661,#272662,#272663,#272664,#272665,#272666,
#272667,#272668,#272669,#272670,#272671,#272672,#272673,#272674,#272675,
#272676,#272677,#272678,#272679,#272680,#272681,#272682,#272683,#272684,
#272685,#272686,#272687,#272688,#272689,#272690,#272691,#272692,#272693,
#272694,#272695,#272696,#272697,#272698,#272699,#272700,#272701,#272702,
#272703,#272704,#272705,#272706,#272707,#272708,#272709,#272710,#272711,
#272712,#272713,#272714,#272715,#272716,#272717,#272718,#272719,#272720,
#272721,#272722,#272723,#272724,#272725,#272726,#272727,#272728,#272729,
#272730,#272731,#272732,#272733,#272734,#272735,#272736,#272737,#272738,
#272739,#272740,#272741,#272742,#272743,#272744,#272745,#272746,#272747,
#272748,#272749,#272750,#272751,#272752,#272753,#272754,#272755,#272756,
#272757,#272758,#272759,#272760,#272761,#272762,#272763,#272764,#272765,
#272766,#272767,#272768,#272769,#272770,#272771,#272772,#272773,#272774,
#272775,#272776,#272777,#272778,#272779,#272780,#272781,#272782,#272783,
#272784,#272785,#272786,#272787,#272788),.UNSPECIFIED.,.F.,.F.,(4,3,3,3,
3,3,3,3,3,3,3,3,3,3,3,3,3,3,3,3,3,3,3,3,3,3,3,3,3,3,3,3,3,3,3,3,3,3,3,3,
3,3,3,3,3,3,3,3,3,3,3,3,3,3,3,3,3,3,3,3,3,3,3,4),(19.9637469595684,20.0690782985152,
20.1794900111743,20.2845353554799,20.3895172806125,20.4944721574661,20.5994363154026,
20.7045140318183,20.8096579909059,20.9149798917531,20.9523719997879,21.0578734648353,
21.1632159338049,21.2684343889456,21.373586807792,21.4787093080487,21.5838379631019,
21.689078658814,21.7943823015801,21.8998680679502,21.9501039997778,22.0556054642515,
22.1609479326213,22.2661663871265,22.3713188053156,22.4764413048939,22.581569959249,
22.6868106542371,22.7921142962635,22.8976000618774,22.9478359997677,23.0533374659502,
23.1586799360592,23.2638983923401,23.3690508123263,23.4741733137208,23.5793019699084,
23.6845426667408,23.7898463106212,23.8953320780843,23.9455679997576,24.0510694651247,
24.1564119344083,24.2616303898528,24.3667828089963,24.4719053095432,24.5770339648792,
24.6822746608604,24.7875783038884,24.8930640705064,24.9432999997475,25.0488014651073,
25.1541439343807,25.2593623898114,25.3645148089389,25.4696373094671,25.5747659647825,
25.6800066607395,25.7853103037412,25.89079607033,25.9410319997374,26.0685438801395,
26.1944144505649,26.2469320748526),.UNSPECIFIED.);
#3824=B_SPLINE_CURVE_WITH_KNOTS('',3,(#272790,#272791,#272792,#272793,#272794,
#272795,#272796,#272797,#272798,#272799),.UNSPECIFIED.,.F.,.F.,(4,1,1,1,
1,1,1,4),(26.246932266748,26.9387639997273,27.9364959997172,28.9342279997071,
29.931959999697,30.9296919996869,31.9274239996768,32.5301175739276),
 .UNSPECIFIED.);
#3825=B_SPLINE_CURVE_WITH_KNOTS('',3,(#272801,#272802,#272803,#272804,#272805,
#272806,#272807,#272808,#272809,#272810),.UNSPECIFIED.,.F.,.F.,(4,1,1,1,
1,1,1,4),(32.5301175739276,32.9251559996667,33.9228879996566,34.9206199996464,
35.9183519996363,36.9160839996262,37.9138159996161,38.813294074911),
 .UNSPECIFIED.);
#3826=B_SPLINE_CURVE_WITH_KNOTS('',3,(#272812,#272813,#272814,#272815,#272816,
#272817,#272818,#272819,#272820,#272821,#272822,#272823,#272824,#272825,
#272826,#272827,#272828,#272829,#272830,#272831,#272832,#272833,#272834,
#272835,#272836,#272837,#272838,#272839,#272840,#272841,#272842,#272843,
#272844,#272845,#272846,#272847,#272848,#272849,#272850,#272851,#272852,
#272853,#272854,#272855,#272856,#272857,#272858,#272859,#272860,#272861,
#272862,#272863,#272864,#272865,#272866,#272867,#272868,#272869,#272870,
#272871,#272872,#272873,#272874,#272875,#272876,#272877,#272878,#272879,
#272880,#272881,#272882,#272883,#272884,#272885,#272886,#272887,#272888,
#272889,#272890,#272891,#272892,#272893,#272894,#272895,#272896,#272897,
#272898,#272899,#272900,#272901,#272902,#272903,#272904,#272905,#272906,
#272907,#272908,#272909,#272910,#272911,#272912,#272913,#272914,#272915,
#272916,#272917,#272918,#272919,#272920,#272921,#272922,#272923,#272924,
#272925,#272926,#272927,#272928,#272929,#272930,#272931,#272932,#272933,
#272934,#272935,#272936,#272937,#272938,#272939,#272940,#272941,#272942,
#272943,#272944,#272945,#272946,#272947,#272948,#272949,#272950,#272951,
#272952,#272953,#272954,#272955,#272956,#272957,#272958,#272959,#272960,
#272961,#272962,#272963,#272964,#272965,#272966,#272967,#272968,#272969,
#272970,#272971,#272972,#272973,#272974,#272975,#272976,#272977,#272978,
#272979,#272980,#272981,#272982,#272983,#272984,#272985,#272986,#272987,
#272988,#272989,#272990,#272991,#272992,#272993,#272994,#272995,#272996,
#272997,#272998,#272999,#273000,#273001),.UNSPECIFIED.,.F.,.F.,(4,3,3,3,
3,3,3,3,3,3,3,3,3,3,3,3,3,3,3,3,3,3,3,3,3,3,3,3,3,3,3,3,3,3,3,3,3,3,3,3,
3,3,3,3,3,3,3,3,3,3,3,3,3,3,3,3,3,3,3,3,3,3,3,4),(38.8133028811072,38.911547999606,
39.0170494650914,39.1223919344932,39.2276103900556,39.3327628093167,39.4378853099806,
39.5430139654329,39.6482546615285,39.7535583046701,39.859044071399,39.9092799995959,
40.0147814650811,40.1201239344827,40.2253423900448,40.3304948093057,40.4356173099693,
40.5407459654213,40.6459866615167,40.751290304658,40.8567760713867,40.9070119995858,
41.0125134650709,41.1178559344726,41.2230743900347,41.3282268092956,41.4333493099592,
41.5384779654113,41.6437186615067,41.749022304648,41.8545080713767,41.9047439995757,
42.0102454650609,42.1155879344627,42.2208063900248,42.3259588092858,42.4310813099494,
42.5362099654016,42.641450661497,42.7467543046384,42.8522400713671,42.9024759995656,
43.0079774650508,43.1133199344525,43.2185383900146,43.3236908092756,43.4288133099392,
43.5339419653913,43.6391826614867,43.7444863046281,43.8499720713568,43.9002079995555,
44.0057094650407,44.1110519344423,44.2162703900044,44.3214228092653,44.4265453099289,
44.5316739653811,44.6369146614765,44.7422183046179,44.8477040713466,44.8979399995454,
45.0494261607052,45.0964881882868),.UNSPECIFIED.);
#3827=B_SPLINE_CURVE_WITH_KNOTS('',3,(#273003,#273004,#273005,#273006,#273007,
#273008,#273009,#273010,#273011,#273012),.UNSPECIFIED.,.F.,.F.,(4,1,1,1,
1,1,1,4),(45.0964914212202,45.8956719995353,46.8934039995252,47.8911359995151,
48.888867999505,49.8865999994949,50.8843319994848,51.3796734954663),
 .UNSPECIFIED.);
#3828=B_SPLINE_CURVE_WITH_KNOTS('',3,(#273014,#273015,#273016,#273017,#273018,
#273019,#273020,#273021,#273022,#273023),.UNSPECIFIED.,.F.,.F.,(4,1,1,1,
1,1,1,4),(51.3796734954663,51.8820639994747,52.8797959994646,53.8775279994545,
54.8752599994444,55.8729919994343,56.8707239994242,57.6628562328904),
 .UNSPECIFIED.);
#3829=B_SPLINE_CURVE_WITH_KNOTS('',3,(#273025,#273026,#273027,#273028,#273029,
#273030,#273031,#273032,#273033,#273034,#273035,#273036,#273037,#273038,
#273039,#273040,#273041,#273042,#273043,#273044,#273045,#273046,#273047,
#273048,#273049,#273050,#273051,#273052,#273053,#273054,#273055,#273056,
#273057,#273058,#273059,#273060,#273061,#273062,#273063,#273064,#273065,
#273066,#273067,#273068,#273069,#273070,#273071,#273072,#273073,#273074,
#273075,#273076,#273077,#273078,#273079,#273080,#273081,#273082,#273083,
#273084,#273085,#273086,#273087,#273088,#273089,#273090,#273091,#273092,
#273093,#273094,#273095,#273096,#273097,#273098,#273099,#273100,#273101,
#273102,#273103,#273104,#273105,#273106,#273107,#273108,#273109,#273110,
#273111,#273112,#273113,#273114,#273115,#273116,#273117,#273118,#273119,
#273120,#273121,#273122,#273123,#273124,#273125,#273126,#273127,#273128,
#273129,#273130,#273131,#273132,#273133,#273134,#273135,#273136,#273137,
#273138,#273139,#273140,#273141,#273142,#273143,#273144,#273145,#273146,
#273147,#273148,#273149,#273150,#273151,#273152,#273153,#273154,#273155,
#273156,#273157,#273158,#273159,#273160,#273161,#273162,#273163,#273164,
#273165,#273166,#273167,#273168,#273169,#273170,#273171,#273172,#273173,
#273174,#273175,#273176,#273177,#273178,#273179,#273180,#273181,#273182,
#273183,#273184,#273185,#273186,#273187,#273188,#273189,#273190,#273191,
#273192,#273193,#273194,#273195,#273196,#273197,#273198,#273199,#273200,
#273201,#273202,#273203,#273204,#273205,#273206,#273207,#273208,#273209,
#273210,#273211,#273212,#273213,#273214),.UNSPECIFIED.,.F.,.F.,(4,3,3,3,
3,3,3,3,3,3,3,3,3,3,3,3,3,3,3,3,3,3,3,3,3,3,3,3,3,3,3,3,3,3,3,3,3,3,3,3,
3,3,3,3,3,3,3,3,3,3,3,3,3,3,3,3,3,3,3,3,3,3,3,4),(57.6628588026459,57.8117407599622,
57.8684559994141,57.9739574648993,58.079299934301,58.1845183898631,58.289670809124,
58.3947933097876,58.4999219652397,58.6051626613351,58.7104663044764,58.8159520712051,
58.866187999404,58.9716894648892,59.0770319342909,59.1822503898531,59.287402809114,
59.3925253097776,59.4976539652298,59.6028946613253,59.7081983044666,59.8136840711954,
59.8639199993939,59.9694214648791,60.0747639342808,60.179982389843,60.2851348091039,
60.3902573097675,60.4953859652196,60.600626661315,60.7059303044564,60.8114160711851,
60.8616519993838,60.967153464869,61.0724959342707,61.1777143898329,61.2828668090938,
61.3879893097574,61.4931179652095,61.5983586613049,61.7036623044463,61.809148071175,
61.8593839993737,61.9648854648589,62.0702279342605,62.1754463898227,62.2805988090836,
62.3857213097472,62.4908499651993,62.5960906612947,62.7013943044361,62.8068800711648,
62.8571159993636,62.9626174648488,63.0679599342505,63.1731783898126,63.2783308090735,
63.3834533097371,63.4885819651894,63.5938226612848,63.6991263044261,63.8046120711549,
63.8548479993535,63.9460441098255),.UNSPECIFIED.);
#3830=B_SPLINE_CURVE_WITH_KNOTS('',3,(#273216,#273217,#273218,#273219,#273220,
#273221,#273222,#273223,#273224,#273225),.UNSPECIFIED.,.F.,.F.,(4,1,1,1,
1,1,1,4),(63.9460528086984,64.8525799993434,65.8503119993333,66.8480439993232,
67.8457759993131,68.843507999303,69.8412399992929,70.2292294170051),
 .UNSPECIFIED.);
#3831=B_SPLINE_CURVE_WITH_KNOTS('',3,(#273227,#273228,#273229,#273230,#273231,
#273232,#273233,#273234,#273235,#273236),.UNSPECIFIED.,.F.,.F.,(4,1,1,1,
1,1,1,4),(70.2292294170051,70.8389719992828,71.8367039992727,72.8344359992626,
73.8321679992525,74.8298999992424,75.8276319992323,76.5124147241847),
 .UNSPECIFIED.);
#3832=B_SPLINE_CURVE_WITH_KNOTS('',3,(#273238,#273239,#273240,#273241,#273242,
#273243,#273244,#273245,#273246,#273247,#273248,#273249,#273250,#273251,
#273252,#273253,#273254,#273255,#273256,#273257,#273258,#273259,#273260,
#273261,#273262,#273263,#273264,#273265,#273266,#273267,#273268,#273269,
#273270,#273271,#273272,#273273,#273274,#273275,#273276,#273277,#273278,
#273279,#273280,#273281,#273282,#273283,#273284,#273285,#273286,#273287,
#273288,#273289,#273290,#273291,#273292,#273293,#273294,#273295,#273296,
#273297,#273298,#273299,#273300,#273301,#273302,#273303,#273304,#273305,
#273306,#273307,#273308,#273309,#273310,#273311,#273312,#273313,#273314,
#273315,#273316,#273317,#273318,#273319,#273320,#273321,#273322,#273323,
#273324,#273325,#273326,#273327,#273328,#273329,#273330,#273331,#273332,
#273333,#273334,#273335,#273336,#273337,#273338,#273339,#273340,#273341,
#273342,#273343,#273344,#273345,#273346,#273347,#273348,#273349,#273350,
#273351,#273352,#273353,#273354,#273355,#273356,#273357,#273358,#273359,
#273360,#273361,#273362,#273363,#273364,#273365,#273366,#273367,#273368,
#273369,#273370,#273371,#273372,#273373,#273374,#273375,#273376,#273377,
#273378,#273379,#273380,#273381,#273382,#273383,#273384,#273385,#273386,
#273387,#273388,#273389,#273390,#273391,#273392,#273393,#273394,#273395,
#273396,#273397,#273398,#273399,#273400,#273401,#273402,#273403,#273404,
#273405,#273406,#273407,#273408,#273409,#273410,#273411,#273412,#273413,
#273414,#273415,#273416,#273417,#273418,#273419,#273420,#273421,#273422,
#273423,#273424,#273425,#273426,#273427),.UNSPECIFIED.,.F.,.F.,(4,3,3,3,
3,3,3,3,3,3,3,3,3,3,3,3,3,3,3,3,3,3,3,3,3,3,3,3,3,3,3,3,3,3,3,3,3,3,3,3,
3,3,3,3,3,3,3,3,3,3,3,3,3,3,3,3,3,3,3,3,3,3,3,4),(76.5124149285909,76.637196824743,
76.7635407964299,76.8253639992222,76.9308654647074,77.0362079341089,77.1414263896711,
77.2465788089319,77.3517013095955,77.4568299650476,77.562070661143,77.6673743042843,
77.772860071013,77.8230959992121,77.9285974646973,78.0339399340991,78.1391583896612,
78.2443108089222,78.3494333095858,78.454561965038,78.5598026611334,78.6651063042747,
78.7705920710035,78.820827999202,78.9263294646872,79.0316719340889,79.1368903896511,
79.242042808912,79.3471653095756,79.4522939650277,79.5575346611232,79.6628383042645,
79.7683240709932,79.8185599991919,79.9240614646771,80.0294039340788,80.134622389641,
80.2397748089019,80.3448973095655,80.4500259650177,80.5552666611131,80.6605703042544,
80.7660560709831,80.8162919991818,80.921793464667,81.0271359340687,81.1323543896309,
81.2375068088918,81.3426293095554,81.4477579650076,81.552998661103,81.6583023042443,
81.763788070973,81.8140239991717,81.9192319607283,82.0287779695578,82.1337006658273,
82.2385600199007,82.3433925828576,82.4482348643447,82.5531902794066,82.6582126869609,
82.7634106837078,82.7956000313643),.UNSPECIFIED.);
#3833=B_SPLINE_CURVE_WITH_KNOTS('',3,(#273429,#273430,#273431,#273432,#273433,
#273434,#273435,#273436,#273437,#273438,#273439,#273440),.UNSPECIFIED.,
 .F.,.F.,(4,2,1,1,1,1,1,1,4),(82.7956000313643,82.8117559991616,83.8094879991515,
84.8072199991414,85.8049519991313,86.8026839991212,87.8004159991111,88.798147999101,
89.0787811501394),.UNSPECIFIED.);
#3834=B_SPLINE_CURVE_WITH_KNOTS('',3,(#273442,#273443,#273444,#273445,#273446,
#273447,#273448,#273449,#273450,#273451,#273452,#273453,#273454,#273455,
#273456,#273457,#273458,#273459,#273460,#273461,#273462,#273463,#273464,
#273465,#273466,#273467,#273468,#273469,#273470,#273471,#273472,#273473,
#273474,#273475,#273476,#273477,#273478,#273479,#273480,#273481,#273482,
#273483,#273484,#273485,#273486,#273487,#273488,#273489,#273490,#273491,
#273492,#273493,#273494,#273495,#273496,#273497,#273498,#273499,#273500,
#273501,#273502,#273503,#273504,#273505,#273506,#273507,#273508,#273509,
#273510,#273511,#273512,#273513,#273514,#273515,#273516,#273517,#273518,
#273519,#273520,#273521,#273522,#273523,#273524,#273525,#273526,#273527,
#273528,#273529,#273530,#273531,#273532,#273533,#273534,#273535,#273536,
#273537,#273538,#273539,#273540,#273541,#273542,#273543,#273544,#273545,
#273546,#273547,#273548,#273549,#273550,#273551,#273552,#273553,#273554,
#273555,#273556,#273557,#273558,#273559,#273560,#273561,#273562,#273563,
#273564,#273565,#273566,#273567,#273568,#273569,#273570,#273571,#273572,
#273573,#273574,#273575,#273576,#273577,#273578,#273579,#273580,#273581,
#273582,#273583,#273584,#273585,#273586,#273587,#273588,#273589,#273590,
#273591,#273592,#273593,#273594,#273595,#273596,#273597,#273598,#273599,
#273600,#273601,#273602,#273603,#273604,#273605,#273606,#273607,#273608,
#273609,#273610,#273611,#273612,#273613,#273614,#273615,#273616,#273617,
#273618,#273619,#273620,#273621,#273622,#273623,#273624,#273625,#273626,
#273627,#273628,#273629,#273630,#273631),.UNSPECIFIED.,.F.,.F.,(4,3,3,3,
3,3,3,3,3,3,3,3,3,3,3,3,3,3,3,3,3,3,3,3,3,3,3,3,3,3,3,3,3,3,3,3,3,3,3,3,
3,3,3,3,3,3,3,3,3,3,3,3,3,3,3,3,3,3,3,3,3,3,3,4),(89.0787853385439,89.1830981544274,
89.2873607770994,89.3916104742801,89.4959590610254,89.6003555960421,89.7049471415805,
89.7958799990909,89.901381464576,90.0067239339778,90.1119423895399,90.2170948088009,
90.3222173094644,90.4273459649163,90.5325866610117,90.6378903041529,90.7433760708817,
90.7936119990808,90.899113464566,91.0044559339678,91.10967438953,91.214826808791,
91.3199493094545,91.4250779649066,91.530318661002,91.6356223041434,91.7411080708722,
91.7913439990707,91.8968454645558,92.0021879339574,92.1074063895196,92.2125588087803,
92.3176813094439,92.4228099648959,92.5280506609912,92.6333543041327,92.7388400708613,
92.7890759990606,92.8945774645458,92.9999199339476,93.1051383895098,93.2102908087707,
93.3154133094343,93.4205419648867,93.5257826609821,93.6310863041234,93.7365720708521,
93.7868079990505,93.8923094645358,93.9976519339373,94.1028703894995,94.2080228087603,
94.313145309424,94.4182739648759,94.5235146609713,94.6288183041127,94.7343040708413,
94.7845399990404,94.8922505472161,94.9997777540247,95.1071208600479,95.2143559113678,
95.3215053251644,95.3619706457235),.UNSPECIFIED.);
#3835=B_SPLINE_CURVE_WITH_KNOTS('',3,(#273633,#273634,#273635,#273636,#273637,
#273638,#273639,#273640,#273641,#273642,#273643,#273644,#273645,#273646,
#273647,#273648,#273649,#273650,#273651,#273652,#273653,#273654,#273655,
#273656,#273657,#273658,#273659,#273660,#273661,#273662,#273663,#273664,
#273665,#273666,#273667,#273668,#273669,#273670,#273671,#273672,#273673,
#273674,#273675,#273676,#273677,#273678,#273679,#273680,#273681,#273682,
#273683,#273684,#273685,#273686,#273687,#273688,#273689,#273690,#273691,
#273692,#273693,#273694,#273695,#273696,#273697,#273698,#273699,#273700,
#273701,#273702,#273703,#273704,#273705,#273706,#273707,#273708,#273709,
#273710,#273711,#273712,#273713,#273714,#273715,#273716,#273717,#273718,
#273719,#273720,#273721,#273722,#273723,#273724,#273725,#273726,#273727,
#273728,#273729,#273730,#273731,#273732,#273733,#273734,#273735,#273736,
#273737,#273738,#273739,#273740,#273741,#273742,#273743,#273744,#273745,
#273746,#273747,#273748,#273749,#273750,#273751,#273752,#273753,#273754,
#273755,#273756,#273757,#273758,#273759,#273760,#273761,#273762,#273763,
#273764,#273765,#273766,#273767,#273768,#273769,#273770,#273771,#273772,
#273773,#273774,#273775,#273776,#273777,#273778,#273779,#273780,#273781,
#273782,#273783,#273784,#273785,#273786,#273787,#273788,#273789,#273790,
#273791,#273792,#273793,#273794,#273795,#273796,#273797,#273798,#273799,
#273800,#273801,#273802,#273803,#273804,#273805,#273806,#273807,#273808,
#273809,#273810,#273811,#273812,#273813,#273814,#273815,#273816,#273817,
#273818,#273819,#273820,#273821,#273822),.UNSPECIFIED.,.F.,.F.,(4,3,3,3,
3,3,3,3,3,3,3,3,3,3,3,3,3,3,3,3,3,3,3,3,3,3,3,3,3,3,3,3,3,3,3,3,3,3,3,3,
3,3,3,3,3,3,3,3,3,3,3,3,3,3,3,3,3,3,3,3,3,3,3,4),(95.3619706460871,95.4766888558802,
95.591751289489,95.7073231093368,95.7822719990302,95.8877734645154,95.9931159339172,
96.0983343894794,96.2034868087403,96.308609309404,96.4137379648561,96.5189786609516,
96.624282304093,96.7297680708218,96.7800039990202,96.8855054645054,96.990847933907,
97.0960663894692,97.2012188087301,97.3063413093937,97.4114699648458,97.5167106609412,
97.6220143040825,97.7275000708112,97.7777359990101,97.8832374644953,97.988579933897,
98.0937983894591,98.19895080872,98.3040733093836,98.4092019648357,98.5144426609311,
98.6197463040725,98.7252320708012,98.775467999,98.8809694644852,98.9863119338869,
99.091530389449,99.1966828087099,99.3018053093735,99.4069339648256,99.512174660921,
99.6174783040623,99.722964070791,99.7731999989899,99.8787014644752,99.984043933877,
100.089262389439,100.1944148087,100.299537309364,100.404665964816,100.509906660912,
100.615210304053,100.720696070782,100.77093199898,100.88020999322,100.984063595876,
101.087819532397,101.191515830589,101.295190429698,101.398937371334,101.502726497014,
101.606663108459,101.645155952903),.UNSPECIFIED.);
#3836=B_SPLINE_CURVE_WITH_KNOTS('',3,(#273824,#273825,#273826,#273827,#273828,
#273829,#273830,#273831,#273832,#273833,#273834),.UNSPECIFIED.,.F.,.F.,
(4,1,1,1,1,1,1,1,4),(101.645155952903,101.76866399897,102.76639599896,103.764127998949,
104.761859998939,105.759591998929,106.757323998919,107.755055998909,107.928341260083),
 .UNSPECIFIED.);
#3837=B_SPLINE_CURVE_WITH_KNOTS('',3,(#273836,#273837,#273838,#273839,#273840,
#273841,#273842,#273843,#273844,#273845,#273846,#273847,#273848,#273849,
#273850,#273851,#273852,#273853,#273854,#273855,#273856,#273857,#273858,
#273859,#273860,#273861,#273862,#273863,#273864,#273865,#273866,#273867,
#273868,#273869,#273870,#273871,#273872,#273873,#273874,#273875,#273876,
#273877,#273878,#273879,#273880,#273881,#273882,#273883,#273884,#273885,
#273886,#273887,#273888,#273889,#273890,#273891,#273892,#273893,#273894,
#273895,#273896,#273897,#273898,#273899,#273900,#273901,#273902,#273903,
#273904,#273905,#273906,#273907,#273908,#273909,#273910,#273911,#273912,
#273913,#273914,#273915,#273916,#273917,#273918,#273919,#273920,#273921,
#273922,#273923,#273924,#273925,#273926,#273927,#273928,#273929,#273930,
#273931,#273932,#273933,#273934,#273935,#273936,#273937,#273938,#273939,
#273940,#273941,#273942,#273943,#273944,#273945,#273946,#273947,#273948,
#273949,#273950,#273951,#273952,#273953,#273954,#273955,#273956,#273957,
#273958,#273959,#273960,#273961,#273962,#273963,#273964,#273965,#273966,
#273967,#273968,#273969,#273970,#273971,#273972,#273973,#273974,#273975,
#273976,#273977,#273978,#273979,#273980,#273981,#273982,#273983,#273984,
#273985,#273986,#273987,#273988,#273989,#273990,#273991,#273992,#273993,
#273994,#273995,#273996,#273997,#273998,#273999,#274000,#274001,#274002,
#274003,#274004,#274005,#274006,#274007,#274008,#274009,#274010,#274011,
#274012,#274013,#274014,#274015,#274016,#274017,#274018,#274019,#274020,
#274021,#274022,#274023,#274024,#274025),.UNSPECIFIED.,.F.,.F.,(4,3,3,3,
3,3,3,3,3,3,3,3,3,3,3,3,3,3,3,3,3,3,3,3,3,3,3,3,3,3,3,3,3,3,3,3,3,3,3,3,
3,3,3,3,3,3,3,3,3,3,3,3,3,3,3,3,3,3,3,3,3,3,3,4),(107.928341260083,108.032099150482,
108.135757208958,108.239353576204,108.342926301162,108.446586291681,108.550286108514,
108.654177288281,108.752787998899,108.858289464384,108.963631933786,109.068850389348,
109.174002808609,109.279125309273,109.384253964725,109.48949466082,109.594798303962,
109.700284070691,109.750519998889,109.856021464374,109.961363933776,110.066582389338,
110.171734808599,110.276857309263,110.381985964715,110.48722666081,110.592530303952,
110.69801607068,110.748251998879,110.853753464364,110.959095933766,111.064314389328,
111.169466808589,111.274589309252,111.379717964704,111.4849586608,111.590262303941,
111.69574807067,111.745983998869,111.851485464354,111.956827933756,112.062046389318,
112.167198808579,112.272321309243,112.377449964695,112.482690660791,112.587994303932,
112.693480070661,112.743715998859,112.849217464344,112.954559933746,113.059778389308,
113.164930808568,113.270053309232,113.375181964683,113.480422660778,113.585726303919,
113.691212070648,113.741447998848,113.858967602029,113.971035808353,114.082867908485,
114.194397089511,114.211526411573),.UNSPECIFIED.);
#3838=B_SPLINE_CURVE_WITH_KNOTS('',3,(#274027,#274028,#274029,#274030,#274031,
#274032,#274033,#274034,#274035,#274036),.UNSPECIFIED.,.F.,.F.,(4,1,1,1,
1,1,1,4),(114.211526567262,114.739179998838,115.736911998828,116.734643998818,
117.732375998808,118.730107998798,119.727839998788,120.494711874442),
 .UNSPECIFIED.);
#3839=B_SPLINE_CURVE_WITH_KNOTS('',3,(#274038,#274039,#274040,#274041,#274042,
#274043,#274044,#274045,#274046,#274047,#274048),.UNSPECIFIED.,.F.,.F.,
(4,1,1,1,1,1,1,1,4),(120.494711874442,120.725571998778,121.723303998768,
122.721035998758,123.718767998747,124.716499998737,125.714231998727,126.711963998717,
126.777897181621),.UNSPECIFIED.);
#3840=B_SPLINE_CURVE_WITH_KNOTS('',3,(#274050,#274051,#274052,#274053,#274054,
#274055,#274056,#274057,#274058,#274059,#274060,#274061,#274062,#274063,
#274064,#274065,#274066,#274067,#274068,#274069,#274070,#274071,#274072,
#274073,#274074,#274075,#274076,#274077,#274078,#274079,#274080,#274081,
#274082,#274083,#274084,#274085,#274086,#274087,#274088,#274089,#274090,
#274091,#274092,#274093,#274094,#274095,#274096,#274097,#274098,#274099,
#274100,#274101,#274102,#274103,#274104,#274105,#274106,#274107,#274108,
#274109,#274110,#274111,#274112,#274113,#274114,#274115,#274116,#274117,
#274118,#274119,#274120,#274121,#274122,#274123,#274124,#274125,#274126,
#274127,#274128,#274129,#274130,#274131,#274132,#274133,#274134,#274135,
#274136,#274137,#274138,#274139,#274140,#274141,#274142,#274143,#274144,
#274145,#274146,#274147,#274148,#274149,#274150,#274151,#274152,#274153,
#274154,#274155,#274156,#274157,#274158,#274159,#274160,#274161,#274162,
#274163,#274164,#274165,#274166,#274167,#274168,#274169,#274170,#274171,
#274172,#274173,#274174,#274175,#274176,#274177,#274178,#274179,#274180,
#274181,#274182,#274183,#274184,#274185,#274186,#274187,#274188,#274189,
#274190,#274191,#274192,#274193,#274194,#274195,#274196,#274197,#274198,
#274199,#274200,#274201,#274202,#274203,#274204,#274205,#274206,#274207,
#274208,#274209,#274210,#274211,#274212,#274213,#274214,#274215,#274216,
#274217,#274218,#274219,#274220,#274221,#274222,#274223,#274224,#274225,
#274226,#274227,#274228,#274229,#274230,#274231,#274232,#274233,#274234,
#274235,#274236),.UNSPECIFIED.,.F.,.F.,(4,3,3,3,3,3,3,3,3,3,3,3,3,3,3,3,
3,3,3,3,3,3,3,3,3,3,3,3,3,3,3,3,3,3,3,3,3,3,3,3,3,3,3,3,3,3,3,3,3,3,3,3,
3,3,3,3,3,3,3,3,3,3,4),(126.777897181621,126.882369364822,126.986673464764,
127.090884174499,127.195039013725,127.299175425165,127.403404764753,127.507677502594,
127.612144068716,127.709695998707,127.815197464192,127.920539933594,128.025758389156,
128.130910808417,128.236033309081,128.341161964533,128.446402660628,128.55170630377,
128.657192070498,128.707427998697,128.812929464182,128.918271933584,129.023490389146,
129.128642808407,129.23376530907,129.338893964523,129.444134660618,129.549438303759,
129.654924070488,129.705159998687,129.810661464172,129.916003933574,130.021222389136,
130.126374808397,130.231497309061,130.336625964513,130.441866660608,130.54717030375,
130.652656070478,130.702891998677,130.808393464162,130.913735933564,131.018954389126,
131.124106808387,131.22922930905,131.334357964503,131.439598660598,131.54490230374,
131.650388070468,131.700623998667,131.806125464152,131.911467933554,132.016686389117,
132.121838808378,132.226961309041,132.332089964493,132.437330660589,132.54263430373,
132.648120070459,132.698355998657,132.818881802562,132.939982145448,133.061082488334),
 .UNSPECIFIED.);
#3841=B_SPLINE_CURVE_WITH_KNOTS('',3,(#274238,#274239,#274240,#274241,#274242,
#274243,#274244,#274245,#274246,#274247,#274248,#274249,#274250,#274251,
#274252,#274253,#274254,#274255,#274256,#274257,#274258,#274259,#274260,
#274261,#274262,#274263,#274264,#274265,#274266,#274267,#274268,#274269,
#274270,#274271,#274272,#274273,#274274,#274275,#274276,#274277,#274278,
#274279,#274280,#274281,#274282,#274283,#274284,#274285,#274286,#274287,
#274288,#274289,#274290,#274291,#274292,#274293,#274294,#274295,#274296,
#274297,#274298,#274299,#274300,#274301,#274302,#274303,#274304,#274305,
#274306,#274307,#274308,#274309,#274310,#274311,#274312,#274313,#274314,
#274315,#274316,#274317,#274318,#274319,#274320,#274321,#274322,#274323,
#274324,#274325,#274326,#274327,#274328,#274329,#274330,#274331,#274332,
#274333,#274334,#274335,#274336,#274337,#274338,#274339,#274340,#274341,
#274342,#274343,#274344,#274345,#274346,#274347,#274348,#274349,#274350,
#274351,#274352,#274353,#274354,#274355,#274356,#274357,#274358,#274359,
#274360,#274361,#274362,#274363,#274364,#274365,#274366,#274367,#274368,
#274369,#274370,#274371,#274372,#274373,#274374,#274375,#274376,#274377,
#274378,#274379,#274380,#274381,#274382,#274383,#274384,#274385,#274386,
#274387,#274388,#274389,#274390,#274391,#274392,#274393,#274394,#274395,
#274396,#274397,#274398,#274399,#274400,#274401,#274402,#274403,#274404,
#274405,#274406,#274407,#274408,#274409,#274410,#274411,#274412,#274413,
#274414,#274415,#274416,#274417,#274418,#274419,#274420,#274421,#274422,
#274423,#274424,#274425,#274426,#274427),.UNSPECIFIED.,.F.,.F.,(4,3,3,3,
3,3,3,3,3,3,3,3,3,3,3,3,3,3,3,3,3,3,3,3,3,3,3,3,3,3,3,3,3,3,3,3,3,3,3,3,
3,3,3,3,3,3,3,3,3,3,3,3,3,3,3,3,3,3,3,3,3,3,3,4),(133.061082488801,133.166734977793,
133.27239290649,133.378316679529,133.484159022686,133.590220236502,133.696087998646,
133.801589464131,133.906931933533,134.012150389095,134.117302808356,134.22242530902,
134.327553964472,134.432794660568,134.538098303709,134.643584070438,134.693819998636,
134.799321464121,134.904663933523,135.009882389085,135.115034808346,135.22015730901,
135.325285964462,135.430526660558,135.535830303699,135.641316070428,135.691551998626,
135.797053464111,135.902395933513,136.007614389075,136.112766808336,136.217889308999,
136.323017964452,136.428258660547,136.533562303688,136.639048070417,136.689283998616,
136.794785464101,136.900127933503,137.005346389065,137.110498808326,137.215621308989,
137.320749964441,137.425990660537,137.531294303678,137.636780070407,137.687015998606,
137.792517464091,137.897859933493,138.003078389055,138.108230808316,138.213353308979,
138.318481964432,138.423722660527,138.529026303669,138.634512070397,138.684747998596,
138.790292825569,138.895681075761,139.000948945222,139.106136392543,139.211278460255,
139.316431600199,139.344267795981),.UNSPECIFIED.);
#3842=B_SPLINE_CURVE_WITH_KNOTS('',3,(#274429,#274430,#274431,#274432,#274433,
#274434,#274435,#274436,#274437,#274438),.UNSPECIFIED.,.F.,.F.,(4,1,1,1,
1,1,1,4),(139.344275098717,139.682479998586,140.680211998576,141.677943998566,
142.675675998556,143.673407998545,144.671139998535,145.627447736301),
 .UNSPECIFIED.);
#3843=B_SPLINE_CURVE_WITH_KNOTS('',3,(#274440,#274441,#274442,#274443,#274444,
#274445,#274446,#274447,#274448,#274449,#274450,#274451,#274452,#274453,
#274454,#274455,#274456,#274457,#274458,#274459,#274460,#274461,#274462,
#274463,#274464,#274465,#274466,#274467,#274468,#274469,#274470,#274471,
#274472,#274473,#274474,#274475,#274476,#274477,#274478,#274479,#274480,
#274481,#274482,#274483,#274484,#274485,#274486,#274487,#274488,#274489,
#274490,#274491,#274492,#274493,#274494,#274495,#274496,#274497,#274498,
#274499,#274500,#274501,#274502,#274503,#274504,#274505,#274506,#274507,
#274508,#274509,#274510,#274511,#274512,#274513,#274514,#274515,#274516,
#274517,#274518,#274519,#274520,#274521,#274522,#274523,#274524,#274525,
#274526,#274527,#274528,#274529,#274530,#274531,#274532,#274533,#274534,
#274535,#274536,#274537,#274538,#274539,#274540,#274541,#274542,#274543,
#274544,#274545,#274546,#274547,#274548,#274549,#274550,#274551,#274552,
#274553,#274554,#274555,#274556,#274557,#274558,#274559,#274560,#274561,
#274562,#274563,#274564,#274565,#274566,#274567,#274568,#274569,#274570,
#274571,#274572,#274573,#274574,#274575,#274576,#274577,#274578,#274579,
#274580,#274581,#274582,#274583,#274584,#274585,#274586,#274587,#274588,
#274589,#274590,#274591,#274592,#274593,#274594,#274595,#274596,#274597,
#274598,#274599,#274600,#274601,#274602,#274603,#274604,#274605,#274606,
#274607,#274608,#274609,#274610,#274611,#274612,#274613,#274614,#274615,
#274616,#274617,#274618,#274619,#274620,#274621,#274622,#274623,#274624,
#274625,#274626,#274627,#274628,#274629),.UNSPECIFIED.,.F.,.F.,(4,3,3,3,
3,3,3,3,3,3,3,3,3,3,3,3,3,3,3,3,3,3,3,3,3,3,3,3,3,3,3,3,3,3,3,3,3,3,3,3,
3,3,3,3,3,3,3,3,3,3,3,3,3,3,3,3,3,3,3,3,3,3,3,4),(145.62745310316,145.668871998525,
145.774373464006,145.879715933403,145.98493438896,146.090086808217,146.195209308876,
146.300337964323,146.405578660414,146.51088230355,146.616368070275,146.666603998515,
146.772105464016,146.877447933434,146.982666389013,147.08781880829,147.192941308969,
147.298069964437,147.403310660548,147.508614303705,147.614100070449,147.664335998505,
147.769837463974,147.875179933359,147.980398388905,148.085550808149,148.190673308797,
148.295801964233,148.401042660313,148.506346303439,148.611832070153,148.662067998495,
148.767569463956,148.872911933333,148.978130388871,149.083282808107,149.188405308746,
149.293533964173,149.398774660243,149.504078303359,149.609564070063,149.659799998485,
149.76530146408,149.870643933592,149.975862389264,150.081014808635,150.186137309408,
150.291265964969,150.396506661172,150.50181030442,150.607296071254,150.657531998475,
150.763033463821,150.868375933084,150.973594388508,151.078746807633,151.183869308161,
151.288997963479,151.394238659443,151.499542302455,151.605028069057,151.655263998465,
151.790594856147,151.910638270564),.UNSPECIFIED.);
#3844=B_SPLINE_CURVE_WITH_KNOTS('',3,(#274631,#274632,#274633,#274634,#274635,
#274636,#274637,#274638,#274639,#274640),.UNSPECIFIED.,.F.,.F.,(4,1,1,1,
1,1,1,4),(151.91063841034,152.652995998454,153.650727998444,154.648459998434,
155.646191998424,156.643923998414,157.641655998404,158.193823717519),
 .UNSPECIFIED.);
#3845=B_SPLINE_CURVE_WITH_KNOTS('',3,(#274642,#274643,#274644,#274645,#274646,
#274647,#274648,#274649,#274650,#274651),.UNSPECIFIED.,.F.,.F.,(4,1,1,1,
1,1,1,4),(158.193823717519,158.639387998394,159.637119998384,160.634851998374,
161.632583998364,162.630315998353,163.628047998343,164.477009024699),
 .UNSPECIFIED.);
#3846=B_SPLINE_CURVE_WITH_KNOTS('',3,(#274653,#274654,#274655,#274656,#274657,
#274658,#274659,#274660,#274661,#274662,#274663),.UNSPECIFIED.,.F.,.F.,
(4,1,1,1,1,1,1,1,4),(164.477009024699,164.625779998333,165.623511998323,
166.621243998313,167.618975998303,168.616707998293,169.614439998283,170.612171998273,
170.760194331878),.UNSPECIFIED.);
#3847=B_SPLINE_CURVE_WITH_KNOTS('',3,(#274668,#274669,#274670,#274671,#274672,
#274673,#274674,#274675,#274676,#274677,#274678,#274679,#274680,#274681,
#274682,#274683,#274684,#274685,#274686,#274687,#274688,#274689,#274690,
#274691,#274692,#274693,#274694,#274695,#274696,#274697,#274698,#274699,
#274700,#274701,#274702,#274703,#274704,#274705,#274706,#274707,#274708,
#274709,#274710,#274711,#274712,#274713,#274714,#274715,#274716,#274717,
#274718,#274719,#274720,#274721,#274722,#274723,#274724,#274725,#274726,
#274727,#274728,#274729,#274730,#274731,#274732,#274733,#274734,#274735,
#274736,#274737,#274738,#274739,#274740,#274741,#274742,#274743,#274744,
#274745,#274746,#274747,#274748,#274749,#274750,#274751,#274752,#274753,
#274754,#274755,#274756,#274757,#274758,#274759,#274760,#274761,#274762,
#274763,#274764,#274765,#274766,#274767,#274768,#274769,#274770,#274771,
#274772,#274773,#274774,#274775,#274776,#274777,#274778,#274779,#274780,
#274781,#274782,#274783,#274784,#274785,#274786,#274787,#274788,#274789,
#274790,#274791,#274792,#274793,#274794,#274795,#274796,#274797,#274798,
#274799,#274800,#274801,#274802,#274803,#274804,#274805,#274806,#274807,
#274808,#274809,#274810,#274811,#274812,#274813,#274814,#274815,#274816,
#274817,#274818,#274819,#274820,#274821,#274822,#274823,#274824,#274825,
#274826,#274827,#274828,#274829,#274830,#274831,#274832,#274833,#274834,
#274835,#274836),.UNSPECIFIED.,.F.,.F.,(4,3,3,3,3,3,3,3,3,3,3,3,3,3,3,3,
3,3,3,3,3,3,3,3,3,3,3,3,3,3,3,3,3,3,3,3,3,3,3,3,3,3,3,3,3,3,3,3,3,3,3,3,
3,3,3,3,4),(-173.021636066298,-172.91157443677,-172.801170755521,-172.690579717821,
-172.579669097854,-172.53875616362,-172.433085791181,-172.327574069382,
-172.222186749637,-172.116865811022,-172.011575408995,-171.906279743881,
-171.800874686078,-171.695407888946,-171.589762867262,-171.541422312964,
-171.435731408906,-171.330195372576,-171.224778225876,-171.119424047321,
-171.014097033089,-170.908761420676,-170.803311614756,-170.697797258801,
-170.592100821095,-170.544088462307,-170.43872635681,-170.333525260378,
-170.228450493165,-170.123443112452,-170.018466785104,-169.913485223641,
-169.808392138527,-169.703236548867,-169.59789827101,-169.54675461165,-169.441215904193,
-169.335835914169,-169.230579733942,-169.125389478107,-169.020229087856,
-168.915062548622,-168.809784359216,-168.704443317738,-168.598920998279,
-168.549420760993,-168.443892091303,-168.33852178728,-168.233274719997,
-168.128093214986,-168.022941198748,-167.917782641628,-167.81251178253,
-167.707177709489,-167.601661723545,-167.552086910337,-167.455359735508),
 .UNSPECIFIED.);
#3848=B_SPLINE_CURVE_WITH_KNOTS('',3,(#274838,#274839,#274840,#274841,#274842,
#274843,#274844,#274845,#274846,#274847),.UNSPECIFIED.,.F.,.F.,(4,1,1,1,
1,1,1,4),(-167.455350961157,-166.55475305968,-165.557419209023,-164.560085358366,
-163.562751507709,-162.565417657053,-161.568083806396,-161.172174428328),
 .UNSPECIFIED.);
#3849=B_SPLINE_CURVE_WITH_KNOTS('',3,(#274849,#274850,#274851,#274852,#274853,
#274854,#274855,#274856,#274857,#274858),.UNSPECIFIED.,.F.,.F.,(4,1,1,1,
1,1,1,4),(-161.172174428328,-160.570749955739,-159.573416105082,-158.576082254426,
-157.578748403769,-156.581414553112,-155.584080702455,-154.888989121148),
 .UNSPECIFIED.);
#3850=B_SPLINE_CURVE_WITH_KNOTS('',3,(#274860,#274861,#274862,#274863,#274864,
#274865,#274866,#274867,#274868,#274869,#274870,#274871,#274872,#274873,
#274874,#274875,#274876,#274877,#274878,#274879,#274880,#274881,#274882,
#274883,#274884,#274885,#274886,#274887,#274888,#274889,#274890,#274891,
#274892,#274893,#274894,#274895,#274896,#274897,#274898,#274899,#274900,
#274901,#274902,#274903,#274904,#274905,#274906,#274907,#274908,#274909,
#274910,#274911,#274912,#274913,#274914,#274915,#274916,#274917,#274918,
#274919,#274920,#274921,#274922,#274923,#274924,#274925,#274926,#274927,
#274928,#274929,#274930,#274931,#274932,#274933,#274934,#274935,#274936,
#274937,#274938,#274939,#274940,#274941,#274942,#274943,#274944,#274945,
#274946,#274947,#274948,#274949,#274950,#274951,#274952,#274953,#274954,
#274955,#274956,#274957,#274958,#274959,#274960,#274961,#274962,#274963,
#274964,#274965,#274966,#274967,#274968,#274969,#274970,#274971,#274972,
#274973,#274974,#274975,#274976,#274977,#274978,#274979,#274980,#274981,
#274982,#274983,#274984,#274985,#274986,#274987,#274988,#274989,#274990,
#274991,#274992,#274993,#274994,#274995,#274996,#274997,#274998,#274999,
#275000,#275001,#275002,#275003,#275004,#275005,#275006,#275007,#275008,
#275009,#275010,#275011,#275012,#275013,#275014,#275015,#275016,#275017,
#275018,#275019,#275020,#275021,#275022,#275023,#275024,#275025,#275026,
#275027,#275028,#275029,#275030,#275031,#275032,#275033,#275034,#275035,
#275036,#275037,#275038,#275039,#275040,#275041,#275042,#275043,#275044,
#275045,#275046,#275047,#275048,#275049),.UNSPECIFIED.,.F.,.F.,(4,3,3,3,
3,3,3,3,3,3,3,3,3,3,3,3,3,3,3,3,3,3,3,3,3,3,3,3,3,3,3,3,3,3,3,3,3,3,3,3,
3,3,3,3,3,3,3,3,3,3,3,3,3,3,3,3,3,3,3,3,3,3,3,4),(-154.888988936303,-154.762828432452,
-154.634933804719,-154.586746851799,-154.481240045005,-154.375892113708,
-154.270668064878,-154.165509965993,-154.060381708233,-153.955247227016,
-153.850000760823,-153.744691297408,-153.63919999852,-153.589413001142,
-153.48390619939,-153.378558273193,-153.273334229522,-153.168176135829,
-153.063047883287,-152.957913407306,-152.85266694634,-152.747357488154,
-152.641866194445,-152.592079150485,-152.486572349276,-152.381224423647,
-152.276000380581,-152.170842287513,-152.065714035617,-151.960579560302,
-151.855333100027,-151.750023642549,-151.644532349564,-151.594745299828,
-151.489238496917,-151.383890569556,-151.27866652472,-151.173508429862,
-151.068380176156,-150.963245699015,-150.857999236903,-150.752689777577,
-150.647198482749,-150.597411449172,-150.491904647082,-150.386556720551,
-150.281332676557,-150.176174582548,-150.071046329696,-149.965911853412,
-149.860665392157,-149.755355933689,-149.649864639712,-149.600077598515,
-149.494628879985,-149.389338992167,-149.284172777986,-149.179072286532,
-149.074001319397,-148.968923722142,-148.863734045917,-148.758480836203,
-148.653046701498,-148.605803814421),.UNSPECIFIED.);
#3851=B_SPLINE_CURVE_WITH_KNOTS('',3,(#275051,#275052,#275053,#275054,#275055,
#275056,#275057,#275058,#275059,#275060,#275061,#275062,#275063,#275064,
#275065,#275066,#275067,#275068,#275069,#275070,#275071,#275072,#275073,
#275074,#275075,#275076,#275077,#275078,#275079,#275080,#275081,#275082,
#275083,#275084,#275085,#275086,#275087,#275088,#275089,#275090,#275091,
#275092,#275093,#275094,#275095,#275096,#275097,#275098,#275099,#275100,
#275101,#275102,#275103,#275104,#275105,#275106,#275107,#275108,#275109,
#275110,#275111,#275112,#275113,#275114,#275115,#275116,#275117,#275118,
#275119,#275120,#275121,#275122,#275123,#275124,#275125,#275126,#275127,
#275128,#275129,#275130,#275131,#275132,#275133,#275134,#275135,#275136,
#275137,#275138,#275139,#275140,#275141,#275142,#275143,#275144,#275145,
#275146,#275147,#275148,#275149,#275150,#275151,#275152,#275153,#275154,
#275155,#275156,#275157,#275158,#275159,#275160,#275161,#275162,#275163,
#275164,#275165,#275166,#275167,#275168,#275169,#275170,#275171,#275172,
#275173,#275174,#275175,#275176,#275177,#275178,#275179,#275180,#275181,
#275182,#275183,#275184,#275185,#275186,#275187,#275188,#275189,#275190,
#275191,#275192,#275193,#275194,#275195,#275196,#275197,#275198,#275199,
#275200,#275201,#275202,#275203,#275204,#275205,#275206,#275207,#275208,
#275209,#275210,#275211,#275212,#275213,#275214,#275215,#275216,#275217,
#275218,#275219,#275220,#275221,#275222,#275223,#275224,#275225,#275226,
#275227,#275228,#275229,#275230,#275231,#275232,#275233,#275234,#275235,
#275236,#275237,#275238,#275239,#275240,#275241,#275242,#275243),
 .UNSPECIFIED.,.F.,.F.,(4,3,3,3,3,3,3,3,3,3,3,3,3,3,3,3,3,3,3,3,3,3,3,3,
3,3,3,3,3,3,3,3,3,3,3,3,3,3,3,3,3,3,3,3,3,3,3,3,3,3,3,3,3,3,3,3,3,3,3,3,
3,3,3,3,4),(-148.605803813969,-148.602743747858,-148.497236945542,-148.391889018784,
-148.286664974561,-148.181506880321,-148.076378627239,-147.971244150725,
-147.865997689241,-147.760688230545,-147.655196936343,-147.605409897201,
-147.499903095014,-147.394555168387,-147.289331124297,-147.184173030192,
-147.079044777245,-146.973910300866,-146.868663839518,-146.763354380959,
-146.657863086891,-146.608076046544,-146.502569244347,-146.397221317709,
-146.29199727361,-146.186839179494,-146.081710926538,-145.97657645015,-145.871329988793,
-145.766020530225,-145.66052923615,-145.610742195888,-145.505235393661,
-145.399887466993,-145.294663422862,-145.189505328716,-145.084377075727,
-144.979242599307,-144.873996137918,-144.768686679317,-144.663195385209,
-144.613408345231,-144.507901543024,-144.402553616376,-144.297329572265,
-144.192171478139,-144.087043225171,-143.981908748772,-143.876662287403,
-143.771352828823,-143.665861534735,-143.616074494574,-143.510567692364,
-143.405219765713,-143.299995721599,-143.19483762747,-143.089709374499,
-142.984574898097,-142.879328436725,-142.774018978142,-142.668527684052,
-142.618740643917,-142.489762712696,-142.362605638187,-142.322618679647),
 .UNSPECIFIED.);
#3852=B_SPLINE_CURVE_WITH_KNOTS('',3,(#275245,#275246,#275247,#275248,#275249,
#275250,#275251,#275252,#275253,#275254),.UNSPECIFIED.,.F.,.F.,(4,1,1,1,
1,1,1,4),(-142.322618506789,-141.621406793261,-140.624072942604,-139.626739091947,
-138.62940524129,-137.632071390634,-136.634737539977,-136.03943319961),
 .UNSPECIFIED.);
#3853=B_SPLINE_CURVE_WITH_KNOTS('',3,(#275256,#275257,#275258,#275259,#275260,
#275261,#275262,#275263,#275264,#275265,#275266,#275267,#275268,#275269,
#275270,#275271,#275272,#275273,#275274,#275275,#275276,#275277,#275278,
#275279,#275280,#275281,#275282,#275283,#275284,#275285,#275286,#275287,
#275288,#275289,#275290,#275291,#275292,#275293,#275294,#275295,#275296,
#275297,#275298,#275299,#275300,#275301,#275302,#275303,#275304,#275305,
#275306,#275307,#275308,#275309,#275310,#275311,#275312,#275313,#275314,
#275315,#275316,#275317,#275318,#275319,#275320,#275321,#275322,#275323,
#275324,#275325,#275326,#275327,#275328,#275329,#275330,#275331,#275332,
#275333,#275334,#275335,#275336,#275337,#275338,#275339,#275340,#275341,
#275342,#275343,#275344,#275345,#275346,#275347,#275348,#275349,#275350,
#275351,#275352,#275353,#275354,#275355,#275356,#275357,#275358,#275359,
#275360,#275361,#275362,#275363,#275364,#275365,#275366,#275367,#275368,
#275369,#275370,#275371,#275372,#275373,#275374,#275375,#275376,#275377,
#275378,#275379,#275380,#275381,#275382,#275383,#275384,#275385,#275386,
#275387,#275388,#275389,#275390,#275391,#275392,#275393,#275394,#275395,
#275396,#275397,#275398,#275399,#275400,#275401,#275402,#275403,#275404,
#275405,#275406,#275407,#275408,#275409,#275410,#275411,#275412,#275413,
#275414,#275415,#275416,#275417,#275418,#275419,#275420,#275421,#275422,
#275423,#275424,#275425,#275426,#275427,#275428,#275429,#275430,#275431,
#275432,#275433,#275434,#275435,#275436,#275437,#275438,#275439,#275440,
#275441,#275442,#275443,#275444,#275445),.UNSPECIFIED.,.F.,.F.,(4,3,3,3,
3,3,3,3,3,3,3,3,3,3,3,3,3,3,3,3,3,3,3,3,3,3,3,3,3,3,3,3,3,3,3,3,3,3,3,3,
3,3,3,3,3,3,3,3,3,3,3,3,3,3,3,3,3,3,3,3,3,3,3,4),(-136.039432767475,-135.923411947058,
-135.806976229731,-135.689983518335,-135.63740368932,-135.531896887108,
-135.426548960456,-135.321324916341,-135.21616682221,-135.111038569238,
-135.005904092834,-134.900657631461,-134.795348172876,-134.689856878784,
-134.640069838663,-134.534563036451,-134.429215109799,-134.323991065684,
-134.218832971554,-134.113704718582,-134.008570242178,-133.903323780805,
-133.798014322221,-133.692523028129,-133.642735988007,-133.537229185795,
-133.431881259143,-133.326657215027,-133.221499120897,-133.116370867924,
-133.01123639152,-132.905989930147,-132.800680471562,-132.69518917747,-132.64540213735,
-132.539895335138,-132.434547408486,-132.32932336437,-132.224165270239,
-132.119037017267,-132.013902540862,-131.908656079489,-131.803346620904,
-131.697855326812,-131.648068286693,-131.542561484481,-131.437213557829,
-131.331989513713,-131.226831419583,-131.12170316661,-131.016568690206,
-130.911322228833,-130.806012770248,-130.700521476156,-130.650734436036,
-130.546565876061,-130.44257619085,-130.338685988997,-130.234857369735,
-130.131052521105,-130.027172036681,-129.923251693136,-129.819169881673,
-129.756247892881),.UNSPECIFIED.);
#3854=B_SPLINE_CURVE_WITH_KNOTS('',3,(#275447,#275448,#275449,#275450,#275451,
#275452,#275453,#275454,#275455,#275456,#275457,#275458,#275459,#275460,
#275461,#275462,#275463,#275464,#275465,#275466,#275467,#275468,#275469,
#275470,#275471,#275472,#275473,#275474,#275475,#275476,#275477,#275478,
#275479,#275480,#275481,#275482,#275483,#275484,#275485,#275486,#275487,
#275488,#275489,#275490,#275491,#275492,#275493,#275494,#275495,#275496,
#275497,#275498,#275499,#275500,#275501,#275502,#275503,#275504,#275505,
#275506,#275507,#275508,#275509,#275510,#275511,#275512,#275513,#275514,
#275515,#275516,#275517,#275518,#275519,#275520,#275521,#275522,#275523,
#275524,#275525,#275526,#275527,#275528,#275529,#275530,#275531,#275532,
#275533,#275534,#275535,#275536,#275537,#275538,#275539,#275540,#275541,
#275542,#275543,#275544,#275545,#275546,#275547,#275548,#275549,#275550,
#275551,#275552,#275553,#275554,#275555,#275556,#275557,#275558,#275559,
#275560,#275561,#275562,#275563,#275564,#275565,#275566,#275567,#275568,
#275569,#275570,#275571,#275572,#275573,#275574,#275575,#275576,#275577,
#275578,#275579,#275580,#275581,#275582,#275583,#275584,#275585,#275586,
#275587,#275588,#275589,#275590,#275591,#275592,#275593,#275594,#275595,
#275596,#275597,#275598,#275599,#275600,#275601,#275602,#275603,#275604,
#275605,#275606,#275607,#275608,#275609,#275610,#275611,#275612,#275613,
#275614,#275615,#275616,#275617,#275618,#275619,#275620,#275621,#275622,
#275623,#275624,#275625,#275626,#275627,#275628,#275629,#275630,#275631,
#275632,#275633,#275634,#275635,#275636),.UNSPECIFIED.,.F.,.F.,(4,3,3,3,
3,3,3,3,3,3,3,3,3,3,3,3,3,3,3,3,3,3,3,3,3,3,3,3,3,3,3,3,3,3,3,3,3,3,3,3,
3,3,3,3,3,3,3,3,3,3,3,3,3,3,3,3,3,3,3,3,3,3,3,4),(-129.75624789243,-129.65340058538,
-129.547893783166,-129.442545856511,-129.337321812392,-129.232163718259,
-129.127035465284,-129.021900988877,-128.9166545275,-128.811345068913,-128.705853774818,
-128.656066734723,-128.550559932512,-128.44521200586,-128.339987961745,
-128.234829867614,-128.129701614642,-128.024567138239,-127.919320676866,
-127.814011218282,-127.70851992419,-127.658732884066,-127.553226081855,
-127.447878155202,-127.342654111087,-127.237496016957,-127.132367763985,
-127.027233287581,-126.921986826208,-126.816677367624,-126.711186073532,
-126.661399033409,-126.555892231197,-126.450544304544,-126.345320260428,
-126.240162166297,-126.135033913324,-126.02989943692,-125.924652975546,
-125.819343516961,-125.713852222868,-125.664065182752,-125.558558380541,
-125.453210453889,-125.347986409774,-125.242828315643,-125.137700062671,
-125.032565586267,-124.927319124894,-124.82200966631,-124.716518372218,
-124.666731332096,-124.561224529884,-124.455876603232,-124.350652559116,
-124.245494464986,-124.140366212013,-124.035231735609,-123.929985274236,
-123.824675815651,-123.719184521559,-123.669397481439,-123.517141233146,
-123.473062585251),.UNSPECIFIED.);
#3855=B_SPLINE_CURVE_WITH_KNOTS('',3,(#275638,#275639,#275640,#275641,#275642,
#275643,#275644,#275645,#275646,#275647),.UNSPECIFIED.,.F.,.F.,(4,1,1,1,
1,1,1,4),(-123.473059165501,-122.672063630782,-121.674729780125,-120.677395929469,
-119.680062078812,-118.682728228155,-117.685394377498,-117.189877278071),
 .UNSPECIFIED.);
#3856=B_SPLINE_CURVE_WITH_KNOTS('',3,(#275649,#275650,#275651,#275652,#275653,
#275654,#275655,#275656,#275657,#275658),.UNSPECIFIED.,.F.,.F.,(4,1,1,1,
1,1,1,4),(-117.189877278071,-116.688060526842,-115.690726676185,-114.693392825528,
-113.696058974871,-112.698725124214,-111.701391273558,-110.906694804064),
 .UNSPECIFIED.);
#3857=B_SPLINE_CURVE_WITH_KNOTS('',3,(#275660,#275661,#275662,#275663,#275664,
#275665,#275666,#275667,#275668,#275669,#275670,#275671,#275672,#275673,
#275674,#275675,#275676,#275677,#275678,#275679,#275680,#275681,#275682,
#275683,#275684,#275685,#275686,#275687,#275688,#275689,#275690,#275691,
#275692,#275693,#275694,#275695,#275696,#275697,#275698,#275699,#275700,
#275701,#275702,#275703,#275704,#275705,#275706,#275707,#275708,#275709,
#275710,#275711,#275712,#275713,#275714,#275715,#275716,#275717,#275718,
#275719,#275720,#275721,#275722,#275723,#275724,#275725,#275726,#275727,
#275728,#275729,#275730,#275731,#275732,#275733,#275734,#275735,#275736,
#275737,#275738,#275739,#275740,#275741,#275742,#275743,#275744,#275745,
#275746,#275747,#275748,#275749,#275750,#275751,#275752,#275753,#275754,
#275755,#275756,#275757,#275758,#275759,#275760,#275761,#275762,#275763,
#275764,#275765,#275766,#275767,#275768,#275769,#275770,#275771,#275772,
#275773,#275774,#275775,#275776,#275777,#275778,#275779,#275780,#275781,
#275782,#275783,#275784,#275785,#275786,#275787,#275788,#275789,#275790,
#275791,#275792,#275793,#275794,#275795,#275796,#275797,#275798,#275799,
#275800,#275801,#275802,#275803,#275804,#275805,#275806,#275807,#275808,
#275809,#275810,#275811,#275812,#275813,#275814,#275815,#275816,#275817,
#275818,#275819,#275820,#275821,#275822,#275823,#275824,#275825,#275826,
#275827,#275828,#275829,#275830,#275831,#275832,#275833,#275834,#275835,
#275836,#275837,#275838,#275839,#275840,#275841,#275842,#275843,#275844,
#275845,#275846,#275847,#275848,#275849),.UNSPECIFIED.,.F.,.F.,(4,3,3,3,
3,3,3,3,3,3,3,3,3,3,3,3,3,3,3,3,3,3,3,3,3,3,3,3,3,3,3,3,3,3,3,3,3,3,3,3,
3,3,3,3,3,3,3,3,3,3,3,3,3,3,3,3,3,3,3,3,3,3,3,4),(-110.906691970891,-110.756832769008,
-110.704057422901,-110.598550620688,-110.493202694035,-110.387978649919,
-110.282820555787,-110.177692302814,-110.072557826409,-109.967311365035,
-109.86200190645,-109.756510612357,-109.706723572244,-109.601216770032,
-109.49586884338,-109.390644799264,-109.285486705133,-109.180358452161,
-109.075223975757,-108.969977514384,-108.864668055799,-108.759176761707,
-108.709389721587,-108.603882919376,-108.498534992724,-108.393310948609,
-108.288152854478,-108.183024601506,-108.077890125102,-107.972643663729,
-107.867334205145,-107.761842911054,-107.712055870931,-107.606549068719,
-107.501201142067,-107.395977097951,-107.29081900382,-107.185690750848,
-107.080556274444,-106.97530981307,-106.870000354486,-106.764509060394,
-106.714722020274,-106.609215218062,-106.503867291409,-106.398643247294,
-106.293485153163,-106.18835690019,-106.083222423786,-105.977975962413,
-105.872666503828,-105.767175209736,-105.717388169617,-105.611881367405,
-105.506533440753,-105.401309396637,-105.296151302506,-105.191023049534,
-105.08588857313,-104.980642111756,-104.875332653172,-104.76984135908,-104.72005431896,
-104.623506663712),.UNSPECIFIED.);
#3858=B_SPLINE_CURVE_WITH_KNOTS('',3,(#275851,#275852,#275853,#275854,#275855,
#275856,#275857,#275858,#275859,#275860),.UNSPECIFIED.,.F.,.F.,(4,1,1,1,
1,1,1,4),(-104.623497903185,-103.722720468304,-102.725386617647,-101.72805276699,
-100.730718916333,-99.7333850656765,-98.7360512150198,-98.3403213565322),
 .UNSPECIFIED.);
#3859=B_SPLINE_CURVE_WITH_KNOTS('',3,(#275862,#275863,#275864,#275865,#275866,
#275867,#275868,#275869,#275870,#275871),.UNSPECIFIED.,.F.,.F.,(4,1,1,1,
1,1,1,4),(-98.3403213565322,-97.738717364363,-96.7413835137062,-95.7440496630495,
-94.7467158123927,-93.7493819617359,-92.7520481110792,-92.0571360493526),
 .UNSPECIFIED.);
#3860=B_SPLINE_CURVE_WITH_KNOTS('',3,(#275873,#275874,#275875,#275876,#275877,
#275878,#275879,#275880,#275881,#275882,#275883,#275884,#275885,#275886,
#275887,#275888,#275889,#275890,#275891,#275892,#275893,#275894,#275895,
#275896,#275897,#275898,#275899,#275900,#275901,#275902,#275903,#275904,
#275905,#275906,#275907,#275908,#275909,#275910,#275911,#275912,#275913,
#275914,#275915,#275916,#275917,#275918,#275919,#275920,#275921,#275922,
#275923,#275924,#275925,#275926,#275927,#275928,#275929,#275930,#275931,
#275932,#275933,#275934,#275935,#275936,#275937,#275938,#275939,#275940,
#275941,#275942,#275943,#275944,#275945,#275946,#275947,#275948,#275949,
#275950,#275951,#275952,#275953,#275954,#275955,#275956,#275957,#275958,
#275959,#275960,#275961,#275962,#275963,#275964,#275965,#275966,#275967,
#275968,#275969,#275970,#275971,#275972,#275973,#275974,#275975,#275976,
#275977,#275978,#275979,#275980,#275981,#275982,#275983,#275984,#275985,
#275986,#275987,#275988,#275989,#275990,#275991,#275992,#275993,#275994,
#275995,#275996,#275997,#275998,#275999,#276000,#276001,#276002,#276003,
#276004,#276005,#276006,#276007,#276008,#276009,#276010,#276011,#276012,
#276013,#276014,#276015,#276016,#276017,#276018,#276019,#276020,#276021,
#276022,#276023,#276024,#276025,#276026,#276027,#276028,#276029,#276030,
#276031,#276032,#276033,#276034,#276035,#276036,#276037,#276038,#276039,
#276040,#276041,#276042,#276043,#276044,#276045,#276046,#276047,#276048,
#276049,#276050,#276051,#276052,#276053,#276054,#276055,#276056,#276057,
#276058,#276059,#276060,#276061,#276062),.UNSPECIFIED.,.F.,.F.,(4,3,3,3,
3,3,3,3,3,3,3,3,3,3,3,3,3,3,3,3,3,3,3,3,3,3,3,3,3,3,3,3,3,3,3,3,3,3,3,3,
3,3,3,3,3,3,3,3,3,3,3,3,3,3,3,3,3,3,3,3,3,3,3,4),(-92.0571358641713,-91.930999755056,
-91.8031327507075,-91.7547142604224,-91.6492074582106,-91.5438595315583,
-91.4386354874429,-91.333477393312,-91.2283491403396,-91.1232146639356,
-91.0179682025622,-90.9126587439777,-90.8071674498857,-90.7573804097656,
-90.6518736075538,-90.5465256809014,-90.4413016367861,-90.3361435426553,
-90.231015289683,-90.1258808132789,-90.0206343519056,-89.9153248933212,
-89.8098335992292,-89.7600465591089,-89.6545397568971,-89.5491918302447,
-89.4439677861294,-89.3388096919985,-89.2336814390262,-89.1285469626221,
-89.0233005012487,-88.9179910426643,-88.8124997485723,-88.7627127084521,
-88.6572059062403,-88.5518579795879,-88.4466339354725,-88.3414758413416,
-88.2363475883693,-88.1312131119652,-88.0259666505918,-87.9206571920073,
-87.8151658979152,-87.7653788577953,-87.6598720555835,-87.5545241289311,
-87.4493000848158,-87.344141990685,-87.2390137377127,-87.1338792613086,
-87.0286327999352,-86.9233233413509,-86.8178320472589,-86.7680450071386,
-86.6625996592658,-86.5573131394121,-86.4521502811752,-86.3470531325385,
-86.2419854899419,-86.136911193783,-86.0317248142074,-85.9264748702226,
-85.8210440559206,-85.7739507426472),.UNSPECIFIED.);
#3861=B_SPLINE_CURVE_WITH_KNOTS('',3,(#276064,#276065,#276066,#276067,#276068,
#276069,#276070,#276071,#276072,#276073,#276074,#276075,#276076,#276077,
#276078,#276079,#276080,#276081,#276082,#276083,#276084,#276085,#276086,
#276087,#276088,#276089,#276090,#276091,#276092,#276093,#276094,#276095,
#276096,#276097,#276098,#276099,#276100,#276101,#276102,#276103,#276104,
#276105,#276106,#276107,#276108,#276109,#276110,#276111,#276112,#276113,
#276114,#276115,#276116,#276117,#276118,#276119,#276120,#276121,#276122,
#276123,#276124,#276125,#276126,#276127,#276128,#276129,#276130,#276131,
#276132,#276133,#276134,#276135,#276136,#276137,#276138,#276139,#276140,
#276141,#276142,#276143,#276144,#276145,#276146,#276147,#276148,#276149,
#276150,#276151,#276152,#276153,#276154,#276155,#276156,#276157,#276158,
#276159,#276160,#276161,#276162,#276163,#276164,#276165,#276166,#276167,
#276168,#276169,#276170,#276171,#276172,#276173,#276174,#276175,#276176,
#276177,#276178,#276179,#276180,#276181,#276182,#276183,#276184,#276185,
#276186,#276187,#276188,#276189,#276190,#276191,#276192,#276193,#276194,
#276195,#276196,#276197,#276198,#276199,#276200,#276201,#276202,#276203,
#276204,#276205,#276206,#276207,#276208,#276209,#276210,#276211,#276212,
#276213,#276214,#276215,#276216,#276217,#276218,#276219,#276220,#276221,
#276222,#276223,#276224,#276225,#276226,#276227,#276228,#276229,#276230,
#276231,#276232,#276233,#276234,#276235,#276236,#276237,#276238,#276239,
#276240,#276241,#276242,#276243,#276244,#276245,#276246,#276247,#276248,
#276249,#276250,#276251,#276252,#276253,#276254,#276255,#276256),
 .UNSPECIFIED.,.F.,.F.,(4,3,3,3,3,3,3,3,3,3,3,3,3,3,3,3,3,3,3,3,3,3,3,3,
3,3,3,3,3,3,3,3,3,3,3,3,3,3,3,3,3,3,3,3,3,3,3,3,3,3,3,3,3,3,3,3,3,3,3,3,
3,3,3,3,4),(-85.773950742173,-85.7707111564818,-85.6652043542701,-85.5598564276176,
-85.4546323835023,-85.3494742893715,-85.2443460363991,-85.139211559995,
-85.0339650986217,-84.9286556400373,-84.8231643459452,-84.7733773058251,
-84.6678705036133,-84.5625225769609,-84.4572985328455,-84.3521404387147,
-84.2470121857423,-84.1418777093383,-84.0366312479649,-83.9313217893805,
-83.8258304952885,-83.7760434551683,-83.6705366529565,-83.5651887263041,
-83.4599646821888,-83.3548065880579,-83.2496783350855,-83.1445438586814,
-83.039297397308,-82.9339879387236,-82.8284966446315,-82.7787096045115,
-82.6732028022997,-82.5678548756473,-82.462630831532,-82.3574727374011,
-82.2523444844288,-82.1472100080247,-82.0419635466513,-81.9366540880669,
-81.8311627939748,-81.7813757538547,-81.6758689516429,-81.5705210249905,
-81.4652969808752,-81.3601388867444,-81.2550106337721,-81.149876157368,
-81.0446296959946,-80.9393202374102,-80.8338289433182,-80.784041903198,
-80.6785351009862,-80.5731871743338,-80.4679631302184,-80.3628050360876,
-80.2576767831152,-80.1525423067111,-80.0472958453377,-79.9419863867533,
-79.8364950926612,-79.7867080525412,-79.657701481349,-79.5305194816838,
-79.4907656074844),.UNSPECIFIED.);
#3862=B_SPLINE_CURVE_WITH_KNOTS('',3,(#276258,#276259,#276260,#276261,#276262,
#276263,#276264,#276265,#276266,#276267),.UNSPECIFIED.,.F.,.F.,(4,1,1,1,
1,1,1,4),(-79.4907654349934,-78.7893742018845,-77.7920403512277,-76.7947065005709,
-75.7973726499142,-74.8000387992574,-73.8027049486006,-73.2075801278138),
 .UNSPECIFIED.);
#3863=B_SPLINE_CURVE_WITH_KNOTS('',3,(#276269,#276270,#276271,#276272,#276273,
#276274,#276275,#276276,#276277,#276278,#276279,#276280,#276281,#276282,
#276283,#276284,#276285,#276286,#276287,#276288,#276289,#276290,#276291,
#276292,#276293,#276294,#276295,#276296,#276297,#276298,#276299,#276300,
#276301,#276302,#276303,#276304,#276305,#276306,#276307,#276308,#276309,
#276310,#276311,#276312,#276313,#276314,#276315,#276316,#276317,#276318,
#276319,#276320,#276321,#276322,#276323,#276324,#276325,#276326,#276327,
#276328,#276329,#276330,#276331,#276332,#276333,#276334,#276335,#276336,
#276337,#276338,#276339,#276340,#276341,#276342,#276343,#276344,#276345,
#276346,#276347,#276348,#276349,#276350,#276351,#276352,#276353,#276354,
#276355,#276356,#276357,#276358,#276359,#276360,#276361,#276362,#276363,
#276364,#276365,#276366,#276367,#276368,#276369,#276370,#276371,#276372,
#276373,#276374,#276375,#276376,#276377,#276378,#276379,#276380,#276381,
#276382,#276383,#276384,#276385,#276386,#276387,#276388,#276389,#276390,
#276391,#276392,#276393,#276394,#276395,#276396,#276397,#276398,#276399,
#276400,#276401,#276402,#276403,#276404,#276405,#276406,#276407,#276408,
#276409,#276410,#276411,#276412,#276413,#276414,#276415,#276416,#276417,
#276418,#276419,#276420,#276421,#276422,#276423,#276424,#276425,#276426,
#276427,#276428,#276429,#276430,#276431,#276432,#276433,#276434,#276435,
#276436,#276437,#276438,#276439,#276440,#276441,#276442,#276443,#276444,
#276445,#276446,#276447,#276448,#276449,#276450,#276451,#276452,#276453,
#276454,#276455,#276456,#276457,#276458),.UNSPECIFIED.,.F.,.F.,(4,3,3,3,
3,3,3,3,3,3,3,3,3,3,3,3,3,3,3,3,3,3,3,3,3,3,3,3,3,3,3,3,3,3,3,3,3,3,3,3,
3,3,3,3,3,3,3,3,3,3,3,3,3,3,3,3,3,3,3,3,3,3,3,4),(-73.2075796961327,-73.0915724254084,
-72.975151035254,-72.8581731739681,-72.8053710979439,-72.6998642957321,
-72.5945163690796,-72.4892923249642,-72.3841342308334,-72.279005977861,
-72.1738715014568,-72.0686250400834,-71.9633155814988,-71.8578242874068,
-71.8080372472871,-71.7025304450754,-71.5971825184229,-71.4919584743076,
-71.3868003801767,-71.2816721272044,-71.1765376508003,-71.0712911894269,
-70.9659817308425,-70.8604904367505,-70.8107033966303,-70.7051965944186,
-70.5998486677662,-70.4946246236509,-70.3894665295201,-70.2843382765477,
-70.1792038001437,-70.0739573387704,-69.968647880186,-69.863156586094,-69.8133695459736,
-69.7078627437618,-69.6025148171094,-69.4972907729941,-69.3921326788632,
-69.2870044258909,-69.1818699494868,-69.0766234881134,-68.971314029529,
-68.8658227354369,-68.8160356953168,-68.710528893105,-68.6051809664526,
-68.4999569223372,-68.3947988282064,-68.289670575234,-68.1845360988299,
-68.0792896374565,-67.973980178872,-67.8684888847799,-67.81870184466,-67.7145345612462,
-67.6105461545448,-67.5066572304383,-67.4028298868347,-67.2990263104663,
-67.195147136985,-67.091228097057,-66.9871477021693,-66.9243948210848),
 .UNSPECIFIED.);
#3864=B_SPLINE_CURVE_WITH_KNOTS('',3,(#276460,#276461,#276462,#276463,#276464,
#276465,#276466,#276467,#276468,#276469,#276470,#276471,#276472,#276473,
#276474,#276475,#276476,#276477,#276478,#276479,#276480,#276481,#276482,
#276483,#276484,#276485,#276486,#276487,#276488,#276489,#276490,#276491,
#276492,#276493,#276494,#276495,#276496,#276497,#276498,#276499,#276500,
#276501,#276502,#276503,#276504,#276505,#276506,#276507,#276508,#276509,
#276510,#276511,#276512,#276513,#276514,#276515,#276516,#276517,#276518,
#276519,#276520,#276521,#276522,#276523,#276524,#276525,#276526,#276527,
#276528,#276529,#276530,#276531,#276532,#276533,#276534,#276535,#276536,
#276537,#276538,#276539,#276540,#276541,#276542,#276543,#276544,#276545,
#276546,#276547,#276548,#276549,#276550,#276551,#276552,#276553,#276554,
#276555,#276556,#276557,#276558,#276559,#276560,#276561,#276562,#276563,
#276564,#276565,#276566,#276567,#276568,#276569,#276570,#276571,#276572,
#276573,#276574,#276575,#276576,#276577,#276578,#276579,#276580,#276581,
#276582,#276583,#276584,#276585,#276586,#276587,#276588,#276589,#276590,
#276591,#276592,#276593,#276594,#276595,#276596,#276597,#276598,#276599,
#276600,#276601,#276602,#276603,#276604,#276605,#276606,#276607,#276608,
#276609,#276610,#276611,#276612,#276613,#276614,#276615,#276616,#276617,
#276618,#276619,#276620,#276621,#276622,#276623,#276624,#276625,#276626,
#276627,#276628,#276629,#276630,#276631,#276632,#276633,#276634,#276635,
#276636,#276637,#276638,#276639,#276640,#276641,#276642,#276643,#276644,
#276645,#276646,#276647,#276648,#276649),.UNSPECIFIED.,.F.,.F.,(4,3,3,3,
3,3,3,3,3,3,3,3,3,3,3,3,3,3,3,3,3,3,3,3,3,3,3,3,3,3,3,3,3,3,3,3,3,3,3,3,
3,3,3,3,3,3,3,3,3,3,3,3,3,3,3,3,3,3,3,3,3,3,3,4),(-66.9243948206342,-66.8213679940033,
-66.7158611917913,-66.6105132651389,-66.5052892210233,-66.4001311268923,
-66.2950028739198,-66.1898683975154,-66.0846219361418,-65.9793124775572,
-65.873821183465,-65.8240341433465,-65.7185273411348,-65.6131794144823,
-65.507955370367,-65.4027972762362,-65.2976690232639,-65.1925345468598,
-65.0872880854865,-64.9819786269021,-64.8764873328101,-64.8267002926897,
-64.721193490478,-64.6158455638255,-64.5106215197102,-64.4054634255794,
-64.3003351726071,-64.1952006962031,-64.0899542348298,-63.9846447762454,
-63.8791534821534,-63.829366442033,-63.7238596398212,-63.6185117131688,
-63.5132876690534,-63.4081295749225,-63.3030013219502,-63.1978668455461,
-63.0926203841727,-62.9873109255882,-62.8818196314961,-62.8320325913762,
-62.7265257891644,-62.6211778625121,-62.5159538183968,-62.410795724266,
-62.3056674712936,-62.2005329948896,-62.0952865335163,-61.9899770749318,
-61.8844857808398,-61.8346987407195,-61.7291919385078,-61.6238440118554,
-61.5186199677401,-61.4134618736093,-61.308333620637,-61.203199144233,-61.0979526828596,
-60.9926432242751,-60.8871519301831,-60.8373648900627,-60.6850374634616,
-60.6412095134546),.UNSPECIFIED.);
#3865=B_SPLINE_CURVE_WITH_KNOTS('',3,(#276651,#276652,#276653,#276654,#276655,
#276656,#276657,#276658,#276659,#276660),.UNSPECIFIED.,.F.,.F.,(4,1,1,1,
1,1,1,4),(-60.6412060771752,-59.8400310394059,-58.8426971887492,-57.8453633380924,
-56.8480294874356,-55.8506956367789,-54.8533617861221,-54.358024206275),
 .UNSPECIFIED.);
#3866=B_SPLINE_CURVE_WITH_KNOTS('',3,(#276662,#276663,#276664,#276665,#276666,
#276667,#276668,#276669,#276670,#276671),.UNSPECIFIED.,.F.,.F.,(4,1,1,1,
1,1,1,4),(-54.358024206275,-53.8560279354653,-52.8586940848086,-51.8613602341518,
-50.864026383495,-49.8666925328383,-48.8693586821815,-48.0748417153853),
 .UNSPECIFIED.);
#3867=B_SPLINE_CURVE_WITH_KNOTS('',3,(#276673,#276674,#276675,#276676,#276677,
#276678,#276679,#276680,#276681,#276682,#276683,#276684,#276685,#276686,
#276687,#276688,#276689,#276690,#276691,#276692,#276693,#276694,#276695,
#276696,#276697,#276698,#276699,#276700,#276701,#276702,#276703,#276704,
#276705,#276706,#276707,#276708,#276709,#276710,#276711,#276712,#276713,
#276714,#276715,#276716,#276717,#276718,#276719,#276720,#276721,#276722,
#276723,#276724,#276725,#276726,#276727,#276728,#276729,#276730,#276731,
#276732,#276733,#276734,#276735,#276736,#276737,#276738,#276739,#276740,
#276741,#276742,#276743,#276744,#276745,#276746,#276747,#276748,#276749,
#276750,#276751,#276752,#276753,#276754,#276755,#276756,#276757,#276758,
#276759,#276760,#276761,#276762,#276763,#276764,#276765,#276766,#276767,
#276768,#276769,#276770,#276771,#276772,#276773,#276774,#276775,#276776,
#276777,#276778,#276779,#276780,#276781,#276782,#276783,#276784,#276785,
#276786,#276787,#276788,#276789,#276790,#276791,#276792,#276793,#276794,
#276795,#276796,#276797,#276798,#276799,#276800,#276801,#276802,#276803,
#276804,#276805,#276806,#276807,#276808,#276809,#276810,#276811,#276812,
#276813,#276814,#276815,#276816,#276817,#276818,#276819,#276820,#276821,
#276822,#276823,#276824,#276825,#276826,#276827,#276828,#276829,#276830,
#276831,#276832,#276833,#276834,#276835,#276836,#276837,#276838,#276839,
#276840,#276841,#276842,#276843,#276844,#276845,#276846,#276847,#276848,
#276849,#276850,#276851,#276852,#276853,#276854,#276855,#276856,#276857,
#276858,#276859,#276860,#276861,#276862),.UNSPECIFIED.,.F.,.F.,(4,3,3,3,
3,3,3,3,3,3,3,3,3,3,3,3,3,3,3,3,3,3,3,3,3,3,3,3,3,3,3,3,3,3,3,3,3,3,3,3,
3,3,3,3,3,3,3,3,3,3,3,3,3,3,3,3,3,3,3,3,3,3,3,4),(-48.0748388990954,-47.9250452568101,
-47.8720248315247,-47.766518029313,-47.6611701026606,-47.5559460585454,
-47.4507879644146,-47.3456597114423,-47.2405252350384,-47.1352787736651,
-47.0299693150807,-46.9244780209887,-46.874690980868,-46.7691841786562,
-46.6638362520038,-46.5586122078884,-46.4534541137576,-46.3483258607852,
-46.2431913843811,-46.1379449230077,-46.0326354644232,-45.9271441703312,
-45.8773571302112,-45.7718503279994,-45.6665024013469,-45.5612783572316,
-45.4561202631007,-45.3509920101283,-45.2458575337242,-45.1406110723508,
-45.0353016137664,-44.9298103196743,-44.8800232795544,-44.7745164773427,
-44.6691685506903,-44.563944506575,-44.4587864124442,-44.3536581594719,
-44.2485236830678,-44.1432772216945,-44.0379677631101,-43.9324764690181,
-43.8826894288977,-43.777182626686,-43.6718347000335,-43.5666106559182,
-43.4614525617874,-43.356324308815,-43.251189832411,-43.1459433710376,-43.0406339124532,
-42.9351426183611,-42.8853555782409,-42.7798487760291,-42.6745008493767,
-42.5692768052613,-42.4641187111305,-42.3589904581581,-42.2538559817541,
-42.1486095203807,-42.0433000617962,-41.9378087677041,-41.8880217275841,
-41.7916535919158),.UNSPECIFIED.);
#3868=B_SPLINE_CURVE_WITH_KNOTS('',3,(#276864,#276865,#276866,#276867,#276868,
#276869,#276870,#276871,#276872,#276873),.UNSPECIFIED.,.F.,.F.,(4,1,1,1,
1,1,1,4),(-41.7916448335886,-40.8906878769274,-39.8933540262706,-38.8960201756138,
-37.8986863249571,-36.9013524743003,-35.9040186236436,-35.5084682847362),
 .UNSPECIFIED.);
#3869=B_SPLINE_CURVE_WITH_KNOTS('',3,(#276875,#276876,#276877,#276878,#276879,
#276880,#276881,#276882,#276883,#276884),.UNSPECIFIED.,.F.,.F.,(4,1,1,1,
1,1,1,4),(-35.5084682847362,-34.9066847729868,-33.90935092233,-32.9120170716733,
-31.9146832210165,-30.9173493703597,-29.920015519703,-29.2252829775566),
 .UNSPECIFIED.);
#3870=B_SPLINE_CURVE_WITH_KNOTS('',3,(#276886,#276887,#276888,#276889,#276890,
#276891,#276892,#276893,#276894,#276895,#276896,#276897,#276898,#276899,
#276900,#276901,#276902,#276903,#276904,#276905,#276906,#276907,#276908,
#276909,#276910,#276911,#276912,#276913,#276914,#276915,#276916,#276917,
#276918,#276919,#276920,#276921,#276922,#276923,#276924,#276925,#276926,
#276927,#276928,#276929,#276930,#276931,#276932,#276933,#276934,#276935,
#276936,#276937,#276938,#276939,#276940,#276941,#276942,#276943,#276944,
#276945,#276946,#276947,#276948,#276949,#276950,#276951,#276952,#276953,
#276954,#276955,#276956,#276957,#276958,#276959,#276960,#276961,#276962,
#276963,#276964,#276965,#276966,#276967,#276968,#276969,#276970,#276971,
#276972,#276973,#276974,#276975,#276976,#276977,#276978,#276979,#276980,
#276981,#276982,#276983,#276984,#276985,#276986,#276987,#276988,#276989,
#276990,#276991,#276992,#276993,#276994,#276995,#276996,#276997,#276998,
#276999,#277000,#277001,#277002,#277003,#277004,#277005,#277006,#277007,
#277008,#277009,#277010,#277011,#277012,#277013,#277014,#277015,#277016,
#277017,#277018,#277019,#277020,#277021,#277022,#277023,#277024,#277025,
#277026,#277027,#277028,#277029,#277030,#277031,#277032,#277033,#277034,
#277035,#277036,#277037,#277038,#277039,#277040,#277041,#277042,#277043,
#277044,#277045,#277046,#277047,#277048,#277049,#277050,#277051,#277052,
#277053,#277054,#277055,#277056,#277057,#277058,#277059,#277060,#277061,
#277062,#277063,#277064,#277065,#277066,#277067,#277068,#277069,#277070,
#277071,#277072,#277073,#277074,#277075),.UNSPECIFIED.,.F.,.F.,(4,3,3,3,
3,3,3,3,3,3,3,3,3,3,3,3,3,3,3,3,3,3,3,3,3,3,3,3,3,3,3,3,3,3,3,3,3,3,3,3,
3,3,3,3,3,3,3,3,3,3,3,3,3,3,3,3,3,3,3,3,3,3,3,4),(-29.2252827920403,-29.0991710721254,
-28.9713316793409,-28.9226816690462,-28.8171748668507,-28.7118269402145,
-28.606602896115,-28.501444802,-28.3963165490433,-28.2911820726547,-28.1859356112964,
-28.0806261527268,-27.9751348586492,-27.9253478183894,-27.8198410162024,
-27.7144930895749,-27.6092690454849,-27.5041109513795,-27.3989826984327,
-27.2938482220543,-27.1886017607065,-27.0832923021477,-26.977801008081,
-26.9280139677327,-26.8225071654109,-26.7171592386482,-26.6119351944228,
-26.506777100182,-26.4016488471,-26.2965143705868,-26.1912679091058,-26.0859584504144,
-25.9804671562175,-25.9306801170759,-25.8251733150019,-25.7198253884868,
-25.6146013445074,-25.5094432505115,-25.404314997673,-25.2991805214014,
-25.1939340601577,-25.0886246017014,-24.983133307734,-24.9333462664191,
-24.8278394643211,-24.7224915377845,-24.6172674937872,-24.5121093997757,
-24.4069811469239,-24.3018466706412,-24.1966002093899,-24.0912907509281,
-23.9857994569581,-23.9360124157624,-23.8305704338793,-23.7252872773173,
-23.620127770382,-23.5150339599447,-23.4099696373072,-23.3048986377144,
-23.1997155503862,-23.094468867793,-22.9890413697073,-22.9420976708737),
 .UNSPECIFIED.);
#3871=B_SPLINE_CURVE_WITH_KNOTS('',3,(#277077,#277078,#277079,#277080,#277081,
#277082,#277083,#277084,#277085,#277086,#277087,#277088,#277089,#277090,
#277091,#277092,#277093,#277094,#277095,#277096,#277097,#277098,#277099,
#277100,#277101,#277102,#277103,#277104,#277105,#277106,#277107,#277108,
#277109,#277110,#277111,#277112,#277113,#277114,#277115,#277116,#277117,
#277118,#277119,#277120,#277121,#277122,#277123,#277124,#277125,#277126,
#277127,#277128,#277129,#277130,#277131,#277132,#277133,#277134,#277135,
#277136,#277137,#277138,#277139,#277140,#277141,#277142,#277143,#277144,
#277145,#277146,#277147,#277148,#277149,#277150,#277151,#277152,#277153,
#277154,#277155,#277156,#277157,#277158,#277159,#277160,#277161,#277162,
#277163,#277164,#277165,#277166,#277167,#277168,#277169,#277170,#277171,
#277172,#277173,#277174,#277175,#277176,#277177,#277178,#277179,#277180,
#277181,#277182,#277183,#277184,#277185,#277186,#277187,#277188,#277189,
#277190,#277191,#277192,#277193,#277194,#277195,#277196,#277197,#277198,
#277199,#277200,#277201,#277202,#277203,#277204,#277205,#277206,#277207,
#277208,#277209,#277210,#277211,#277212,#277213,#277214,#277215,#277216,
#277217,#277218,#277219,#277220,#277221,#277222,#277223,#277224,#277225,
#277226,#277227,#277228,#277229,#277230,#277231,#277232,#277233,#277234,
#277235,#277236,#277237,#277238,#277239,#277240,#277241,#277242,#277243,
#277244,#277245,#277246,#277247,#277248,#277249,#277250,#277251,#277252,
#277253,#277254,#277255,#277256,#277257,#277258,#277259,#277260,#277261,
#277262,#277263,#277264,#277265,#277266,#277267,#277268,#277269),
 .UNSPECIFIED.,.F.,.F.,(4,3,3,3,3,3,3,3,3,3,3,3,3,3,3,3,3,3,3,3,3,3,3,3,
3,3,3,3,3,3,3,3,3,3,3,3,3,3,3,3,3,3,3,3,3,3,3,3,3,3,3,3,3,3,3,3,3,3,3,3,
3,3,3,3,4),(-22.9420976703771,-22.9386785651056,-22.833171763997,-22.7278238384453,
-22.6225997954218,-22.5174417023766,-22.4123134504822,-22.3071789751466,
-22.2019325148207,-22.0966230572732,-21.9911317641911,-21.9413447144488,
-21.8358379126161,-21.7304899863559,-21.62526594265,-21.520107848939,-21.4149795963963,
-21.3098451204308,-21.2045986595064,-21.0992892013775,-20.9937979077462,
-20.9440108637921,-20.8385040568042,-20.7331561253577,-20.6279320764448,
-20.5227739775171,-20.4176457197557,-20.3125112385776,-20.2072647724855,
-20.1019553092069,-19.9964640105077,-19.9466770131353,-19.8411702194118,
-19.7358223012373,-19.6305982655446,-19.5254401797971,-19.4203119351568,
-19.3151774670212,-19.2099310137648,-19.1046215632227,-18.9991302769745,
-18.9493431624785,-18.8438363600323,-18.7384884332319,-18.6332643890952,
-18.5281062950215,-18.4229780421838,-18.3178435659912,-18.2125971049424,
-18.1072876467475,-18.0017963531398,-17.9520093118218,-17.8465024793659,
-17.7411545223281,-17.6359304477663,-17.530772323169,-17.425644039756,-17.3205095329828,
-17.2152630415555,-17.1099535530528,-17.0044622295655,-16.954675461165,
-16.8256403797072,-16.6984335818362,-16.6589125353209),.UNSPECIFIED.);
#3872=B_SPLINE_CURVE_WITH_KNOTS('',3,(#277271,#277272,#277273,#277274,#277275,
#277276,#277277,#277278,#277279,#277280),.UNSPECIFIED.,.F.,.F.,(4,1,1,1,
1,1,1,4),(-16.6589123631975,-15.9573416105082,-14.9600077598515,-13.9626739091947,
-12.9653400585379,-11.9680062078812,-10.9706723572244,-10.3757270560179),
 .UNSPECIFIED.);
#3873=B_SPLINE_CURVE_WITH_KNOTS('',3,(#277281,#277282,#277283,#277284,#277285,
#277286,#277287,#277288,#277289,#277290),.UNSPECIFIED.,.F.,.F.,(4,1,1,1,
1,1,1,4),(-10.3757270560179,-9.97333850656766,-8.97600465591089,-7.97867080525412,
-6.98133695459736,-5.98400310394059,-4.98666925328383,-4.09255055993695),
 .UNSPECIFIED.);
#3874=B_SPLINE_CURVE_WITH_KNOTS('',3,(#277293,#277294,#277295,#277296,#277297,
#277298,#277299,#277300,#277301,#277302,#277303,#277304,#277305,#277306,
#277307,#277308,#277309,#277310,#277311,#277312,#277313,#277314,#277315,
#277316,#277317,#277318,#277319,#277320,#277321,#277322,#277323,#277324,
#277325,#277326,#277327,#277328,#277329,#277330,#277331,#277332,#277333,
#277334,#277335,#277336,#277337,#277338,#277339,#277340,#277341,#277342,
#277343,#277344,#277345,#277346,#277347,#277348,#277349,#277350,#277351,
#277352,#277353,#277354,#277355,#277356,#277357,#277358,#277359,#277360,
#277361,#277362,#277363,#277364,#277365,#277366,#277367,#277368),
 .UNSPECIFIED.,.F.,.F.,(4,3,3,3,3,3,3,3,3,3,3,3,3,3,3,3,3,3,3,3,3,3,3,3,
3,4),(182.609476336781,182.720981410639,182.832583305898,182.944230107119,
183.056086738955,183.156843832074,183.268703246413,183.380368125164,183.491924434765,
183.603414787061,183.714881699591,183.826450437116,183.93806614918,184.049898405165,
184.154177682731,184.264652382406,184.375509776279,184.485678175887,184.595782248961,
184.705866563965,184.81727780632,184.927534423388,185.039522978388,185.151511533388,
185.3342658208,185.353966561798),.UNSPECIFIED.);
#3875=B_SPLINE_CURVE_WITH_KNOTS('',3,(#277369,#277370,#277371,#277372,#277373,
#277374,#277375,#277376,#277377,#277378,#277379,#277380,#277381,#277382,
#277383,#277384,#277385,#277386,#277387,#277388,#277389,#277390),
 .UNSPECIFIED.,.F.,.F.,(4,3,3,3,3,3,3,4),(185.353966562125,185.466365028953,
185.578618560049,185.690768460106,185.805287691091,185.917389176518,186.033117280281,
186.148845384045),.UNSPECIFIED.);
#3876=B_SPLINE_CURVE_WITH_KNOTS('',3,(#277391,#277392,#277393,#277394,#277395,
#277396,#277397,#277398,#277399,#277400,#277401,#277402,#277403,#277404,
#277405,#277406,#277407,#277408,#277409,#277410,#277411,#277412,#277413,
#277414,#277415,#277416,#277417,#277418,#277419,#277420,#277421,#277422,
#277423,#277424,#277425,#277426,#277427,#277428,#277429,#277430,#277431,
#277432,#277433,#277434,#277435,#277436,#277437,#277438,#277439,#277440,
#277441,#277442,#277443,#277444,#277445,#277446,#277447,#277448,#277449,
#277450,#277451,#277452,#277453,#277454),.UNSPECIFIED.,.F.,.F.,(4,3,3,3,
3,3,3,3,3,3,3,3,3,3,3,3,3,3,3,3,3,4),(182.608828346121,182.720452013284,
182.832284778709,182.913686920972,183.024155546641,183.135063468431,183.245225477106,
183.355323083989,183.465400865193,183.576905379135,183.687155538369,183.799287229665,
183.911418920962,184.02624684209,184.140827409106,184.255261915833,184.369585299384,
184.48383233761,184.598072078494,184.712299653782,184.826611607649,184.909150920952),
 .UNSPECIFIED.);
#3877=B_SPLINE_CURVE_WITH_KNOTS('',3,(#277456,#277457,#277458,#277459,#277460,
#277461,#277462,#277463,#277464,#277465,#277466,#277467,#277468,#277469,
#277470,#277471,#277472,#277473,#277474,#277475,#277476,#277477,#277478,
#277479,#277480,#277481,#277482,#277483),.UNSPECIFIED.,.F.,.F.,(4,3,3,3,
3,3,3,3,3,4),(-0.271362855059747,-0.249815162449229,-0.228817987081128,
-0.214757039459256,-0.202712716314943,-0.199280160428694,-0.179100594986104,
-0.172574196593642,-0.151847730093891,-0.1354956858039),.UNSPECIFIED.);
#3878=B_SPLINE_CURVE_WITH_KNOTS('',3,(#278196,#278197,#278198,#278199,#278200,
#278201,#278202,#278203,#278204,#278205,#278206,#278207,#278208,#278209,
#278210,#278211,#278212,#278213,#278214,#278215,#278216,#278217,#278218,
#278219,#278220,#278221,#278222,#278223,#278224,#278225,#278226,#278227,
#278228,#278229,#278230,#278231,#278232,#278233,#278234,#278235,#278236,
#278237,#278238,#278239,#278240,#278241,#278242,#278243,#278244,#278245,
#278246,#278247,#278248,#278249,#278250,#278251,#278252,#278253,#278254,
#278255,#278256,#278257,#278258,#278259,#278260,#278261,#278262,#278263,
#278264,#278265,#278266,#278267,#278268,#278269,#278270,#278271,#278272,
#278273,#278274,#278275,#278276,#278277,#278278,#278279,#278280),
 .UNSPECIFIED.,.F.,.F.,(4,3,3,3,3,3,3,3,3,3,3,3,3,3,3,3,3,3,3,3,3,3,3,3,
3,3,3,3,4),(-0.364629307890672,-0.35088498418457,-0.32922248441233,-0.318977271176652,
-0.31373572999827,-0.309363560225569,-0.288064487980142,-0.26690192544149,
-0.264003434189125,-0.260297566857666,-0.239602118261299,-0.219188400900535,
-0.199416811699232,-0.194875855288817,-0.191398750352895,-0.171813098007178,
-0.16617324728061,-0.146077800662944,-0.126706278567434,-0.123378888671009,
-0.103932070266397,-0.0846696063770791,-0.0655665987659766,-0.0621850320486812,
-0.058954655734169,-0.0403439049005739,-0.0223158895279108,-0.00443448004250249,
-3.33131800984143E-15),.UNSPECIFIED.);
#3879=B_SPLINE_CURVE_WITH_KNOTS('',3,(#279001,#279002,#279003,#279004,#279005,
#279006,#279007,#279008,#279009,#279010,#279011,#279012,#279013,#279014,
#279015,#279016,#279017,#279018,#279019,#279020,#279021,#279022,#279023,
#279024,#279025,#279026,#279027,#279028,#279029,#279030,#279031,#279032,
#279033,#279034,#279035,#279036,#279037,#279038,#279039,#279040,#279041,
#279042,#279043,#279044,#279045,#279046,#279047,#279048,#279049,#279050,
#279051,#279052,#279053,#279054,#279055,#279056,#279057,#279058,#279059,
#279060,#279061,#279062,#279063,#279064,#279065,#279066,#279067,#279068,
#279069,#279070,#279071,#279072,#279073,#279074,#279075,#279076,#279077,
#279078,#279079,#279080,#279081,#279082),.UNSPECIFIED.,.F.,.F.,(4,3,3,3,
3,3,3,3,3,3,3,3,3,3,3,3,3,3,3,3,3,3,3,3,3,3,3,4),(-0.366397579005839,-0.355373790886745,
-0.337291596355845,-0.327068869252799,-0.321659955027813,-0.303056283858023,
-0.2839439572191,-0.281261647266766,-0.277594690433741,-0.258106988423997,
-0.238287343590241,-0.225542977825418,-0.218358221560673,-0.214836850115746,
-0.194406992337549,-0.187160363760496,-0.167265720489167,-0.149318298208285,
-0.146103234631719,-0.125762615585401,-0.104752145197835,-0.0837416748102686,
-0.0753034310399412,-0.0721935754585015,-0.0505500221103818,-0.028856412602834,
-0.00762632909558976,0.),.UNSPECIFIED.);
#4509=LINE('',#260677,#5146);
#4510=LINE('',#260922,#5147);
#4511=LINE('',#260963,#5148);
#4512=LINE('',#261083,#5149);
#4513=LINE('',#261485,#5150);
#4514=LINE('',#261919,#5151);
#4515=LINE('',#262377,#5152);
#4516=LINE('',#262803,#5153);
#4517=LINE('',#263315,#5154);
#4518=LINE('',#263737,#5155);
#4519=LINE('',#264073,#5156);
#4520=LINE('',#264425,#5157);
#4521=LINE('',#264744,#5158);
#4522=LINE('',#265107,#5159);
#4523=LINE('',#265535,#5160);
#4524=LINE('',#265877,#5161);
#4525=LINE('',#266240,#5162);
#4526=LINE('',#266675,#5163);
#4527=LINE('',#267132,#5164);
#4528=LINE('',#267561,#5165);
#4529=LINE('',#267888,#5166);
#4530=LINE('',#268252,#5167);
#4531=LINE('',#268695,#5168);
#4532=LINE('',#269146,#5169);
#4533=LINE('',#269595,#5170);
#4534=LINE('',#270058,#5171);
#4535=LINE('',#270495,#5172);
#4536=LINE('',#270944,#5173);
#4537=LINE('',#271395,#5174);
#4538=LINE('',#271814,#5175);
#4539=LINE('',#279086,#5176);
#4540=LINE('',#279088,#5177);
#4541=LINE('',#279090,#5178);
#4542=LINE('',#279091,#5179);
#4543=LINE('',#279094,#5180);
#4544=LINE('',#279096,#5181);
#4545=LINE('',#279097,#5182);
#4546=LINE('',#279100,#5183);
#4547=LINE('',#279102,#5184);
#4548=LINE('',#279103,#5185);
#4549=LINE('',#279106,#5186);
#4550=LINE('',#279108,#5187);
#4551=LINE('',#279109,#5188);
#4552=LINE('',#279112,#5189);
#4553=LINE('',#279114,#5190);
#4554=LINE('',#279115,#5191);
#4555=LINE('',#279117,#5192);
#4556=LINE('',#279118,#5193);
#4557=LINE('',#279125,#5194);
#5146=VECTOR('',#19945,1.5);
#5147=VECTOR('',#19950,1.5);
#5148=VECTOR('',#19957,1.5555);
#5149=VECTOR('',#19962,1.5555);
#5150=VECTOR('',#19965,1.5555);
#5151=VECTOR('',#19968,1.5555);
#5152=VECTOR('',#19971,1.5555);
#5153=VECTOR('',#19974,1.5555);
#5154=VECTOR('',#19977,1.5555);
#5155=VECTOR('',#19980,1.5555);
#5156=VECTOR('',#19983,1.5555);
#5157=VECTOR('',#19986,1.5555);
#5158=VECTOR('',#19989,1.5555);
#5159=VECTOR('',#19992,1.5555);
#5160=VECTOR('',#19995,1.5555);
#5161=VECTOR('',#19998,1.5555);
#5162=VECTOR('',#20001,1.5555);
#5163=VECTOR('',#20004,1.5555);
#5164=VECTOR('',#20007,1.5555);
#5165=VECTOR('',#20010,1.5555);
#5166=VECTOR('',#20013,1.5555);
#5167=VECTOR('',#20016,1.5555);
#5168=VECTOR('',#20019,1.5555);
#5169=VECTOR('',#20022,1.5555);
#5170=VECTOR('',#20025,1.5555);
#5171=VECTOR('',#20028,1.5555);
#5172=VECTOR('',#20031,1.5555);
#5173=VECTOR('',#20034,1.5555);
#5174=VECTOR('',#20037,1.5555);
#5175=VECTOR('',#20040,1.5555);
#5176=VECTOR('',#20055,10.);
#5177=VECTOR('',#20056,10.);
#5178=VECTOR('',#20057,10.);
#5179=VECTOR('',#20058,10.);
#5180=VECTOR('',#20061,10.);
#5181=VECTOR('',#20062,10.);
#5182=VECTOR('',#20063,10.);
#5183=VECTOR('',#20066,10.);
#5184=VECTOR('',#20067,10.);
#5185=VECTOR('',#20068,10.);
#5186=VECTOR('',#20071,10.);
#5187=VECTOR('',#20072,10.);
#5188=VECTOR('',#20073,10.);
#5189=VECTOR('',#20076,10.);
#5190=VECTOR('',#20077,10.);
#5191=VECTOR('',#20078,10.);
#5192=VECTOR('',#20081,10.);
#5193=VECTOR('',#20082,10.);
#5194=VECTOR('',#20091,3.5);
#7147=VERTEX_POINT('',#260675);
#7148=VERTEX_POINT('',#260676);
#7149=VERTEX_POINT('',#260678);
#7150=VERTEX_POINT('',#260680);
#7151=VERTEX_POINT('',#260919);
#7152=VERTEX_POINT('',#260921);
#7153=VERTEX_POINT('',#260924);
#7154=VERTEX_POINT('',#260961);
#7155=VERTEX_POINT('',#260962);
#7156=VERTEX_POINT('',#260964);
#7157=VERTEX_POINT('',#261038);
#7158=VERTEX_POINT('',#261081);
#7159=VERTEX_POINT('',#261082);
#7160=VERTEX_POINT('',#261084);
#7161=VERTEX_POINT('',#261285);
#7162=VERTEX_POINT('',#261483);
#7163=VERTEX_POINT('',#261484);
#7164=VERTEX_POINT('',#261917);
#7165=VERTEX_POINT('',#261918);
#7166=VERTEX_POINT('',#261920);
#7167=VERTEX_POINT('',#262147);
#7168=VERTEX_POINT('',#262375);
#7169=VERTEX_POINT('',#262376);
#7170=VERTEX_POINT('',#262801);
#7171=VERTEX_POINT('',#262802);
#7172=VERTEX_POINT('',#262804);
#7173=VERTEX_POINT('',#263063);
#7174=VERTEX_POINT('',#263313);
#7175=VERTEX_POINT('',#263314);
#7176=VERTEX_POINT('',#263735);
#7177=VERTEX_POINT('',#263736);
#7178=VERTEX_POINT('',#263738);
#7179=VERTEX_POINT('',#263971);
#7180=VERTEX_POINT('',#264071);
#7181=VERTEX_POINT('',#264072);
#7182=VERTEX_POINT('',#264292);
#7183=VERTEX_POINT('',#264423);
#7184=VERTEX_POINT('',#264424);
#7185=VERTEX_POINT('',#264426);
#7186=VERTEX_POINT('',#264742);
#7187=VERTEX_POINT('',#264743);
#7188=VERTEX_POINT('',#264745);
#7189=VERTEX_POINT('',#264879);
#7190=VERTEX_POINT('',#265105);
#7191=VERTEX_POINT('',#265106);
#7192=VERTEX_POINT('',#265533);
#7193=VERTEX_POINT('',#265534);
#7194=VERTEX_POINT('',#265536);
#7195=VERTEX_POINT('',#265655);
#7196=VERTEX_POINT('',#265875);
#7197=VERTEX_POINT('',#265876);
#7198=VERTEX_POINT('',#265878);
#7199=VERTEX_POINT('',#266238);
#7200=VERTEX_POINT('',#266239);
#7201=VERTEX_POINT('',#266447);
#7202=VERTEX_POINT('',#266673);
#7203=VERTEX_POINT('',#266674);
#7204=VERTEX_POINT('',#266676);
#7205=VERTEX_POINT('',#267130);
#7206=VERTEX_POINT('',#267131);
#7207=VERTEX_POINT('',#267349);
#7208=VERTEX_POINT('',#267559);
#7209=VERTEX_POINT('',#267560);
#7210=VERTEX_POINT('',#267562);
#7211=VERTEX_POINT('',#267797);
#7212=VERTEX_POINT('',#267886);
#7213=VERTEX_POINT('',#267887);
#7214=VERTEX_POINT('',#268115);
#7215=VERTEX_POINT('',#268250);
#7216=VERTEX_POINT('',#268251);
#7217=VERTEX_POINT('',#268253);
#7218=VERTEX_POINT('',#268693);
#7219=VERTEX_POINT('',#268694);
#7220=VERTEX_POINT('',#268922);
#7221=VERTEX_POINT('',#269144);
#7222=VERTEX_POINT('',#269145);
#7223=VERTEX_POINT('',#269147);
#7224=VERTEX_POINT('',#269593);
#7225=VERTEX_POINT('',#269594);
#7226=VERTEX_POINT('',#269818);
#7227=VERTEX_POINT('',#270056);
#7228=VERTEX_POINT('',#270057);
#7229=VERTEX_POINT('',#270059);
#7230=VERTEX_POINT('',#270493);
#7231=VERTEX_POINT('',#270494);
#7232=VERTEX_POINT('',#270708);
#7233=VERTEX_POINT('',#270942);
#7234=VERTEX_POINT('',#270943);
#7235=VERTEX_POINT('',#270945);
#7236=VERTEX_POINT('',#271393);
#7237=VERTEX_POINT('',#271394);
#7238=VERTEX_POINT('',#271602);
#7239=VERTEX_POINT('',#271812);
#7240=VERTEX_POINT('',#271813);
#7241=VERTEX_POINT('',#271815);
#7242=VERTEX_POINT('',#272106);
#7243=VERTEX_POINT('',#272284);
#7244=VERTEX_POINT('',#272285);
#7245=VERTEX_POINT('',#272347);
#7246=VERTEX_POINT('',#272349);
#7247=VERTEX_POINT('',#272384);
#7248=VERTEX_POINT('',#272575);
#7249=VERTEX_POINT('',#272586);
#7250=VERTEX_POINT('',#272598);
#7251=VERTEX_POINT('',#272789);
#7252=VERTEX_POINT('',#272800);
#7253=VERTEX_POINT('',#272811);
#7254=VERTEX_POINT('',#273002);
#7255=VERTEX_POINT('',#273013);
#7256=VERTEX_POINT('',#273024);
#7257=VERTEX_POINT('',#273215);
#7258=VERTEX_POINT('',#273226);
#7259=VERTEX_POINT('',#273237);
#7260=VERTEX_POINT('',#273428);
#7261=VERTEX_POINT('',#273441);
#7262=VERTEX_POINT('',#273632);
#7263=VERTEX_POINT('',#273823);
#7264=VERTEX_POINT('',#273835);
#7265=VERTEX_POINT('',#274026);
#7266=VERTEX_POINT('',#274037);
#7267=VERTEX_POINT('',#274049);
#7268=VERTEX_POINT('',#274237);
#7269=VERTEX_POINT('',#274428);
#7270=VERTEX_POINT('',#274439);
#7271=VERTEX_POINT('',#274630);
#7272=VERTEX_POINT('',#274641);
#7273=VERTEX_POINT('',#274652);
#7274=VERTEX_POINT('',#274665);
#7275=VERTEX_POINT('',#274667);
#7276=VERTEX_POINT('',#274837);
#7277=VERTEX_POINT('',#274848);
#7278=VERTEX_POINT('',#274859);
#7279=VERTEX_POINT('',#275050);
#7280=VERTEX_POINT('',#275244);
#7281=VERTEX_POINT('',#275255);
#7282=VERTEX_POINT('',#275446);
#7283=VERTEX_POINT('',#275637);
#7284=VERTEX_POINT('',#275648);
#7285=VERTEX_POINT('',#275659);
#7286=VERTEX_POINT('',#275850);
#7287=VERTEX_POINT('',#275861);
#7288=VERTEX_POINT('',#275872);
#7289=VERTEX_POINT('',#276063);
#7290=VERTEX_POINT('',#276257);
#7291=VERTEX_POINT('',#276268);
#7292=VERTEX_POINT('',#276459);
#7293=VERTEX_POINT('',#276650);
#7294=VERTEX_POINT('',#276661);
#7295=VERTEX_POINT('',#276672);
#7296=VERTEX_POINT('',#276863);
#7297=VERTEX_POINT('',#276874);
#7298=VERTEX_POINT('',#276885);
#7299=VERTEX_POINT('',#277076);
#7300=VERTEX_POINT('',#277270);
#7301=VERTEX_POINT('',#277292);
#7302=VERTEX_POINT('',#279084);
#7303=VERTEX_POINT('',#279085);
#7304=VERTEX_POINT('',#279087);
#7305=VERTEX_POINT('',#279089);
#7306=VERTEX_POINT('',#279093);
#7307=VERTEX_POINT('',#279095);
#7308=VERTEX_POINT('',#279099);
#7309=VERTEX_POINT('',#279101);
#7310=VERTEX_POINT('',#279105);
#7311=VERTEX_POINT('',#279107);
#7312=VERTEX_POINT('',#279111);
#7313=VERTEX_POINT('',#279113);
#7314=VERTEX_POINT('',#279121);
#7315=VERTEX_POINT('',#279124);
#9863=EDGE_CURVE('',#7147,#7148,#4509,.T.);
#9864=EDGE_CURVE('',#7149,#7147,#1972,.T.);
#9865=EDGE_CURVE('',#7150,#7149,#3729,.T.);
#9866=EDGE_CURVE('',#7151,#7150,#1973,.T.);
#9867=EDGE_CURVE('',#7151,#7152,#4510,.T.);
#9868=EDGE_CURVE('',#7152,#7152,#1974,.T.);
#9869=EDGE_CURVE('',#7153,#7151,#1975,.T.);
#9870=EDGE_CURVE('',#7148,#7153,#3730,.T.);
#9871=EDGE_CURVE('',#7154,#7155,#4511,.T.);
#9872=EDGE_CURVE('',#7156,#7154,#3731,.T.);
#9873=EDGE_CURVE('',#7157,#7156,#1976,.T.);
#9874=EDGE_CURVE('',#7157,#7155,#3732,.T.);
#9875=EDGE_CURVE('',#7158,#7159,#4512,.T.);
#9876=EDGE_CURVE('',#7160,#7158,#3733,.F.);
#9877=EDGE_CURVE('',#7154,#7160,#3734,.T.);
#9878=EDGE_CURVE('',#7155,#7161,#3735,.T.);
#9879=EDGE_CURVE('',#7161,#7159,#3736,.T.);
#9880=EDGE_CURVE('',#7162,#7163,#4513,.T.);
#9881=EDGE_CURVE('',#7158,#7162,#3737,.F.);
#9882=EDGE_CURVE('',#7159,#7163,#3738,.T.);
#9883=EDGE_CURVE('',#7164,#7165,#4514,.T.);
#9884=EDGE_CURVE('',#7166,#7164,#3739,.F.);
#9885=EDGE_CURVE('',#7162,#7166,#3740,.F.);
#9886=EDGE_CURVE('',#7163,#7167,#3741,.T.);
#9887=EDGE_CURVE('',#7167,#7165,#3742,.T.);
#9888=EDGE_CURVE('',#7168,#7169,#4515,.T.);
#9889=EDGE_CURVE('',#7164,#7168,#3743,.F.);
#9890=EDGE_CURVE('',#7165,#7169,#3744,.T.);
#9891=EDGE_CURVE('',#7170,#7171,#4516,.T.);
#9892=EDGE_CURVE('',#7172,#7170,#3745,.F.);
#9893=EDGE_CURVE('',#7168,#7172,#3746,.F.);
#9894=EDGE_CURVE('',#7169,#7173,#3747,.T.);
#9895=EDGE_CURVE('',#7173,#7171,#3748,.T.);
#9896=EDGE_CURVE('',#7174,#7175,#4517,.T.);
#9897=EDGE_CURVE('',#7170,#7174,#3749,.F.);
#9898=EDGE_CURVE('',#7171,#7175,#3750,.T.);
#9899=EDGE_CURVE('',#7176,#7177,#4518,.T.);
#9900=EDGE_CURVE('',#7178,#7176,#3751,.F.);
#9901=EDGE_CURVE('',#7174,#7178,#3752,.F.);
#9902=EDGE_CURVE('',#7175,#7179,#3753,.T.);
#9903=EDGE_CURVE('',#7179,#7177,#3754,.T.);
#9904=EDGE_CURVE('',#7180,#7181,#4519,.T.);
#9905=EDGE_CURVE('',#7176,#7180,#3755,.F.);
#9906=EDGE_CURVE('',#7177,#7182,#3756,.T.);
#9907=EDGE_CURVE('',#7182,#7181,#3757,.T.);
#9908=EDGE_CURVE('',#7183,#7184,#4520,.T.);
#9909=EDGE_CURVE('',#7185,#7183,#3758,.T.);
#9910=EDGE_CURVE('',#7180,#7185,#3759,.F.);
#9911=EDGE_CURVE('',#7181,#7184,#3760,.T.);
#9912=EDGE_CURVE('',#7186,#7187,#4521,.T.);
#9913=EDGE_CURVE('',#7188,#7186,#3761,.F.);
#9914=EDGE_CURVE('',#7183,#7188,#3762,.T.);
#9915=EDGE_CURVE('',#7184,#7189,#3763,.T.);
#9916=EDGE_CURVE('',#7189,#7187,#3764,.T.);
#9917=EDGE_CURVE('',#7190,#7191,#4522,.T.);
#9918=EDGE_CURVE('',#7186,#7190,#3765,.F.);
#9919=EDGE_CURVE('',#7187,#7191,#3766,.T.);
#9920=EDGE_CURVE('',#7192,#7193,#4523,.T.);
#9921=EDGE_CURVE('',#7194,#7192,#3767,.T.);
#9922=EDGE_CURVE('',#7190,#7194,#3768,.F.);
#9923=EDGE_CURVE('',#7191,#7195,#3769,.T.);
#9924=EDGE_CURVE('',#7195,#7193,#3770,.T.);
#9925=EDGE_CURVE('',#7196,#7197,#4524,.T.);
#9926=EDGE_CURVE('',#7198,#7196,#3771,.F.);
#9927=EDGE_CURVE('',#7192,#7198,#3772,.T.);
#9928=EDGE_CURVE('',#7193,#7197,#3773,.T.);
#9929=EDGE_CURVE('',#7199,#7200,#4525,.T.);
#9930=EDGE_CURVE('',#7196,#7199,#3774,.F.);
#9931=EDGE_CURVE('',#7197,#7201,#3775,.T.);
#9932=EDGE_CURVE('',#7201,#7200,#3776,.T.);
#9933=EDGE_CURVE('',#7202,#7203,#4526,.T.);
#9934=EDGE_CURVE('',#7204,#7202,#3777,.F.);
#9935=EDGE_CURVE('',#7199,#7204,#3778,.F.);
#9936=EDGE_CURVE('',#7200,#7203,#3779,.T.);
#9937=EDGE_CURVE('',#7205,#7206,#4527,.T.);
#9938=EDGE_CURVE('',#7202,#7205,#3780,.F.);
#9939=EDGE_CURVE('',#7203,#7207,#3781,.T.);
#9940=EDGE_CURVE('',#7207,#7206,#3782,.T.);
#9941=EDGE_CURVE('',#7208,#7209,#4528,.T.);
#9942=EDGE_CURVE('',#7210,#7208,#3783,.F.);
#9943=EDGE_CURVE('',#7205,#7210,#3784,.F.);
#9944=EDGE_CURVE('',#7206,#7211,#3785,.T.);
#9945=EDGE_CURVE('',#7211,#7209,#3786,.T.);
#9946=EDGE_CURVE('',#7212,#7213,#4529,.T.);
#9947=EDGE_CURVE('',#7208,#7212,#3787,.F.);
#9948=EDGE_CURVE('',#7209,#7214,#3788,.T.);
#9949=EDGE_CURVE('',#7214,#7213,#3789,.T.);
#9950=EDGE_CURVE('',#7215,#7216,#4530,.T.);
#9951=EDGE_CURVE('',#7217,#7215,#3790,.F.);
#9952=EDGE_CURVE('',#7212,#7217,#3791,.F.);
#9953=EDGE_CURVE('',#7213,#7216,#3792,.T.);
#9954=EDGE_CURVE('',#7218,#7219,#4531,.T.);
#9955=EDGE_CURVE('',#7215,#7218,#3793,.F.);
#9956=EDGE_CURVE('',#7216,#7220,#3794,.T.);
#9957=EDGE_CURVE('',#7220,#7219,#3795,.T.);
#9958=EDGE_CURVE('',#7221,#7222,#4532,.T.);
#9959=EDGE_CURVE('',#7223,#7221,#3796,.F.);
#9960=EDGE_CURVE('',#7218,#7223,#3797,.F.);
#9961=EDGE_CURVE('',#7219,#7222,#3798,.T.);
#9962=EDGE_CURVE('',#7224,#7225,#4533,.T.);
#9963=EDGE_CURVE('',#7221,#7224,#3799,.F.);
#9964=EDGE_CURVE('',#7222,#7226,#3800,.T.);
#9965=EDGE_CURVE('',#7226,#7225,#3801,.T.);
#9966=EDGE_CURVE('',#7227,#7228,#4534,.T.);
#9967=EDGE_CURVE('',#7229,#7227,#3802,.F.);
#9968=EDGE_CURVE('',#7224,#7229,#3803,.F.);
#9969=EDGE_CURVE('',#7225,#7228,#3804,.T.);
#9970=EDGE_CURVE('',#7230,#7231,#4535,.T.);
#9971=EDGE_CURVE('',#7227,#7230,#3805,.F.);
#9972=EDGE_CURVE('',#7228,#7232,#3806,.T.);
#9973=EDGE_CURVE('',#7232,#7231,#3807,.T.);
#9974=EDGE_CURVE('',#7233,#7234,#4536,.T.);
#9975=EDGE_CURVE('',#7235,#7233,#3808,.F.);
#9976=EDGE_CURVE('',#7230,#7235,#3809,.F.);
#9977=EDGE_CURVE('',#7231,#7234,#3810,.T.);
#9978=EDGE_CURVE('',#7236,#7237,#4537,.T.);
#9979=EDGE_CURVE('',#7233,#7236,#3811,.F.);
#9980=EDGE_CURVE('',#7234,#7238,#3812,.T.);
#9981=EDGE_CURVE('',#7238,#7237,#3813,.T.);
#9982=EDGE_CURVE('',#7239,#7240,#4538,.T.);
#9983=EDGE_CURVE('',#7241,#7239,#3814,.T.);
#9984=EDGE_CURVE('',#7236,#7241,#3815,.F.);
#9985=EDGE_CURVE('',#7237,#7242,#3816,.T.);
#9986=EDGE_CURVE('',#7242,#7240,#3817,.T.);
#9987=EDGE_CURVE('',#7243,#7244,#3818,.T.);
#9988=EDGE_CURVE('',#7244,#7245,#1977,.F.);
#9989=EDGE_CURVE('',#7245,#7246,#3819,.T.);
#9990=EDGE_CURVE('',#7246,#7247,#3820,.T.);
#9991=EDGE_CURVE('',#7247,#7248,#3821,.T.);
#9992=EDGE_CURVE('',#7248,#7249,#3822,.T.);
#9993=EDGE_CURVE('',#7249,#7250,#3823,.T.);
#9994=EDGE_CURVE('',#7250,#7251,#3824,.T.);
#9995=EDGE_CURVE('',#7251,#7252,#3825,.T.);
#9996=EDGE_CURVE('',#7252,#7253,#3826,.T.);
#9997=EDGE_CURVE('',#7253,#7254,#3827,.T.);
#9998=EDGE_CURVE('',#7254,#7255,#3828,.T.);
#9999=EDGE_CURVE('',#7255,#7256,#3829,.T.);
#10000=EDGE_CURVE('',#7256,#7257,#3830,.T.);
#10001=EDGE_CURVE('',#7257,#7258,#3831,.T.);
#10002=EDGE_CURVE('',#7258,#7259,#3832,.T.);
#10003=EDGE_CURVE('',#7259,#7260,#3833,.T.);
#10004=EDGE_CURVE('',#7260,#7261,#3834,.T.);
#10005=EDGE_CURVE('',#7261,#7262,#3835,.T.);
#10006=EDGE_CURVE('',#7262,#7263,#3836,.T.);
#10007=EDGE_CURVE('',#7263,#7264,#3837,.T.);
#10008=EDGE_CURVE('',#7264,#7265,#3838,.T.);
#10009=EDGE_CURVE('',#7265,#7266,#3839,.T.);
#10010=EDGE_CURVE('',#7266,#7267,#3840,.T.);
#10011=EDGE_CURVE('',#7267,#7268,#3841,.T.);
#10012=EDGE_CURVE('',#7268,#7269,#3842,.T.);
#10013=EDGE_CURVE('',#7269,#7270,#3843,.T.);
#10014=EDGE_CURVE('',#7270,#7271,#3844,.T.);
#10015=EDGE_CURVE('',#7271,#7272,#3845,.T.);
#10016=EDGE_CURVE('',#7272,#7273,#3846,.T.);
#10017=EDGE_CURVE('',#7273,#7149,#1978,.T.);
#10018=EDGE_CURVE('',#7147,#7274,#1979,.T.);
#10019=EDGE_CURVE('',#7274,#7275,#3847,.T.);
#10020=EDGE_CURVE('',#7275,#7276,#3848,.T.);
#10021=EDGE_CURVE('',#7276,#7277,#3849,.T.);
#10022=EDGE_CURVE('',#7277,#7278,#3850,.T.);
#10023=EDGE_CURVE('',#7278,#7279,#3851,.T.);
#10024=EDGE_CURVE('',#7279,#7280,#3852,.T.);
#10025=EDGE_CURVE('',#7280,#7281,#3853,.T.);
#10026=EDGE_CURVE('',#7281,#7282,#3854,.T.);
#10027=EDGE_CURVE('',#7282,#7283,#3855,.T.);
#10028=EDGE_CURVE('',#7283,#7284,#3856,.T.);
#10029=EDGE_CURVE('',#7284,#7285,#3857,.T.);
#10030=EDGE_CURVE('',#7285,#7286,#3858,.T.);
#10031=EDGE_CURVE('',#7286,#7287,#3859,.T.);
#10032=EDGE_CURVE('',#7287,#7288,#3860,.T.);
#10033=EDGE_CURVE('',#7288,#7289,#3861,.T.);
#10034=EDGE_CURVE('',#7289,#7290,#3862,.T.);
#10035=EDGE_CURVE('',#7290,#7291,#3863,.T.);
#10036=EDGE_CURVE('',#7291,#7292,#3864,.T.);
#10037=EDGE_CURVE('',#7292,#7293,#3865,.T.);
#10038=EDGE_CURVE('',#7293,#7294,#3866,.T.);
#10039=EDGE_CURVE('',#7294,#7295,#3867,.T.);
#10040=EDGE_CURVE('',#7295,#7296,#3868,.T.);
#10041=EDGE_CURVE('',#7296,#7297,#3869,.T.);
#10042=EDGE_CURVE('',#7297,#7298,#3870,.T.);
#10043=EDGE_CURVE('',#7298,#7299,#3871,.T.);
#10044=EDGE_CURVE('',#7299,#7300,#3872,.T.);
#10045=EDGE_CURVE('',#7300,#7243,#3873,.T.);
#10046=EDGE_CURVE('',#7240,#7301,#3874,.T.);
#10047=EDGE_CURVE('',#7301,#7153,#3875,.T.);
#10048=EDGE_CURVE('',#7239,#7150,#3876,.T.);
#10049=EDGE_CURVE('',#7274,#7148,#3877,.T.);
#10050=EDGE_CURVE('',#7244,#7157,#3878,.T.);
#10051=EDGE_CURVE('',#7156,#7245,#3879,.T.);
#10052=EDGE_CURVE('',#7302,#7303,#4539,.T.);
#10053=EDGE_CURVE('',#7302,#7304,#4540,.T.);
#10054=EDGE_CURVE('',#7304,#7305,#4541,.T.);
#10055=EDGE_CURVE('',#7303,#7305,#4542,.T.);
#10056=EDGE_CURVE('',#7306,#7302,#4543,.T.);
#10057=EDGE_CURVE('',#7306,#7307,#4544,.T.);
#10058=EDGE_CURVE('',#7307,#7304,#4545,.T.);
#10059=EDGE_CURVE('',#7308,#7306,#4546,.T.);
#10060=EDGE_CURVE('',#7308,#7309,#4547,.T.);
#10061=EDGE_CURVE('',#7309,#7307,#4548,.T.);
#10062=EDGE_CURVE('',#7310,#7308,#4549,.T.);
#10063=EDGE_CURVE('',#7310,#7311,#4550,.T.);
#10064=EDGE_CURVE('',#7311,#7309,#4551,.T.);
#10065=EDGE_CURVE('',#7312,#7310,#4552,.T.);
#10066=EDGE_CURVE('',#7312,#7313,#4553,.T.);
#10067=EDGE_CURVE('',#7313,#7311,#4554,.T.);
#10068=EDGE_CURVE('',#7303,#7312,#4555,.T.);
#10069=EDGE_CURVE('',#7305,#7313,#4556,.T.);
#10070=EDGE_CURVE('',#7314,#7314,#1980,.T.);
#10071=EDGE_CURVE('',#7314,#7315,#4557,.T.);
#10072=EDGE_CURVE('',#7315,#7315,#1981,.T.);
#15103=ORIENTED_EDGE('',*,*,#9863,.F.);
#15104=ORIENTED_EDGE('',*,*,#9864,.F.);
#15105=ORIENTED_EDGE('',*,*,#9865,.F.);
#15106=ORIENTED_EDGE('',*,*,#9866,.F.);
#15107=ORIENTED_EDGE('',*,*,#9867,.T.);
#15108=ORIENTED_EDGE('',*,*,#9868,.F.);
#15109=ORIENTED_EDGE('',*,*,#9867,.F.);
#15110=ORIENTED_EDGE('',*,*,#9869,.F.);
#15111=ORIENTED_EDGE('',*,*,#9870,.F.);
#15112=ORIENTED_EDGE('',*,*,#9871,.F.);
#15113=ORIENTED_EDGE('',*,*,#9872,.F.);
#15114=ORIENTED_EDGE('',*,*,#9873,.F.);
#15115=ORIENTED_EDGE('',*,*,#9874,.T.);
#15116=ORIENTED_EDGE('',*,*,#9875,.F.);
#15117=ORIENTED_EDGE('',*,*,#9876,.F.);
#15118=ORIENTED_EDGE('',*,*,#9877,.F.);
#15119=ORIENTED_EDGE('',*,*,#9871,.T.);
#15120=ORIENTED_EDGE('',*,*,#9878,.T.);
#15121=ORIENTED_EDGE('',*,*,#9879,.T.);
#15122=ORIENTED_EDGE('',*,*,#9880,.F.);
#15123=ORIENTED_EDGE('',*,*,#9881,.F.);
#15124=ORIENTED_EDGE('',*,*,#9875,.T.);
#15125=ORIENTED_EDGE('',*,*,#9882,.T.);
#15126=ORIENTED_EDGE('',*,*,#9883,.F.);
#15127=ORIENTED_EDGE('',*,*,#9884,.F.);
#15128=ORIENTED_EDGE('',*,*,#9885,.F.);
#15129=ORIENTED_EDGE('',*,*,#9880,.T.);
#15130=ORIENTED_EDGE('',*,*,#9886,.T.);
#15131=ORIENTED_EDGE('',*,*,#9887,.T.);
#15132=ORIENTED_EDGE('',*,*,#9888,.F.);
#15133=ORIENTED_EDGE('',*,*,#9889,.F.);
#15134=ORIENTED_EDGE('',*,*,#9883,.T.);
#15135=ORIENTED_EDGE('',*,*,#9890,.T.);
#15136=ORIENTED_EDGE('',*,*,#9891,.F.);
#15137=ORIENTED_EDGE('',*,*,#9892,.F.);
#15138=ORIENTED_EDGE('',*,*,#9893,.F.);
#15139=ORIENTED_EDGE('',*,*,#9888,.T.);
#15140=ORIENTED_EDGE('',*,*,#9894,.T.);
#15141=ORIENTED_EDGE('',*,*,#9895,.T.);
#15142=ORIENTED_EDGE('',*,*,#9896,.F.);
#15143=ORIENTED_EDGE('',*,*,#9897,.F.);
#15144=ORIENTED_EDGE('',*,*,#9891,.T.);
#15145=ORIENTED_EDGE('',*,*,#9898,.T.);
#15146=ORIENTED_EDGE('',*,*,#9899,.F.);
#15147=ORIENTED_EDGE('',*,*,#9900,.F.);
#15148=ORIENTED_EDGE('',*,*,#9901,.F.);
#15149=ORIENTED_EDGE('',*,*,#9896,.T.);
#15150=ORIENTED_EDGE('',*,*,#9902,.T.);
#15151=ORIENTED_EDGE('',*,*,#9903,.T.);
#15152=ORIENTED_EDGE('',*,*,#9904,.F.);
#15153=ORIENTED_EDGE('',*,*,#9905,.F.);
#15154=ORIENTED_EDGE('',*,*,#9899,.T.);
#15155=ORIENTED_EDGE('',*,*,#9906,.T.);
#15156=ORIENTED_EDGE('',*,*,#9907,.T.);
#15157=ORIENTED_EDGE('',*,*,#9908,.F.);
#15158=ORIENTED_EDGE('',*,*,#9909,.F.);
#15159=ORIENTED_EDGE('',*,*,#9910,.F.);
#15160=ORIENTED_EDGE('',*,*,#9904,.T.);
#15161=ORIENTED_EDGE('',*,*,#9911,.T.);
#15162=ORIENTED_EDGE('',*,*,#9912,.F.);
#15163=ORIENTED_EDGE('',*,*,#9913,.F.);
#15164=ORIENTED_EDGE('',*,*,#9914,.F.);
#15165=ORIENTED_EDGE('',*,*,#9908,.T.);
#15166=ORIENTED_EDGE('',*,*,#9915,.T.);
#15167=ORIENTED_EDGE('',*,*,#9916,.T.);
#15168=ORIENTED_EDGE('',*,*,#9917,.F.);
#15169=ORIENTED_EDGE('',*,*,#9918,.F.);
#15170=ORIENTED_EDGE('',*,*,#9912,.T.);
#15171=ORIENTED_EDGE('',*,*,#9919,.T.);
#15172=ORIENTED_EDGE('',*,*,#9920,.F.);
#15173=ORIENTED_EDGE('',*,*,#9921,.F.);
#15174=ORIENTED_EDGE('',*,*,#9922,.F.);
#15175=ORIENTED_EDGE('',*,*,#9917,.T.);
#15176=ORIENTED_EDGE('',*,*,#9923,.T.);
#15177=ORIENTED_EDGE('',*,*,#9924,.T.);
#15178=ORIENTED_EDGE('',*,*,#9925,.F.);
#15179=ORIENTED_EDGE('',*,*,#9926,.F.);
#15180=ORIENTED_EDGE('',*,*,#9927,.F.);
#15181=ORIENTED_EDGE('',*,*,#9920,.T.);
#15182=ORIENTED_EDGE('',*,*,#9928,.T.);
#15183=ORIENTED_EDGE('',*,*,#9929,.F.);
#15184=ORIENTED_EDGE('',*,*,#9930,.F.);
#15185=ORIENTED_EDGE('',*,*,#9925,.T.);
#15186=ORIENTED_EDGE('',*,*,#9931,.T.);
#15187=ORIENTED_EDGE('',*,*,#9932,.T.);
#15188=ORIENTED_EDGE('',*,*,#9933,.F.);
#15189=ORIENTED_EDGE('',*,*,#9934,.F.);
#15190=ORIENTED_EDGE('',*,*,#9935,.F.);
#15191=ORIENTED_EDGE('',*,*,#9929,.T.);
#15192=ORIENTED_EDGE('',*,*,#9936,.T.);
#15193=ORIENTED_EDGE('',*,*,#9937,.F.);
#15194=ORIENTED_EDGE('',*,*,#9938,.F.);
#15195=ORIENTED_EDGE('',*,*,#9933,.T.);
#15196=ORIENTED_EDGE('',*,*,#9939,.T.);
#15197=ORIENTED_EDGE('',*,*,#9940,.T.);
#15198=ORIENTED_EDGE('',*,*,#9941,.F.);
#15199=ORIENTED_EDGE('',*,*,#9942,.F.);
#15200=ORIENTED_EDGE('',*,*,#9943,.F.);
#15201=ORIENTED_EDGE('',*,*,#9937,.T.);
#15202=ORIENTED_EDGE('',*,*,#9944,.T.);
#15203=ORIENTED_EDGE('',*,*,#9945,.T.);
#15204=ORIENTED_EDGE('',*,*,#9946,.F.);
#15205=ORIENTED_EDGE('',*,*,#9947,.F.);
#15206=ORIENTED_EDGE('',*,*,#9941,.T.);
#15207=ORIENTED_EDGE('',*,*,#9948,.T.);
#15208=ORIENTED_EDGE('',*,*,#9949,.T.);
#15209=ORIENTED_EDGE('',*,*,#9950,.F.);
#15210=ORIENTED_EDGE('',*,*,#9951,.F.);
#15211=ORIENTED_EDGE('',*,*,#9952,.F.);
#15212=ORIENTED_EDGE('',*,*,#9946,.T.);
#15213=ORIENTED_EDGE('',*,*,#9953,.T.);
#15214=ORIENTED_EDGE('',*,*,#9954,.F.);
#15215=ORIENTED_EDGE('',*,*,#9955,.F.);
#15216=ORIENTED_EDGE('',*,*,#9950,.T.);
#15217=ORIENTED_EDGE('',*,*,#9956,.T.);
#15218=ORIENTED_EDGE('',*,*,#9957,.T.);
#15219=ORIENTED_EDGE('',*,*,#9958,.F.);
#15220=ORIENTED_EDGE('',*,*,#9959,.F.);
#15221=ORIENTED_EDGE('',*,*,#9960,.F.);
#15222=ORIENTED_EDGE('',*,*,#9954,.T.);
#15223=ORIENTED_EDGE('',*,*,#9961,.T.);
#15224=ORIENTED_EDGE('',*,*,#9962,.F.);
#15225=ORIENTED_EDGE('',*,*,#9963,.F.);
#15226=ORIENTED_EDGE('',*,*,#9958,.T.);
#15227=ORIENTED_EDGE('',*,*,#9964,.T.);
#15228=ORIENTED_EDGE('',*,*,#9965,.T.);
#15229=ORIENTED_EDGE('',*,*,#9966,.F.);
#15230=ORIENTED_EDGE('',*,*,#9967,.F.);
#15231=ORIENTED_EDGE('',*,*,#9968,.F.);
#15232=ORIENTED_EDGE('',*,*,#9962,.T.);
#15233=ORIENTED_EDGE('',*,*,#9969,.T.);
#15234=ORIENTED_EDGE('',*,*,#9970,.F.);
#15235=ORIENTED_EDGE('',*,*,#9971,.F.);
#15236=ORIENTED_EDGE('',*,*,#9966,.T.);
#15237=ORIENTED_EDGE('',*,*,#9972,.T.);
#15238=ORIENTED_EDGE('',*,*,#9973,.T.);
#15239=ORIENTED_EDGE('',*,*,#9974,.F.);
#15240=ORIENTED_EDGE('',*,*,#9975,.F.);
#15241=ORIENTED_EDGE('',*,*,#9976,.F.);
#15242=ORIENTED_EDGE('',*,*,#9970,.T.);
#15243=ORIENTED_EDGE('',*,*,#9977,.T.);
#15244=ORIENTED_EDGE('',*,*,#9978,.F.);
#15245=ORIENTED_EDGE('',*,*,#9979,.F.);
#15246=ORIENTED_EDGE('',*,*,#9974,.T.);
#15247=ORIENTED_EDGE('',*,*,#9980,.T.);
#15248=ORIENTED_EDGE('',*,*,#9981,.T.);
#15249=ORIENTED_EDGE('',*,*,#9982,.F.);
#15250=ORIENTED_EDGE('',*,*,#9983,.F.);
#15251=ORIENTED_EDGE('',*,*,#9984,.F.);
#15252=ORIENTED_EDGE('',*,*,#9978,.T.);
#15253=ORIENTED_EDGE('',*,*,#9985,.T.);
#15254=ORIENTED_EDGE('',*,*,#9986,.T.);
#15255=ORIENTED_EDGE('',*,*,#9987,.T.);
#15256=ORIENTED_EDGE('',*,*,#9988,.T.);
#15257=ORIENTED_EDGE('',*,*,#9989,.T.);
#15258=ORIENTED_EDGE('',*,*,#9990,.T.);
#15259=ORIENTED_EDGE('',*,*,#9991,.T.);
#15260=ORIENTED_EDGE('',*,*,#9992,.T.);
#15261=ORIENTED_EDGE('',*,*,#9993,.T.);
#15262=ORIENTED_EDGE('',*,*,#9994,.T.);
#15263=ORIENTED_EDGE('',*,*,#9995,.T.);
#15264=ORIENTED_EDGE('',*,*,#9996,.T.);
#15265=ORIENTED_EDGE('',*,*,#9997,.T.);
#15266=ORIENTED_EDGE('',*,*,#9998,.T.);
#15267=ORIENTED_EDGE('',*,*,#9999,.T.);
#15268=ORIENTED_EDGE('',*,*,#10000,.T.);
#15269=ORIENTED_EDGE('',*,*,#10001,.T.);
#15270=ORIENTED_EDGE('',*,*,#10002,.T.);
#15271=ORIENTED_EDGE('',*,*,#10003,.T.);
#15272=ORIENTED_EDGE('',*,*,#10004,.T.);
#15273=ORIENTED_EDGE('',*,*,#10005,.T.);
#15274=ORIENTED_EDGE('',*,*,#10006,.T.);
#15275=ORIENTED_EDGE('',*,*,#10007,.T.);
#15276=ORIENTED_EDGE('',*,*,#10008,.T.);
#15277=ORIENTED_EDGE('',*,*,#10009,.T.);
#15278=ORIENTED_EDGE('',*,*,#10010,.T.);
#15279=ORIENTED_EDGE('',*,*,#10011,.T.);
#15280=ORIENTED_EDGE('',*,*,#10012,.T.);
#15281=ORIENTED_EDGE('',*,*,#10013,.T.);
#15282=ORIENTED_EDGE('',*,*,#10014,.T.);
#15283=ORIENTED_EDGE('',*,*,#10015,.T.);
#15284=ORIENTED_EDGE('',*,*,#10016,.T.);
#15285=ORIENTED_EDGE('',*,*,#10017,.T.);
#15286=ORIENTED_EDGE('',*,*,#9864,.T.);
#15287=ORIENTED_EDGE('',*,*,#10018,.T.);
#15288=ORIENTED_EDGE('',*,*,#10019,.T.);
#15289=ORIENTED_EDGE('',*,*,#10020,.T.);
#15290=ORIENTED_EDGE('',*,*,#10021,.T.);
#15291=ORIENTED_EDGE('',*,*,#10022,.T.);
#15292=ORIENTED_EDGE('',*,*,#10023,.T.);
#15293=ORIENTED_EDGE('',*,*,#10024,.T.);
#15294=ORIENTED_EDGE('',*,*,#10025,.T.);
#15295=ORIENTED_EDGE('',*,*,#10026,.T.);
#15296=ORIENTED_EDGE('',*,*,#10027,.T.);
#15297=ORIENTED_EDGE('',*,*,#10028,.T.);
#15298=ORIENTED_EDGE('',*,*,#10029,.T.);
#15299=ORIENTED_EDGE('',*,*,#10030,.T.);
#15300=ORIENTED_EDGE('',*,*,#10031,.T.);
#15301=ORIENTED_EDGE('',*,*,#10032,.T.);
#15302=ORIENTED_EDGE('',*,*,#10033,.T.);
#15303=ORIENTED_EDGE('',*,*,#10034,.T.);
#15304=ORIENTED_EDGE('',*,*,#10035,.T.);
#15305=ORIENTED_EDGE('',*,*,#10036,.T.);
#15306=ORIENTED_EDGE('',*,*,#10037,.T.);
#15307=ORIENTED_EDGE('',*,*,#10038,.T.);
#15308=ORIENTED_EDGE('',*,*,#10039,.T.);
#15309=ORIENTED_EDGE('',*,*,#10040,.T.);
#15310=ORIENTED_EDGE('',*,*,#10041,.T.);
#15311=ORIENTED_EDGE('',*,*,#10042,.T.);
#15312=ORIENTED_EDGE('',*,*,#10043,.T.);
#15313=ORIENTED_EDGE('',*,*,#10044,.T.);
#15314=ORIENTED_EDGE('',*,*,#10045,.T.);
#15315=ORIENTED_EDGE('',*,*,#9982,.T.);
#15316=ORIENTED_EDGE('',*,*,#10046,.T.);
#15317=ORIENTED_EDGE('',*,*,#10047,.T.);
#15318=ORIENTED_EDGE('',*,*,#9869,.T.);
#15319=ORIENTED_EDGE('',*,*,#9866,.T.);
#15320=ORIENTED_EDGE('',*,*,#10048,.F.);
#15321=ORIENTED_EDGE('',*,*,#9863,.T.);
#15322=ORIENTED_EDGE('',*,*,#10049,.F.);
#15323=ORIENTED_EDGE('',*,*,#10018,.F.);
#15324=ORIENTED_EDGE('',*,*,#10049,.T.);
#15325=ORIENTED_EDGE('',*,*,#9870,.T.);
#15326=ORIENTED_EDGE('',*,*,#10047,.F.);
#15327=ORIENTED_EDGE('',*,*,#10046,.F.);
#15328=ORIENTED_EDGE('',*,*,#9986,.F.);
#15329=ORIENTED_EDGE('',*,*,#9985,.F.);
#15330=ORIENTED_EDGE('',*,*,#9981,.F.);
#15331=ORIENTED_EDGE('',*,*,#9980,.F.);
#15332=ORIENTED_EDGE('',*,*,#9977,.F.);
#15333=ORIENTED_EDGE('',*,*,#9973,.F.);
#15334=ORIENTED_EDGE('',*,*,#9972,.F.);
#15335=ORIENTED_EDGE('',*,*,#9969,.F.);
#15336=ORIENTED_EDGE('',*,*,#9965,.F.);
#15337=ORIENTED_EDGE('',*,*,#9964,.F.);
#15338=ORIENTED_EDGE('',*,*,#9961,.F.);
#15339=ORIENTED_EDGE('',*,*,#9957,.F.);
#15340=ORIENTED_EDGE('',*,*,#9956,.F.);
#15341=ORIENTED_EDGE('',*,*,#9953,.F.);
#15342=ORIENTED_EDGE('',*,*,#9949,.F.);
#15343=ORIENTED_EDGE('',*,*,#9948,.F.);
#15344=ORIENTED_EDGE('',*,*,#9945,.F.);
#15345=ORIENTED_EDGE('',*,*,#9944,.F.);
#15346=ORIENTED_EDGE('',*,*,#9940,.F.);
#15347=ORIENTED_EDGE('',*,*,#9939,.F.);
#15348=ORIENTED_EDGE('',*,*,#9936,.F.);
#15349=ORIENTED_EDGE('',*,*,#9932,.F.);
#15350=ORIENTED_EDGE('',*,*,#9931,.F.);
#15351=ORIENTED_EDGE('',*,*,#9928,.F.);
#15352=ORIENTED_EDGE('',*,*,#9924,.F.);
#15353=ORIENTED_EDGE('',*,*,#9923,.F.);
#15354=ORIENTED_EDGE('',*,*,#9919,.F.);
#15355=ORIENTED_EDGE('',*,*,#9916,.F.);
#15356=ORIENTED_EDGE('',*,*,#9915,.F.);
#15357=ORIENTED_EDGE('',*,*,#9911,.F.);
#15358=ORIENTED_EDGE('',*,*,#9907,.F.);
#15359=ORIENTED_EDGE('',*,*,#9906,.F.);
#15360=ORIENTED_EDGE('',*,*,#9903,.F.);
#15361=ORIENTED_EDGE('',*,*,#9902,.F.);
#15362=ORIENTED_EDGE('',*,*,#9898,.F.);
#15363=ORIENTED_EDGE('',*,*,#9895,.F.);
#15364=ORIENTED_EDGE('',*,*,#9894,.F.);
#15365=ORIENTED_EDGE('',*,*,#9890,.F.);
#15366=ORIENTED_EDGE('',*,*,#9887,.F.);
#15367=ORIENTED_EDGE('',*,*,#9886,.F.);
#15368=ORIENTED_EDGE('',*,*,#9882,.F.);
#15369=ORIENTED_EDGE('',*,*,#9879,.F.);
#15370=ORIENTED_EDGE('',*,*,#9878,.F.);
#15371=ORIENTED_EDGE('',*,*,#9874,.F.);
#15372=ORIENTED_EDGE('',*,*,#10050,.F.);
#15373=ORIENTED_EDGE('',*,*,#9987,.F.);
#15374=ORIENTED_EDGE('',*,*,#10045,.F.);
#15375=ORIENTED_EDGE('',*,*,#10044,.F.);
#15376=ORIENTED_EDGE('',*,*,#10043,.F.);
#15377=ORIENTED_EDGE('',*,*,#10042,.F.);
#15378=ORIENTED_EDGE('',*,*,#10041,.F.);
#15379=ORIENTED_EDGE('',*,*,#10040,.F.);
#15380=ORIENTED_EDGE('',*,*,#10039,.F.);
#15381=ORIENTED_EDGE('',*,*,#10038,.F.);
#15382=ORIENTED_EDGE('',*,*,#10037,.F.);
#15383=ORIENTED_EDGE('',*,*,#10036,.F.);
#15384=ORIENTED_EDGE('',*,*,#10035,.F.);
#15385=ORIENTED_EDGE('',*,*,#10034,.F.);
#15386=ORIENTED_EDGE('',*,*,#10033,.F.);
#15387=ORIENTED_EDGE('',*,*,#10032,.F.);
#15388=ORIENTED_EDGE('',*,*,#10031,.F.);
#15389=ORIENTED_EDGE('',*,*,#10030,.F.);
#15390=ORIENTED_EDGE('',*,*,#10029,.F.);
#15391=ORIENTED_EDGE('',*,*,#10028,.F.);
#15392=ORIENTED_EDGE('',*,*,#10027,.F.);
#15393=ORIENTED_EDGE('',*,*,#10026,.F.);
#15394=ORIENTED_EDGE('',*,*,#10025,.F.);
#15395=ORIENTED_EDGE('',*,*,#10024,.F.);
#15396=ORIENTED_EDGE('',*,*,#10023,.F.);
#15397=ORIENTED_EDGE('',*,*,#10022,.F.);
#15398=ORIENTED_EDGE('',*,*,#10021,.F.);
#15399=ORIENTED_EDGE('',*,*,#10020,.F.);
#15400=ORIENTED_EDGE('',*,*,#10019,.F.);
#15401=ORIENTED_EDGE('',*,*,#9865,.T.);
#15402=ORIENTED_EDGE('',*,*,#10017,.F.);
#15403=ORIENTED_EDGE('',*,*,#10016,.F.);
#15404=ORIENTED_EDGE('',*,*,#10015,.F.);
#15405=ORIENTED_EDGE('',*,*,#10014,.F.);
#15406=ORIENTED_EDGE('',*,*,#10013,.F.);
#15407=ORIENTED_EDGE('',*,*,#10012,.F.);
#15408=ORIENTED_EDGE('',*,*,#10011,.F.);
#15409=ORIENTED_EDGE('',*,*,#10010,.F.);
#15410=ORIENTED_EDGE('',*,*,#10009,.F.);
#15411=ORIENTED_EDGE('',*,*,#10008,.F.);
#15412=ORIENTED_EDGE('',*,*,#10007,.F.);
#15413=ORIENTED_EDGE('',*,*,#10006,.F.);
#15414=ORIENTED_EDGE('',*,*,#10005,.F.);
#15415=ORIENTED_EDGE('',*,*,#10004,.F.);
#15416=ORIENTED_EDGE('',*,*,#10003,.F.);
#15417=ORIENTED_EDGE('',*,*,#10002,.F.);
#15418=ORIENTED_EDGE('',*,*,#10001,.F.);
#15419=ORIENTED_EDGE('',*,*,#10000,.F.);
#15420=ORIENTED_EDGE('',*,*,#9999,.F.);
#15421=ORIENTED_EDGE('',*,*,#9998,.F.);
#15422=ORIENTED_EDGE('',*,*,#9997,.F.);
#15423=ORIENTED_EDGE('',*,*,#9996,.F.);
#15424=ORIENTED_EDGE('',*,*,#9995,.F.);
#15425=ORIENTED_EDGE('',*,*,#9994,.F.);
#15426=ORIENTED_EDGE('',*,*,#9993,.F.);
#15427=ORIENTED_EDGE('',*,*,#9992,.F.);
#15428=ORIENTED_EDGE('',*,*,#9991,.F.);
#15429=ORIENTED_EDGE('',*,*,#9990,.F.);
#15430=ORIENTED_EDGE('',*,*,#9989,.F.);
#15431=ORIENTED_EDGE('',*,*,#10051,.F.);
#15432=ORIENTED_EDGE('',*,*,#9872,.T.);
#15433=ORIENTED_EDGE('',*,*,#9877,.T.);
#15434=ORIENTED_EDGE('',*,*,#9876,.T.);
#15435=ORIENTED_EDGE('',*,*,#9881,.T.);
#15436=ORIENTED_EDGE('',*,*,#9885,.T.);
#15437=ORIENTED_EDGE('',*,*,#9884,.T.);
#15438=ORIENTED_EDGE('',*,*,#9889,.T.);
#15439=ORIENTED_EDGE('',*,*,#9893,.T.);
#15440=ORIENTED_EDGE('',*,*,#9892,.T.);
#15441=ORIENTED_EDGE('',*,*,#9897,.T.);
#15442=ORIENTED_EDGE('',*,*,#9901,.T.);
#15443=ORIENTED_EDGE('',*,*,#9900,.T.);
#15444=ORIENTED_EDGE('',*,*,#9905,.T.);
#15445=ORIENTED_EDGE('',*,*,#9910,.T.);
#15446=ORIENTED_EDGE('',*,*,#9909,.T.);
#15447=ORIENTED_EDGE('',*,*,#9914,.T.);
#15448=ORIENTED_EDGE('',*,*,#9913,.T.);
#15449=ORIENTED_EDGE('',*,*,#9918,.T.);
#15450=ORIENTED_EDGE('',*,*,#9922,.T.);
#15451=ORIENTED_EDGE('',*,*,#9921,.T.);
#15452=ORIENTED_EDGE('',*,*,#9927,.T.);
#15453=ORIENTED_EDGE('',*,*,#9926,.T.);
#15454=ORIENTED_EDGE('',*,*,#9930,.T.);
#15455=ORIENTED_EDGE('',*,*,#9935,.T.);
#15456=ORIENTED_EDGE('',*,*,#9934,.T.);
#15457=ORIENTED_EDGE('',*,*,#9938,.T.);
#15458=ORIENTED_EDGE('',*,*,#9943,.T.);
#15459=ORIENTED_EDGE('',*,*,#9942,.T.);
#15460=ORIENTED_EDGE('',*,*,#9947,.T.);
#15461=ORIENTED_EDGE('',*,*,#9952,.T.);
#15462=ORIENTED_EDGE('',*,*,#9951,.T.);
#15463=ORIENTED_EDGE('',*,*,#9955,.T.);
#15464=ORIENTED_EDGE('',*,*,#9960,.T.);
#15465=ORIENTED_EDGE('',*,*,#9959,.T.);
#15466=ORIENTED_EDGE('',*,*,#9963,.T.);
#15467=ORIENTED_EDGE('',*,*,#9968,.T.);
#15468=ORIENTED_EDGE('',*,*,#9967,.T.);
#15469=ORIENTED_EDGE('',*,*,#9971,.T.);
#15470=ORIENTED_EDGE('',*,*,#9976,.T.);
#15471=ORIENTED_EDGE('',*,*,#9975,.T.);
#15472=ORIENTED_EDGE('',*,*,#9979,.T.);
#15473=ORIENTED_EDGE('',*,*,#9984,.T.);
#15474=ORIENTED_EDGE('',*,*,#9983,.T.);
#15475=ORIENTED_EDGE('',*,*,#10048,.T.);
#15476=ORIENTED_EDGE('',*,*,#10052,.F.);
#15477=ORIENTED_EDGE('',*,*,#10053,.T.);
#15478=ORIENTED_EDGE('',*,*,#10054,.T.);
#15479=ORIENTED_EDGE('',*,*,#10055,.F.);
#15480=ORIENTED_EDGE('',*,*,#10056,.F.);
#15481=ORIENTED_EDGE('',*,*,#10057,.T.);
#15482=ORIENTED_EDGE('',*,*,#10058,.T.);
#15483=ORIENTED_EDGE('',*,*,#10053,.F.);
#15484=ORIENTED_EDGE('',*,*,#10059,.F.);
#15485=ORIENTED_EDGE('',*,*,#10060,.T.);
#15486=ORIENTED_EDGE('',*,*,#10061,.T.);
#15487=ORIENTED_EDGE('',*,*,#10057,.F.);
#15488=ORIENTED_EDGE('',*,*,#10062,.F.);
#15489=ORIENTED_EDGE('',*,*,#10063,.T.);
#15490=ORIENTED_EDGE('',*,*,#10064,.T.);
#15491=ORIENTED_EDGE('',*,*,#10060,.F.);
#15492=ORIENTED_EDGE('',*,*,#10065,.F.);
#15493=ORIENTED_EDGE('',*,*,#10066,.T.);
#15494=ORIENTED_EDGE('',*,*,#10067,.T.);
#15495=ORIENTED_EDGE('',*,*,#10063,.F.);
#15496=ORIENTED_EDGE('',*,*,#10068,.F.);
#15497=ORIENTED_EDGE('',*,*,#10055,.T.);
#15498=ORIENTED_EDGE('',*,*,#10069,.T.);
#15499=ORIENTED_EDGE('',*,*,#10066,.F.);
#15500=ORIENTED_EDGE('',*,*,#10069,.F.);
#15501=ORIENTED_EDGE('',*,*,#10054,.F.);
#15502=ORIENTED_EDGE('',*,*,#10058,.F.);
#15503=ORIENTED_EDGE('',*,*,#10061,.F.);
#15504=ORIENTED_EDGE('',*,*,#10064,.F.);
#15505=ORIENTED_EDGE('',*,*,#10067,.F.);
#15506=ORIENTED_EDGE('',*,*,#10070,.T.);
#15507=ORIENTED_EDGE('',*,*,#10050,.T.);
#15508=ORIENTED_EDGE('',*,*,#9873,.T.);
#15509=ORIENTED_EDGE('',*,*,#10051,.T.);
#15510=ORIENTED_EDGE('',*,*,#9988,.F.);
#15511=ORIENTED_EDGE('',*,*,#10070,.F.);
#15512=ORIENTED_EDGE('',*,*,#10071,.T.);
#15513=ORIENTED_EDGE('',*,*,#10072,.T.);
#15514=ORIENTED_EDGE('',*,*,#10071,.F.);
#15515=ORIENTED_EDGE('',*,*,#10072,.F.);
#15516=ORIENTED_EDGE('',*,*,#10052,.T.);
#15517=ORIENTED_EDGE('',*,*,#10068,.T.);
#15518=ORIENTED_EDGE('',*,*,#10065,.T.);
#15519=ORIENTED_EDGE('',*,*,#10062,.T.);
#15520=ORIENTED_EDGE('',*,*,#10059,.T.);
#15521=ORIENTED_EDGE('',*,*,#10056,.T.);
#15522=ORIENTED_EDGE('',*,*,#9868,.T.);
#16157=CYLINDRICAL_SURFACE('',#17794,1.5555);
#16158=CYLINDRICAL_SURFACE('',#17796,1.5555);
#16159=CYLINDRICAL_SURFACE('',#17797,1.5555);
#16160=CYLINDRICAL_SURFACE('',#17798,1.5555);
#16161=CYLINDRICAL_SURFACE('',#17799,1.5555);
#16162=CYLINDRICAL_SURFACE('',#17800,1.5555);
#16163=CYLINDRICAL_SURFACE('',#17801,1.5555);
#16164=CYLINDRICAL_SURFACE('',#17802,1.5555);
#16165=CYLINDRICAL_SURFACE('',#17803,1.5555);
#16166=CYLINDRICAL_SURFACE('',#17804,1.5555);
#16167=CYLINDRICAL_SURFACE('',#17805,1.5555);
#16168=CYLINDRICAL_SURFACE('',#17806,1.5555);
#16169=CYLINDRICAL_SURFACE('',#17807,1.5555);
#16170=CYLINDRICAL_SURFACE('',#17808,1.5555);
#16171=CYLINDRICAL_SURFACE('',#17809,1.5555);
#16172=CYLINDRICAL_SURFACE('',#17810,1.5555);
#16173=CYLINDRICAL_SURFACE('',#17811,1.5555);
#16174=CYLINDRICAL_SURFACE('',#17812,1.5555);
#16175=CYLINDRICAL_SURFACE('',#17813,1.5555);
#16176=CYLINDRICAL_SURFACE('',#17814,1.5555);
#16177=CYLINDRICAL_SURFACE('',#17815,1.5555);
#16178=CYLINDRICAL_SURFACE('',#17816,1.5555);
#16179=CYLINDRICAL_SURFACE('',#17817,1.5555);
#16180=CYLINDRICAL_SURFACE('',#17818,1.5555);
#16181=CYLINDRICAL_SURFACE('',#17819,1.5555);
#16182=CYLINDRICAL_SURFACE('',#17820,1.5555);
#16183=CYLINDRICAL_SURFACE('',#17821,1.5555);
#16184=CYLINDRICAL_SURFACE('',#17822,1.5555);
#16185=CYLINDRICAL_SURFACE('',#17823,1.954);
#16186=CYLINDRICAL_SURFACE('',#17827,1.5555);
#16187=CYLINDRICAL_SURFACE('',#17838,3.5);
#16780=ADVANCED_FACE('',(#1012),#116,.T.);
#16781=ADVANCED_FACE('',(#1013),#16157,.T.);
#16782=ADVANCED_FACE('',(#1014),#16158,.T.);
#16783=ADVANCED_FACE('',(#1015),#16159,.T.);
#16784=ADVANCED_FACE('',(#1016),#16160,.T.);
#16785=ADVANCED_FACE('',(#1017),#16161,.T.);
#16786=ADVANCED_FACE('',(#1018),#16162,.T.);
#16787=ADVANCED_FACE('',(#1019),#16163,.T.);
#16788=ADVANCED_FACE('',(#1020),#16164,.T.);
#16789=ADVANCED_FACE('',(#1021),#16165,.T.);
#16790=ADVANCED_FACE('',(#1022),#16166,.T.);
#16791=ADVANCED_FACE('',(#1023),#16167,.T.);
#16792=ADVANCED_FACE('',(#1024),#16168,.T.);
#16793=ADVANCED_FACE('',(#1025),#16169,.T.);
#16794=ADVANCED_FACE('',(#1026),#16170,.T.);
#16795=ADVANCED_FACE('',(#1027),#16171,.T.);
#16796=ADVANCED_FACE('',(#1028),#16172,.T.);
#16797=ADVANCED_FACE('',(#1029),#16173,.T.);
#16798=ADVANCED_FACE('',(#1030),#16174,.T.);
#16799=ADVANCED_FACE('',(#1031),#16175,.T.);
#16800=ADVANCED_FACE('',(#1032),#16176,.T.);
#16801=ADVANCED_FACE('',(#1033),#16177,.T.);
#16802=ADVANCED_FACE('',(#1034),#16178,.T.);
#16803=ADVANCED_FACE('',(#1035),#16179,.T.);
#16804=ADVANCED_FACE('',(#1036),#16180,.T.);
#16805=ADVANCED_FACE('',(#1037),#16181,.T.);
#16806=ADVANCED_FACE('',(#1038),#16182,.T.);
#16807=ADVANCED_FACE('',(#1039),#16183,.T.);
#16808=ADVANCED_FACE('',(#1040),#16184,.T.);
#16809=ADVANCED_FACE('',(#1041),#16185,.T.);
#16810=ADVANCED_FACE('',(#1042),#16186,.T.);
#16811=ADVANCED_FACE('',(#1043),#117,.T.);
#16812=ADVANCED_FACE('',(#1044),#299,.F.);
#16813=ADVANCED_FACE('',(#1045),#300,.F.);
#16814=ADVANCED_FACE('',(#1046),#403,.F.);
#16815=ADVANCED_FACE('',(#1047),#404,.F.);
#16816=ADVANCED_FACE('',(#1048),#405,.F.);
#16817=ADVANCED_FACE('',(#1049),#406,.F.);
#16818=ADVANCED_FACE('',(#1050),#407,.F.);
#16819=ADVANCED_FACE('',(#1051),#408,.F.);
#16820=ADVANCED_FACE('',(#1052),#409,.F.);
#16821=ADVANCED_FACE('',(#1053,#269),#410,.T.);
#16822=ADVANCED_FACE('',(#1054),#16187,.T.);
#16823=ADVANCED_FACE('',(#1055,#270),#411,.F.);
#16824=ADVANCED_FACE('',(#1056),#412,.T.);
#16856=CLOSED_SHELL('',(#16780,#16781,#16782,#16783,#16784,#16785,#16786,
#16787,#16788,#16789,#16790,#16791,#16792,#16793,#16794,#16795,#16796,#16797,
#16798,#16799,#16800,#16801,#16802,#16803,#16804,#16805,#16806,#16807,#16808,
#16809,#16810,#16811,#16812,#16813,#16814,#16815,#16816,#16817,#16818,#16819,
#16820,#16821,#16822,#16823,#16824));
#17788=AXIS2_PLACEMENT_3D('',#260673,#19941,#19942);
#17789=AXIS2_PLACEMENT_3D('',#260674,#19943,#19944);
#17790=AXIS2_PLACEMENT_3D('',#260679,#19946,#19947);
#17791=AXIS2_PLACEMENT_3D('',#260920,#19948,#19949);
#17792=AXIS2_PLACEMENT_3D('',#260923,#19951,#19952);
#17793=AXIS2_PLACEMENT_3D('',#260925,#19953,#19954);
#17794=AXIS2_PLACEMENT_3D('',#260960,#19955,#19956);
#17795=AXIS2_PLACEMENT_3D('',#261039,#19958,#19959);
#17796=AXIS2_PLACEMENT_3D('',#261080,#19960,#19961);
#17797=AXIS2_PLACEMENT_3D('',#261482,#19963,#19964);
#17798=AXIS2_PLACEMENT_3D('',#261916,#19966,#19967);
#17799=AXIS2_PLACEMENT_3D('',#262374,#19969,#19970);
#17800=AXIS2_PLACEMENT_3D('',#262800,#19972,#19973);
#17801=AXIS2_PLACEMENT_3D('',#263312,#19975,#19976);
#17802=AXIS2_PLACEMENT_3D('',#263734,#19978,#19979);
#17803=AXIS2_PLACEMENT_3D('',#264070,#19981,#19982);
#17804=AXIS2_PLACEMENT_3D('',#264422,#19984,#19985);
#17805=AXIS2_PLACEMENT_3D('',#264741,#19987,#19988);
#17806=AXIS2_PLACEMENT_3D('',#265104,#19990,#19991);
#17807=AXIS2_PLACEMENT_3D('',#265532,#19993,#19994);
#17808=AXIS2_PLACEMENT_3D('',#265874,#19996,#19997);
#17809=AXIS2_PLACEMENT_3D('',#266237,#19999,#20000);
#17810=AXIS2_PLACEMENT_3D('',#266672,#20002,#20003);
#17811=AXIS2_PLACEMENT_3D('',#267129,#20005,#20006);
#17812=AXIS2_PLACEMENT_3D('',#267558,#20008,#20009);
#17813=AXIS2_PLACEMENT_3D('',#267885,#20011,#20012);
#17814=AXIS2_PLACEMENT_3D('',#268249,#20014,#20015);
#17815=AXIS2_PLACEMENT_3D('',#268692,#20017,#20018);
#17816=AXIS2_PLACEMENT_3D('',#269143,#20020,#20021);
#17817=AXIS2_PLACEMENT_3D('',#269592,#20023,#20024);
#17818=AXIS2_PLACEMENT_3D('',#270055,#20026,#20027);
#17819=AXIS2_PLACEMENT_3D('',#270492,#20029,#20030);
#17820=AXIS2_PLACEMENT_3D('',#270941,#20032,#20033);
#17821=AXIS2_PLACEMENT_3D('',#271392,#20035,#20036);
#17822=AXIS2_PLACEMENT_3D('',#271811,#20038,#20039);
#17823=AXIS2_PLACEMENT_3D('',#272283,#20041,#20042);
#17824=AXIS2_PLACEMENT_3D('',#272348,#20043,#20044);
#17825=AXIS2_PLACEMENT_3D('',#274664,#20045,#20046);
#17826=AXIS2_PLACEMENT_3D('',#274666,#20047,#20048);
#17827=AXIS2_PLACEMENT_3D('',#277291,#20049,#20050);
#17828=AXIS2_PLACEMENT_3D('',#277455,#20051,#20052);
#17829=AXIS2_PLACEMENT_3D('',#279083,#20053,#20054);
#17830=AXIS2_PLACEMENT_3D('',#279092,#20059,#20060);
#17831=AXIS2_PLACEMENT_3D('',#279098,#20064,#20065);
#17832=AXIS2_PLACEMENT_3D('',#279104,#20069,#20070);
#17833=AXIS2_PLACEMENT_3D('',#279110,#20074,#20075);
#17834=AXIS2_PLACEMENT_3D('',#279116,#20079,#20080);
#17835=AXIS2_PLACEMENT_3D('',#279119,#20083,#20084);
#17836=AXIS2_PLACEMENT_3D('',#279120,#20085,#20086);
#17837=AXIS2_PLACEMENT_3D('',#279122,#20087,#20088);
#17838=AXIS2_PLACEMENT_3D('',#279123,#20089,#20090);
#17839=AXIS2_PLACEMENT_3D('',#279126,#20092,#20093);
#17840=AXIS2_PLACEMENT_3D('',#279127,#20094,#20095);
#17841=AXIS2_PLACEMENT_3D('',#279128,#20096,#20097);
#19941=DIRECTION('axis',(0.,0.,1.));
#19942=DIRECTION('refdir',(1.,0.,0.));
#19943=DIRECTION('center_axis',(0.,0.,-1.));
#19944=DIRECTION('ref_axis',(1.,0.,0.));
#19945=DIRECTION('',(0.707106781186547,-8.65956056235493E-17,0.707106781186548));
#19946=DIRECTION('center_axis',(0.,0.,-1.));
#19947=DIRECTION('ref_axis',(1.,0.,0.));
#19948=DIRECTION('center_axis',(0.,0.,-1.));
#19949=DIRECTION('ref_axis',(1.,-1.0233845463423E-13,0.));
#19950=DIRECTION('',(0.707106781186547,-8.65956056235493E-17,0.707106781186548));
#19951=DIRECTION('center_axis',(0.,0.,1.));
#19952=DIRECTION('ref_axis',(1.,0.,0.));
#19953=DIRECTION('center_axis',(0.,0.,-1.));
#19954=DIRECTION('ref_axis',(1.,-1.0233845463423E-13,0.));
#19955=DIRECTION('center_axis',(0.,0.,1.));
#19956=DIRECTION('ref_axis',(-0.922260805897494,-0.386568242235837,0.));
#19957=DIRECTION('',(0.,0.,-1.));
#19958=DIRECTION('center_axis',(0.,0.,-1.));
#19959=DIRECTION('ref_axis',(1.,-1.0233845463423E-13,0.));
#19960=DIRECTION('center_axis',(0.,0.,1.));
#19961=DIRECTION('ref_axis',(-0.922260805897494,-0.386568242235837,0.));
#19962=DIRECTION('',(0.,0.,-1.));
#19963=DIRECTION('center_axis',(0.,0.,1.));
#19964=DIRECTION('ref_axis',(-0.922260805897494,-0.386568242235837,0.));
#19965=DIRECTION('',(0.,0.,-1.));
#19966=DIRECTION('center_axis',(0.,0.,1.));
#19967=DIRECTION('ref_axis',(-0.922260805897494,-0.386568242235837,0.));
#19968=DIRECTION('',(0.,0.,-1.));
#19969=DIRECTION('center_axis',(0.,0.,1.));
#19970=DIRECTION('ref_axis',(-0.922260805897494,-0.386568242235837,0.));
#19971=DIRECTION('',(0.,0.,-1.));
#19972=DIRECTION('center_axis',(0.,0.,1.));
#19973=DIRECTION('ref_axis',(-0.922260805897494,-0.386568242235837,0.));
#19974=DIRECTION('',(0.,0.,-1.));
#19975=DIRECTION('center_axis',(0.,0.,1.));
#19976=DIRECTION('ref_axis',(-0.922260805897494,-0.386568242235837,0.));
#19977=DIRECTION('',(0.,0.,-1.));
#19978=DIRECTION('center_axis',(0.,0.,1.));
#19979=DIRECTION('ref_axis',(-0.922260805897494,-0.386568242235837,0.));
#19980=DIRECTION('',(0.,0.,-1.));
#19981=DIRECTION('center_axis',(0.,0.,1.));
#19982=DIRECTION('ref_axis',(-0.922260805897494,-0.386568242235837,0.));
#19983=DIRECTION('',(0.,0.,-1.));
#19984=DIRECTION('center_axis',(0.,0.,1.));
#19985=DIRECTION('ref_axis',(-0.922260805897494,-0.386568242235837,0.));
#19986=DIRECTION('',(0.,0.,-1.));
#19987=DIRECTION('center_axis',(0.,0.,1.));
#19988=DIRECTION('ref_axis',(-0.922260805897494,-0.386568242235837,0.));
#19989=DIRECTION('',(0.,0.,-1.));
#19990=DIRECTION('center_axis',(0.,0.,1.));
#19991=DIRECTION('ref_axis',(-0.922260805897494,-0.386568242235837,0.));
#19992=DIRECTION('',(0.,0.,-1.));
#19993=DIRECTION('center_axis',(0.,0.,1.));
#19994=DIRECTION('ref_axis',(-0.922260805897494,-0.386568242235837,0.));
#19995=DIRECTION('',(0.,0.,-1.));
#19996=DIRECTION('center_axis',(0.,0.,1.));
#19997=DIRECTION('ref_axis',(-0.922260805897494,-0.386568242235837,0.));
#19998=DIRECTION('',(0.,0.,-1.));
#19999=DIRECTION('center_axis',(0.,0.,1.));
#20000=DIRECTION('ref_axis',(-0.922260805897494,-0.386568242235837,0.));
#20001=DIRECTION('',(0.,0.,-1.));
#20002=DIRECTION('center_axis',(0.,0.,1.));
#20003=DIRECTION('ref_axis',(-0.922260805897494,-0.386568242235837,0.));
#20004=DIRECTION('',(0.,0.,-1.));
#20005=DIRECTION('center_axis',(0.,0.,1.));
#20006=DIRECTION('ref_axis',(-0.922260805897494,-0.386568242235837,0.));
#20007=DIRECTION('',(0.,0.,-1.));
#20008=DIRECTION('center_axis',(0.,0.,1.));
#20009=DIRECTION('ref_axis',(-0.922260805897494,-0.386568242235837,0.));
#20010=DIRECTION('',(0.,0.,-1.));
#20011=DIRECTION('center_axis',(0.,0.,1.));
#20012=DIRECTION('ref_axis',(-0.922260805897494,-0.386568242235837,0.));
#20013=DIRECTION('',(0.,0.,-1.));
#20014=DIRECTION('center_axis',(0.,0.,1.));
#20015=DIRECTION('ref_axis',(-0.922260805897494,-0.386568242235837,0.));
#20016=DIRECTION('',(0.,0.,-1.));
#20017=DIRECTION('center_axis',(0.,0.,1.));
#20018=DIRECTION('ref_axis',(-0.922260805897494,-0.386568242235837,0.));
#20019=DIRECTION('',(0.,0.,-1.));
#20020=DIRECTION('center_axis',(0.,0.,1.));
#20021=DIRECTION('ref_axis',(-0.922260805897494,-0.386568242235837,0.));
#20022=DIRECTION('',(0.,0.,-1.));
#20023=DIRECTION('center_axis',(0.,0.,1.));
#20024=DIRECTION('ref_axis',(-0.922260805897494,-0.386568242235837,0.));
#20025=DIRECTION('',(0.,0.,-1.));
#20026=DIRECTION('center_axis',(0.,0.,1.));
#20027=DIRECTION('ref_axis',(-0.922260805897494,-0.386568242235837,0.));
#20028=DIRECTION('',(0.,0.,-1.));
#20029=DIRECTION('center_axis',(0.,0.,1.));
#20030=DIRECTION('ref_axis',(-0.922260805897494,-0.386568242235837,0.));
#20031=DIRECTION('',(0.,0.,-1.));
#20032=DIRECTION('center_axis',(0.,0.,1.));
#20033=DIRECTION('ref_axis',(-0.922260805897494,-0.386568242235837,0.));
#20034=DIRECTION('',(0.,0.,-1.));
#20035=DIRECTION('center_axis',(0.,0.,1.));
#20036=DIRECTION('ref_axis',(-0.922260805897494,-0.386568242235837,0.));
#20037=DIRECTION('',(0.,0.,-1.));
#20038=DIRECTION('center_axis',(0.,0.,1.));
#20039=DIRECTION('ref_axis',(-0.922260805897494,-0.386568242235837,0.));
#20040=DIRECTION('',(0.,0.,-1.));
#20041=DIRECTION('center_axis',(0.,0.,1.));
#20042=DIRECTION('ref_axis',(1.,0.,0.));
#20043=DIRECTION('center_axis',(0.,0.,-1.));
#20044=DIRECTION('ref_axis',(1.,0.,0.));
#20045=DIRECTION('center_axis',(-0.00364373213059557,0.0569212501344872,
0.998372022093612));
#20046=DIRECTION('ref_axis',(-0.980992657570465,-0.193900834380623,0.00747477219278287));
#20047=DIRECTION('center_axis',(0.,0.,-1.));
#20048=DIRECTION('ref_axis',(1.,0.,0.));
#20049=DIRECTION('center_axis',(0.,0.,1.));
#20050=DIRECTION('ref_axis',(-0.922260805897494,-0.386568242235837,0.));
#20051=DIRECTION('center_axis',(0.,0.,-1.));
#20052=DIRECTION('ref_axis',(1.,0.,0.));
#20053=DIRECTION('center_axis',(-1.60246890531964E-16,-1.,0.));
#20054=DIRECTION('ref_axis',(1.,-1.60246890531964E-16,0.));
#20055=DIRECTION('',(1.,-1.60246890531964E-16,0.));
#20056=DIRECTION('',(0.,0.,1.));
#20057=DIRECTION('',(1.,-1.60246890531964E-16,0.));
#20058=DIRECTION('',(0.,0.,1.));
#20059=DIRECTION('center_axis',(-0.866025403784439,-0.5,0.));
#20060=DIRECTION('ref_axis',(0.5,-0.866025403784439,0.));
#20061=DIRECTION('',(0.5,-0.866025403784439,0.));
#20062=DIRECTION('',(0.,0.,1.));
#20063=DIRECTION('',(0.5,-0.866025403784439,0.));
#20064=DIRECTION('center_axis',(-0.866025403784439,0.5,0.));
#20065=DIRECTION('ref_axis',(-0.5,-0.866025403784439,0.));
#20066=DIRECTION('',(-0.5,-0.866025403784439,0.));
#20067=DIRECTION('',(0.,0.,1.));
#20068=DIRECTION('',(-0.5,-0.866025403784439,0.));
#20069=DIRECTION('center_axis',(1.60246890531964E-16,1.,0.));
#20070=DIRECTION('ref_axis',(-1.,1.60246890531964E-16,0.));
#20071=DIRECTION('',(-1.,1.60246890531964E-16,0.));
#20072=DIRECTION('',(0.,0.,1.));
#20073=DIRECTION('',(-1.,1.60246890531964E-16,0.));
#20074=DIRECTION('center_axis',(0.866025403784439,0.5,0.));
#20075=DIRECTION('ref_axis',(-0.5,0.866025403784439,0.));
#20076=DIRECTION('',(-0.5,0.866025403784439,0.));
#20077=DIRECTION('',(0.,0.,1.));
#20078=DIRECTION('',(-0.5,0.866025403784439,0.));
#20079=DIRECTION('center_axis',(0.866025403784439,-0.5,0.));
#20080=DIRECTION('ref_axis',(0.5,0.866025403784439,0.));
#20081=DIRECTION('',(0.5,0.866025403784439,0.));
#20082=DIRECTION('',(0.5,0.866025403784439,0.));
#20083=DIRECTION('center_axis',(0.,0.,1.));
#20084=DIRECTION('ref_axis',(1.,0.,0.));
#20085=DIRECTION('center_axis',(0.,0.,1.));
#20086=DIRECTION('ref_axis',(1.,0.,0.));
#20087=DIRECTION('center_axis',(0.,0.,1.));
#20088=DIRECTION('ref_axis',(1.,0.,0.));
#20089=DIRECTION('center_axis',(0.,0.,1.));
#20090=DIRECTION('ref_axis',(1.,0.,0.));
#20091=DIRECTION('',(0.,0.,-1.));
#20092=DIRECTION('center_axis',(0.,0.,1.));
#20093=DIRECTION('ref_axis',(1.,0.,0.));
#20094=DIRECTION('center_axis',(0.,0.,1.));
#20095=DIRECTION('ref_axis',(1.,0.,0.));
#20096=DIRECTION('center_axis',(0.,0.,1.));
#20097=DIRECTION('ref_axis',(1.,0.,0.));
#260673=CARTESIAN_POINT('',(0.,0.,0.));
#260674=CARTESIAN_POINT('Origin',(0.,0.,19.5));
#260675=CARTESIAN_POINT('',(-1.954,2.39295984553393E-16,19.046));
#260676=CARTESIAN_POINT('',(-1.76525906551972,0.00187739100781801,19.2347399361577));
#260677=CARTESIAN_POINT('',(-1.5,1.83697019872103E-16,19.5));
#260678=CARTESIAN_POINT('',(-1.91639047105473,-0.379636187408775,19.0463684911581));
#260679=CARTESIAN_POINT('Origin',(0.,0.,19.046));
#260680=CARTESIAN_POINT('',(-1.40413430885517,0.669318379170786,19.4445));
#260681=CARTESIAN_POINT('Ctrl Pts',(-1.40413430885493,0.669318379171303,
19.4445));
#260682=CARTESIAN_POINT('Ctrl Pts',(-1.38217147333919,0.721346567327714,
19.4419383467048));
#260683=CARTESIAN_POINT('Ctrl Pts',(-1.35733080539739,0.771980546116191,
19.4395076811575));
#260684=CARTESIAN_POINT('Ctrl Pts',(-1.32979496729222,0.821092768858667,
19.4371346858709));
#260685=CARTESIAN_POINT('Ctrl Pts',(-1.32816523228221,0.823999522904693,
19.4369942378671));
#260686=CARTESIAN_POINT('Ctrl Pts',(-1.32652604274719,0.826900953081449,
19.4368539918808));
#260687=CARTESIAN_POINT('Ctrl Pts',(-1.3248774314762,0.829797035270251,
19.4367139327115));
#260688=CARTESIAN_POINT('Ctrl Pts',(-1.29585145900179,0.880786376041457,
19.4342480065928));
#260689=CARTESIAN_POINT('Ctrl Pts',(-1.26390831139223,0.930115053534165,
19.4318396036553));
#260690=CARTESIAN_POINT('Ctrl Pts',(-1.22923552529087,0.977600394819607,
19.4294196905002));
#260691=CARTESIAN_POINT('Ctrl Pts',(-1.21062500144787,1.00308802288625,
19.4281208086814));
#260692=CARTESIAN_POINT('Ctrl Pts',(-1.19122789539636,1.02804396868633,
19.4268188866479));
#260693=CARTESIAN_POINT('Ctrl Pts',(-1.17107268993615,1.05243613342277,
19.42550545887));
#260694=CARTESIAN_POINT('Ctrl Pts',(-1.16329639586048,1.06184713379721,
19.4249987113368));
#260695=CARTESIAN_POINT('Ctrl Pts',(-1.15540926681824,1.07117162708454,
19.4244904029669));
#260696=CARTESIAN_POINT('Ctrl Pts',(-1.14741992670891,1.08040030926175,
19.4239805469279));
#260697=CARTESIAN_POINT('Ctrl Pts',(-1.10629043233698,1.1279099942262,19.4213557843321));
#260698=CARTESIAN_POINT('Ctrl Pts',(-1.06240353091898,1.17294124127734,
19.4186842000219));
#260699=CARTESIAN_POINT('Ctrl Pts',(-1.01605870517633,1.21527920720128,
19.4159296594468));
#260700=CARTESIAN_POINT('Ctrl Pts',(-0.969336626725759,1.25796180949049,
19.4131526965651));
#260701=CARTESIAN_POINT('Ctrl Pts',(-0.92011662502485,1.2979067796946,19.4102913361356));
#260702=CARTESIAN_POINT('Ctrl Pts',(-0.86869609931806,1.33488789533211,
19.4073422821979));
#260703=CARTESIAN_POINT('Ctrl Pts',(-0.855531220514918,1.34435594138338,
19.4065872541787));
#260704=CARTESIAN_POINT('Ctrl Pts',(-0.842222042258913,1.3536296915388,
19.4058266516426));
#260705=CARTESIAN_POINT('Ctrl Pts',(-0.828773418670833,1.36270530490215,
19.4050607762351));
#260706=CARTESIAN_POINT('Ctrl Pts',(-0.819370051506753,1.36905103419823,
19.4045252710504));
#260707=CARTESIAN_POINT('Ctrl Pts',(-0.809900124623619,1.37529870996624,
19.4039872839289));
#260708=CARTESIAN_POINT('Ctrl Pts',(-0.80037510752539,1.38144110703308,
19.4034475126238));
#260709=CARTESIAN_POINT('Ctrl Pts',(-0.746541592567262,1.41615672181531,
19.4003968318404));
#260710=CARTESIAN_POINT('Ctrl Pts',(-0.690868048765296,1.44756602956533,
19.3972819523276));
#260711=CARTESIAN_POINT('Ctrl Pts',(-0.633694512627027,1.47552898535086,
19.3941499067646));
#260712=CARTESIAN_POINT('Ctrl Pts',(-0.576880995505364,1.50331585974414,
19.3910375835424));
#260713=CARTESIAN_POINT('Ctrl Pts',(-0.518586721712705,1.52770092579246,
19.3879087670402));
#260714=CARTESIAN_POINT('Ctrl Pts',(-0.459095719137883,1.54854391708141,
19.3848352584146));
#260715=CARTESIAN_POINT('Ctrl Pts',(-0.418361167794408,1.56281548525247,
19.3827307721983));
#260716=CARTESIAN_POINT('Ctrl Pts',(-0.377064475020572,1.5754263952828,
19.3806527559442));
#260717=CARTESIAN_POINT('Ctrl Pts',(-0.33528224562359,1.58632535588287,
19.3786294936236));
#260718=CARTESIAN_POINT('Ctrl Pts',(-0.310052201624067,1.59290665275136,
19.3774077541878));
#260719=CARTESIAN_POINT('Ctrl Pts',(-0.284644882455448,1.59886359739272,
19.3762060545926));
#260720=CARTESIAN_POINT('Ctrl Pts',(-0.259075039617233,1.60418323521717,
19.3750311608205));
#260721=CARTESIAN_POINT('Ctrl Pts',(-0.248347253480673,1.60641508064797,
19.3745382360418));
#260722=CARTESIAN_POINT('Ctrl Pts',(-0.237590851597929,1.60853462095232,
19.3740500399615));
#260723=CARTESIAN_POINT('Ctrl Pts',(-0.226821249685733,1.61053844914986,
19.3735677156736));
#260724=CARTESIAN_POINT('Ctrl Pts',(-0.220750353363047,1.61166802045017,
19.3732958262603));
#260725=CARTESIAN_POINT('Ctrl Pts',(-0.214674129358586,1.61276106547953,
19.3730257502935));
#260726=CARTESIAN_POINT('Ctrl Pts',(-0.208592782959594,1.61381751167616,
19.3727575748846));
#260727=CARTESIAN_POINT('Ctrl Pts',(-0.148510985974506,1.62425486908805,
19.3701080858705));
#260728=CARTESIAN_POINT('Ctrl Pts',(-0.0879270076695866,1.63112400483074,
19.3676429980082));
#260729=CARTESIAN_POINT('Ctrl Pts',(-0.0270872981813738,1.63451635283288,
19.3652592164502));
#260730=CARTESIAN_POINT('Ctrl Pts',(0.0364354134851305,1.63805830176435,
19.3627703112623));
#260731=CARTESIAN_POINT('Ctrl Pts',(0.100237386887145,1.63780868765977,
19.3603694038062));
#260732=CARTESIAN_POINT('Ctrl Pts',(0.164005042467492,1.63382964290583,
19.3579595145087));
#260733=CARTESIAN_POINT('Ctrl Pts',(0.217259240175272,1.63050662853301,
19.3559469468529));
#260734=CARTESIAN_POINT('Ctrl Pts',(0.270488824308838,1.62458148559031,
19.3539283785832));
#260735=CARTESIAN_POINT('Ctrl Pts',(0.323492638541354,1.61607910238884,
19.3518619134404));
#260736=CARTESIAN_POINT('Ctrl Pts',(0.338458321045913,1.61367844558012,
19.3512784448414));
#260737=CARTESIAN_POINT('Ctrl Pts',(0.353405905971691,1.61107229073373,
19.3506912477853));
#260738=CARTESIAN_POINT('Ctrl Pts',(0.368330639185305,1.60826113415862,
19.350099598337));
#260739=CARTESIAN_POINT('Ctrl Pts',(0.38115751140529,1.60584512137882,19.3495911127403));
#260740=CARTESIAN_POINT('Ctrl Pts',(0.393969332268037,1.60327717012554,
19.3490792625555));
#260741=CARTESIAN_POINT('Ctrl Pts',(0.40674169518067,1.60056250715929,19.3485645196005));
#260742=CARTESIAN_POINT('Ctrl Pts',(0.470470193764487,1.58701752756673,
19.345996177634));
#260743=CARTESIAN_POINT('Ctrl Pts',(0.533333555532824,1.56979974871069,
19.3433481324206));
#260744=CARTESIAN_POINT('Ctrl Pts',(0.594966184623827,1.54907512073393,
19.3405969475373));
#260745=CARTESIAN_POINT('Ctrl Pts',(0.657354927780642,1.52809624134921,
19.3378120108958));
#260746=CARTESIAN_POINT('Ctrl Pts',(0.718482121739586,1.50352435200272,
19.334921431136));
#260747=CARTESIAN_POINT('Ctrl Pts',(0.777981910400626,1.47552326328266,
19.3319398232081));
#260748=CARTESIAN_POINT('Ctrl Pts',(0.826996029950355,1.45245681647784,
19.3294836651156));
#260749=CARTESIAN_POINT('Ctrl Pts',(0.874906109707342,1.42706346889986,
19.326966518312));
#260750=CARTESIAN_POINT('Ctrl Pts',(0.921515992464549,1.39942577748952,
19.3244152569714));
#260751=CARTESIAN_POINT('Ctrl Pts',(0.93827791171197,1.38948666749393,19.3234977683609));
#260752=CARTESIAN_POINT('Ctrl Pts',(0.954871747356156,1.3792571955302,19.3225760189452));
#260753=CARTESIAN_POINT('Ctrl Pts',(0.971288581433974,1.36874078310259,
19.3216517525399));
#260754=CARTESIAN_POINT('Ctrl Pts',(0.981502107975134,1.36219812957159,
19.3210767318376));
#260755=CARTESIAN_POINT('Ctrl Pts',(0.991648267010085,1.35554352163652,
19.3205006731938));
#260756=CARTESIAN_POINT('Ctrl Pts',(1.00170977076115,1.34878827155813,19.3199249224124));
#260757=CARTESIAN_POINT('Ctrl Pts',(1.05661188860429,1.31192722722129,19.3167832511439));
#260758=CARTESIAN_POINT('Ctrl Pts',(1.10909531883384,1.27200922248131,19.3136431788134));
#260759=CARTESIAN_POINT('Ctrl Pts',(1.158902268571,1.22924104627546,19.3105953658323));
#260760=CARTESIAN_POINT('Ctrl Pts',(1.20768794730778,1.18734981391638,19.3076100470016));
#260761=CARTESIAN_POINT('Ctrl Pts',(1.25390751013265,1.1427249055078,19.3047139013212));
#260762=CARTESIAN_POINT('Ctrl Pts',(1.29733348672402,1.09549346531942,19.3020070352522));
#260763=CARTESIAN_POINT('Ctrl Pts',(1.341120979724,1.0478688286627,19.2992776348253));
#260764=CARTESIAN_POINT('Ctrl Pts',(1.38207405852357,0.997587493706231,
19.2967407157757));
#260765=CARTESIAN_POINT('Ctrl Pts',(1.42008879260803,0.944878769103382,
19.294289571119));
#260766=CARTESIAN_POINT('Ctrl Pts',(1.42805622448871,0.933831653217788,
19.2937758406261));
#260767=CARTESIAN_POINT('Ctrl Pts',(1.43589434238337,0.922677932764241,
19.2932659152927));
#260768=CARTESIAN_POINT('Ctrl Pts',(1.44360182306019,0.911419779173646,
19.2927588812907));
#260769=CARTESIAN_POINT('Ctrl Pts',(1.44978667999563,0.902385689795456,
19.2923520125751));
#260770=CARTESIAN_POINT('Ctrl Pts',(1.45588680057798,0.893285102373578,
19.2919470432148));
#260771=CARTESIAN_POINT('Ctrl Pts',(1.46189466840029,0.884130048077785,
19.2915439825939));
#260772=CARTESIAN_POINT('Ctrl Pts',(1.49777716073971,0.829450721675864,
19.2891366693722));
#260773=CARTESIAN_POINT('Ctrl Pts',(1.53044031248222,0.772728762214373,
19.2867908163825));
#260774=CARTESIAN_POINT('Ctrl Pts',(1.55980601960137,0.714292045780207,
19.2844219792007));
#260775=CARTESIAN_POINT('Ctrl Pts',(1.58977562232586,0.654653598493742,
19.282004427702));
#260776=CARTESIAN_POINT('Ctrl Pts',(1.61630980664176,0.593228839250153,
19.2795625518933));
#260777=CARTESIAN_POINT('Ctrl Pts',(1.63929945845588,0.530374359964422,
19.2770375290792));
#260778=CARTESIAN_POINT('Ctrl Pts',(1.65454361180149,0.488696333327143,
19.2753632177286));
#260779=CARTESIAN_POINT('Ctrl Pts',(1.6682288198921,0.446389900533039,19.2736530086561));
#260780=CARTESIAN_POINT('Ctrl Pts',(1.68031976473865,0.403561252742655,
19.2718980942992));
#260781=CARTESIAN_POINT('Ctrl Pts',(1.68822718816244,0.375551510158863,
19.270750388221));
#260782=CARTESIAN_POINT('Ctrl Pts',(1.69545268369885,0.347318448255623,
19.2695836996519));
#260783=CARTESIAN_POINT('Ctrl Pts',(1.70198595783479,0.318892072697381,
19.268397171781));
#260784=CARTESIAN_POINT('Ctrl Pts',(1.70459399601933,0.307544458719828,
19.2679235180004));
#260785=CARTESIAN_POINT('Ctrl Pts',(1.70709220223344,0.296163727665992,
19.2674466196719));
#260786=CARTESIAN_POINT('Ctrl Pts',(1.70947835319687,0.284759283781793,
19.2669667949665));
#260787=CARTESIAN_POINT('Ctrl Pts',(1.72348149822569,0.217832218340065,
19.2641509400432));
#260788=CARTESIAN_POINT('Ctrl Pts',(1.73358381185407,0.15029952798712,19.2612401281409));
#260789=CARTESIAN_POINT('Ctrl Pts',(1.73978101893805,0.0825694731200911,
19.2582607222238));
#260790=CARTESIAN_POINT('Ctrl Pts',(1.74595863583035,0.0150535219194175,
19.255290734603));
#260791=CARTESIAN_POINT('Ctrl Pts',(1.74825682320413,-0.052658285708984,
19.2522529617856));
#260792=CARTESIAN_POINT('Ctrl Pts',(1.74666231828795,-0.120199700306727,
19.2492066877895));
#260793=CARTESIAN_POINT('Ctrl Pts',(1.74508290680785,-0.18710177412028,
19.2461892495414));
#260794=CARTESIAN_POINT('Ctrl Pts',(1.73968555964442,-0.253836874474994,
19.2431639318862));
#260795=CARTESIAN_POINT('Ctrl Pts',(1.7304302287371,-0.320086946822075,
19.2402146636442));
#260796=CARTESIAN_POINT('Ctrl Pts',(1.72812829181856,-0.33656431418136,
19.2394811372563));
#260797=CARTESIAN_POINT('Ctrl Pts',(1.72558751100087,-0.353011850793722,
19.238752424137));
#260798=CARTESIAN_POINT('Ctrl Pts',(1.72280683630334,-0.369424990628833,
19.2380300175898));
#260799=CARTESIAN_POINT('Ctrl Pts',(1.72042618759322,-0.383476947232057,
19.2374115359614));
#260800=CARTESIAN_POINT('Ctrl Pts',(1.71786899991573,-0.397506569820592,
19.2367975566759));
#260801=CARTESIAN_POINT('Ctrl Pts',(1.71513970148883,-0.411486473048876,
19.2361901142341));
#260802=CARTESIAN_POINT('Ctrl Pts',(1.70823937626494,-0.446831042892538,
19.2346543531164));
#260803=CARTESIAN_POINT('Ctrl Pts',(1.70023434220433,-0.48188991188231,
19.2331589061797));
#260804=CARTESIAN_POINT('Ctrl Pts',(1.69112876633472,-0.516623403070588,
19.2317194100129));
#260805=CARTESIAN_POINT('Ctrl Pts',(1.67534951013464,-0.576813847259032,
19.2292248748907));
#260806=CARTESIAN_POINT('Ctrl Pts',(1.65626626225344,-0.6360319925359,19.2268976068215));
#260807=CARTESIAN_POINT('Ctrl Pts',(1.63403606258769,-0.694112962325006,
19.2246502715508));
#260808=CARTESIAN_POINT('Ctrl Pts',(1.63285826468605,-0.697190201637802,
19.22453120349));
#260809=CARTESIAN_POINT('Ctrl Pts',(1.6316716230637,-0.700264255588732,
19.2244123598069));
#260810=CARTESIAN_POINT('Ctrl Pts',(1.63047615768359,-0.703335101765461,
19.2242937275129));
#260811=CARTESIAN_POINT('Ctrl Pts',(1.60639738687566,-0.765187333127124,
19.2219042649107));
#260812=CARTESIAN_POINT('Ctrl Pts',(1.57874194851366,-0.825734976747993,
19.2196000450605));
#260813=CARTESIAN_POINT('Ctrl Pts',(1.5476754838404,-0.884731553557858,
19.2172915759605));
#260814=CARTESIAN_POINT('Ctrl Pts',(1.53362609556929,-0.91141195710507,
19.2162476020472));
#260815=CARTESIAN_POINT('Ctrl Pts',(1.51887890613618,-0.937774530179484,
19.2152030301504));
#260816=CARTESIAN_POINT('Ctrl Pts',(1.50344875767458,-0.963793647972006,
19.2141510806274));
#260817=CARTESIAN_POINT('Ctrl Pts',(1.49369512739682,-0.980240725959191,
19.2134861274194));
#260818=CARTESIAN_POINT('Ctrl Pts',(1.48366860524787,-0.996550535912571,
19.2128182462234));
#260819=CARTESIAN_POINT('Ctrl Pts',(1.47337295255235,-1.01271628114316,
19.2121459446014));
#260820=CARTESIAN_POINT('Ctrl Pts',(1.46691247836072,-1.0228602111046,19.2117240784598));
#260821=CARTESIAN_POINT('Ctrl Pts',(1.46034546319633,-1.03294810149321,
19.2113004423879));
#260822=CARTESIAN_POINT('Ctrl Pts',(1.45368231464851,-1.04296449077561,
19.2108752975433));
#260823=CARTESIAN_POINT('Ctrl Pts',(1.4155369652389,-1.10030655155332,19.2084414183452));
#260824=CARTESIAN_POINT('Ctrl Pts',(1.37417401990408,-1.15541367197863,
19.2059507779562));
#260825=CARTESIAN_POINT('Ctrl Pts',(1.3298832499431,-1.20801974313988,19.2033639327079));
#260826=CARTESIAN_POINT('Ctrl Pts',(1.28497334126005,-1.26136119225234,
19.2007409260638));
#260827=CARTESIAN_POINT('Ctrl Pts',(1.23705341007497,-1.31213075452912,
19.1980189316072));
#260828=CARTESIAN_POINT('Ctrl Pts',(1.18641672157972,-1.36005143141289,
19.1951940455184));
#260829=CARTESIAN_POINT('Ctrl Pts',(1.1376127125647,-1.40623772866376,19.1924713997404));
#260830=CARTESIAN_POINT('Ctrl Pts',(1.08628548983792,-1.44977771216266,
19.1896534817836));
#260831=CARTESIAN_POINT('Ctrl Pts',(1.03268431088215,-1.49042618895111,
19.1867688755557));
#260832=CARTESIAN_POINT('Ctrl Pts',(1.01557153862312,-1.5034036670497,19.1858479329497));
#260833=CARTESIAN_POINT('Ctrl Pts',(0.998226853649716,-1.51608643285646,
19.1849204260313));
#260834=CARTESIAN_POINT('Ctrl Pts',(0.980657938559474,-1.52846650461766,
19.1839879272984));
#260835=CARTESIAN_POINT('Ctrl Pts',(0.971285926992347,-1.53507056497949,
19.183490492547));
#260836=CARTESIAN_POINT('Ctrl Pts',(0.961858628457918,-1.54158248085602,
19.1829920951222));
#260837=CARTESIAN_POINT('Ctrl Pts',(0.952377750096971,-1.54800136299127,
19.1824930265051));
#260838=CARTESIAN_POINT('Ctrl Pts',(0.894011222757722,-1.58751751807428,
19.1794206421777));
#260839=CARTESIAN_POINT('Ctrl Pts',(0.833616384678822,-1.62350908373234,
19.1763206322423));
#260840=CARTESIAN_POINT('Ctrl Pts',(0.771507211253566,-1.65580953440538,
19.1732738050698));
#260841=CARTESIAN_POINT('Ctrl Pts',(0.710499521310594,-1.68753714839546,
19.1702810122633));
#260842=CARTESIAN_POINT('Ctrl Pts',(0.647837989219365,-1.71570510025019,
19.1673401380913));
#260843=CARTESIAN_POINT('Ctrl Pts',(0.583758119910228,-1.74014799595924,
19.1645467615866));
#260844=CARTESIAN_POINT('Ctrl Pts',(0.556870881118297,-1.75040397776415,
19.1633746902025));
#260845=CARTESIAN_POINT('Ctrl Pts',(0.52973315938917,-1.7600039036222,19.1622287671939));
#260846=CARTESIAN_POINT('Ctrl Pts',(0.502358946186095,-1.7689339647992,
19.1611166750896));
#260847=CARTESIAN_POINT('Ctrl Pts',(0.465569379798908,-1.78093551808863,
19.1596220792086));
#260848=CARTESIAN_POINT('Ctrl Pts',(0.428352078372298,-1.79172753015431,
19.1581885667143));
#260849=CARTESIAN_POINT('Ctrl Pts',(0.390751179581378,-1.80130877931094,
19.1567963208677));
#260850=CARTESIAN_POINT('Ctrl Pts',(0.372997738975067,-1.80583261100927,
19.1561389654655));
#260851=CARTESIAN_POINT('Ctrl Pts',(0.355158831924743,-1.81008642879012,
19.155490820199));
#260852=CARTESIAN_POINT('Ctrl Pts',(0.337239394906132,-1.8140696190854,
19.1548498726756));
#260853=CARTESIAN_POINT('Ctrl Pts',(0.325750913958142,-1.81662331570947,
19.1544389494192));
#260854=CARTESIAN_POINT('Ctrl Pts',(0.314237804738062,-1.81906386364226,
19.1540312889368));
#260855=CARTESIAN_POINT('Ctrl Pts',(0.302705048111772,-1.82139090102721,
19.1536264840241));
#260856=CARTESIAN_POINT('Ctrl Pts',(0.234929258408644,-1.83506645159538,
19.1512475235102));
#260857=CARTESIAN_POINT('Ctrl Pts',(0.166434815429164,-1.84483320125462,
19.1489639169012));
#260858=CARTESIAN_POINT('Ctrl Pts',(0.0975457067868387,-1.85075006770947,
19.1466810911127));
#260859=CARTESIAN_POINT('Ctrl Pts',(0.0272216740891075,-1.85679017939388,
19.1443507152586));
#260860=CARTESIAN_POINT('Ctrl Pts',(-0.0435137040245961,-1.85881719306894,
19.1420207113177));
#260861=CARTESIAN_POINT('Ctrl Pts',(-0.114293132667689,-1.85686692883475,
19.1396189337732));
#260862=CARTESIAN_POINT('Ctrl Pts',(-0.166082490785135,-1.85543991911195,
19.1378615514411));
#260863=CARTESIAN_POINT('Ctrl Pts',(-0.217894900467354,-1.85188299001889,
19.1360663381086));
#260864=CARTESIAN_POINT('Ctrl Pts',(-0.269579462386977,-1.84620588131199,
19.1342161854245));
#260865=CARTESIAN_POINT('Ctrl Pts',(-0.295213725564894,-1.8433901759393,
19.1332985554967));
#260866=CARTESIAN_POINT('Ctrl Pts',(-0.320816455402674,-1.84005288874687,
19.1323675628624));
#260867=CARTESIAN_POINT('Ctrl Pts',(-0.346368798976254,-1.83619504657529,
19.1314220396323));
#260868=CARTESIAN_POINT('Ctrl Pts',(-0.358227790062144,-1.83440459961328,
19.1309832168087));
#260869=CARTESIAN_POINT('Ctrl Pts',(-0.370075924525137,-1.83250202697373,
19.1305412729349));
#260870=CARTESIAN_POINT('Ctrl Pts',(-0.381911299618988,-1.83048742568155,
19.1300961371357));
#260871=CARTESIAN_POINT('Ctrl Pts',(-0.393814699867741,-1.82846124524093,
19.1296484428682));
#260872=CARTESIAN_POINT('Ctrl Pts',(-0.405696656235154,-1.82632317212201,
19.1291978400046));
#260873=CARTESIAN_POINT('Ctrl Pts',(-0.417551343430059,-1.8240746132133,
19.1287444538574));
#260874=CARTESIAN_POINT('Ctrl Pts',(-0.488299309374712,-1.81065536675976,
19.1260386762039));
#260875=CARTESIAN_POINT('Ctrl Pts',(-0.558119265200875,-1.7932942644785,
19.1232290772346));
#260876=CARTESIAN_POINT('Ctrl Pts',(-0.626627057207316,-1.77214222704198,
19.1203325981202));
#260877=CARTESIAN_POINT('Ctrl Pts',(-0.695199571035156,-1.75097020650063,
19.1174333825958));
#260878=CARTESIAN_POINT('Ctrl Pts',(-0.762457421690977,-1.72600098288857,
19.1144474078632));
#260879=CARTESIAN_POINT('Ctrl Pts',(-0.828042384602747,-1.69736752390752,
19.1114262784009));
#260880=CARTESIAN_POINT('Ctrl Pts',(-0.89245263817879,-1.66924692626062,
19.1084592611746));
#260881=CARTESIAN_POINT('Ctrl Pts',(-0.955249947312068,-1.63759322616612,
19.1054587713829));
#260882=CARTESIAN_POINT('Ctrl Pts',(-1.01611693502786,-1.60250014671125,
19.1025015557688));
#260883=CARTESIAN_POINT('Ctrl Pts',(-1.03057405121755,-1.59416484466702,
19.1017991584375));
#260884=CARTESIAN_POINT('Ctrl Pts',(-1.04492234147161,-1.58563532190556,
19.101099311358));
#260885=CARTESIAN_POINT('Ctrl Pts',(-1.0591576702315,-1.57691245590169,
19.1004032364767));
#260886=CARTESIAN_POINT('Ctrl Pts',(-1.06905904189517,-1.5708452733495,
19.0999190821434));
#260887=CARTESIAN_POINT('Ctrl Pts',(-1.07890500175412,-1.56468492224003,
19.0994367911956));
#260888=CARTESIAN_POINT('Ctrl Pts',(-1.08868331635203,-1.55843892477285,
19.0989573267413));
#260889=CARTESIAN_POINT('Ctrl Pts',(-1.1485032800246,-1.5202283172244,19.0960241478228));
#260890=CARTESIAN_POINT('Ctrl Pts',(-1.20589981934606,-1.47875182222852,
19.0931906358257));
#260891=CARTESIAN_POINT('Ctrl Pts',(-1.26063694790006,-1.43414075412667,
19.0905589254817));
#260892=CARTESIAN_POINT('Ctrl Pts',(-1.31217626795552,-1.39213591796416,
19.0880809628026));
#260893=CARTESIAN_POINT('Ctrl Pts',(-1.36136390512813,-1.34734673374201,
19.0857816278819));
#260894=CARTESIAN_POINT('Ctrl Pts',(-1.40810241422692,-1.29998288058792,
19.0835689684277));
#260895=CARTESIAN_POINT('Ctrl Pts',(-1.41071415027776,-1.29733620046965,
19.0834453255778));
#260896=CARTESIAN_POINT('Ctrl Pts',(-1.41331824040473,-1.29468146749932,
19.083321953376));
#260897=CARTESIAN_POINT('Ctrl Pts',(-1.41591466796309,-1.29201871356806,
19.0831988357779));
#260898=CARTESIAN_POINT('Ctrl Pts',(-1.46597636629649,-1.24067817698608,
19.0808250063846));
#260899=CARTESIAN_POINT('Ctrl Pts',(-1.51318808537753,-1.18635991928918,
19.0785452366125));
#260900=CARTESIAN_POINT('Ctrl Pts',(-1.55736793020904,-1.12932494144644,
19.0762615319601));
#260901=CARTESIAN_POINT('Ctrl Pts',(-1.57332878905255,-1.10871990686648,
19.0754364976546));
#260902=CARTESIAN_POINT('Ctrl Pts',(-1.58889343781319,-1.08776040053795,
19.0746111510968));
#260903=CARTESIAN_POINT('Ctrl Pts',(-1.60405173792419,-1.06645922023027,
19.073781620285));
#260904=CARTESIAN_POINT('Ctrl Pts',(-1.61079267917436,-1.05698652184314,
19.07341272546));
#260905=CARTESIAN_POINT('Ctrl Pts',(-1.61744777951959,-1.04745393357941,
19.0730433076787));
#260906=CARTESIAN_POINT('Ctrl Pts',(-1.62401578653282,-1.03786400668304,
19.0726731021241));
#260907=CARTESIAN_POINT('Ctrl Pts',(-1.66505382599379,-0.977944491127087,
19.0703599940341));
#260908=CARTESIAN_POINT('Ctrl Pts',(-1.70270243524567,-0.915773144665256,
19.0680128538593));
#260909=CARTESIAN_POINT('Ctrl Pts',(-1.73682775615862,-0.851717698488315,
19.0655766511745));
#260910=CARTESIAN_POINT('Ctrl Pts',(-1.77141300513714,-0.786798937427839,
19.0631076142787));
#260911=CARTESIAN_POINT('Ctrl Pts',(-1.80237881470471,-0.719945139265139,
19.0605469389338));
#260912=CARTESIAN_POINT('Ctrl Pts',(-1.82957727414585,-0.651537475102388,
19.0578738239924));
#260913=CARTESIAN_POINT('Ctrl Pts',(-1.85665818679246,-0.583425456421352,
19.0552122617677));
#260914=CARTESIAN_POINT('Ctrl Pts',(-1.88000423467638,-0.513773421692869,
19.0524392860477));
#260915=CARTESIAN_POINT('Ctrl Pts',(-1.89946522179181,-0.442951007160264,
19.0495708873325));
#260916=CARTESIAN_POINT('Ctrl Pts',(-1.90524807804013,-0.421906039606916,
19.0487185391276));
#260917=CARTESIAN_POINT('Ctrl Pts',(-1.91068785454722,-0.400757658309688,
19.0478580070861));
#260918=CARTESIAN_POINT('Ctrl Pts',(-1.91578049784076,-0.379515351958551,
19.0469903179249));
#260919=CARTESIAN_POINT('',(-1.5555,1.90493809607371E-16,19.4445));
#260920=CARTESIAN_POINT('Origin',(0.,0.,19.4445));
#260921=CARTESIAN_POINT('',(-1.,-1.22464679914735E-16,20.));
#260922=CARTESIAN_POINT('',(-1.5,1.83697019872103E-16,19.5));
#260923=CARTESIAN_POINT('Origin',(0.,0.,20.));
#260924=CARTESIAN_POINT('',(-1.08942750315406,-1.11028283125135,19.4445));
#260925=CARTESIAN_POINT('Origin',(0.,0.,19.4445));
#260926=CARTESIAN_POINT('Ctrl Pts',(-1.76525906551972,0.00187739100781683,
19.2347399361577));
#260927=CARTESIAN_POINT('Ctrl Pts',(-1.76288673923925,-0.0135139808696315,
19.2371286301425));
#260928=CARTESIAN_POINT('Ctrl Pts',(-1.76030651728755,-0.0288864918497785,
19.2395239781913));
#260929=CARTESIAN_POINT('Ctrl Pts',(-1.7575179265608,-0.0442367894856103,
19.2419254407942));
#260930=CARTESIAN_POINT('Ctrl Pts',(-1.74580272373018,-0.108725223944406,
19.2520142721216));
#260931=CARTESIAN_POINT('Ctrl Pts',(-1.73048046950318,-0.172445835478701,
19.2621498573833));
#260932=CARTESIAN_POINT('Ctrl Pts',(-1.71163450897447,-0.235094626728941,
19.2722956920152));
#260933=CARTESIAN_POINT('Ctrl Pts',(-1.69287082259393,-0.297469917675188,
19.2823972338715));
#260934=CARTESIAN_POINT('Ctrl Pts',(-1.6706129121074,-0.358782641587655,
19.2925086605069));
#260935=CARTESIAN_POINT('Ctrl Pts',(-1.644932474297,-0.418687137158304,
19.3026191459137));
#260936=CARTESIAN_POINT('Ctrl Pts',(-1.61976488651821,-0.477395312686684,
19.3125277203252));
#260937=CARTESIAN_POINT('Ctrl Pts',(-1.59130934495902,-0.534750477092066,
19.3224352424608));
#260938=CARTESIAN_POINT('Ctrl Pts',(-1.55963814107745,-0.590386771328957,
19.3323586504096));
#260939=CARTESIAN_POINT('Ctrl Pts',(-1.54639843002514,-0.613644758694142,
19.336506994577));
#260940=CARTESIAN_POINT('Ctrl Pts',(-1.53259688928402,-0.636601914221633,
19.3406584579712));
#260941=CARTESIAN_POINT('Ctrl Pts',(-1.51823942349062,-0.659229681251031,
19.3448158049077));
#260942=CARTESIAN_POINT('Ctrl Pts',(-1.51248796700394,-0.668294137286167,
19.346481196304));
#260943=CARTESIAN_POINT('Ctrl Pts',(-1.50665198420563,-0.677298321778638,
19.3481461842204));
#260944=CARTESIAN_POINT('Ctrl Pts',(-1.5007335643467,-0.686238803116579,
19.3498106393327));
#260945=CARTESIAN_POINT('Ctrl Pts',(-1.46657740072041,-0.737835775071166,
19.3594164805062));
#260946=CARTESIAN_POINT('Ctrl Pts',(-1.42966243454859,-0.787334493623003,
19.3690067664155));
#260947=CARTESIAN_POINT('Ctrl Pts',(-1.39012993525811,-0.834466342447257,
19.3786439892553));
#260948=CARTESIAN_POINT('Ctrl Pts',(-1.35128540926912,-0.880777968563028,
19.3881134981348));
#260949=CARTESIAN_POINT('Ctrl Pts',(-1.30991393831839,-0.924804577147456,
19.3976285642955));
#260950=CARTESIAN_POINT('Ctrl Pts',(-1.26613409219736,-0.966278551040951,
19.407269709704));
#260951=CARTESIAN_POINT('Ctrl Pts',(-1.22690813773515,-1.00343848547323,
19.415908002532));
#260952=CARTESIAN_POINT('Ctrl Pts',(-1.18574947917021,-1.0385488873518,
19.4246478209494));
#260953=CARTESIAN_POINT('Ctrl Pts',(-1.14272687263894,-1.07140620588509,
19.433559460605));
#260954=CARTESIAN_POINT('Ctrl Pts',(-1.139121171214,-1.07415996001129,19.434306340313));
#260955=CARTESIAN_POINT('Ctrl Pts',(-1.13550239128299,-1.07689786122677,
19.4350544268978));
#260956=CARTESIAN_POINT('Ctrl Pts',(-1.13187058166182,-1.07961977480601,
19.435803761741));
#260957=CARTESIAN_POINT('Ctrl Pts',(-1.11791505753042,-1.09007894932254,
19.4386831418786));
#260958=CARTESIAN_POINT('Ctrl Pts',(-1.10376673475157,-1.10030239106308,
19.4415810402526));
#260959=CARTESIAN_POINT('Ctrl Pts',(-1.08942750315449,-1.11028283125093,
19.4445));
#260960=CARTESIAN_POINT('Origin',(0.,0.,-1.29405622560371));
#260961=CARTESIAN_POINT('',(1.43457668357355,0.601306900797843,0.288226974368355));
#260962=CARTESIAN_POINT('',(1.43457668357355,0.601306900797845,0.150256559003723));
#260963=CARTESIAN_POINT('',(1.43457668357355,0.601306900797845,-1.29405622560371));
#260964=CARTESIAN_POINT('',(-0.903577205789261,-1.26614710171373,4.16052298801706E-5));
#260965=CARTESIAN_POINT('Ctrl Pts',(-0.903577205789261,-1.26614710171373,
4.16052298801706E-5));
#260966=CARTESIAN_POINT('Ctrl Pts',(-0.854906687410512,-1.3008804837524,
0.00434792480590926));
#260967=CARTESIAN_POINT('Ctrl Pts',(-0.804117853215522,-1.33288363666962,
0.00865424438193803));
#260968=CARTESIAN_POINT('Ctrl Pts',(-0.751556329563241,-1.36188961868921,
0.0129605639579671));
#260969=CARTESIAN_POINT('Ctrl Pts',(-0.701486215864377,-1.38952072061988,
0.0170627644995997));
#260970=CARTESIAN_POINT('Ctrl Pts',(-0.649808186603321,-1.4144320453083,
0.0211649650412323));
#260971=CARTESIAN_POINT('Ctrl Pts',(-0.596852682617935,-1.43643556251291,
0.0252671655828649));
#260972=CARTESIAN_POINT('Ctrl Pts',(-0.543944822024556,-1.45841928343353,
0.0293656754269535));
#260973=CARTESIAN_POINT('Ctrl Pts',(-0.489762251131014,-1.47750017440538,
0.0334641852710426));
#260974=CARTESIAN_POINT('Ctrl Pts',(-0.434658662711666,-1.49353677454883,
0.0375626951151311));
#260975=CARTESIAN_POINT('Ctrl Pts',(-0.379582507432974,-1.50956539092352,
0.0416591645295442));
#260976=CARTESIAN_POINT('Ctrl Pts',(-0.323586752688759,-1.5225525717234,
0.0457556339439569));
#260977=CARTESIAN_POINT('Ctrl Pts',(-0.267041427119008,-1.53240631889922,
0.0498521033583699));
#260978=CARTESIAN_POINT('Ctrl Pts',(-0.21050153208121,-1.54225911973529,
0.0539481793537368));
#260979=CARTESIAN_POINT('Ctrl Pts',(-0.153412694621264,-1.54897899533739,
0.0580442553491035));
#260980=CARTESIAN_POINT('Ctrl Pts',(-0.0961540102568588,-1.55252525142476,
0.0621403313444704));
#260981=CARTESIAN_POINT('Ctrl Pts',(-0.0388403927829789,-1.5560749097362,
0.0662403370527458));
#260982=CARTESIAN_POINT('Ctrl Pts',(0.0186428655038344,-1.55644484119256,
0.0703403427610216));
#260983=CARTESIAN_POINT('Ctrl Pts',(0.0759143162520156,-1.55364644195132,
0.074440348469297));
#260984=CARTESIAN_POINT('Ctrl Pts',(0.133217967513464,-1.55084646932769,
0.078542659380016));
#260985=CARTESIAN_POINT('Ctrl Pts',(0.190309046039257,-1.54487467884722,
0.0826449702907347));
#260986=CARTESIAN_POINT('Ctrl Pts',(0.246812163846152,-1.53579425893496,
0.0867472812014536));
#260987=CARTESIAN_POINT('Ctrl Pts',(0.303412116575455,-1.52669827701848,
0.0908566226438342));
#260988=CARTESIAN_POINT('Ctrl Pts',(0.359421580968227,-1.51448315467192,
0.0949659640862152));
#260989=CARTESIAN_POINT('Ctrl Pts',(0.414477772298942,-1.49926262751731,
0.0990753055285958));
#260990=CARTESIAN_POINT('Ctrl Pts',(0.43376155614573,-1.49393154033911,
0.100514628703922));
#260991=CARTESIAN_POINT('Ctrl Pts',(0.452928558882729,-1.48823218964303,
0.101953951879249));
#260992=CARTESIAN_POINT('Ctrl Pts',(0.471963787350009,-1.48217085163291,
0.103393275054576));
#260993=CARTESIAN_POINT('Ctrl Pts',(0.526915051038866,-1.46467286447328,
0.107548340883011));
#260994=CARTESIAN_POINT('Ctrl Pts',(0.581002785657055,-1.44407949213653,
0.111703406711447));
#260995=CARTESIAN_POINT('Ctrl Pts',(0.633855123512789,-1.42049566433572,
0.115858472539883));
#260996=CARTESIAN_POINT('Ctrl Pts',(0.686616524499013,-1.39695241448394,
0.1200063892299));
#260997=CARTESIAN_POINT('Ctrl Pts',(0.738146278099265,-1.37042913259137,
0.124154305919917));
#260998=CARTESIAN_POINT('Ctrl Pts',(0.78808935185062,-1.34107994672192,
0.128302222609935));
#260999=CARTESIAN_POINT('Ctrl Pts',(0.837984422238826,-1.31175897016202,
0.132446152481837));
#261000=CARTESIAN_POINT('Ctrl Pts',(0.886295389703398,-1.27961773351875,
0.136590082353739));
#261001=CARTESIAN_POINT('Ctrl Pts',(0.93269042664768,-1.24485694681749,
0.140734012225641));
#261002=CARTESIAN_POINT('Ctrl Pts',(0.9790585299433,-1.21011633974919,0.144875536427485));
#261003=CARTESIAN_POINT('Ctrl Pts',(1.02351249349905,-1.17275950805182,
0.149017060629328));
#261004=CARTESIAN_POINT('Ctrl Pts',(1.06575002859973,-1.13303006426999,
0.153158584831171));
#261005=CARTESIAN_POINT('Ctrl Pts',(1.10797911960402,-1.09330856316882,
0.157299281062597));
#261006=CARTESIAN_POINT('Ctrl Pts',(1.14799228441944,-1.05121574719031,
0.161439977294023));
#261007=CARTESIAN_POINT('Ctrl Pts',(1.18552251205272,-1.00703357611165,
0.165580673525449));
#261008=CARTESIAN_POINT('Ctrl Pts',(1.22308759591479,-0.962810370806427,
0.169725215431796));
#261009=CARTESIAN_POINT('Ctrl Pts',(1.25816479723646,-0.91649432854441,
0.173869757338144));
#261010=CARTESIAN_POINT('Ctrl Pts',(1.29052691186693,-0.86840113988134,
0.178014299244492));
#261011=CARTESIAN_POINT('Ctrl Pts',(1.32290291632652,-0.820287309607535,
0.182160619989446));
#261012=CARTESIAN_POINT('Ctrl Pts',(1.35256124440086,-0.770395258639722,
0.1863069407344));
#261013=CARTESIAN_POINT('Ctrl Pts',(1.37931939623386,-0.719067627677031,
0.190453261479354));
#261014=CARTESIAN_POINT('Ctrl Pts',(1.40612981146247,-0.667639744787388,
0.194607680720901));
#261015=CARTESIAN_POINT('Ctrl Pts',(1.4300285150549,-0.614771152497881,
0.198762099962448));
#261016=CARTESIAN_POINT('Ctrl Pts',(1.45088053259173,-0.560826114001785,
0.202916519203995));
#261017=CARTESIAN_POINT('Ctrl Pts',(1.47034269628481,-0.510476685329655,
0.206794033079372));
#261018=CARTESIAN_POINT('Ctrl Pts',(1.48715117737244,-0.459190042068452,
0.210671546954749));
#261019=CARTESIAN_POINT('Ctrl Pts',(1.50123608373896,-0.407271986367974,
0.214549060830126));
#261020=CARTESIAN_POINT('Ctrl Pts',(1.51627927690493,-0.35182161130828,
0.218690386921559));
#261021=CARTESIAN_POINT('Ctrl Pts',(1.52827855468159,-0.295417015861604,
0.222831713012991));
#261022=CARTESIAN_POINT('Ctrl Pts',(1.53711874677415,-0.238424428940231,
0.226973039104424));
#261023=CARTESIAN_POINT('Ctrl Pts',(1.54594565440517,-0.181517486744757,
0.231108141882315));
#261024=CARTESIAN_POINT('Ctrl Pts',(1.55162280443562,-0.124024815736767,
0.235243244660206));
#261025=CARTESIAN_POINT('Ctrl Pts',(1.55408530296203,-0.0663258706494377,
0.239378347438097));
#261026=CARTESIAN_POINT('Ctrl Pts',(1.5565451271801,-0.00868958743533708,
0.243508959435686));
#261027=CARTESIAN_POINT('Ctrl Pts',(1.55579719833732,0.0491520062809331,
0.247639571433274));
#261028=CARTESIAN_POINT('Ctrl Pts',(1.55182832188269,0.106813432688756,
0.251770183430863));
#261029=CARTESIAN_POINT('Ctrl Pts',(1.54786212709918,0.164435898704758,
0.25589800447665));
#261030=CARTESIAN_POINT('Ctrl Pts',(1.54067933707812,0.221877918651016,
0.260025825522438));
#261031=CARTESIAN_POINT('Ctrl Pts',(1.53031882756835,0.278755333563033,
0.264153646568225));
#261032=CARTESIAN_POINT('Ctrl Pts',(1.51995666694747,0.335641812790993,
0.268282125447604));
#261033=CARTESIAN_POINT('Ctrl Pts',(1.50641585292148,0.391962989945588,
0.272410604326983));
#261034=CARTESIAN_POINT('Ctrl Pts',(1.48978676610489,0.4473428679869,0.276539083206362));
#261035=CARTESIAN_POINT('Ctrl Pts',(1.47409422634919,0.499603761649568,
0.280435046927026));
#261036=CARTESIAN_POINT('Ctrl Pts',(1.45565201597827,0.551026120008104,
0.284331010647691));
#261037=CARTESIAN_POINT('Ctrl Pts',(1.43457668357355,0.601306900797843,
0.288226974368356));
#261038=CARTESIAN_POINT('',(0.903606778650206,-1.26612599672284,0.));
#261039=CARTESIAN_POINT('Origin',(0.,0.,0.));
#261040=CARTESIAN_POINT('Ctrl Pts',(0.903606778650177,-1.26612599672286,
0.));
#261041=CARTESIAN_POINT('Ctrl Pts',(0.951853445040324,-1.23169339292967,
0.00424530167179309));
#261042=CARTESIAN_POINT('Ctrl Pts',(0.998167624735184,-1.19447231163877,
0.00849060334358664));
#261043=CARTESIAN_POINT('Ctrl Pts',(1.04222559460503,-1.15470604915286,
0.0127359050153797));
#261044=CARTESIAN_POINT('Ctrl Pts',(1.08626235513991,-1.11495892999069,
0.0169791630154963));
#261045=CARTESIAN_POINT('Ctrl Pts',(1.12804469970472,-1.07266938416111,
0.0212224210156127));
#261046=CARTESIAN_POINT('Ctrl Pts',(1.16728248039808,-1.02812054787155,
0.0254656790157293));
#261047=CARTESIAN_POINT('Ctrl Pts',(1.20651063791617,-0.98358263730848,
0.0297078963449737));
#261048=CARTESIAN_POINT('Ctrl Pts',(1.24319514989636,-0.936786900956853,
0.033950113674218));
#261049=CARTESIAN_POINT('Ctrl Pts',(1.27708449593244,-0.888051485134154,
0.0381923310034624));
#261050=CARTESIAN_POINT('Ctrl Pts',(1.31097578868278,-0.839313269790677,
0.0424347920194664));
#261051=CARTESIAN_POINT('Ctrl Pts',(1.34207131961844,-0.788635552747116,
0.0466772530354706));
#261052=CARTESIAN_POINT('Ctrl Pts',(1.37016249066737,-0.736366076872226,
0.0509197140514746));
#261053=CARTESIAN_POINT('Ctrl Pts',(1.3982637792545,-0.684077775209748,
0.055163703065772));
#261054=CARTESIAN_POINT('Ctrl Pts',(1.42335832940938,-0.630197004108925,
0.0594076920800693));
#261055=CARTESIAN_POINT('Ctrl Pts',(1.44528398878409,-0.57509515887751,
0.0636516810943668));
#261056=CARTESIAN_POINT('Ctrl Pts',(1.46724280081557,-0.519909996992712,
0.0679020872251905));
#261057=CARTESIAN_POINT('Ctrl Pts',(1.48602297562656,-0.463500527170074,
0.0721524933560141));
#261058=CARTESIAN_POINT('Ctrl Pts',(1.50151122687381,-0.406256428345346,
0.0764028994868378));
#261059=CARTESIAN_POINT('Ctrl Pts',(1.51701148192575,-0.348967963828759,
0.0806565997949225));
#261060=CARTESIAN_POINT('Ctrl Pts',(1.52921462989051,-0.290844057345651,
0.0849103001030079));
#261061=CARTESIAN_POINT('Ctrl Pts',(1.5380585220928,-0.232284809270268,
0.0891640004110927));
#261062=CARTESIAN_POINT('Ctrl Pts',(1.54692121356449,-0.173601083074211,
0.0934267427174556));
#261063=CARTESIAN_POINT('Ctrl Pts',(1.55241033518493,-0.114480651008706,
0.0976894850238181));
#261064=CARTESIAN_POINT('Ctrl Pts',(1.55451568512429,-0.0553284258095596,
0.101952227330181));
#261065=CARTESIAN_POINT('Ctrl Pts',(1.55602358171541,-0.0129623387910441,
0.105005294410597));
#261066=CARTESIAN_POINT('Ctrl Pts',(1.55579679794536,0.0294199928847578,
0.108058361491013));
#261067=CARTESIAN_POINT('Ctrl Pts',(1.55384796201767,0.0716712001681464,
0.11111142857143));
#261068=CARTESIAN_POINT('Ctrl Pts',(1.55122812972079,0.128469761735095,
0.115215685696485));
#261069=CARTESIAN_POINT('Ctrl Pts',(1.54548304431742,0.185269471839644,
0.11931994282154));
#261070=CARTESIAN_POINT('Ctrl Pts',(1.53660820824037,0.241692913359763,
0.123424199946596));
#261071=CARTESIAN_POINT('Ctrl Pts',(1.52774704327412,0.298029438218638,
0.127522134729082));
#261072=CARTESIAN_POINT('Ctrl Pts',(1.51576574869432,0.353990320940755,
0.131620069511569));
#261073=CARTESIAN_POINT('Ctrl Pts',(1.50071177189604,0.409199740582322,
0.135718004294056));
#261074=CARTESIAN_POINT('Ctrl Pts',(1.48567802726089,0.464334960163706,
0.139810431556096));
#261075=CARTESIAN_POINT('Ctrl Pts',(1.46757992691381,0.518720207923678,
0.143902858818138));
#261076=CARTESIAN_POINT('Ctrl Pts',(1.44651611159788,0.57198897619425,0.147995286080179));
#261077=CARTESIAN_POINT('Ctrl Pts',(1.44263650403733,0.581800205215399,
0.14874904372136));
#261078=CARTESIAN_POINT('Ctrl Pts',(1.43865642718691,0.591573593139283,
0.149502801362542));
#261079=CARTESIAN_POINT('Ctrl Pts',(1.43457668357355,0.601306900797845,
0.150256559003723));
#261080=CARTESIAN_POINT('Origin',(0.,0.,-1.29405622560371));
#261081=CARTESIAN_POINT('',(1.43457668375786,0.60130690035812,0.986840263175809));
#261082=CARTESIAN_POINT('',(1.43457651222227,0.601307309601495,0.849135319448151));
#261083=CARTESIAN_POINT('',(1.43457668357355,0.601306900797845,-1.29405622560371));
#261084=CARTESIAN_POINT('',(-1.55549983609988,0.000714068102024366,0.594056225567426));
#261085=CARTESIAN_POINT('Ctrl Pts',(1.43457668375786,0.601306900358119,
0.986840263175809));
#261086=CARTESIAN_POINT('Ctrl Pts',(1.44583683266777,0.574442836313328,
0.984800154295232));
#261087=CARTESIAN_POINT('Ctrl Pts',(1.45634171559164,0.547264094095289,
0.982798230949018));
#261088=CARTESIAN_POINT('Ctrl Pts',(1.5016386947571,0.419506152666243,0.973602132403835));
#261089=CARTESIAN_POINT('Ctrl Pts',(1.52681576497426,0.315818555124705,
0.966729676129621));
#261090=CARTESIAN_POINT('Ctrl Pts',(1.55200054342739,0.131306418546304,
0.954382233635514));
#261091=CARTESIAN_POINT('Ctrl Pts',(1.55669114739927,0.0515453269029813,
0.949009910860428));
#261092=CARTESIAN_POINT('Ctrl Pts',(1.55503050182964,-0.0399874426081019,
0.942614787105728));
#261093=CARTESIAN_POINT('Ctrl Pts',(1.55468331354602,-0.0517555638892538,
0.941788406907512));
#261094=CARTESIAN_POINT('Ctrl Pts',(1.55390373565351,-0.0708307180837244,
0.940441594681791));
#261095=CARTESIAN_POINT('Ctrl Pts',(1.55355328974435,-0.0781407890977374,
0.939923719208182));
#261096=CARTESIAN_POINT('Ctrl Pts',(1.55283814721328,-0.0911396245309655,
0.938999600702741));
#261097=CARTESIAN_POINT('Ctrl Pts',(1.55249373789135,-0.0968294109483699,
0.938593999056129));
#261098=CARTESIAN_POINT('Ctrl Pts',(1.55170255476728,-0.108807993407129,
0.937737712596411));
#261099=CARTESIAN_POINT('Ctrl Pts',(1.55124880613886,-0.115096208412715,
0.937286816518539));
#261100=CARTESIAN_POINT('Ctrl Pts',(1.54994702760356,-0.131727602263499,
0.93609050347328));
#261101=CARTESIAN_POINT('Ctrl Pts',(1.54903370532627,-0.142065195007226,
0.935343056035774));
#261102=CARTESIAN_POINT('Ctrl Pts',(1.54423920383262,-0.190768135507098,
0.931802825306857));
#261103=CARTESIAN_POINT('Ctrl Pts',(1.53903603749094,-0.228986438630815,
0.928969073221727));
#261104=CARTESIAN_POINT('Ctrl Pts',(1.50668529352395,-0.41468172861502,
0.91491317193785));
#261105=CARTESIAN_POINT('Ctrl Pts',(1.45972829211868,-0.557889095625831,
0.903075161689915));
#261106=CARTESIAN_POINT('Ctrl Pts',(1.37552200936693,-0.727371015370615,
0.888647490019427));
#261107=CARTESIAN_POINT('Ctrl Pts',(1.3566756322814,-0.761945713191154,
0.885686831980741));
#261108=CARTESIAN_POINT('Ctrl Pts',(1.33313924907402,-0.801476183990503,
0.882310973640917));
#261109=CARTESIAN_POINT('Ctrl Pts',(1.32970608363188,-0.807159257075366,
0.881825881744756));
#261110=CARTESIAN_POINT('Ctrl Pts',(1.32409519286424,-0.816314255253958,
0.881045032225767));
#261111=CARTESIAN_POINT('Ctrl Pts',(1.32193999950714,-0.819799781559014,
0.880747885295143));
#261112=CARTESIAN_POINT('Ctrl Pts',(1.31808609700508,-0.825977860214509,
0.880221500845305));
#261113=CARTESIAN_POINT('Ctrl Pts',(1.31639287452608,-0.828673750809956,
0.879991913156345));
#261114=CARTESIAN_POINT('Ctrl Pts',(1.31272131505667,-0.834479829133666,
0.879497697023913));
#261115=CARTESIAN_POINT('Ctrl Pts',(1.31074019856379,-0.837588185726855,
0.879233255729667));
#261116=CARTESIAN_POINT('Ctrl Pts',(1.30519091059809,-0.846227070277718,
0.878498621396459));
#261117=CARTESIAN_POINT('Ctrl Pts',(1.30159860292242,-0.851742125626637,
0.878029990405404));
#261118=CARTESIAN_POINT('Ctrl Pts',(1.2805189302889,-0.883659664339501,
0.875318910789927));
#261119=CARTESIAN_POINT('Ctrl Pts',(1.26226201999178,-0.90954828932622,
0.873124099818739));
#261120=CARTESIAN_POINT('Ctrl Pts',(1.15562739257571,-1.05135604147518,
0.861014440896718));
#261121=CARTESIAN_POINT('Ctrl Pts',(1.05208641855925,-1.15496612643482,
0.851764217583685));
#261122=CARTESIAN_POINT('Ctrl Pts',(0.896211870003822,-1.27232798631137,
0.838604529048586));
#261123=CARTESIAN_POINT('Ctrl Pts',(0.855413467858603,-1.30010814549373,
0.835225745583971));
#261124=CARTESIAN_POINT('Ctrl Pts',(0.803513894797133,-1.3319456825008,
0.830964050857422));
#261125=CARTESIAN_POINT('Ctrl Pts',(0.793593493674383,-1.33788012703242,
0.830151086826246));
#261126=CARTESIAN_POINT('Ctrl Pts',(0.77787772791332,-1.34704509766607,
0.828865282310385));
#261127=CARTESIAN_POINT('Ctrl Pts',(0.772126116221676,-1.35035014455731,
0.828395140960181));
#261128=CARTESIAN_POINT('Ctrl Pts',(0.761473707929256,-1.35638102632723,
0.827525108222961));
#261129=CARTESIAN_POINT('Ctrl Pts',(0.756578951128922,-1.35911735536161,
0.827125601815906));
#261130=CARTESIAN_POINT('Ctrl Pts',(0.74570004676794,-1.36512203917527,
0.826238212423495));
#261131=CARTESIAN_POINT('Ctrl Pts',(0.739709019438026,-1.36837761798925,
0.825749884067379));
#261132=CARTESIAN_POINT('Ctrl Pts',(0.722457791994227,-1.377605694766,0.824344634524997));
#261133=CARTESIAN_POINT('Ctrl Pts',(0.711145565991381,-1.38347919299422,
0.823424248217281));
#261134=CARTESIAN_POINT('Ctrl Pts',(0.622488371515749,-1.42813685766515,
0.816217503291865));
#261135=CARTESIAN_POINT('Ctrl Pts',(0.542115755639979,-1.46053831291564,
0.809709917775539));
#261136=CARTESIAN_POINT('Ctrl Pts',(0.377990293606597,-1.51128390508164,
0.796508520150517));
#261137=CARTESIAN_POINT('Ctrl Pts',(0.294568798929559,-1.5297334385913,
0.789841846258124));
#261138=CARTESIAN_POINT('Ctrl Pts',(0.195970410793646,-1.54317139823791,
0.782201433144978));
#261139=CARTESIAN_POINT('Ctrl Pts',(0.181857865565668,-1.54489808818141,
0.781113760269311));
#261140=CARTESIAN_POINT('Ctrl Pts',(0.130414398780697,-1.55047755945355,
0.777174362278981));
#261141=CARTESIAN_POINT('Ctrl Pts',(0.0929673423124462,-1.55317295339527,
0.774355140186107));
#261142=CARTESIAN_POINT('Ctrl Pts',(0.0489134361121352,-1.55474453976543,
0.771121280070015));
#261143=CARTESIAN_POINT('Ctrl Pts',(0.0423694202775905,-1.55493663678642,
0.770643051405062));
#261144=CARTESIAN_POINT('Ctrl Pts',(0.0317545303461609,-1.55518116985824,
0.76987101495676));
#261145=CARTESIAN_POINT('Ctrl Pts',(0.0276844110498078,-1.55525894811373,
0.769575867994204));
#261146=CARTESIAN_POINT('Ctrl Pts',(0.02043167322982,-1.55536906426782,
0.769051552171228));
#261147=CARTESIAN_POINT('Ctrl Pts',(0.0172492255206549,-1.55540761353498,
0.768822045318464));
#261148=CARTESIAN_POINT('Ctrl Pts',(0.0103578028953234,-1.55546993610137,
0.768326277651991));
#261149=CARTESIAN_POINT('Ctrl Pts',(0.0066488593930855,-1.55549021200496,
0.768060213422123));
#261150=CARTESIAN_POINT('Ctrl Pts',(-0.0037390581158609,-1.55550984474637,
0.767317056100492));
#261151=CARTESIAN_POINT('Ctrl Pts',(-0.0104181154392727,-1.55547945175207,
0.766841581495767));
#261152=CARTESIAN_POINT('Ctrl Pts',(-0.0503949996502374,-1.55504002823789,
0.764008609472395));
#261153=CARTESIAN_POINT('Ctrl Pts',(-0.0836759185716972,-1.55360480951411,
0.761703837418819));
#261154=CARTESIAN_POINT('Ctrl Pts',(-0.284293527021595,-1.53848664680285,
0.747996011796078));
#261155=CARTESIAN_POINT('Ctrl Pts',(-0.448557735259256,-1.49885642117692,
0.737430691408286));
#261156=CARTESIAN_POINT('Ctrl Pts',(-0.607948811440686,-1.43178338495197,
0.725569150060148));
#261157=CARTESIAN_POINT('Ctrl Pts',(-0.61256343664806,-1.42981518173776,
0.725224384787615));
#261158=CARTESIAN_POINT('Ctrl Pts',(-0.640236731658547,-1.4178535707448,
0.723148504670547));
#261159=CARTESIAN_POINT('Ctrl Pts',(-0.663058805574347,-1.40732537722207,
0.721401427403274));
#261160=CARTESIAN_POINT('Ctrl Pts',(-0.69388534553605,-1.39218830365224,
0.71898797335305));
#261161=CARTESIAN_POINT('Ctrl Pts',(-0.702119507105201,-1.38805379463114,
0.718337982667155));
#261162=CARTESIAN_POINT('Ctrl Pts',(-0.715162553455551,-1.38135891288846,
0.717299638859661));
#261163=CARTESIAN_POINT('Ctrl Pts',(-0.719995653991411,-1.37884595983052,
0.716912950453329));
#261164=CARTESIAN_POINT('Ctrl Pts',(-0.729785059115935,-1.37369049090167,
0.716125730075693));
#261165=CARTESIAN_POINT('Ctrl Pts',(-0.734740445846722,-1.37104641534058,
0.715725147568553));
#261166=CARTESIAN_POINT('Ctrl Pts',(-0.746102777245424,-1.36490445795701,
0.714801754036403));
#261167=CARTESIAN_POINT('Ctrl Pts',(-0.752499593381453,-1.36138822242585,
0.7142782969495));
#261168=CARTESIAN_POINT('Ctrl Pts',(-0.765896063194354,-1.3539011156939,
0.713174342222554));
#261169=CARTESIAN_POINT('Ctrl Pts',(-0.772890104387216,-1.34992069867341,
0.712593513653113));
#261170=CARTESIAN_POINT('Ctrl Pts',(-0.791411080072929,-1.33918900786861,
0.711043305278424));
#261171=CARTESIAN_POINT('Ctrl Pts',(-0.80288223880487,-1.33234334405815,
0.710070559185372));
#261172=CARTESIAN_POINT('Ctrl Pts',(-0.8377042366089,-1.31094955358406,
0.707078210080837));
#261173=CARTESIAN_POINT('Ctrl Pts',(-0.860757373378667,-1.29592966307172,
0.705041934049246));
#261174=CARTESIAN_POINT('Ctrl Pts',(-1.00693362455144,-1.19506954839168,
0.691764309725466));
#261175=CARTESIAN_POINT('Ctrl Pts',(-1.11745434185532,-1.09242339138263,
0.679900215287483));
#261176=CARTESIAN_POINT('Ctrl Pts',(-1.23408884375215,-0.947573631162822,
0.66575961475814));
#261177=CARTESIAN_POINT('Ctrl Pts',(-1.25564760575025,-0.918814812967962,
0.663063603983283));
#261178=CARTESIAN_POINT('Ctrl Pts',(-1.27989063175237,-0.884026046909663,
0.659953526457898));
#261179=CARTESIAN_POINT('Ctrl Pts',(-1.28355537936585,-0.878696576104198,
0.659481133277693));
#261180=CARTESIAN_POINT('Ctrl Pts',(-1.28945899758859,-0.869995471623355,
0.658716649011529));
#261181=CARTESIAN_POINT('Ctrl Pts',(-1.29171808997526,-0.866637758319201,
0.658423260080281));
#261182=CARTESIAN_POINT('Ctrl Pts',(-1.29572802539076,-0.860627234249489,
0.657901016846207));
#261183=CARTESIAN_POINT('Ctrl Pts',(-1.29748386336071,-0.857977841859926,
0.657671832800638));
#261184=CARTESIAN_POINT('Ctrl Pts',(-1.30127644662579,-0.852216925735819,
0.657175698681653));
#261185=CARTESIAN_POINT('Ctrl Pts',(-1.30331015654204,-0.849103477612566,
0.656908950816116));
#261186=CARTESIAN_POINT('Ctrl Pts',(-1.30900020576421,-0.840323856965594,
0.656160542682049));
#261187=CARTESIAN_POINT('Ctrl Pts',(-1.31263095339804,-0.834641065297778,
0.65568054488375));
#261188=CARTESIAN_POINT('Ctrl Pts',(-1.33468636739009,-0.799620356293605,
0.652748375330769));
#261189=CARTESIAN_POINT('Ctrl Pts',(-1.3521653760523,-0.769694534397481,
0.650353475751293));
#261190=CARTESIAN_POINT('Ctrl Pts',(-1.44293941695222,-0.601627629744189,
0.637358374259133));
#261191=CARTESIAN_POINT('Ctrl Pts',(-1.49608206256403,-0.453626562026999,
0.627473876281463));
#261192=CARTESIAN_POINT('Ctrl Pts',(-1.53302315291613,-0.265796578912042,
0.61444331740302));
#261193=CARTESIAN_POINT('Ctrl Pts',(-1.53862046399076,-0.231202424336528,
0.612029060712096));
#261194=CARTESIAN_POINT('Ctrl Pts',(-1.5444090236771,-0.185735557307904,
0.608822535556316));
#261195=CARTESIAN_POINT('Ctrl Pts',(-1.54566155104945,-0.175006539541205,
0.608063484638057));
#261196=CARTESIAN_POINT('Ctrl Pts',(-1.54754357025943,-0.157284558829741,
0.606805336392547));
#261197=CARTESIAN_POINT('Ctrl Pts',(-1.54823765337242,-0.150298702760661,
0.606308269918999));
#261198=CARTESIAN_POINT('Ctrl Pts',(-1.54937570252006,-0.137998617920497,
0.605431010400524));
#261199=CARTESIAN_POINT('Ctrl Pts',(-1.54983967763059,-0.132686315988006,
0.605051451799069));
#261200=CARTESIAN_POINT('Ctrl Pts',(-1.55071152669844,-0.122074806719921,
0.604291869365344));
#261201=CARTESIAN_POINT('Ctrl Pts',(-1.55111957480982,-0.116775685896486,
0.603911856346569));
#261202=CARTESIAN_POINT('Ctrl Pts',(-1.55194821440675,-0.105242706461097,
0.603083235705015));
#261203=CARTESIAN_POINT('Ctrl Pts',(-1.55235841796768,-0.0990082194109238,
0.602634308592144));
#261204=CARTESIAN_POINT('Ctrl Pts',(-1.55350212664309,-0.0798657920501435,
0.601252778639819));
#261205=CARTESIAN_POINT('Ctrl Pts',(-1.55411225540398,-0.0669513333700773,
0.600316343869313));
#261206=CARTESIAN_POINT('Ctrl Pts',(-1.55519646398222,-0.0357569299454874,
0.598043315606796));
#261207=CARTESIAN_POINT('Ctrl Pts',(-1.5555093069421,-0.0174738240725086,
0.596701878951661));
#261208=CARTESIAN_POINT('Ctrl Pts',(-1.55549978924273,0.000809731943940699,
0.595350860080746));
#261209=CARTESIAN_POINT('Ctrl Pts',(1.43457668357355,0.601306900797843,
0.288226974368356));
#261210=CARTESIAN_POINT('Ctrl Pts',(1.4122238834107,0.65463541887017,0.292359089431473));
#261211=CARTESIAN_POINT('Ctrl Pts',(1.38690886232638,0.706679132697199,
0.29649120449459));
#261212=CARTESIAN_POINT('Ctrl Pts',(1.35881626030268,0.757098818343448,
0.300623319557707));
#261213=CARTESIAN_POINT('Ctrl Pts',(1.33039637739596,0.808105897041636,
0.304803574065702));
#261214=CARTESIAN_POINT('Ctrl Pts',(1.29913405570535,0.857450390029285,
0.308983828573697));
#261215=CARTESIAN_POINT('Ctrl Pts',(1.26526508811455,0.904811862653489,
0.313164083081692));
#261216=CARTESIAN_POINT('Ctrl Pts',(1.23139612052375,0.952173335277694,
0.317344337589686));
#261217=CARTESIAN_POINT('Ctrl Pts',(1.1949209015692,0.997551404037723,0.321524592097681));
#261218=CARTESIAN_POINT('Ctrl Pts',(1.15611469137679,1.04066280340116,0.325704846605676));
#261219=CARTESIAN_POINT('Ctrl Pts',(1.11759806302803,1.08345249450068,0.329853906987747));
#261220=CARTESIAN_POINT('Ctrl Pts',(1.07662202823306,1.12419052654482,0.334002967369818));
#261221=CARTESIAN_POINT('Ctrl Pts',(1.03343365835562,1.16258123319522,0.338152027751889));
#261222=CARTESIAN_POINT('Ctrl Pts',(0.990322062582344,1.20090369434065,
0.3422937125281));
#261223=CARTESIAN_POINT('Ctrl Pts',(0.94500632367177,1.23688676954466,0.346435397304311));
#261224=CARTESIAN_POINT('Ctrl Pts',(0.897771534387028,1.2702702555143,0.350577082080523));
#261225=CARTESIAN_POINT('Ctrl Pts',(0.850583732070946,1.30362053314676,
0.354714646901596));
#261226=CARTESIAN_POINT('Ctrl Pts',(0.801481084624065,1.33437604625786,
0.35885221172267));
#261227=CARTESIAN_POINT('Ctrl Pts',(0.750781715163885,1.36231680095915,
0.362989776543744));
#261228=CARTESIAN_POINT('Ctrl Pts',(0.70011331515327,1.39024048819387,0.367124813954588));
#261229=CARTESIAN_POINT('Ctrl Pts',(0.647850581517572,1.41535257465031,
0.371259851365431));
#261230=CARTESIAN_POINT('Ctrl Pts',(0.594338702158597,1.43747756751764,
0.375394888776275));
#261231=CARTESIAN_POINT('Ctrl Pts',(0.540838967678637,1.45959753896983,
0.379528987712714));
#261232=CARTESIAN_POINT('Ctrl Pts',(0.486091131091245,1.47873156394323,
0.383663086649154));
#261233=CARTESIAN_POINT('Ctrl Pts',(0.430460919615824,1.49475203518293,
0.387797185585594));
#261234=CARTESIAN_POINT('Ctrl Pts',(0.374780584803872,1.51078694101581,
0.39193500938352));
#261235=CARTESIAN_POINT('Ctrl Pts',(0.318216787375974,1.52370254132316,
0.396072833181446));
#261236=CARTESIAN_POINT('Ctrl Pts',(0.261149698318672,1.53342136579222,
0.400210656979373));
#261237=CARTESIAN_POINT('Ctrl Pts',(0.204059136497248,1.54314418779607,
0.40435018274184));
#261238=CARTESIAN_POINT('Ctrl Pts',(0.146465388528611,1.54966755249864,
0.408489708504307));
#261239=CARTESIAN_POINT('Ctrl Pts',(0.0887548629313491,1.55296581556261,
0.412629234266774));
#261240=CARTESIAN_POINT('Ctrl Pts',(0.0309320153197847,1.55627049803703,
0.416776816789547));
#261241=CARTESIAN_POINT('Ctrl Pts',(-0.0270075416867453,1.55633753304818,
0.420924399312321));
#261242=CARTESIAN_POINT('Ctrl Pts',(-0.0846771964969704,1.55319349161443,
0.425071981835094));
#261243=CARTESIAN_POINT('Ctrl Pts',(-0.139315241988193,1.55021472783564,
0.429001532017137));
#261244=CARTESIAN_POINT('Ctrl Pts',(-0.193710669010352,1.54435410883403,
0.43293108219918));
#261245=CARTESIAN_POINT('Ctrl Pts',(-0.247542712744338,1.53567667670222,
0.436860632381223));
#261246=CARTESIAN_POINT('Ctrl Pts',(-0.304376617262698,1.5265153609684,
0.441009307860645));
#261247=CARTESIAN_POINT('Ctrl Pts',(-0.360820124387077,1.51417557510158,
0.445157983340067));
#261248=CARTESIAN_POINT('Ctrl Pts',(-0.41649089269227,1.49870463611227,
0.449306658819489));
#261249=CARTESIAN_POINT('Ctrl Pts',(-0.472063006489406,1.48326111326829,
0.453447982405791));
#261250=CARTESIAN_POINT('Ctrl Pts',(-0.52686460200474,1.46469758906535,
0.457589305992092));
#261251=CARTESIAN_POINT('Ctrl Pts',(-0.58052252409489,1.44311255590772,
0.461730629578393));
#261252=CARTESIAN_POINT('Ctrl Pts',(-0.634127255235985,1.42154891993347,
0.465867847882132));
#261253=CARTESIAN_POINT('Ctrl Pts',(-0.686590078628672,1.39696990278649,
0.470005066185871));
#261254=CARTESIAN_POINT('Ctrl Pts',(-0.737553723513263,1.36952355033848,
0.47414228448961));
#261255=CARTESIAN_POINT('Ctrl Pts',(-0.78848642321298,1.34209386334783,
0.478276990669548));
#261256=CARTESIAN_POINT('Ctrl Pts',(-0.837921291451408,1.31180053869827,
0.482411696849487));
#261257=CARTESIAN_POINT('Ctrl Pts',(-0.885523783309722,1.27883848831384,
0.486546403029425));
#261258=CARTESIAN_POINT('Ctrl Pts',(-0.93311565385724,1.24588379259023,
0.49068018665263));
#261259=CARTESIAN_POINT('Ctrl Pts',(-0.978875531894772,1.21026184954031,
0.494813970275835));
#261260=CARTESIAN_POINT('Ctrl Pts',(-1.02249798073055,1.17221078710356,
0.49894775389904));
#261261=CARTESIAN_POINT('Ctrl Pts',(-1.06616003071023,1.13412518131496,
0.503085290235915));
#261262=CARTESIAN_POINT('Ctrl Pts',(-1.10768037977828,1.09360639149896,
0.50722282657279));
#261263=CARTESIAN_POINT('Ctrl Pts',(-1.14678789423033,1.05093186061075,
0.511360362909665));
#261264=CARTESIAN_POINT('Ctrl Pts',(-1.18591163465964,1.00823962376557,
0.515499615938882));
#261265=CARTESIAN_POINT('Ctrl Pts',(-1.22262021326341,0.963390265701144,
0.519638868968098));
#261266=CARTESIAN_POINT('Ctrl Pts',(-1.25668267034715,0.916694559844863,
0.523778121997314));
#261267=CARTESIAN_POINT('Ctrl Pts',(-1.29081166554661,0.869907637894784,
0.527925460705623));
#261268=CARTESIAN_POINT('Ctrl Pts',(-1.32228392475959,0.821267598677886,
0.532072799413932));
#261269=CARTESIAN_POINT('Ctrl Pts',(-1.35091225879012,0.771113687500481,
0.536220138122241));
#261270=CARTESIAN_POINT('Ctrl Pts',(-1.37805479274566,0.723562745986234,
0.540152231467085));
#261271=CARTESIAN_POINT('Ctrl Pts',(-1.40264115933879,0.674651551227338,
0.544084324811929));
#261272=CARTESIAN_POINT('Ctrl Pts',(-1.42455194944463,0.624685515546427,
0.548016418156773));
#261273=CARTESIAN_POINT('Ctrl Pts',(-1.44997193394591,0.566717005672345,
0.552578268797517));
#261274=CARTESIAN_POINT('Ctrl Pts',(-1.47188282144215,0.507119559173282,
0.557140119438261));
#261275=CARTESIAN_POINT('Ctrl Pts',(-1.49009537948839,0.446313802192301,
0.561701970079005));
#261276=CARTESIAN_POINT('Ctrl Pts',(-1.50824984121549,0.385702009763373,
0.566249268852294));
#261277=CARTESIAN_POINT('Ctrl Pts',(-1.52272935208436,0.323889902948767,
0.570796567625584));
#261278=CARTESIAN_POINT('Ctrl Pts',(-1.53339289085846,0.261316842673301,
0.575343866398873));
#261279=CARTESIAN_POINT('Ctrl Pts',(-1.54400289564074,0.199057916923692,
0.579868336441431));
#261280=CARTESIAN_POINT('Ctrl Pts',(-1.5508350072412,0.136045979691595,
0.584392806483988));
#261281=CARTESIAN_POINT('Ctrl Pts',(-1.55379868266219,0.0727317245584089,
0.588917276526546));
#261282=CARTESIAN_POINT('Ctrl Pts',(-1.55492074239655,0.048760686504574,
0.590630259540173));
#261283=CARTESIAN_POINT('Ctrl Pts',(-1.5554888037788,0.0247464728286803,
0.5923432425538));
#261284=CARTESIAN_POINT('Ctrl Pts',(-1.55549983609988,0.000714068102024366,
0.594056225567427));
#261285=CARTESIAN_POINT('',(-1.55549967037724,0.00101264816652329,0.455943774396293));
#261286=CARTESIAN_POINT('Ctrl Pts',(1.43457668357355,0.601306900797845,
0.150256559003723));
#261287=CARTESIAN_POINT('Ctrl Pts',(1.41244477849698,0.654108415205522,
0.154345564134033));
#261288=CARTESIAN_POINT('Ctrl Pts',(1.38737593218696,0.70572879733375,0.158434569264343));
#261289=CARTESIAN_POINT('Ctrl Pts',(1.3595270376115,0.755821727660225,0.162523574394653));
#261290=CARTESIAN_POINT('Ctrl Pts',(1.33168522965499,0.805901910999285,
0.166611539008934));
#261291=CARTESIAN_POINT('Ctrl Pts',(1.30106503569729,0.854454947945978,
0.170699503623215));
#261292=CARTESIAN_POINT('Ctrl Pts',(1.26786928821999,0.901159096934901,
0.174787468237496));
#261293=CARTESIAN_POINT('Ctrl Pts',(1.23464388225231,0.947904973393733,
0.178879085212951));
#261294=CARTESIAN_POINT('Ctrl Pts',(1.1988386337529,0.992798225217377,0.182970702188406));
#261295=CARTESIAN_POINT('Ctrl Pts',(1.1606988486626,1.03554740727468,0.187062319163861));
#261296=CARTESIAN_POINT('Ctrl Pts',(1.12254294605259,1.07831465474014,0.191155665218731));
#261297=CARTESIAN_POINT('Ctrl Pts',(1.08205091879801,1.11893564946202,0.195249011273601));
#261298=CARTESIAN_POINT('Ctrl Pts',(1.03950505573736,1.15715577563977,0.199342357328471));
#261299=CARTESIAN_POINT('Ctrl Pts',(0.996876335681916,1.19545033454887,
0.203443675071499));
#261300=CARTESIAN_POINT('Ctrl Pts',(0.952186207559337,1.231334351474,0.207544992814528));
#261301=CARTESIAN_POINT('Ctrl Pts',(0.905749257284517,1.2645942167069,0.211646310557557));
#261302=CARTESIAN_POINT('Ctrl Pts',(0.865831796715821,1.29318458173082,
0.215171826085992));
#261303=CARTESIAN_POINT('Ctrl Pts',(0.824624245025244,1.31983651539173,
0.218697341614427));
#261304=CARTESIAN_POINT('Ctrl Pts',(0.782340582356172,1.34444169200401,
0.222222857142862));
#261305=CARTESIAN_POINT('Ctrl Pts',(0.732513694933871,1.3734363269925,0.226377309577972));
#261306=CARTESIAN_POINT('Ctrl Pts',(0.680970078865944,1.39971700644518,
0.230531762013082));
#261307=CARTESIAN_POINT('Ctrl Pts',(0.62803644998017,1.42307781498283,0.234686214448193));
#261308=CARTESIAN_POINT('Ctrl Pts',(0.57519685881554,1.44639712254567,0.23883328640991));
#261309=CARTESIAN_POINT('Ctrl Pts',(0.520972627697919,1.46680664842633,
0.242980358371627));
#261310=CARTESIAN_POINT('Ctrl Pts',(0.465715749510109,1.48414591285973,
0.247127430333344));
#261311=CARTESIAN_POINT('Ctrl Pts',(0.410513858184165,1.50146792275814,
0.251270375488036));
#261312=CARTESIAN_POINT('Ctrl Pts',(0.354281848696871,1.51572557079087,
0.255413320642728));
#261313=CARTESIAN_POINT('Ctrl Pts',(0.297390804141844,1.5268067852914,0.25955626579742));
#261314=CARTESIAN_POINT('Ctrl Pts',(0.240534695323457,1.53788119502338,
0.263696666846234));
#261315=CARTESIAN_POINT('Ctrl Pts',(0.183020862092417,1.5457829393312,0.267837067895047));
#261316=CARTESIAN_POINT('Ctrl Pts',(0.125232503307728,1.55045060228157,
0.271977468943861));
#261317=CARTESIAN_POINT('Ctrl Pts',(0.067457613491804,1.55511717732068,
0.276116904972495));
#261318=CARTESIAN_POINT('Ctrl Pts',(0.00940884214340416,1.55655112581271,
0.28025634100113));
#261319=CARTESIAN_POINT('Ctrl Pts',(-0.0485257237120171,1.5547429061225,
0.284395777029764));
#261320=CARTESIAN_POINT('Ctrl Pts',(-0.106511142221802,1.55293309924906,
0.28853884649047));
#261321=CARTESIAN_POINT('Ctrl Pts',(-0.164381634955927,1.54787545179417,
0.292681915951174));
#261322=CARTESIAN_POINT('Ctrl Pts',(-0.221750711946079,1.53961257196459,
0.29682498541188));
#261323=CARTESIAN_POINT('Ctrl Pts',(-0.279142820729782,1.53134637486109,
0.30096971817842));
#261324=CARTESIAN_POINT('Ctrl Pts',(-0.336032602252372,1.51987248074845,
0.305114450944961));
#261325=CARTESIAN_POINT('Ctrl Pts',(-0.392043455057559,1.50528475025376,
0.309259183711501));
#261326=CARTESIAN_POINT('Ctrl Pts',(-0.448161169267607,1.49066918827113,
0.3134118240878));
#261327=CARTESIAN_POINT('Ctrl Pts',(-0.503396107270761,1.47292807543389,
0.317564464464097));
#261328=CARTESIAN_POINT('Ctrl Pts',(-0.557387425489713,1.45220505022739,
0.321717104840396));
#261329=CARTESIAN_POINT('Ctrl Pts',(-0.607735063982491,1.43288054740007,
0.325589498465025));
#261330=CARTESIAN_POINT('Ctrl Pts',(-0.65700115741559,1.41096367186595,
0.329461892089654));
#261331=CARTESIAN_POINT('Ctrl Pts',(-0.704912530853615,1.3866068562666,
0.333334285714283));
#261332=CARTESIAN_POINT('Ctrl Pts',(-0.756323677456407,1.36047085289833,
0.33748954535419));
#261333=CARTESIAN_POINT('Ctrl Pts',(-0.806382918185656,1.33141907534589,
0.341644804994096));
#261334=CARTESIAN_POINT('Ctrl Pts',(-0.854740172399903,1.29961513060051,
0.345800064634003));
#261335=CARTESIAN_POINT('Ctrl Pts',(-0.903014298954577,1.26786585784872,
0.349948181250295));
#261336=CARTESIAN_POINT('Ctrl Pts',(-0.949591816794133,1.23337409208899,
0.354096297866587));
#261337=CARTESIAN_POINT('Ctrl Pts',(-0.994147203454296,1.19634927502966,
0.35824441448288));
#261338=CARTESIAN_POINT('Ctrl Pts',(-1.03865980786,1.15936000934277,0.362388548061566));
#261339=CARTESIAN_POINT('Ctrl Pts',(-1.08115373165124,1.11984284205106,
0.366532681640253));
#261340=CARTESIAN_POINT('Ctrl Pts',(-1.12133387389361,1.0780494391533,0.370676815218939));
#261341=CARTESIAN_POINT('Ctrl Pts',(-1.16149072443867,1.03628026313071,
0.374818546518798));
#261342=CARTESIAN_POINT('Ctrl Pts',(-1.19933609381815,0.992237840738684,
0.378960277818658));
#261343=CARTESIAN_POINT('Ctrl Pts',(-1.2346109588276,0.946211408905432,
0.383102009118517));
#261344=CARTESIAN_POINT('Ctrl Pts',(-1.26987879766862,0.900194144774516,
0.38724291545415));
#261345=CARTESIAN_POINT('Ctrl Pts',(-1.30257683354686,0.852194067482814,
0.391383821789783));
#261346=CARTESIAN_POINT('Ctrl Pts',(-1.33248704857027,0.802532563446794,
0.395524728125416));
#261347=CARTESIAN_POINT('Ctrl Pts',(-1.36242502786447,0.752824960930891,
0.399669478273095));
#261348=CARTESIAN_POINT('Ctrl Pts',(-1.38956974624266,0.701453294866358,
0.403814228420773));
#261349=CARTESIAN_POINT('Ctrl Pts',(-1.4137479156562,0.648765813662959,
0.407958978568452));
#261350=CARTESIAN_POINT('Ctrl Pts',(-1.4379364745439,0.596055692398786,
0.412105509734944));
#261351=CARTESIAN_POINT('Ctrl Pts',(-1.45915575217786,0.542029112222462,
0.416252040901436));
#261352=CARTESIAN_POINT('Ctrl Pts',(-1.47728092802937,0.487053703076643,
0.420398572067927));
#261353=CARTESIAN_POINT('Ctrl Pts',(-1.49544144876342,0.431971089488012,
0.424553189150835));
#261354=CARTESIAN_POINT('Ctrl Pts',(-1.51049567417953,0.375936451861113,
0.428707806233743));
#261355=CARTESIAN_POINT('Ctrl Pts',(-1.52236917594838,0.319331085430567,
0.432862423316651));
#261356=CARTESIAN_POINT('Ctrl Pts',(-1.53340382511625,0.266724839039212,
0.43672352030634));
#261357=CARTESIAN_POINT('Ctrl Pts',(-1.54169180343469,0.213626099992122,
0.440584617296028));
#261358=CARTESIAN_POINT('Ctrl Pts',(-1.54721364558081,0.160343958191551,
0.444445714285717));
#261359=CARTESIAN_POINT('Ctrl Pts',(-1.55269485753403,0.107453871006541,
0.448278400989242));
#261360=CARTESIAN_POINT('Ctrl Pts',(-1.55546499597033,0.0542750055122627,
0.452111087692767));
#261361=CARTESIAN_POINT('Ctrl Pts',(-1.55549967037724,0.00101264816652329,
0.455943774396293));
#261362=CARTESIAN_POINT('Ctrl Pts',(-1.55549962174471,0.001084782031638,
0.45701111646594));
#261363=CARTESIAN_POINT('Ctrl Pts',(-1.55556478756272,-0.092358326631673,
0.463326330326788));
#261364=CARTESIAN_POINT('Ctrl Pts',(-1.54720985703089,-0.185626612070271,
0.469388769574297));
#261365=CARTESIAN_POINT('Ctrl Pts',(-1.51615471673349,-0.356853835541594,
0.480887140309857));
#261366=CARTESIAN_POINT('Ctrl Pts',(-1.495645018522,-0.434871419763208,
0.486275595113444));
#261367=CARTESIAN_POINT('Ctrl Pts',(-1.4632104215784,-0.528135211178076,
0.493126909322226));
#261368=CARTESIAN_POINT('Ctrl Pts',(-1.45693067234935,-0.545219686314061,
0.494399037463768));
#261369=CARTESIAN_POINT('Ctrl Pts',(-1.44750248897834,-0.569542790921271,
0.496236682839665));
#261370=CARTESIAN_POINT('Ctrl Pts',(-1.44459632749319,-0.57687424343297,
0.496794078538821));
#261371=CARTESIAN_POINT('Ctrl Pts',(-1.43945269032168,-0.589567600206732,
0.497765371087175));
#261372=CARTESIAN_POINT('Ctrl Pts',(-1.43724067089907,-0.59493970712838,
0.498178399808053));
#261373=CARTESIAN_POINT('Ctrl Pts',(-1.43292091393862,-0.605265966163441,
0.498976163203582));
#261374=CARTESIAN_POINT('Ctrl Pts',(-1.43081744478663,-0.61022182338937,
0.499360747493974));
#261375=CARTESIAN_POINT('Ctrl Pts',(-1.42577821069415,-0.621925148668543,
0.50027307258386));
#261376=CARTESIAN_POINT('Ctrl Pts',(-1.42282023327047,-0.628662848399482,
0.500801568303666));
#261377=CARTESIAN_POINT('Ctrl Pts',(-1.41222960331019,-0.652328607565677,
0.502669591634947));
#261378=CARTESIAN_POINT('Ctrl Pts',(-1.40434202246575,-0.66914011446761,
0.504017847988341));
#261379=CARTESIAN_POINT('Ctrl Pts',(-1.34593810188269,-0.788038167100328,
0.513710469081188));
#261380=CARTESIAN_POINT('Ctrl Pts',(-1.28465389742191,-0.884425076127365,
0.522442806288046));
#261381=CARTESIAN_POINT('Ctrl Pts',(-1.17148338845351,-1.02552364289129,
0.536476917782565));
#261382=CARTESIAN_POINT('Ctrl Pts',(-1.12621258351813,-1.07504335234977,
0.541688821325403));
#261383=CARTESIAN_POINT('Ctrl Pts',(-1.06111819536346,-1.13760684771389,
0.548547534586683));
#261384=CARTESIAN_POINT('Ctrl Pts',(-1.04398946837079,-1.15334612585476,
0.550298708421727));
#261385=CARTESIAN_POINT('Ctrl Pts',(-1.01902861948883,-1.17527024941115,
0.552768101193112));
#261386=CARTESIAN_POINT('Ctrl Pts',(-1.01148081493563,-1.18177242329834,
0.553504419840321));
#261387=CARTESIAN_POINT('Ctrl Pts',(-0.999688535024922,-1.19173531451974,
0.554638156960422));
#261388=CARTESIAN_POINT('Ctrl Pts',(-0.995487539136939,-1.19524674804193,
0.555038831952612));
#261389=CARTESIAN_POINT('Ctrl Pts',(-0.987610576480531,-1.2017604267163,
0.555783986126916));
#261390=CARTESIAN_POINT('Ctrl Pts',(-0.983939256244129,-1.20476815845657,
0.556128837487998));
#261391=CARTESIAN_POINT('Ctrl Pts',(-0.977722779393625,-1.20981364090498,
0.556708554006494));
#261392=CARTESIAN_POINT('Ctrl Pts',(-0.975184902858981,-1.2118602580989,
0.556944050584216));
#261393=CARTESIAN_POINT('Ctrl Pts',(-0.970292107171644,-1.21578062688915,
0.557395792764991));
#261394=CARTESIAN_POINT('Ctrl Pts',(-0.96793818281847,-1.21765552625629,
0.55761212507198));
#261395=CARTESIAN_POINT('Ctrl Pts',(-0.961754672744856,-1.22255142679077,
0.558177834815716));
#261396=CARTESIAN_POINT('Ctrl Pts',(-0.957916250883631,-1.2255612998578,
0.5585264273765));
#261397=CARTESIAN_POINT('Ctrl Pts',(-0.944540132935304,-1.23594885892021,
0.559732555535832));
#261398=CARTESIAN_POINT('Ctrl Pts',(-0.934930539456697,-1.24323390985299,
0.560583894509932));
#261399=CARTESIAN_POINT('Ctrl Pts',(-0.845670155910563,-1.30928201112414,
0.568363473303099));
#261400=CARTESIAN_POINT('Ctrl Pts',(-0.760652362002066,-1.36043801285723,
0.574852016429284));
#261401=CARTESIAN_POINT('Ctrl Pts',(-0.5663806517194,-1.45338589709508,
0.58902664040184));
#261402=CARTESIAN_POINT('Ctrl Pts',(-0.456139335157796,-1.49165982425734,
0.596697567974007));
#261403=CARTESIAN_POINT('Ctrl Pts',(-0.329632462533139,-1.52023069026283,
0.60575448640276));
#261404=CARTESIAN_POINT('Ctrl Pts',(-0.316557342524543,-1.52300700633236,
0.606692991139996));
#261405=CARTESIAN_POINT('Ctrl Pts',(-0.29657088110863,-1.52698236214167,
0.608132008131028));
#261406=CARTESIAN_POINT('Ctrl Pts',(-0.289684276929093,-1.5283037782484,
0.608628637152534));
#261407=CARTESIAN_POINT('Ctrl Pts',(-0.277131991510636,-1.53062444960719,
0.609535405835375));
#261408=CARTESIAN_POINT('Ctrl Pts',(-0.271469220883094,-1.53163892838432,
0.609945055743816));
#261409=CARTESIAN_POINT('Ctrl Pts',(-0.259214779273337,-1.53376420336377,
0.61083286000168));
#261410=CARTESIAN_POINT('Ctrl Pts',(-0.252621338661832,-1.53486396465486,
0.611311354156501));
#261411=CARTESIAN_POINT('Ctrl Pts',(-0.234653516730676,-1.53774201824591,
0.612617632606351));
#261412=CARTESIAN_POINT('Ctrl Pts',(-0.223266352886277,-1.53943655603616,
0.613448031172105));
#261413=CARTESIAN_POINT('Ctrl Pts',(-0.165196978701336,-1.547420099724,
0.617696485776978));
#261414=CARTESIAN_POINT('Ctrl Pts',(-0.118269986974262,-1.55171207053808,
0.621176149199674));
#261415=CARTESIAN_POINT('Ctrl Pts',(0.0776121458416323,-1.56069074976918,
0.635906204788179));
#261416=CARTESIAN_POINT('Ctrl Pts',(0.226628083829469,-1.54609452974489,
0.647699001427363));
#261417=CARTESIAN_POINT('Ctrl Pts',(0.400224041998137,-1.50342586392974,
0.661210471652759));
#261418=CARTESIAN_POINT('Ctrl Pts',(0.42896008176016,-1.4954805807889,0.663435421038839));
#261419=CARTESIAN_POINT('Ctrl Pts',(0.463704861335473,-1.48478983238796,
0.6660974766062));
#261420=CARTESIAN_POINT('Ctrl Pts',(0.469945298320114,-1.48282651224931,
0.66657447812802));
#261421=CARTESIAN_POINT('Ctrl Pts',(0.479711343937671,-1.47968614527584,
0.667319002318261));
#261422=CARTESIAN_POINT('Ctrl Pts',(0.483245339847857,-1.47853576362622,
0.667588014762107));
#261423=CARTESIAN_POINT('Ctrl Pts',(0.489851787363023,-1.47635902448932,
0.668090103164967));
#261424=CARTESIAN_POINT('Ctrl Pts',(0.492925129760577,-1.47533574469503,
0.668323344702695));
#261425=CARTESIAN_POINT('Ctrl Pts',(0.499925620123423,-1.47298059041426,
0.668853888605112));
#261426=CARTESIAN_POINT('Ctrl Pts',(0.503850651445381,-1.47164260861902,
0.669150829604249));
#261427=CARTESIAN_POINT('Ctrl Pts',(0.51424635642346,-1.46805240901666,
0.669936024435849));
#261428=CARTESIAN_POINT('Ctrl Pts',(0.520707676404355,-1.46577307622874,
0.67042274041432));
#261429=CARTESIAN_POINT('Ctrl Pts',(0.567575198396854,-1.44889079255949,
0.673945068790048));
#261430=CARTESIAN_POINT('Ctrl Pts',(0.607380539713545,-1.43266040582839,
0.676892920079519));
#261431=CARTESIAN_POINT('Ctrl Pts',(0.747361424869308,-1.36869874581491,
0.687276342988381));
#261432=CARTESIAN_POINT('Ctrl Pts',(0.843039364190159,-1.31193479532248,
0.694426294518487));
#261433=CARTESIAN_POINT('Ctrl Pts',(0.982647523431453,-1.20747919055378,
0.70604754353356));
#261434=CARTESIAN_POINT('Ctrl Pts',(1.03104924552293,-1.16642105784593,
0.710338162096891));
#261435=CARTESIAN_POINT('Ctrl Pts',(1.08846185699101,-1.11134687965338,
0.715873791633387));
#261436=CARTESIAN_POINT('Ctrl Pts',(1.09994191376926,-1.09998584230692,
0.717004875541091));
#261437=CARTESIAN_POINT('Ctrl Pts',(1.11652765822755,-1.08305276127474,
0.718676369477237));
#261438=CARTESIAN_POINT('Ctrl Pts',(1.12177323737976,-1.07761871530082,
0.719210667734281));
#261439=CARTESIAN_POINT('Ctrl Pts',(1.13097290706534,-1.06794855221589,
0.720157921503731));
#261440=CARTESIAN_POINT('Ctrl Pts',(1.13494332232841,-1.06372810442214,
0.720570164248097));
#261441=CARTESIAN_POINT('Ctrl Pts',(1.14266501472118,-1.0554277007378,0.721378698299613));
#261442=CARTESIAN_POINT('Ctrl Pts',(1.14641825408431,-1.05134968140428,
0.721774897393359));
#261443=CARTESIAN_POINT('Ctrl Pts',(1.15651984933984,-1.04025555278575,
0.722850019852584));
#261444=CARTESIAN_POINT('Ctrl Pts',(1.16282602213382,-1.03320153499968,
0.723530700116591));
#261445=CARTESIAN_POINT('Ctrl Pts',(1.18645679048247,-1.00627802557985,
0.726118137399223));
#261446=CARTESIAN_POINT('Ctrl Pts',(1.20333874726648,-0.986027830375289,
0.728042874818006));
#261447=CARTESIAN_POINT('Ctrl Pts',(1.3259517603024,-0.831110696873445,
0.742620883490304));
#261448=CARTESIAN_POINT('Ctrl Pts',(1.40930272161761,-0.68024490813505,
0.756195352769671));
#261449=CARTESIAN_POINT('Ctrl Pts',(1.4775797733656,-0.48730148935837,0.7717212422228));
#261450=CARTESIAN_POINT('Ctrl Pts',(1.48774236961112,-0.455332621677893,
0.774231956399745));
#261451=CARTESIAN_POINT('Ctrl Pts',(1.49869891412714,-0.416566101032296,
0.777183870802785));
#261452=CARTESIAN_POINT('Ctrl Pts',(1.50049132328187,-0.410062854876716,
0.777675970128448));
#261453=CARTESIAN_POINT('Ctrl Pts',(1.50321422759375,-0.399926614190292,
0.778437952446022));
#261454=CARTESIAN_POINT('Ctrl Pts',(1.50417395767503,-0.396301673775831,
0.778709457725458));
#261455=CARTESIAN_POINT('Ctrl Pts',(1.50593359648075,-0.389556960175037,
0.779212736876146));
#261456=CARTESIAN_POINT('Ctrl Pts',(1.50673691828212,-0.386438199026311,
0.779444697140971));
#261457=CARTESIAN_POINT('Ctrl Pts',(1.5085472860492,-0.379318280836124,
0.779972542843319));
#261458=CARTESIAN_POINT('Ctrl Pts',(1.50954810254671,-0.375315599970667,
0.780268068227494));
#261459=CARTESIAN_POINT('Ctrl Pts',(1.51212031595461,-0.364851501223028,
0.78103758624613));
#261460=CARTESIAN_POINT('Ctrl Pts',(1.51366624885886,-0.358383815372678,
0.781510166402932));
#261461=CARTESIAN_POINT('Ctrl Pts',(1.52391556767919,-0.314254258189725,
0.784715160089142));
#261462=CARTESIAN_POINT('Ctrl Pts',(1.53125484938355,-0.276285368156949,
0.787376444756763));
#261463=CARTESIAN_POINT('Ctrl Pts',(1.56009630481926,-0.0900684029963861,
0.800138251818949));
#261464=CARTESIAN_POINT('Ctrl Pts',(1.5615253191562,0.0604792571434754,
0.809644097899242));
#261465=CARTESIAN_POINT('Ctrl Pts',(1.53794014872663,0.234491756868512,
0.821587607966767));
#261466=CARTESIAN_POINT('Ctrl Pts',(1.53383820216485,0.259974099753254,
0.823358629138951));
#261467=CARTESIAN_POINT('Ctrl Pts',(1.52567544239771,0.303717167850341,
0.826445174071594));
#261468=CARTESIAN_POINT('Ctrl Pts',(1.52191559076324,0.322028812019329,
0.827751418801301));
#261469=CARTESIAN_POINT('Ctrl Pts',(1.51607662230241,0.348074615712525,
0.829631715009493));
#261470=CARTESIAN_POINT('Ctrl Pts',(1.5142662595924,0.355867887778959,0.830197200003529));
#261471=CARTESIAN_POINT('Ctrl Pts',(1.51102638306974,0.36934243790031,0.831180071202483));
#261472=CARTESIAN_POINT('Ctrl Pts',(1.50962473352477,0.375030304084151,
0.83159655633343));
#261473=CARTESIAN_POINT('Ctrl Pts',(1.50686844770303,0.385949389414232,
0.832399225539762));
#261474=CARTESIAN_POINT('Ctrl Pts',(1.50551861245698,0.39118174300281,0.832785249448855));
#261475=CARTESIAN_POINT('Ctrl Pts',(1.50226905505131,0.403511988455546,
0.833698269500556));
#261476=CARTESIAN_POINT('Ctrl Pts',(1.50034626408984,0.410603608100247,
0.834226004733339));
#261477=CARTESIAN_POINT('Ctrl Pts',(1.49344662401361,0.435355107610311,
0.836077292494928));
#261478=CARTESIAN_POINT('Ctrl Pts',(1.48820780252188,0.452939699594645,
0.837409280222865));
#261479=CARTESIAN_POINT('Ctrl Pts',(1.46857535280717,0.514815922319064,
0.842157835421304));
#261480=CARTESIAN_POINT('Ctrl Pts',(1.45252572406699,0.558484750630163,
0.84562283105088));
#261481=CARTESIAN_POINT('Ctrl Pts',(1.43457651222198,0.60130730960218,0.849135319448207));
#261482=CARTESIAN_POINT('Origin',(0.,0.,-1.29405622560371));
#261483=CARTESIAN_POINT('',(1.4345768916211,0.601306404445136,1.68861155768855));
#261484=CARTESIAN_POINT('',(1.4345766830264,0.601306902103224,1.55150291788058));
#261485=CARTESIAN_POINT('',(1.43457668357355,0.601306900797845,-1.29405622560371));
#261486=CARTESIAN_POINT('Ctrl Pts',(1.43457689162107,0.601306404445218,
1.68861155768856));
#261487=CARTESIAN_POINT('Ctrl Pts',(1.46947702985195,0.518042811291588,
1.68163625042359));
#261488=CARTESIAN_POINT('Ctrl Pts',(1.49709936625474,0.43181080253797,1.67456902722138));
#261489=CARTESIAN_POINT('Ctrl Pts',(1.52411100373657,0.312534953445863,
1.66530616586023));
#261490=CARTESIAN_POINT('Ctrl Pts',(1.53018504882352,0.281294393143988,
1.6629273033566));
#261491=CARTESIAN_POINT('Ctrl Pts',(1.53635576224867,0.243381714307792,
1.66011367482268));
#261492=CARTESIAN_POINT('Ctrl Pts',(1.53737320840994,0.236869815059113,
1.65963300038737));
#261493=CARTESIAN_POINT('Ctrl Pts',(1.53889542922779,0.226704014713604,
1.65888686010136));
#261494=CARTESIAN_POINT('Ctrl Pts',(1.53942863370877,0.22305455582014,1.65861985209019));
#261495=CARTESIAN_POINT('Ctrl Pts',(1.54039792179454,0.21625130867358,1.65812372998711));
#261496=CARTESIAN_POINT('Ctrl Pts',(1.54083729919612,0.213098108130243,
1.65789444121242));
#261497=CARTESIAN_POINT('Ctrl Pts',(1.54181982153206,0.205885075323176,
1.65737141436685));
#261498=CARTESIAN_POINT('Ctrl Pts',(1.54235661422442,0.201824433371913,
1.65707803584684));
#261499=CARTESIAN_POINT('Ctrl Pts',(1.54372048119464,0.191183950640804,
1.65631194094036));
#261500=CARTESIAN_POINT('Ctrl Pts',(1.54452154029196,0.184600765889703,
1.65584063722624));
#261501=CARTESIAN_POINT('Ctrl Pts',(1.54976293713854,0.139101556098071,
1.65260043595468));
#261502=CARTESIAN_POINT('Ctrl Pts',(1.55277456447938,0.100031003265328,
1.64990466842952));
#261503=CARTESIAN_POINT('Ctrl Pts',(1.56016830440318,-0.0887222602398739,
1.63711712084431));
#261504=CARTESIAN_POINT('Ctrl Pts',(1.54439998293609,-0.238393758104582,
1.62761359938984));
#261505=CARTESIAN_POINT('Ctrl Pts',(1.4978912336626,-0.421206422828224,
1.61478063638543));
#261506=CARTESIAN_POINT('Ctrl Pts',(1.48689220023166,-0.458523882902704,
1.61209884915661));
#261507=CARTESIAN_POINT('Ctrl Pts',(1.47119250802525,-0.505253580466083,
1.60864153569624));
#261508=CARTESIAN_POINT('Ctrl Pts',(1.46777896106303,-0.515085903845827,
1.60790845192241));
#261509=CARTESIAN_POINT('Ctrl Pts',(1.4621372395123,-0.530824624202725,
1.60672555992134));
#261510=CARTESIAN_POINT('Ctrl Pts',(1.45997128996035,-0.536753126851962,
1.60627781758587));
#261511=CARTESIAN_POINT('Ctrl Pts',(1.45578092220531,-0.548009709820546,
1.60542346358882));
#261512=CARTESIAN_POINT('Ctrl Pts',(1.45376317860275,-0.553340179694012,
1.60501708030802));
#261513=CARTESIAN_POINT('Ctrl Pts',(1.44909161791738,-0.565479563135545,
1.6040873953556));
#261514=CARTESIAN_POINT('Ctrl Pts',(1.44641903938144,-0.5722810608259,1.60356347223093));
#261515=CARTESIAN_POINT('Ctrl Pts',(1.43932985624929,-0.589955541496785,
1.6021939266074));
#261516=CARTESIAN_POINT('Ctrl Pts',(1.43483802551425,-0.600797638584102,
1.60134579023391));
#261517=CARTESIAN_POINT('Ctrl Pts',(1.39944658893884,-0.683562043775598,
1.59480835568747));
#261518=CARTESIAN_POINT('Ctrl Pts',(1.36328550187317,-0.753098071601887,
1.5889393615278));
#261519=CARTESIAN_POINT('Ctrl Pts',(1.26525957859566,-0.911216729579384,
1.57469059987665));
#261520=CARTESIAN_POINT('Ctrl Pts',(1.19910246823174,-0.996669405168262,
1.56622513101214));
#261521=CARTESIAN_POINT('Ctrl Pts',(1.09860471082236,-1.10184787091824,
1.55515355218109));
#261522=CARTESIAN_POINT('Ctrl Pts',(1.07157998861481,-1.12814801935732,
1.5523232740925));
#261523=CARTESIAN_POINT('Ctrl Pts',(1.03850671127694,-1.15807239764615,
1.54905389778769));
#261524=CARTESIAN_POINT('Ctrl Pts',(1.03335890032715,-1.16266816221884,
1.54855035221874));
#261525=CARTESIAN_POINT('Ctrl Pts',(1.02536270944577,-1.1697117873204,1.54777659413747));
#261526=CARTESIAN_POINT('Ctrl Pts',(1.02253585091559,-1.17218376789684,
1.54750465378764));
#261527=CARTESIAN_POINT('Ctrl Pts',(1.01730113813029,-1.17672797861439,
1.54700407515689));
#261528=CARTESIAN_POINT('Ctrl Pts',(1.01489590356021,-1.17880305675275,
1.54677523240642));
#261529=CARTESIAN_POINT('Ctrl Pts',(1.00944435880158,-1.18347723716559,
1.54625915666706));
#261530=CARTESIAN_POINT('Ctrl Pts',(1.00639436303822,-1.18607195035641,
1.54597224579061));
#261531=CARTESIAN_POINT('Ctrl Pts',(0.997143947400219,-1.19388015411474,
1.54510742757344));
#261532=CARTESIAN_POINT('Ctrl Pts',(0.990912657518758,-1.19905712412734,
1.5445321010844));
#261533=CARTESIAN_POINT('Ctrl Pts',(0.92541120981102,-1.25261649877008,
1.53855602084028));
#261534=CARTESIAN_POINT('Ctrl Pts',(0.862679011506789,-1.29661968602737,
1.53343762221019));
#261535=CARTESIAN_POINT('Ctrl Pts',(0.738559735937297,-1.37066889415537,
1.52387977958753));
#261536=CARTESIAN_POINT('Ctrl Pts',(0.67794524001386,-1.40163973610215,
1.51943809280941));
#261537=CARTESIAN_POINT('Ctrl Pts',(0.567678406388989,-1.44914898940796,
1.51146861785002));
#261538=CARTESIAN_POINT('Ctrl Pts',(0.518857327712806,-1.46733701175572,
1.50797639726936));
#261539=CARTESIAN_POINT('Ctrl Pts',(0.43938951931784,-1.492479811296,1.5022683428947));
#261540=CARTESIAN_POINT('Ctrl Pts',(0.409283745432885,-1.50101489646662,
1.50010099034716));
#261541=CARTESIAN_POINT('Ctrl Pts',(0.369570520878116,-1.51099015944331,
1.49722571107295));
#261542=CARTESIAN_POINT('Ctrl Pts',(0.360176691740485,-1.51325687675424,
1.49654442952803));
#261543=CARTESIAN_POINT('Ctrl Pts',(0.344772843703926,-1.51682224888713,
1.49542510164577));
#261544=CARTESIAN_POINT('Ctrl Pts',(0.338775061828581,-1.51817308103593,
1.49498873392159));
#261545=CARTESIAN_POINT('Ctrl Pts',(0.327153392927051,-1.52071823852205,
1.49414208908193));
#261546=CARTESIAN_POINT('Ctrl Pts',(0.321530573539484,-1.52191701223284,
1.49373196180002));
#261547=CARTESIAN_POINT('Ctrl Pts',(0.308527789413606,-1.52461390547677,
1.4927823166758));
#261548=CARTESIAN_POINT('Ctrl Pts',(0.301143386536314,-1.52608964830419,
1.49224209532387));
#261549=CARTESIAN_POINT('Ctrl Pts',(0.277256729467131,-1.53068318037579,
1.4904915009633));
#261550=CARTESIAN_POINT('Ctrl Pts',(0.260715127902871,-1.53358725662914,
1.48927440076023));
#261551=CARTESIAN_POINT('Ctrl Pts',(0.106842591276076,-1.55804005939559,
1.47790392897099));
#261552=CARTESIAN_POINT('Ctrl Pts',(-0.032722773851731,-1.56135060755476,
1.46714572098148));
#261553=CARTESIAN_POINT('Ctrl Pts',(-0.240844015057567,-1.5383550710855,
1.45092701946117));
#261554=CARTESIAN_POINT('Ctrl Pts',(-0.310260935249755,-1.52587110136056,
1.44550465560754));
#261555=CARTESIAN_POINT('Ctrl Pts',(-0.390844694214705,-1.50564938384172,
1.43935027825852));
#261556=CARTESIAN_POINT('Ctrl Pts',(-0.40305275318308,-1.50242741842925,
1.43842191607972));
#261557=CARTESIAN_POINT('Ctrl Pts',(-0.419834660048688,-1.49777903234407,
1.43715250077954));
#261558=CARTESIAN_POINT('Ctrl Pts',(-0.424442734661721,-1.49647971524599,
1.43680464517902));
#261559=CARTESIAN_POINT('Ctrl Pts',(-0.432210598619843,-1.49425068039647,
1.43621954316593));
#261560=CARTESIAN_POINT('Ctrl Pts',(-0.435373537421865,-1.4933321737233,
1.43598165949231));
#261561=CARTESIAN_POINT('Ctrl Pts',(-0.441396814462889,-1.49156227093823,
1.43552936711224));
#261562=CARTESIAN_POINT('Ctrl Pts',(-0.444257644164275,-1.49071268255076,
1.43531485230392));
#261563=CARTESIAN_POINT('Ctrl Pts',(-0.45179755210692,-1.4884499025236,
1.43475025069703));
#261564=CARTESIAN_POINT('Ctrl Pts',(-0.456472496883849,-1.48702286523591,
1.43440096272407));
#261565=CARTESIAN_POINT('Ctrl Pts',(-0.472917467684116,-1.48191814020581,
1.43317477187758));
#261566=CARTESIAN_POINT('Ctrl Pts',(-0.48465081702012,-1.47812242940753,
1.43230440566613));
#261567=CARTESIAN_POINT('Ctrl Pts',(-0.573096397349444,-1.44834404074764,
1.42576895241146));
#261568=CARTESIAN_POINT('Ctrl Pts',(-0.647730605375835,-1.41654114789611,
1.42039554307145));
#261569=CARTESIAN_POINT('Ctrl Pts',(-0.789923212516117,-1.34234906570331,
1.40982159961455));
#261570=CARTESIAN_POINT('Ctrl Pts',(-0.857373351170098,-1.3003037932978,
1.40463336501362));
#261571=CARTESIAN_POINT('Ctrl Pts',(-0.967449016110154,-1.21938532508896,
1.39546327076228));
#261572=CARTESIAN_POINT('Ctrl Pts',(-1.01166641417249,-1.18295730768821,
1.39155692237752));
#261573=CARTESIAN_POINT('Ctrl Pts',(-1.06235332445162,-1.1362753902485,
1.38673354107849));
#261574=CARTESIAN_POINT('Ctrl Pts',(-1.0708451767133,-1.12827609336263,
1.38591303010189));
#261575=CARTESIAN_POINT('Ctrl Pts',(-1.08399003772638,-1.11561160094031,
1.3846227937056));
#261576=CARTESIAN_POINT('Ctrl Pts',(-1.08870487708301,-1.11101095144756,
1.38415586041571));
#261577=CARTESIAN_POINT('Ctrl Pts',(-1.09701426352902,-1.10279912742805,
1.38332545373235));
#261578=CARTESIAN_POINT('Ctrl Pts',(-1.10062058289263,-1.0991999550681,
1.38296251096572));
#261579=CARTESIAN_POINT('Ctrl Pts',(-1.10889608061512,-1.09085930117704,
1.38212372074988));
#261580=CARTESIAN_POINT('Ctrl Pts',(-1.11355261563634,-1.08610547472691,
1.3816473280956));
#261581=CARTESIAN_POINT('Ctrl Pts',(-1.12627847264442,-1.07294586165086,
1.3803330570039));
#261582=CARTESIAN_POINT('Ctrl Pts',(-1.13428392403261,-1.06447920877463,
1.37949244521473));
#261583=CARTESIAN_POINT('Ctrl Pts',(-1.17659177373673,-1.01871477913086,
1.37497402674284));
#261584=CARTESIAN_POINT('Ctrl Pts',(-1.20914748061511,-0.979851669508349,
1.37122404324996));
#261585=CARTESIAN_POINT('Ctrl Pts',(-1.32874744011104,-0.822025411168555,
1.35630750471059));
#261586=CARTESIAN_POINT('Ctrl Pts',(-1.40059358326385,-0.692548704305531,
1.34463305868347));
#261587=CARTESIAN_POINT('Ctrl Pts',(-1.46344952503628,-0.527947840398722,
1.33132394168275));
#261588=CARTESIAN_POINT('Ctrl Pts',(-1.47299520060752,-0.500698369684845,
1.32917043733586));
#261589=CARTESIAN_POINT('Ctrl Pts',(-1.48372638718087,-0.467094522767675,
1.32658763593252));
#261590=CARTESIAN_POINT('Ctrl Pts',(-1.48563744191302,-0.460980129983615,
1.32612059549288));
#261591=CARTESIAN_POINT('Ctrl Pts',(-1.48857736898995,-0.451365674866176,
1.32539095751953));
#261592=CARTESIAN_POINT('Ctrl Pts',(-1.48963176629998,-0.44787359543901,
1.32512692426015));
#261593=CARTESIAN_POINT('Ctrl Pts',(-1.49158520023677,-0.441320763556021,
1.32463334585756));
#261594=CARTESIAN_POINT('Ctrl Pts',(-1.49248709623981,-0.438260988160894,
1.32440364433014));
#261595=CARTESIAN_POINT('Ctrl Pts',(-1.49452372650491,-0.431272308302537,
1.32388072335258));
#261596=CARTESIAN_POINT('Ctrl Pts',(-1.49565238449056,-0.427341688574858,
1.3235878583072));
#261597=CARTESIAN_POINT('Ctrl Pts',(-1.49860481923419,-0.416904669953052,
1.32281338064514));
#261598=CARTESIAN_POINT('Ctrl Pts',(-1.50040175098156,-0.410390665213693,
1.32233326918413));
#261599=CARTESIAN_POINT('Ctrl Pts',(-1.51309915801623,-0.36316327768386,
1.31887454049316));
#261600=CARTESIAN_POINT('Ctrl Pts',(-1.52238455704785,-0.322028997005506,
1.31598072507761));
#261601=CARTESIAN_POINT('Ctrl Pts',(-1.54687992645591,-0.188449381937575,
1.3068121129331));
#261602=CARTESIAN_POINT('Ctrl Pts',(-1.55541936552532,-0.094992260473266,
1.3007353902558));
#261603=CARTESIAN_POINT('Ctrl Pts',(-1.55557348769334,0.085302141614542,
1.28881070820183));
#261604=CARTESIAN_POINT('Ctrl Pts',(-1.54841048352085,0.171775820456287,
1.28300010839956));
#261605=CARTESIAN_POINT('Ctrl Pts',(-1.53212304440099,0.268925011977032,
1.27612020331118));
#261606=CARTESIAN_POINT('Ctrl Pts',(-1.53002224142329,0.280630739985389,
1.27528554538495));
#261607=CARTESIAN_POINT('Ctrl Pts',(-1.52640536660373,0.299534636872861,
1.27392785856942));
#261608=CARTESIAN_POINT('Ctrl Pts',(-1.52497206801355,0.306748317530233,
1.27340745450651));
#261609=CARTESIAN_POINT('Ctrl Pts',(-1.52233616893067,0.319539339119536,
1.27248045259176));
#261610=CARTESIAN_POINT('Ctrl Pts',(-1.52115392963752,0.325120779465095,
1.27207451030199));
#261611=CARTESIAN_POINT('Ctrl Pts',(-1.51860446781096,0.33683860255135,
1.27121917272598));
#261612=CARTESIAN_POINT('Ctrl Pts',(-1.51723069829119,0.342973438976443,
1.27076957468061));
#261613=CARTESIAN_POINT('Ctrl Pts',(-1.51350931723417,0.359131983730321,
1.26958056130195));
#261614=CARTESIAN_POINT('Ctrl Pts',(-1.51109935284875,0.36914085582507,
1.26883916035103));
#261615=CARTESIAN_POINT('Ctrl Pts',(-1.49942019375988,0.415613846987299,
1.26537320132012));
#261616=CARTESIAN_POINT('Ctrl Pts',(-1.4889300865898,0.451754947024388,
1.26260974702371));
#261617=CARTESIAN_POINT('Ctrl Pts',(-1.42994710317126,0.630483563644251,
1.24858609467863));
#261618=CARTESIAN_POINT('Ctrl Pts',(-1.36223632885688,0.765869029319142,
1.2366981416937));
#261619=CARTESIAN_POINT('Ctrl Pts',(-1.25342286279638,0.92200490502971,
1.22218514922512));
#261620=CARTESIAN_POINT('Ctrl Pts',(-1.2294382870733,0.953752631892701,
1.21919274905108));
#261621=CARTESIAN_POINT('Ctrl Pts',(-1.20004644150441,0.989703549733059,
1.21578522031566));
#261622=CARTESIAN_POINT('Ctrl Pts',(-1.19579916855584,0.994831106691519,
1.21529875563426));
#261623=CARTESIAN_POINT('Ctrl Pts',(-1.18888095655569,1.00307485364047,
1.21451611628556));
#261624=CARTESIAN_POINT('Ctrl Pts',(-1.18623043963367,1.00620794868729,
1.21421854255951));
#261625=CARTESIAN_POINT('Ctrl Pts',(-1.18150126728005,1.01175350031487,
1.21369167087887));
#261626=CARTESIAN_POINT('Ctrl Pts',(-1.17942757545345,1.01417009665563,
1.21346202045505));
#261627=CARTESIAN_POINT('Ctrl Pts',(-1.17493963846848,1.01936777371926,
1.21296797429861));
#261628=CARTESIAN_POINT('Ctrl Pts',(-1.17252293641021,1.02214665116949,
1.21270376409842));
#261629=CARTESIAN_POINT('Ctrl Pts',(-1.16577010957281,1.02985601532426,
1.21197047833673));
#261630=CARTESIAN_POINT('Ctrl Pts',(-1.16141253366209,1.03476774757171,
1.21150295529719));
#261631=CARTESIAN_POINT('Ctrl Pts',(-1.13603727428098,1.06300775983557,
1.20881193715266));
#261632=CARTESIAN_POINT('Ctrl Pts',(-1.11434635301835,1.08572498707744,
1.20663525466513));
#261633=CARTESIAN_POINT('Ctrl Pts',(-0.98805269827552,1.21021832758287,
1.19452812336636));
#261634=CARTESIAN_POINT('Ctrl Pts',(-0.870219668701142,1.29753718960344,
1.18526742193276));
#261635=CARTESIAN_POINT('Ctrl Pts',(-0.69850814393012,1.39072194000651,
1.1720915300266));
#261636=CARTESIAN_POINT('Ctrl Pts',(-0.653991108301251,1.41220251344607,
1.16870808846952));
#261637=CARTESIAN_POINT('Ctrl Pts',(-0.597888450156065,1.43605131667649,
1.16444121945438));
#261638=CARTESIAN_POINT('Ctrl Pts',(-0.587195965302839,1.44045647921834,
1.16362794962157));
#261639=CARTESIAN_POINT('Ctrl Pts',(-0.570293514032257,1.44720059922895,
1.16234177608077));
#261640=CARTESIAN_POINT('Ctrl Pts',(-0.56411584152675,1.44961980581849,
1.16187157423817));
#261641=CARTESIAN_POINT('Ctrl Pts',(-0.552688576281814,1.4540106711347,
1.16100149744248));
#261642=CARTESIAN_POINT('Ctrl Pts',(-0.54744341125555,1.45599361402702,
1.16060200790133));
#261643=CARTESIAN_POINT('Ctrl Pts',(-0.535798177752869,1.46032429099681,
1.15971473977937));
#261644=CARTESIAN_POINT('Ctrl Pts',(-0.529393198540841,1.46265838826402,
1.15922651632774));
#261645=CARTESIAN_POINT('Ctrl Pts',(-0.510974953709208,1.46923352475853,
1.15782182289244));
#261646=CARTESIAN_POINT('Ctrl Pts',(-0.498924905618295,1.47336908959832,
1.15690189176821));
#261647=CARTESIAN_POINT('Ctrl Pts',(-0.404891761676893,1.50435536065194,
1.14971427206073));
#261648=CARTESIAN_POINT('Ctrl Pts',(-0.320869261092523,1.52448691265095,
1.14322671525037));
#261649=CARTESIAN_POINT('Ctrl Pts',(-0.156310616436556,1.54970506991017,
1.13043476339516));
#261650=CARTESIAN_POINT('Ctrl Pts',(-0.0761772999499947,1.55570410311018,
1.12417006138014));
#261651=CARTESIAN_POINT('Ctrl Pts',(0.0600159012072503,1.55534866897435,
1.11368697014316));
#261652=CARTESIAN_POINT('Ctrl Pts',(0.115931073947269,1.55218328581326,
1.10943274265708));
#261653=CARTESIAN_POINT('Ctrl Pts',(0.179369142170793,1.54514358233649,
1.10474350499066));
#261654=CARTESIAN_POINT('Ctrl Pts',(0.187171545926944,1.54421785980289,
1.10416917537605));
#261655=CARTESIAN_POINT('Ctrl Pts',(0.198942925122992,1.54273070375616,
1.10330666627319));
#261656=CARTESIAN_POINT('Ctrl Pts',(0.202917137718063,1.54221300343609,
1.10301615429863));
#261657=CARTESIAN_POINT('Ctrl Pts',(0.21003819328198,1.54125737663815,1.10249689241487));
#261658=CARTESIAN_POINT('Ctrl Pts',(0.213185721119119,1.54082516614265,
1.102267830215));
#261659=CARTESIAN_POINT('Ctrl Pts',(0.220048544778588,1.53986134865761,
1.10176937874498));
#261660=CARTESIAN_POINT('Ctrl Pts',(0.223763242681018,1.53932593922779,
1.10150020595733));
#261661=CARTESIAN_POINT('Ctrl Pts',(0.234291303737873,1.53776958551781,
1.10073901430338));
#261662=CARTESIAN_POINT('Ctrl Pts',(0.241099988262787,1.53671679678208,
1.1002487450018));
#261663=CARTESIAN_POINT('Ctrl Pts',(0.28486852338225,1.52965105171671,1.09710873078209));
#261664=CARTESIAN_POINT('Ctrl Pts',(0.321611753136779,1.52234978643954,
1.09452597050568));
#261665=CARTESIAN_POINT('Ctrl Pts',(0.446436204462301,1.49282365835129,
1.08582332454664));
#261666=CARTESIAN_POINT('Ctrl Pts',(0.532819344676398,1.46421784164596,
1.07991637005052));
#261667=CARTESIAN_POINT('Ctrl Pts',(0.703502164570861,1.39057602712734,
1.06765060524126));
#261668=CARTESIAN_POINT('Ctrl Pts',(0.787136958830996,1.34500123516558,
1.06130476085849));
#261669=CARTESIAN_POINT('Ctrl Pts',(0.876016849973839,1.28542512671853,
1.05383229113049));
#261670=CARTESIAN_POINT('Ctrl Pts',(0.885873630831345,1.27865209264722,
1.0529930084074));
#261671=CARTESIAN_POINT('Ctrl Pts',(0.901616177077629,1.26756528408968,
1.05163482202807));
#261672=CARTESIAN_POINT('Ctrl Pts',(0.90755153417416,1.26332248050222,1.05111861572351));
#261673=CARTESIAN_POINT('Ctrl Pts',(0.918081768272671,1.2556825902466,1.05019525393344));
#261674=CARTESIAN_POINT('Ctrl Pts',(0.92268822089766,1.25230161946119,1.04978872487825));
#261675=CARTESIAN_POINT('Ctrl Pts',(0.932298319974304,1.24516634357961,
1.04893507346716));
#261676=CARTESIAN_POINT('Ctrl Pts',(0.937298146254264,1.24140709017123,
1.04848776320533));
#261677=CARTESIAN_POINT('Ctrl Pts',(0.950351644777962,1.23146865340416,
1.04731145205751));
#261678=CARTESIAN_POINT('Ctrl Pts',(0.958367625511021,1.2252407022056,1.04658054199366));
#261679=CARTESIAN_POINT('Ctrl Pts',(0.994582899057056,1.19653070897553,
1.04323856656561));
#261680=CARTESIAN_POINT('Ctrl Pts',(1.02205382972573,1.17315235604944,1.04059192817647));
#261681=CARTESIAN_POINT('Ctrl Pts',(1.14870224678509,1.05754521446165,1.02783211658105));
#261682=CARTESIAN_POINT('Ctrl Pts',(1.23635695789021,0.953586940733363,
1.01722326506742));
#261683=CARTESIAN_POINT('Ctrl Pts',(1.33955176781088,0.792650913198052,
1.00250881300004));
#261684=CARTESIAN_POINT('Ctrl Pts',(1.36712815246778,0.744081036960375,
0.998266531269419));
#261685=CARTESIAN_POINT('Ctrl Pts',(1.39554107001377,0.687100459326392,
0.993588779202292));
#261686=CARTESIAN_POINT('Ctrl Pts',(1.39899222286615,0.680046091520333,
0.993014731862127));
#261687=CARTESIAN_POINT('Ctrl Pts',(1.40412343565381,0.669353182435813,
0.992152560980039));
#261688=CARTESIAN_POINT('Ctrl Pts',(1.4058430349553,0.665733931413195,0.991862107628564));
#261689=CARTESIAN_POINT('Ctrl Pts',(1.40890082906937,0.65923349061345,0.991342931714634));
#261690=CARTESIAN_POINT('Ctrl Pts',(1.41024419491643,0.65635482220917,0.991113896958817));
#261691=CARTESIAN_POINT('Ctrl Pts',(1.41315528437642,0.650066515635028,
0.99061549895062));
#261692=CARTESIAN_POINT('Ctrl Pts',(1.41471948915563,0.646655318017194,
0.990346352190897));
#261693=CARTESIAN_POINT('Ctrl Pts',(1.41912069779765,0.63696481244076,0.989585115389858));
#261694=CARTESIAN_POINT('Ctrl Pts',(1.42192839346087,0.630672161887732,
0.989094776230573));
#261695=CARTESIAN_POINT('Ctrl Pts',(1.42805041300984,0.616702667701304,
0.988014564795362));
#261696=CARTESIAN_POINT('Ctrl Pts',(1.43134466050347,0.609017746848256,
0.987425839742894));
#261697=CARTESIAN_POINT('Ctrl Pts',(1.43457668375786,0.601306900358119,
0.986840263175809));
#261698=CARTESIAN_POINT('Ctrl Pts',(1.43457651222198,0.60130730960218,0.849135319448207));
#261699=CARTESIAN_POINT('Ctrl Pts',(1.38252124128554,0.725498830028205,
0.859322036099769));
#261700=CARTESIAN_POINT('Ctrl Pts',(1.31448918024001,0.842567569839434,
0.869970240706755));
#261701=CARTESIAN_POINT('Ctrl Pts',(1.21137563149819,0.976371402887454,
0.882789016303748));
#261702=CARTESIAN_POINT('Ctrl Pts',(1.189783341211,1.00257073499454,0.885330749105257));
#261703=CARTESIAN_POINT('Ctrl Pts',(1.16287889282022,1.03312084419423,0.888313744286222));
#261704=CARTESIAN_POINT('Ctrl Pts',(1.15837550673526,1.03816770705299,0.888807180358547));
#261705=CARTESIAN_POINT('Ctrl Pts',(1.15132316219203,1.04596811695431,0.889570627367972));
#261706=CARTESIAN_POINT('Ctrl Pts',(1.14879699377079,1.04874200516475,0.889842273298709));
#261707=CARTESIAN_POINT('Ctrl Pts',(1.14408330598466,1.05388045562734,0.890345729967646));
#261708=CARTESIAN_POINT('Ctrl Pts',(1.14189849863544,1.05624734078522,0.890577727452879));
#261709=CARTESIAN_POINT('Ctrl Pts',(1.13690032532251,1.06162841884838,0.891105409001971));
#261710=CARTESIAN_POINT('Ctrl Pts',(1.13408231802333,1.06463822326139,0.891400734663236));
#261711=CARTESIAN_POINT('Ctrl Pts',(1.12669988399016,1.0724605421027,0.892168848503456));
#261712=CARTESIAN_POINT('Ctrl Pts',(1.12211652159247,1.07725519681762,0.892640236320011));
#261713=CARTESIAN_POINT('Ctrl Pts',(1.09092229591283,1.10947235526492,0.89581283530405));
#261714=CARTESIAN_POINT('Ctrl Pts',(1.06333674677543,1.13593834694746,0.898444651305174));
#261715=CARTESIAN_POINT('Ctrl Pts',(0.923085691486571,1.26090521743907,
0.911172564597422));
#261716=CARTESIAN_POINT('Ctrl Pts',(0.79759056472164,1.34380982122556,0.920669819155478));
#261717=CARTESIAN_POINT('Ctrl Pts',(0.626333663297266,1.42437898806925,
0.933537487226954));
#261718=CARTESIAN_POINT('Ctrl Pts',(0.589862043573178,1.43986515860209,
0.93626745608184));
#261719=CARTESIAN_POINT('Ctrl Pts',(0.542973172057567,1.45769401865363,
0.939784966099226));
#261720=CARTESIAN_POINT('Ctrl Pts',(0.533066943695342,1.46134572958528,
0.940528505651257));
#261721=CARTESIAN_POINT('Ctrl Pts',(0.517099285981078,1.4670478899907,0.94172800107995));
#261722=CARTESIAN_POINT('Ctrl Pts',(0.511060914949056,1.46916231985436,
0.942181832208195));
#261723=CARTESIAN_POINT('Ctrl Pts',(0.499547569433473,1.47311432911384,
0.94304766663842));
#261724=CARTESIAN_POINT('Ctrl Pts',(0.494075056038687,1.47495879200626,
0.943459434697607));
#261725=CARTESIAN_POINT('Ctrl Pts',(0.481565043745473,1.47909774831759,
0.944401294543088));
#261726=CARTESIAN_POINT('Ctrl Pts',(0.474521230095981,1.48137255243881,
0.944932022237243));
#261727=CARTESIAN_POINT('Ctrl Pts',(0.456126223567672,1.48716857297521,
0.946319232153606));
#261728=CARTESIAN_POINT('Ctrl Pts',(0.444750627721582,1.4906100633129,0.947178287525633));
#261729=CARTESIAN_POINT('Ctrl Pts',(0.331054454726678,1.523589562191,0.955777998203588));
#261730=CARTESIAN_POINT('Ctrl Pts',(0.226017324457541,1.5426695990472,0.963862607440416));
#261731=CARTESIAN_POINT('Ctrl Pts',(0.0375777904095188,1.55723530395187,
0.978479558492936));
#261732=CARTESIAN_POINT('Ctrl Pts',(-0.04509950512612,1.55703592468897,
0.984921688476582));
#261733=CARTESIAN_POINT('Ctrl Pts',(-0.161636295081288,1.54746110488474,
0.993797166607807));
#261734=CARTESIAN_POINT('Ctrl Pts',(-0.195800477696142,1.54351054130787,
0.996372583099473));
#261735=CARTESIAN_POINT('Ctrl Pts',(-0.23653025993098,1.53742637980791,
0.999390396331067));
#261736=CARTESIAN_POINT('Ctrl Pts',(-0.243245311703895,1.53637826074077,
0.99988621036928));
#261737=CARTESIAN_POINT('Ctrl Pts',(-0.253667506920813,1.53468146722319,
1.0006528385931));
#261738=CARTESIAN_POINT('Ctrl Pts',(-0.257379419060607,1.53406331204561,
1.00092530246312));
#261739=CARTESIAN_POINT('Ctrl Pts',(-0.264266450442967,1.53289069452681,
1.00142971633006));
#261740=CARTESIAN_POINT('Ctrl Pts',(-0.267442064678358,1.53233983848057,
1.00166185695803));
#261741=CARTESIAN_POINT('Ctrl Pts',(-0.2746710671701,1.53106270652627,1.00218931038214));
#261742=CARTESIAN_POINT('Ctrl Pts',(-0.278723295630357,1.53033020357775,
1.00248426798976));
#261743=CARTESIAN_POINT('Ctrl Pts',(-0.289277435482008,1.52837906747988,
1.0032507629536));
#261744=CARTESIAN_POINT('Ctrl Pts',(-0.29577465647734,1.52713501868479,
1.00372090975551));
#261745=CARTESIAN_POINT('Ctrl Pts',(-0.339382301186448,1.51849654135683,
1.0068661021311));
#261746=CARTESIAN_POINT('Ctrl Pts',(-0.376223917661278,1.5097907943711,
1.00947311473199));
#261747=CARTESIAN_POINT('Ctrl Pts',(-0.421681062435962,1.49728147402012,
1.01266876901983));
#261748=CARTESIAN_POINT('Ctrl Pts',(-0.430625114309803,1.49473367118787,
1.0132965053976));
#261749=CARTESIAN_POINT('Ctrl Pts',(-0.520999676594754,1.46811104695537,
1.01963385005443));
#261750=CARTESIAN_POINT('Ctrl Pts',(-0.6003558147064,1.43748570540251,1.0251597029698));
#261751=CARTESIAN_POINT('Ctrl Pts',(-0.758675402697065,1.36097655669677,
1.03677743699352));
#261752=CARTESIAN_POINT('Ctrl Pts',(-0.836893915015948,1.31432506738727,
1.04286326187219));
#261753=CARTESIAN_POINT('Ctrl Pts',(-0.921088524245512,1.25353261447549,
1.05011908101066));
#261754=CARTESIAN_POINT('Ctrl Pts',(-0.931496399183518,1.24581801460567,
1.05102903771146));
#261755=CARTESIAN_POINT('Ctrl Pts',(-0.947309802829804,1.23378774658048,
1.05243241903047));
#261756=CARTESIAN_POINT('Ctrl Pts',(-0.952785115111711,1.22956438943957,
1.05292223614388));
#261757=CARTESIAN_POINT('Ctrl Pts',(-0.962706253104655,1.22180570561005,
1.05381702475892));
#261758=CARTESIAN_POINT('Ctrl Pts',(-0.967161245844507,1.2182822476736,
1.0542215212823));
#261759=CARTESIAN_POINT('Ctrl Pts',(-0.97683796289859,1.21054239413973,
1.05510610983604));
#261760=CARTESIAN_POINT('Ctrl Pts',(-0.98205187507166,1.20631646172496,
1.0555865786323));
#261761=CARTESIAN_POINT('Ctrl Pts',(-0.996263111772014,1.19464490539579,
1.05690686548452));
#261762=CARTESIAN_POINT('Ctrl Pts',(-1.00520402692733,1.18713162214269,
1.05774940952945));
#261763=CARTESIAN_POINT('Ctrl Pts',(-1.05177222238781,1.14709587205882,
1.06220183249665));
#261764=CARTESIAN_POINT('Ctrl Pts',(-1.08790417430716,1.11288689203241,
1.06588098051816));
#261765=CARTESIAN_POINT('Ctrl Pts',(-1.22430212971465,0.970749038285334,
1.08071090171115));
#261766=CARTESIAN_POINT('Ctrl Pts',(-1.31064717441965,0.85056667771223,
1.09237420420515));
#261767=CARTESIAN_POINT('Ctrl Pts',(-1.39251463357061,0.693801356321801,
1.10574303195069));
#261768=CARTESIAN_POINT('Ctrl Pts',(-1.40547258343405,0.667161485649584,
1.10795391944232));
#261769=CARTESIAN_POINT('Ctrl Pts',(-1.42034187203205,0.634233071156714,
1.11059983230143));
#261770=CARTESIAN_POINT('Ctrl Pts',(-1.42298360279155,0.628283608094607,
1.11107449419389));
#261771=CARTESIAN_POINT('Ctrl Pts',(-1.42706768767903,0.618927899193213,
1.11181540451949));
#261772=CARTESIAN_POINT('Ctrl Pts',(-1.42853533249328,0.615532886376711,
1.11208313600966));
#261773=CARTESIAN_POINT('Ctrl Pts',(-1.4312620000841,0.609163172322001,
1.11258329415791));
#261774=CARTESIAN_POINT('Ctrl Pts',(-1.43252385342851,0.606189816019058,
1.11281588291632));
#261775=CARTESIAN_POINT('Ctrl Pts',(-1.43538126528477,0.599398030131703,
1.11334518069764));
#261776=CARTESIAN_POINT('Ctrl Pts',(-1.4369708542588,0.595577148935932,
1.11364152785334));
#261777=CARTESIAN_POINT('Ctrl Pts',(-1.44114511426338,0.585429514616591,
1.11442493148459));
#261778=CARTESIAN_POINT('Ctrl Pts',(-1.44370340878653,0.579091900247909,
1.11491045541016));
#261779=CARTESIAN_POINT('Ctrl Pts',(-1.46194340211918,0.533034076933747,
1.11841333137365));
#261780=CARTESIAN_POINT('Ctrl Pts',(-1.47602703377542,0.492695490252898,
1.12134380955399));
#261781=CARTESIAN_POINT('Ctrl Pts',(-1.51662619730622,0.358950586458834,
1.13077519117541));
#261782=CARTESIAN_POINT('Ctrl Pts',(-1.53606582667053,0.263637374739793,
1.13706437900492));
#261783=CARTESIAN_POINT('Ctrl Pts',(-1.55246975725895,0.111846837466457,
1.14717764206141));
#261784=CARTESIAN_POINT('Ctrl Pts',(-1.55547510902623,0.0562885750329613,
1.15089681480198));
#261785=CARTESIAN_POINT('Ctrl Pts',(-1.55550236599615,-0.00497133169592584,
1.15508610382524));
#261786=CARTESIAN_POINT('Ctrl Pts',(-1.5554739555871,-0.01063467066421,
1.15547420582998));
#261787=CARTESIAN_POINT('Ctrl Pts',(-1.55537238880768,-0.0203280044423647,
1.15613995724327));
#261788=CARTESIAN_POINT('Ctrl Pts',(-1.55531449397086,-0.0243581608166827,
1.15641719143077));
#261789=CARTESIAN_POINT('Ctrl Pts',(-1.55479239393149,-0.0529614741374404,
1.15838804467652));
#261790=CARTESIAN_POINT('Ctrl Pts',(-1.5537615336251,-0.0775195895801902,
1.16009719197776));
#261791=CARTESIAN_POINT('Ctrl Pts',(-1.55154601512956,-0.111219642694066,
1.16247078817666));
#261792=CARTESIAN_POINT('Ctrl Pts',(-1.55086126777126,-0.120391725709347,
1.16311967475016));
#261793=CARTESIAN_POINT('Ctrl Pts',(-1.54963805580057,-0.135026941878215,
1.1641598740465));
#261794=CARTESIAN_POINT('Ctrl Pts',(-1.54915193533731,-0.140494337443032,
1.1645495449719));
#261795=CARTESIAN_POINT('Ctrl Pts',(-1.54809140733786,-0.151746627362062,
1.16535378797963));
#261796=CARTESIAN_POINT('Ctrl Pts',(-1.54751348834385,-0.157531095649165,
1.1657684640257));
#261797=CARTESIAN_POINT('Ctrl Pts',(-1.54609446047687,-0.170972221383311,
1.16673498023718));
#261798=CARTESIAN_POINT('Ctrl Pts',(-1.54522888264341,-0.178626082901079,
1.16728757946257));
#261799=CARTESIAN_POINT('Ctrl Pts',(-1.54227350249389,-0.203127814151401,
1.1690639200104));
#261800=CARTESIAN_POINT('Ctrl Pts',(-1.53996477971028,-0.219947494202914,
1.17029448681145));
#261801=CARTESIAN_POINT('Ctrl Pts',(-1.52674913907203,-0.305774691445692,
1.17663348793641));
#261802=CARTESIAN_POINT('Ctrl Pts',(-1.51147889498719,-0.374018726176664,
1.18187726894355));
#261803=CARTESIAN_POINT('Ctrl Pts',(-1.46263193063276,-0.539244088618074,
1.19505902221553));
#261804=CARTESIAN_POINT('Ctrl Pts',(-1.42395333003346,-0.634375148820113,
1.20309185189433));
#261805=CARTESIAN_POINT('Ctrl Pts',(-1.36916336120564,-0.738376720585995,
1.21208109386595));
#261806=CARTESIAN_POINT('Ctrl Pts',(-1.36192718835405,-0.751640108515646,
1.21323114937633));
#261807=CARTESIAN_POINT('Ctrl Pts',(-1.33971479523699,-0.79097954526294,
1.21664920723525));
#261808=CARTESIAN_POINT('Ctrl Pts',(-1.32417344773885,-0.816730903254209,
1.21889602967302));
#261809=CARTESIAN_POINT('Ctrl Pts',(-1.30422376742877,-0.84771845841536,
1.22159716373092));
#261810=CARTESIAN_POINT('Ctrl Pts',(-1.30051624307651,-0.853395410272971,
1.22209190194828));
#261811=CARTESIAN_POINT('Ctrl Pts',(-1.29467367034061,-0.862215036046148,
1.22286012446978));
#261812=CARTESIAN_POINT('Ctrl Pts',(-1.29256408861742,-0.865374345998211,
1.22313523233649));
#261813=CARTESIAN_POINT('Ctrl Pts',(-1.28864621004977,-0.871195471691298,
1.22364193293743));
#261814=CARTESIAN_POINT('Ctrl Pts',(-1.28684123972178,-0.873859387261356,
1.22387373303335));
#261815=CARTESIAN_POINT('Ctrl Pts',(-1.282737601231,-0.879875569033461,
1.22439706421126));
#261816=CARTESIAN_POINT('Ctrl Pts',(-1.28043405500053,-0.883224434899434,
1.22468826153219));
#261817=CARTESIAN_POINT('Ctrl Pts',(-1.27341448094159,-0.893344219461222,
1.2255680071401));
#261818=CARTESIAN_POINT('Ctrl Pts',(-1.26865757858146,-0.900086824119339,
1.22615387685606));
#261819=CARTESIAN_POINT('Ctrl Pts',(-1.25753405228508,-0.91559031891837,
1.22750113780947));
#261820=CARTESIAN_POINT('Ctrl Pts',(-1.25112906567896,-0.924323321020851,
1.2282601533158));
#261821=CARTESIAN_POINT('Ctrl Pts',(-1.22894868431004,-0.953912563954547,
1.23083497205084));
#261822=CARTESIAN_POINT('Ctrl Pts',(-1.2127380344378,-0.97443865103255,
1.23262650848742));
#261823=CARTESIAN_POINT('Ctrl Pts',(-1.12141374953853,-1.0842628208825,
1.24230248775796));
#261824=CARTESIAN_POINT('Ctrl Pts',(-1.03694961046443,-1.16530431190777,
1.2498048468105));
#261825=CARTESIAN_POINT('Ctrl Pts',(-0.89007153830761,-1.27749524643152,
1.26212606699102));
#261826=CARTESIAN_POINT('Ctrl Pts',(-0.833280868150213,-1.31524238070048,
1.26674248916005));
#261827=CARTESIAN_POINT('Ctrl Pts',(-0.764198252988644,-1.35488537484497,
1.27230860882707));
#261828=CARTESIAN_POINT('Ctrl Pts',(-0.754128585887999,-1.36051586253214,
1.27311864235395));
#261829=CARTESIAN_POINT('Ctrl Pts',(-0.737590325471856,-1.36952327115748,
1.27444743516849));
#261830=CARTESIAN_POINT('Ctrl Pts',(-0.731158826443947,-1.37296767832018,
1.27496379519455));
#261831=CARTESIAN_POINT('Ctrl Pts',(-0.719605741538495,-1.37905076687507,
1.27589077815736));
#261832=CARTESIAN_POINT('Ctrl Pts',(-0.714493242178622,-1.3817064978211,
1.27630079115074));
#261833=CARTESIAN_POINT('Ctrl Pts',(-0.703622064163257,-1.38727715301918,
1.27717228645444));
#261834=CARTESIAN_POINT('Ctrl Pts',(-0.697859775376042,-1.39018475033367,
1.2776340158875));
#261835=CARTESIAN_POINT('Ctrl Pts',(-0.682388600382008,-1.3978709326538,
1.27887326095563));
#261836=CARTESIAN_POINT('Ctrl Pts',(-0.672647821402575,-1.40258413068884,
1.27965302791472));
#261837=CARTESIAN_POINT('Ctrl Pts',(-0.624113562018207,-1.4254461791857,
1.28353670135107));
#261838=CARTESIAN_POINT('Ctrl Pts',(-0.584634855556928,-1.44208736654561,
1.28669153479107));
#261839=CARTESIAN_POINT('Ctrl Pts',(-0.392282042439899,-1.51397139325813,
1.30205889371115));
#261840=CARTESIAN_POINT('Ctrl Pts',(-0.232101698918667,-1.54664414741534,
1.31498316018246));
#261841=CARTESIAN_POINT('Ctrl Pts',(-0.0656800867438431,-1.55411816806265,
1.32750373701108));
#261842=CARTESIAN_POINT('Ctrl Pts',(-0.061572006395244,-1.55428634520056,
1.32781215649388));
#261843=CARTESIAN_POINT('Ctrl Pts',(-0.0374539076559448,-1.55517792429528,
1.32961887860166));
#261844=CARTESIAN_POINT('Ctrl Pts',(-0.0174308413185623,-1.55553124004874,
1.33110279299082));
#261845=CARTESIAN_POINT('Ctrl Pts',(0.00855751168281875,-1.55548788948749,
1.33300343140338));
#261846=CARTESIAN_POINT('Ctrl Pts',(0.0145203586239918,-1.5554436562103,
1.33343778559679));
#261847=CARTESIAN_POINT('Ctrl Pts',(0.0240608367071122,-1.55531801563273,
1.33412981839654));
#261848=CARTESIAN_POINT('Ctrl Pts',(0.0276386165324073,-1.55525855123701,
1.33438867895905));
#261849=CARTESIAN_POINT('Ctrl Pts',(0.0344768081015319,-1.55512129285711,
1.33488213799023));
#261850=CARTESIAN_POINT('Ctrl Pts',(0.0377371430473449,-1.5550455922745,
1.33511684100221));
#261851=CARTESIAN_POINT('Ctrl Pts',(0.0454336231117314,-1.5548426706669,
1.33566958485374));
#261852=CARTESIAN_POINT('Ctrl Pts',(0.049869498113839,-1.55470671803476,
1.33598713792246));
#261853=CARTESIAN_POINT('Ctrl Pts',(0.0645463066209577,-1.55419401641856,
1.33703461476313));
#261854=CARTESIAN_POINT('Ctrl Pts',(0.0747843859017205,-1.55373504074466,
1.33776014691153));
#261855=CARTESIAN_POINT('Ctrl Pts',(0.0992979569339379,-1.55239321921494,
1.33948659489171));
#261856=CARTESIAN_POINT('Ctrl Pts',(0.113567523707308,-1.55141459437482,
1.34048284793426));
#261857=CARTESIAN_POINT('Ctrl Pts',(0.167120684669559,-1.54699896582576,
1.34419581403078));
#261858=CARTESIAN_POINT('Ctrl Pts',(0.206285017593711,-1.54226525313204,
1.34685881021484));
#261859=CARTESIAN_POINT('Ctrl Pts',(0.382747902410267,-1.5140929555056,
1.3587881029105));
#261860=CARTESIAN_POINT('Ctrl Pts',(0.516688037151767,-1.47377321780688,
1.36771260038848));
#261861=CARTESIAN_POINT('Ctrl Pts',(0.648963766604163,-1.41366991402574,
1.37766025153078));
#261862=CARTESIAN_POINT('Ctrl Pts',(0.654437904623114,-1.41114408322439,
1.3780739488346));
#261863=CARTESIAN_POINT('Ctrl Pts',(0.660733584551883,-1.40819467169567,
1.37855214045405));
#261864=CARTESIAN_POINT('Ctrl Pts',(0.661569655888474,-1.40780207896875,
1.37861569382389));
#261865=CARTESIAN_POINT('Ctrl Pts',(0.685429427676946,-1.3965723341067,
1.38043078712612));
#261866=CARTESIAN_POINT('Ctrl Pts',(0.708182882465273,-1.38517315222568,
1.38219930606845));
#261867=CARTESIAN_POINT('Ctrl Pts',(0.738879068239845,-1.36884073468109,
1.38464248585462));
#261868=CARTESIAN_POINT('Ctrl Pts',(0.747072966504511,-1.36438601955547,
1.3853003535355));
#261869=CARTESIAN_POINT('Ctrl Pts',(0.760046894423242,-1.35718067175175,
1.3863513505034));
#261870=CARTESIAN_POINT('Ctrl Pts',(0.764853308343698,-1.3544777860084,
1.38674277496615));
#261871=CARTESIAN_POINT('Ctrl Pts',(0.774687543373235,-1.34887847038192,
1.38754796251197));
#261872=CARTESIAN_POINT('Ctrl Pts',(0.779713726449343,-1.34597935378947,
1.38796181734543));
#261873=CARTESIAN_POINT('Ctrl Pts',(0.791307006733607,-1.33920558918164,
1.3889218864577));
#261874=CARTESIAN_POINT('Ctrl Pts',(0.797862020718454,-1.33531066836961,
1.38946882777489));
#261875=CARTESIAN_POINT('Ctrl Pts',(0.81855282885753,-1.32280966102261,
1.39120849553862));
#261876=CARTESIAN_POINT('Ctrl Pts',(0.832579620378503,-1.31402635793779,
1.39240765564676));
#261877=CARTESIAN_POINT('Ctrl Pts',(0.902242356786235,-1.26884170102616,
1.39846573704371));
#261878=CARTESIAN_POINT('Ctrl Pts',(0.955636517604137,-1.22912858624269,
1.4034467655288));
#261879=CARTESIAN_POINT('Ctrl Pts',(1.07772192882836,-1.12555027518561,
1.41567175539374));
#261880=CARTESIAN_POINT('Ctrl Pts',(1.14350548523559,-1.05865076097756,
1.42299202352713));
#261881=CARTESIAN_POINT('Ctrl Pts',(1.23840459474117,-0.942908036495083,
1.43451282115944));
#261882=CARTESIAN_POINT('Ctrl Pts',(1.27157681244589,-0.89767226346097,
1.43877428982523));
#261883=CARTESIAN_POINT('Ctrl Pts',(1.30657310116219,-0.844102963157296,
1.4434758864979));
#261884=CARTESIAN_POINT('Ctrl Pts',(1.31085768188657,-0.837433714417966,
1.44405537460208));
#261885=CARTESIAN_POINT('Ctrl Pts',(1.3172551840952,-0.827306139236497,
1.44492622033476));
#261886=CARTESIAN_POINT('Ctrl Pts',(1.3194057954242,-0.823871965814587,
1.44521994484258));
#261887=CARTESIAN_POINT('Ctrl Pts',(1.3232398344969,-0.817696117369825,
1.44574529724105));
#261888=CARTESIAN_POINT('Ctrl Pts',(1.32492819013956,-0.814957601094243,
1.44597724209685));
#261889=CARTESIAN_POINT('Ctrl Pts',(1.32859703020646,-0.808965197342127,
1.44648258006633));
#261890=CARTESIAN_POINT('Ctrl Pts',(1.33057406037041,-0.805709271322412,
1.44675574787305));
#261891=CARTESIAN_POINT('Ctrl Pts',(1.33615953519471,-0.796434051337235,
1.44753004415994));
#261892=CARTESIAN_POINT('Ctrl Pts',(1.33973929443662,-0.790397450350637,
1.44802935450888));
#261893=CARTESIAN_POINT('Ctrl Pts',(1.36290014509709,-0.750731493259817,
1.45128154703851));
#261894=CARTESIAN_POINT('Ctrl Pts',(1.38125625693912,-0.716398193365103,
1.45396217975873));
#261895=CARTESIAN_POINT('Ctrl Pts',(1.44911985158528,-0.577136554520089,
1.46445757801275));
#261896=CARTESIAN_POINT('Ctrl Pts',(1.48811314193984,-0.467502050116821,
1.47191792241935));
#261897=CARTESIAN_POINT('Ctrl Pts',(1.53023523057209,-0.287563374418997,
1.48423302958865));
#261898=CARTESIAN_POINT('Ctrl Pts',(1.54145243529622,-0.21962462648746,
1.48889255798115));
#261899=CARTESIAN_POINT('Ctrl Pts',(1.54926363249993,-0.13963137424281,
1.49450878233733));
#261900=CARTESIAN_POINT('Ctrl Pts',(1.55026150334837,-0.128078031365681,
1.49532292982615));
#261901=CARTESIAN_POINT('Ctrl Pts',(1.55167789447218,-0.109222011713531,
1.49665709768085));
#261902=CARTESIAN_POINT('Ctrl Pts',(1.5521742583683,-0.10192548454021,1.49717468526005));
#261903=CARTESIAN_POINT('Ctrl Pts',(1.55296969674995,-0.0888739452898519,
1.49810299123497));
#261904=CARTESIAN_POINT('Ctrl Pts',(1.55328828124881,-0.0831202194113083,
1.49851309238664));
#261905=CARTESIAN_POINT('Ctrl Pts',(1.55389532834674,-0.0709300297506218,
1.49938384468053));
#261906=CARTESIAN_POINT('Ctrl Pts',(1.55417578578885,-0.064493295309973,
1.49984473803982));
#261907=CARTESIAN_POINT('Ctrl Pts',(1.55481823282952,-0.047291873891471,
1.50107949860333));
#261908=CARTESIAN_POINT('Ctrl Pts',(1.55510841098274,-0.036525028762168,
1.50185558925807));
#261909=CARTESIAN_POINT('Ctrl Pts',(1.55598557209485,0.0164421218369805,
1.50569010319984));
#261910=CARTESIAN_POINT('Ctrl Pts',(1.55496665518451,0.0586473530331255,
1.508797915883));
#261911=CARTESIAN_POINT('Ctrl Pts',(1.54219579600323,0.255394608700159,
1.52354541272151));
#261912=CARTESIAN_POINT('Ctrl Pts',(1.50911166648446,0.407629890403857,
1.53582378684819));
#261913=CARTESIAN_POINT('Ctrl Pts',(1.44786201765657,0.568843929349383,
1.54887888437283));
#261914=CARTESIAN_POINT('Ctrl Pts',(1.44135635704005,0.585132196267513,
1.55019705218249));
#261915=CARTESIAN_POINT('Ctrl Pts',(1.4345766830264,0.601306902103224,1.55150291788058));
#261916=CARTESIAN_POINT('Origin',(0.,0.,-1.29405622560371));
#261917=CARTESIAN_POINT('',(1.43457668658422,0.601306893615097,2.38964409368597));
#261918=CARTESIAN_POINT('',(1.43457657517513,0.6013071594109,2.25008958711186));
#261919=CARTESIAN_POINT('',(1.43457668357355,0.601306900797845,-1.29405622560371));
#261920=CARTESIAN_POINT('',(-1.5555004206877,-1.78579724124609E-5,1.99259704609395));
#261921=CARTESIAN_POINT('Ctrl Pts',(1.43457668658422,0.601306893615097,
2.38964409368597));
#261922=CARTESIAN_POINT('Ctrl Pts',(1.43678610929841,0.596035731168367,
2.38924668108184));
#261923=CARTESIAN_POINT('Ctrl Pts',(1.43896666337616,0.59075195326909,2.38884831054688));
#261924=CARTESIAN_POINT('Ctrl Pts',(1.44553656171715,0.574579937460446,
2.38762886929659));
#261925=CARTESIAN_POINT('Ctrl Pts',(1.44983152026026,0.563654686304953,
2.38680484467955));
#261926=CARTESIAN_POINT('Ctrl Pts',(1.45659918601195,0.545850235705615,
2.38546108115142));
#261927=CARTESIAN_POINT('Ctrl Pts',(1.4591478381475,0.539000233439249,2.38494387871763));
#261928=CARTESIAN_POINT('Ctrl Pts',(1.46359794946082,0.526776783272011,
2.38402046400456));
#261929=CARTESIAN_POINT('Ctrl Pts',(1.46551834029303,0.521410327613212,
2.38361488891971));
#261930=CARTESIAN_POINT('Ctrl Pts',(1.46950291902844,0.51007965365925,2.38275814456882));
#261931=CARTESIAN_POINT('Ctrl Pts',(1.47156038367609,0.504113198732518,
2.38230676137573));
#261932=CARTESIAN_POINT('Ctrl Pts',(1.47691373036322,0.488276927815953,
2.38110795487899));
#261933=CARTESIAN_POINT('Ctrl Pts',(1.48014693243878,0.478386427255533,
2.38035848671231));
#261934=CARTESIAN_POINT('Ctrl Pts',(1.49498575289909,0.43140285306159,2.37679401952542));
#261935=CARTESIAN_POINT('Ctrl Pts',(1.50529671741136,0.393918922890391,
2.37393737433536));
#261936=CARTESIAN_POINT('Ctrl Pts',(1.54847768374483,0.210302185578863,
2.35986792856474));
#261937=CARTESIAN_POINT('Ctrl Pts',(1.5615235007313,0.0603330201707153,
2.34804286310328));
#261938=CARTESIAN_POINT('Ctrl Pts',(1.55069848759065,-0.128256212374082,
2.33364373382289));
#261939=CARTESIAN_POINT('Ctrl Pts',(1.54697570840915,-0.167278970863317,
2.33069680404698));
#261940=CARTESIAN_POINT('Ctrl Pts',(1.54090371940103,-0.212696879512762,
2.32733457800986));
#261941=CARTESIAN_POINT('Ctrl Pts',(1.53998282667357,-0.219264982976112,
2.32685002305705));
#261942=CARTESIAN_POINT('Ctrl Pts',(1.53842526391811,-0.229879827650328,
2.32606984496707));
#261943=CARTESIAN_POINT('Ctrl Pts',(1.53781458206121,-0.233930203403862,
2.32577283670139));
#261944=CARTESIAN_POINT('Ctrl Pts',(1.53670082221325,-0.241124384585699,
2.32524657931238));
#261945=CARTESIAN_POINT('Ctrl Pts',(1.53620408593838,-0.244269099314983,
2.32501698094244));
#261946=CARTESIAN_POINT('Ctrl Pts',(1.53511107999725,-0.251053427668052,
2.32452260811069));
#261947=CARTESIAN_POINT('Ctrl Pts',(1.53451152127388,-0.254692448490967,
2.3242580215438));
#261948=CARTESIAN_POINT('Ctrl Pts',(1.53280456371452,-0.264827961491769,
2.32352263929779));
#261949=CARTESIAN_POINT('Ctrl Pts',(1.53166879664065,-0.271319703048497,
2.32305341053326));
#261950=CARTESIAN_POINT('Ctrl Pts',(1.52481143993769,-0.30909857269985,
2.32033205082952));
#261951=CARTESIAN_POINT('Ctrl Pts',(1.51817208260253,-0.340214272863052,
2.31812797496159));
#261952=CARTESIAN_POINT('Ctrl Pts',(1.47581071834769,-0.51264514435571,
2.30601115615178));
#261953=CARTESIAN_POINT('Ctrl Pts',(1.42131820898492,-0.64860250446206,
2.29676096859634));
#261954=CARTESIAN_POINT('Ctrl Pts',(1.32419373939082,-0.817623560151233,
2.28361163953145));
#261955=CARTESIAN_POINT('Ctrl Pts',(1.29769404248287,-0.859061520411838,
2.28024426477329));
#261956=CARTESIAN_POINT('Ctrl Pts',(1.26260409914782,-0.908594783141957,
2.27599536734309));
#261957=CARTESIAN_POINT('Ctrl Pts',(1.25582449039136,-0.917942496977848,
2.27518327465635));
#261958=CARTESIAN_POINT('Ctrl Pts',(1.24498915198541,-0.932537520370693,
2.27389855692975));
#261959=CARTESIAN_POINT('Ctrl Pts',(1.24100276469926,-0.937835993657894,
2.27342862352172));
#261960=CARTESIAN_POINT('Ctrl Pts',(1.23358271634179,-0.947568138914866,
2.27255880197799));
#261961=CARTESIAN_POINT('Ctrl Pts',(1.23015870603126,-0.952009061095374,
2.27215929765912));
#261962=CARTESIAN_POINT('Ctrl Pts',(1.22251650452936,-0.961810884728172,
2.27127169829564));
#261963=CARTESIAN_POINT('Ctrl Pts',(1.21828693224431,-0.967162721473227,
2.2707831566448));
#261964=CARTESIAN_POINT('Ctrl Pts',(1.2060445395556,-0.98244574969127,2.26937664268453));
#261965=CARTESIAN_POINT('Ctrl Pts',(1.19794470160068,-0.99230618073998,
2.26845519522419));
#261966=CARTESIAN_POINT('Ctrl Pts',(1.13358226689048,-1.06872191575334,
2.26120185383137));
#261967=CARTESIAN_POINT('Ctrl Pts',(1.0719482159986,-1.13052961366926,2.25464533705512));
#261968=CARTESIAN_POINT('Ctrl Pts',(0.935154014689978,-1.24641949876183,
2.24086439806583));
#261969=CARTESIAN_POINT('Ctrl Pts',(0.859678980927541,-1.29962543300971,
2.23364978730705));
#261970=CARTESIAN_POINT('Ctrl Pts',(0.765218397286501,-1.35436720140672,
2.22530153127022));
#261971=CARTESIAN_POINT('Ctrl Pts',(0.750358554990978,-1.36265615309226,
2.22400726819537));
#261972=CARTESIAN_POINT('Ctrl Pts',(0.71045926054688,-1.3840616792585,2.22058743254789));
#261973=CARTESIAN_POINT('Ctrl Pts',(0.685191622707292,-1.39674328315993,
2.21847850344823));
#261974=CARTESIAN_POINT('Ctrl Pts',(0.653617823016518,-1.41152664984378,
2.21592428952644));
#261975=CARTESIAN_POINT('Ctrl Pts',(0.647627382874243,-1.41428516180637,
2.21544321704364));
#261976=CARTESIAN_POINT('Ctrl Pts',(0.638222636378641,-1.41854362651684,
2.21469367173399));
#261977=CARTESIAN_POINT('Ctrl Pts',(0.634820266992627,-1.42006949947069,
2.21442367204616));
#261978=CARTESIAN_POINT('Ctrl Pts',(0.628798046681575,-1.42274433742558,
2.21394786686686));
#261979=CARTESIAN_POINT('Ctrl Pts',(0.626180524578857,-1.4238983054019,
2.21374176152263));
#261980=CARTESIAN_POINT('Ctrl Pts',(0.620005327180566,-1.42660039860182,
2.21325716122959));
#261981=CARTESIAN_POINT('Ctrl Pts',(0.616445034239869,-1.42814243815917,
2.2129790388802));
#261982=CARTESIAN_POINT('Ctrl Pts',(0.605994470590375,-1.43262244077089,
2.21216627941702));
#261983=CARTESIAN_POINT('Ctrl Pts',(0.599088572995391,-1.43552403110779,
2.21163378624781));
#261984=CARTESIAN_POINT('Ctrl Pts',(0.541806936928805,-1.45910618477904,
2.20725263587288));
#261985=CARTESIAN_POINT('Ctrl Pts',(0.490391329979952,-1.47718093741309,
2.20354693949995));
#261986=CARTESIAN_POINT('Ctrl Pts',(0.308130978808746,-1.53068309418289,
2.19083910864413));
#261987=CARTESIAN_POINT('Ctrl Pts',(0.17371079658686,-1.55169632297072,
2.18216175852264));
#261988=CARTESIAN_POINT('Ctrl Pts',(0.00120546028995934,-1.55594120670977,
2.17041158087723));
#261989=CARTESIAN_POINT('Ctrl Pts',(-0.0358720376666462,-1.55552798529379,
2.16785440830424));
#261990=CARTESIAN_POINT('Ctrl Pts',(-0.0835559209501208,-1.55329086795311,
2.16450791626522));
#261991=CARTESIAN_POINT('Ctrl Pts',(-0.0942091586292589,-1.55268114458328,
2.16375657035142));
#261992=CARTESIAN_POINT('Ctrl Pts',(-0.111210263763817,-1.55153250058144,
2.16255124547342));
#261993=CARTESIAN_POINT('Ctrl Pts',(-0.117562694432409,-1.55106409726087,
2.16209947646046));
#261994=CARTESIAN_POINT('Ctrl Pts',(-0.12901495873897,-1.55014889513055,
2.16128241086261));
#261995=CARTESIAN_POINT('Ctrl Pts',(-0.134115832388011,-1.54971590912812,
2.16091755257312));
#261996=CARTESIAN_POINT('Ctrl Pts',(-0.146114833788221,-1.54863769343651,
2.16005703117796));
#261997=CARTESIAN_POINT('Ctrl Pts',(-0.153010922460385,-1.54797154525459,
2.15956071864182));
#261998=CARTESIAN_POINT('Ctrl Pts',(-0.173104313523285,-1.5458949845325,
2.15810934853828));
#261999=CARTESIAN_POINT('Ctrl Pts',(-0.18628800127005,-1.54436173445071,
2.15715046185232));
#262000=CARTESIAN_POINT('Ctrl Pts',(-0.314728477263464,-1.52775570111333,
2.14774150665099));
#262001=CARTESIAN_POINT('Ctrl Pts',(-0.427947542120583,-1.49998035679443,
2.13887672629642));
#262002=CARTESIAN_POINT('Ctrl Pts',(-0.630096265997753,-1.42562263696625,
2.12218677420738));
#262003=CARTESIAN_POINT('Ctrl Pts',(-0.719718212567711,-1.38254501764455,
2.11444849765602));
#262004=CARTESIAN_POINT('Ctrl Pts',(-0.814878654287223,-1.32502692653596,
2.10621687176514));
#262005=CARTESIAN_POINT('Ctrl Pts',(-0.825053000972391,-1.31871571852921,
2.10533678675925));
#262006=CARTESIAN_POINT('Ctrl Pts',(-0.839158840664227,-1.30973860991628,
2.10411772407558));
#262007=CARTESIAN_POINT('Ctrl Pts',(-0.843152190556915,-1.30717143914941,
2.10377273335587));
#262008=CARTESIAN_POINT('Ctrl Pts',(-0.849865099423164,-1.30281240720588,
2.10319308925342));
#262009=CARTESIAN_POINT('Ctrl Pts',(-0.852590862541924,-1.30103023686938,
2.10295780792959));
#262010=CARTESIAN_POINT('Ctrl Pts',(-0.857793811955234,-1.29760504843669,
2.10250888922487));
#262011=CARTESIAN_POINT('Ctrl Pts',(-0.860271918645518,-1.29596346860348,
2.10229515591094));
#262012=CARTESIAN_POINT('Ctrl Pts',(-0.866360056846332,-1.29190532686278,
2.10177022300406));
#262013=CARTESIAN_POINT('Ctrl Pts',(-0.869964729811259,-1.28948070624696,
2.10145955972542));
#262014=CARTESIAN_POINT('Ctrl Pts',(-0.882805769328071,-1.28076504829234,
2.10035319022252));
#262015=CARTESIAN_POINT('Ctrl Pts',(-0.891984735415166,-1.27438941699862,
2.0995629277965));
#262016=CARTESIAN_POINT('Ctrl Pts',(-0.945887088008152,-1.23608155805066,
2.09492050776294));
#262017=CARTESIAN_POINT('Ctrl Pts',(-0.988966929288186,-1.20189262821392,
2.09120263997248));
#262018=CARTESIAN_POINT('Ctrl Pts',(-1.1069636989661,-1.0975979403738,2.08070607756059));
#262019=CARTESIAN_POINT('Ctrl Pts',(-1.17687619950312,-1.02227833783407,
2.07407380692125));
#262020=CARTESIAN_POINT('Ctrl Pts',(-1.27561529786001,-0.892232060693595,
2.06314391828747));
#262021=CARTESIAN_POINT('Ctrl Pts',(-1.30948804563383,-0.84173158121097,
2.05900941019903));
#262022=CARTESIAN_POINT('Ctrl Pts',(-1.34599267974516,-0.779749310318439,
2.0539798148085));
#262023=CARTESIAN_POINT('Ctrl Pts',(-1.35156298258034,-0.770053747148933,
2.0531944003065));
#262024=CARTESIAN_POINT('Ctrl Pts',(-1.36051819034682,-0.75406994874633,
2.05190130437675));
#262025=CARTESIAN_POINT('Ctrl Pts',(-1.36396524770807,-0.747816845115493,
2.05139585044705));
#262026=CARTESIAN_POINT('Ctrl Pts',(-1.37007758263689,-0.736545957316435,
2.05048543989793));
#262027=CARTESIAN_POINT('Ctrl Pts',(-1.37275866916872,-0.73153685097631,
2.05008105343884));
#262028=CARTESIAN_POINT('Ctrl Pts',(-1.37840614616144,-0.720845223401461,
2.04921833292539));
#262029=CARTESIAN_POINT('Ctrl Pts',(-1.38136496417427,-0.715158844841251,
2.04875974091322));
#262030=CARTESIAN_POINT('Ctrl Pts',(-1.38923911182671,-0.699794796298017,
2.04752123586148));
#262031=CARTESIAN_POINT('Ctrl Pts',(-1.39408835039792,-0.690083855001626,
2.04673903020258));
#262032=CARTESIAN_POINT('Ctrl Pts',(-1.41826233301869,-0.640378913816671,
2.04273761372666));
#262033=CARTESIAN_POINT('Ctrl Pts',(-1.43596738234061,-0.599624998511741,
2.03946331280328));
#262034=CARTESIAN_POINT('Ctrl Pts',(-1.48248932051099,-0.478613517406358,
2.02974938906059));
#262035=CARTESIAN_POINT('Ctrl Pts',(-1.50648069938332,-0.396683811319334,
2.02317447377145));
#262036=CARTESIAN_POINT('Ctrl Pts',(-1.54209589229059,-0.223431707399583,
2.00945799042065));
#262037=CARTESIAN_POINT('Ctrl Pts',(-1.55258247384778,-0.132185124857028,
2.00233764832531));
#262038=CARTESIAN_POINT('Ctrl Pts',(-1.55521973276162,-0.0310229204717739,
1.9948613494224));
#262039=CARTESIAN_POINT('Ctrl Pts',(-1.555380450164,-0.0215059495709297,
1.99416218843355));
#262040=CARTESIAN_POINT('Ctrl Pts',(-1.55547726732396,-0.00894362252634021,
1.99324532762615));
#262041=CARTESIAN_POINT('Ctrl Pts',(-1.555491792201,-0.00589935211516795,
1.9930236087652));
#262042=CARTESIAN_POINT('Ctrl Pts',(-1.55549911544723,-0.00190944265546296,
1.99273364645012));
#262043=CARTESIAN_POINT('Ctrl Pts',(-1.55549998878868,-0.000963856086597575,
1.99266497327083));
#262044=CARTESIAN_POINT('Ctrl Pts',(-1.55549999989275,-1.82662448845978E-5,
1.99259634653107));
#262045=CARTESIAN_POINT('Ctrl Pts',(-1.55549999989689,-1.79106135396723E-5,
1.99259632072092));
#262046=CARTESIAN_POINT('Ctrl Pts',(-1.55550001419639,0.00122397189078814,
1.99250619038201));
#262047=CARTESIAN_POINT('Ctrl Pts',(-1.55549854125183,0.0024658604726738,
1.99241614011376));
#262048=CARTESIAN_POINT('Ctrl Pts',(-1.55548839673815,0.00672173958508773,
1.99210782204593));
#262049=CARTESIAN_POINT('Ctrl Pts',(-1.55547245236403,0.00973573472252594,
1.99188995188346));
#262050=CARTESIAN_POINT('Ctrl Pts',(-1.5554216770202,0.0159302645811493,
1.99144318405574));
#262051=CARTESIAN_POINT('Ctrl Pts',(-1.55538585119196,0.0191107512606468,
1.99121434951327));
#262052=CARTESIAN_POINT('Ctrl Pts',(-1.55527764779643,0.0266605291434597,
1.99067241280553));
#262053=CARTESIAN_POINT('Ctrl Pts',(-1.55519661253696,0.0310297140168148,
1.99035979047689));
#262054=CARTESIAN_POINT('Ctrl Pts',(-1.55487169938468,0.0453034971727461,
1.9893415923815));
#262055=CARTESIAN_POINT('Ctrl Pts',(-1.55455160002381,0.0552063828148327,
1.98864008556239));
#262056=CARTESIAN_POINT('Ctrl Pts',(-1.55371304455279,0.0752234716368273,
1.98723077622798));
#262057=CARTESIAN_POINT('Ctrl Pts',(-1.5531903950852,0.0853370074145378,
1.98652321169287));
#262058=CARTESIAN_POINT('Ctrl Pts',(-1.55101132197374,0.120783184334668,
1.98405676230046));
#262059=CARTESIAN_POINT('Ctrl Pts',(-1.54883349697656,0.146080987139074,
1.98232054345841));
#262060=CARTESIAN_POINT('Ctrl Pts',(-1.52946455362371,0.320875943342886,
1.97042121525242));
#262061=CARTESIAN_POINT('Ctrl Pts',(-1.49127930262326,0.467242146655841,
1.96087082834798));
#262062=CARTESIAN_POINT('Ctrl Pts',(-1.41795514707373,0.640631973628924,
1.94805158680147));
#262063=CARTESIAN_POINT('Ctrl Pts',(-1.40198728668171,0.674861004225701,
1.9454461799346));
#262064=CARTESIAN_POINT('Ctrl Pts',(-1.38009638921,0.717649252686303,1.9420748319237));
#262065=CARTESIAN_POINT('Ctrl Pts',(-1.37531073844183,0.72677840984685,
1.94134874078717));
#262066=CARTESIAN_POINT('Ctrl Pts',(-1.36745937970235,0.74140046830073,
1.94017443625196));
#262067=CARTESIAN_POINT('Ctrl Pts',(-1.36445040457722,0.746923624521823,
1.93972823462468));
#262068=CARTESIAN_POINT('Ctrl Pts',(-1.35864854721157,0.757421229779946,
1.93887503909602));
#262069=CARTESIAN_POINT('Ctrl Pts',(-1.35586162734086,0.7623988720296,1.93846826339771));
#262070=CARTESIAN_POINT('Ctrl Pts',(-1.3494217067841,0.773754046179482,
1.9375351592846));
#262071=CARTESIAN_POINT('Ctrl Pts',(-1.3457507850193,0.780121200777997,
1.93700819278008));
#262072=CARTESIAN_POINT('Ctrl Pts',(-1.33603076072164,0.796707650176765,
1.93562545575384));
#262073=CARTESIAN_POINT('Ctrl Pts',(-1.32990961254919,0.806883933006071,
1.93476709137393));
#262074=CARTESIAN_POINT('Ctrl Pts',(-1.26940322177066,0.904915448829829,
1.9263986265754));
#262075=CARTESIAN_POINT('Ctrl Pts',(-1.20651956868282,0.987197473210816,
1.91856558891341));
#262076=CARTESIAN_POINT('Ctrl Pts',(-1.08510869471353,1.11698719679562,
1.90482909823418));
#262077=CARTESIAN_POINT('Ctrl Pts',(-1.0304200461595,1.16762843184032,1.8990223214414));
#262078=CARTESIAN_POINT('Ctrl Pts',(-0.948527679079825,1.23320890041879,
1.89099589884613));
#262079=CARTESIAN_POINT('Ctrl Pts',(-0.924184084959288,1.25155622552125,
1.88868566335576));
#262080=CARTESIAN_POINT('Ctrl Pts',(-0.884704823860423,1.27953049176129,
1.88507468077004));
#262081=CARTESIAN_POINT('Ctrl Pts',(-0.869915568752658,1.28963090942132,
1.88375087845846));
#262082=CARTESIAN_POINT('Ctrl Pts',(-0.851551850914984,1.30171282680102,
1.88214527982586));
#262083=CARTESIAN_POINT('Ctrl Pts',(-0.848140521747118,1.3039380716193,
1.88184860630438));
#262084=CARTESIAN_POINT('Ctrl Pts',(-0.84157321761236,1.30818531455725,
1.8812805707));
#262085=CARTESIAN_POINT('Ctrl Pts',(-0.838418602781028,1.31020935164603,
1.88100907925787));
#262086=CARTESIAN_POINT('Ctrl Pts',(-0.832630539148359,1.31389357482074,
1.88051348643079));
#262087=CARTESIAN_POINT('Ctrl Pts',(-0.829999428162655,1.31555725469188,
1.88028916042363));
#262088=CARTESIAN_POINT('Ctrl Pts',(-0.824071527267918,1.31928066702593,
1.87978589619794));
#262089=CARTESIAN_POINT('Ctrl Pts',(-0.82077200685949,1.32133594293423,
1.87950725195935));
#262090=CARTESIAN_POINT('Ctrl Pts',(-0.811380379494651,1.3271372480057,
1.87871820931261));
#262091=CARTESIAN_POINT('Ctrl Pts',(-0.805269988564278,1.33085372825764,
1.87820969243765));
#262092=CARTESIAN_POINT('Ctrl Pts',(-0.766455829364956,1.35409618904179,
1.87500861558817));
#262093=CARTESIAN_POINT('Ctrl Pts',(-0.733066475141972,1.37245953278343,
1.87238479674321));
#262094=CARTESIAN_POINT('Ctrl Pts',(-0.56645380388515,1.45627463095802,
1.8597461301558));
#262095=CARTESIAN_POINT('Ctrl Pts',(-0.425009595465675,1.50365518876915,
1.85032423358379));
#262096=CARTESIAN_POINT('Ctrl Pts',(-0.238621175762419,1.53763571528676,
1.83745759292732));
#262097=CARTESIAN_POINT('Ctrl Pts',(-0.197985151011992,1.54339399908261,
1.83463214355934));
#262098=CARTESIAN_POINT('Ctrl Pts',(-0.146637237718799,1.54860901894201,
1.83101347968691));
#262099=CARTESIAN_POINT('Ctrl Pts',(-0.136092201497207,1.54957132003462,
1.8302678219552));
#262100=CARTESIAN_POINT('Ctrl Pts',(-0.119207433701079,1.55093848412426,
1.82906948443873));
#262101=CARTESIAN_POINT('Ctrl Pts',(-0.112873483647187,1.55141231408734,
1.82861896930488));
#262102=CARTESIAN_POINT('Ctrl Pts',(-0.100858842132922,1.55223713915853,
1.82776245321388));
#262103=CARTESIAN_POINT('Ctrl Pts',(-0.0951787643389158,1.55259577593654,
1.82735669865388));
#262104=CARTESIAN_POINT('Ctrl Pts',(-0.0822723549671218,1.55333958850972,
1.82643279439289));
#262105=CARTESIAN_POINT('Ctrl Pts',(-0.0750450926790592,1.55370552177986,
1.82591405151677));
#262106=CARTESIAN_POINT('Ctrl Pts',(-0.056327483516959,1.5545223362645,
1.82456687443632));
#262107=CARTESIAN_POINT('Ctrl Pts',(-0.0448344048639791,1.55489624807369,
1.8237360593247));
#262108=CARTESIAN_POINT('Ctrl Pts',(0.0363500978597772,1.55663664853768,
1.81784067734403));
#262109=CARTESIAN_POINT('Ctrl Pts',(0.106049312290989,1.55344450346363,
1.81263499302348));
#262110=CARTESIAN_POINT('Ctrl Pts',(0.315395539172179,1.52970185517637,
1.79656972815335));
#262111=CARTESIAN_POINT('Ctrl Pts',(0.452678852057619,1.49483838672386,
1.78539095311863));
#262112=CARTESIAN_POINT('Ctrl Pts',(0.59369970741916,1.43778467629534,1.77405784404128));
#262113=CARTESIAN_POINT('Ctrl Pts',(0.603972194002272,1.43349981667712,
1.77323366411187));
#262114=CARTESIAN_POINT('Ctrl Pts',(0.621925383880897,1.42578392677025,
1.77179671640506));
#262115=CARTESIAN_POINT('Ctrl Pts',(0.629625777317752,1.42240021722516,
1.77118152167332));
#262116=CARTESIAN_POINT('Ctrl Pts',(0.64100733787043,1.41728838715945,1.77027431798438));
#262117=CARTESIAN_POINT('Ctrl Pts',(0.644709614890929,1.41560810009983,
1.76997954572683));
#262118=CARTESIAN_POINT('Ctrl Pts',(0.65129681426246,1.41258728182764,1.76945572138618));
#262119=CARTESIAN_POINT('Ctrl Pts',(0.654184246032052,1.41125240193651,
1.76922633270959));
#262120=CARTESIAN_POINT('Ctrl Pts',(0.660429662715938,1.40834181527724,
1.7687306669433));
#262121=CARTESIAN_POINT('Ctrl Pts',(0.66378610875806,1.40676295467731,1.76846458718092));
#262122=CARTESIAN_POINT('Ctrl Pts',(0.67301685914613,1.40238044915316,1.76773357575377));
#262123=CARTESIAN_POINT('Ctrl Pts',(0.678879353614273,1.39955187259324,
1.76727014596271));
#262124=CARTESIAN_POINT('Ctrl Pts',(0.709072087295222,1.38474991746273,
1.76488686325054));
#262125=CARTESIAN_POINT('Ctrl Pts',(0.733105794834983,1.37217771734653,
1.76300136101093));
#262126=CARTESIAN_POINT('Ctrl Pts',(0.77266394948833,1.35014827679315,1.75989673219746));
#262127=CARTESIAN_POINT('Ctrl Pts',(0.7883722841313,1.34103659188896,1.75866357564278));
#262128=CARTESIAN_POINT('Ctrl Pts',(0.882929419251218,1.28395245030337,
1.75121624498494));
#262129=CARTESIAN_POINT('Ctrl Pts',(0.957543059242679,1.22931347021834,
1.74522565333123));
#262130=CARTESIAN_POINT('Ctrl Pts',(1.09234809824048,1.11083473925866,1.73335461401746));
#262131=CARTESIAN_POINT('Ctrl Pts',(1.15285859151246,1.04789875654755,1.72750663759628));
#262132=CARTESIAN_POINT('Ctrl Pts',(1.21581750678459,0.970325143893713,
1.72052444175251));
#262133=CARTESIAN_POINT('Ctrl Pts',(1.22373672547135,0.960318439021049,
1.71962795593485));
#262134=CARTESIAN_POINT('Ctrl Pts',(1.23569882941055,0.944814895266383,
1.71824473691866));
#262135=CARTESIAN_POINT('Ctrl Pts',(1.23983029878132,0.939386827064705,
1.71776150360598));
#262136=CARTESIAN_POINT('Ctrl Pts',(1.24729275858127,0.929447400600994,
1.71687846043688));
#262137=CARTESIAN_POINT('Ctrl Pts',(1.25063532968746,0.924944845231504,
1.71647911170693));
#262138=CARTESIAN_POINT('Ctrl Pts',(1.25787689958614,0.915079187808012,
1.71560548311861));
#262139=CARTESIAN_POINT('Ctrl Pts',(1.26176608340618,0.909709053884518,
1.71513083375291));
#262140=CARTESIAN_POINT('Ctrl Pts',(1.27233378375205,0.894919172739021,
1.71382591642106));
#262141=CARTESIAN_POINT('Ctrl Pts',(1.2789418120262,0.88544983544469,1.71299297838618));
#262142=CARTESIAN_POINT('Ctrl Pts',(1.31312552045382,0.835283346940942,
1.7085925973663));
#262143=CARTESIAN_POINT('Ctrl Pts',(1.33886288296008,0.793373868182999,
1.70495740101626));
#262144=CARTESIAN_POINT('Ctrl Pts',(1.38923264894595,0.701903118062805,
1.69710031627947));
#262145=CARTESIAN_POINT('Ctrl Pts',(1.41326210986097,0.652158504367882,
1.69287163113236));
#262146=CARTESIAN_POINT('Ctrl Pts',(1.43457689162107,0.601306404445218,
1.68861155768856));
#262147=CARTESIAN_POINT('',(-1.55549938654046,-0.00138147466141999,1.85539356957841));
#262148=CARTESIAN_POINT('Ctrl Pts',(1.4345766830264,0.601306902103224,1.55150291788058));
#262149=CARTESIAN_POINT('Ctrl Pts',(1.42949793920172,0.613423589013786,
1.55248115921441));
#262150=CARTESIAN_POINT('Ctrl Pts',(1.42426542712662,0.625476549069427,
1.55345249348743));
#262151=CARTESIAN_POINT('Ctrl Pts',(1.41633033900459,0.643138661774095,
1.55487178320529));
#262152=CARTESIAN_POINT('Ctrl Pts',(1.4137462589228,0.6487992650372,1.55532603237192));
#262153=CARTESIAN_POINT('Ctrl Pts',(1.40944611972224,0.658071326022222,
1.556068884512));
#262154=CARTESIAN_POINT('Ctrl Pts',(1.40775001343898,0.661691873281577,
1.55635864851411));
#262155=CARTESIAN_POINT('Ctrl Pts',(1.40466500343922,0.668211652089188,
1.55687984476214));
#262156=CARTESIAN_POINT('Ctrl Pts',(1.40328106519625,0.671113132438782,
1.55711157102549));
#262157=CARTESIAN_POINT('Ctrl Pts',(1.40021806432876,0.677483931037409,
1.5576198891324));
#262158=CARTESIAN_POINT('Ctrl Pts',(1.39853510143924,0.680951301782332,
1.55789623606678));
#262159=CARTESIAN_POINT('Ctrl Pts',(1.39365850047321,0.6909041128148,1.55868867763136));
#262160=CARTESIAN_POINT('Ctrl Pts',(1.39043245945046,0.697373709107659,
1.55920281757204));
#262161=CARTESIAN_POINT('Ctrl Pts',(1.3672564223466,0.743051394906098,1.56282763042489));
#262162=CARTESIAN_POINT('Ctrl Pts',(1.34569387037553,0.781424593151184,
1.56584566725153));
#262163=CARTESIAN_POINT('Ctrl Pts',(1.28259567922718,0.883336705198955,
1.57392930813408));
#262164=CARTESIAN_POINT('Ctrl Pts',(1.2379930195827,0.944833370609119,1.57888734305577));
#262165=CARTESIAN_POINT('Ctrl Pts',(1.12281510440974,1.08140208053106,1.59065878281291));
#262166=CARTESIAN_POINT('Ctrl Pts',(1.04893893423033,1.15319844964057,1.59749006433035));
#262167=CARTESIAN_POINT('Ctrl Pts',(0.959168498732369,1.22463022042804,
1.60550191833294));
#262168=CARTESIAN_POINT('Ctrl Pts',(0.949721307648552,1.23197110742839,
1.60634152159061));
#262169=CARTESIAN_POINT('Ctrl Pts',(0.934276113839804,1.24368947520281,
1.6077090730623));
#262170=CARTESIAN_POINT('Ctrl Pts',(0.928329666999248,1.24813436518062,
1.60823437875882));
#262171=CARTESIAN_POINT('Ctrl Pts',(0.917701113890401,1.25596109490459,
1.60917129753163));
#262172=CARTESIAN_POINT('Ctrl Pts',(0.913031528153976,1.25935977119364,
1.6095822488111));
#262173=CARTESIAN_POINT('Ctrl Pts',(0.903162867687791,1.26645876618844,
1.6104493938483));
#262174=CARTESIAN_POINT('Ctrl Pts',(0.897959745182865,1.27015324501291,
1.61090580166129));
#262175=CARTESIAN_POINT('Ctrl Pts',(0.884142810635234,1.27983663183219,
1.61211583395515));
#262176=CARTESIAN_POINT('Ctrl Pts',(0.875491020225945,1.28577049945362,
1.61287152777009));
#262177=CARTESIAN_POINT('Ctrl Pts',(0.834492921488233,1.31328357399765,
1.61644384867149));
#262178=CARTESIAN_POINT('Ctrl Pts',(0.801407613239618,1.3337306780114,1.61930205921672));
#262179=CARTESIAN_POINT('Ctrl Pts',(0.637036195741412,1.42698888555464,
1.63339930743493));
#262180=CARTESIAN_POINT('Ctrl Pts',(0.49644928956724,1.48176788807067,1.64525271623756));
#262181=CARTESIAN_POINT('Ctrl Pts',(0.312686866350959,1.52423522319639,
1.6596225523211));
#262182=CARTESIAN_POINT('Ctrl Pts',(0.274816419531242,1.53151645114127,
1.66252053084479));
#262183=CARTESIAN_POINT('Ctrl Pts',(0.230139881534336,1.53839529596743,
1.66583737893387));
#262184=CARTESIAN_POINT('Ctrl Pts',(0.223562299561263,1.5393649190997,1.66632312995626));
#262185=CARTESIAN_POINT('Ctrl Pts',(0.212891388633283,1.54086811343609,
1.66710678251544));
#262186=CARTESIAN_POINT('Ctrl Pts',(0.20880189007726,1.54142760391925,1.66740606536487));
#262187=CARTESIAN_POINT('Ctrl Pts',(0.201515529782023,1.54239493215045,
1.66793739230427));
#262188=CARTESIAN_POINT('Ctrl Pts',(0.19831958767141,1.54280911888772,1.66816978525784));
#262189=CARTESIAN_POINT('Ctrl Pts',(0.191399234354368,1.54368412111581,
1.66867156779913));
#262190=CARTESIAN_POINT('Ctrl Pts',(0.187674439745266,1.5441413918967,1.66894075718334));
#262191=CARTESIAN_POINT('Ctrl Pts',(0.17723912503843,1.54538415598162,1.66969251809616));
#262192=CARTESIAN_POINT('Ctrl Pts',(0.170524979162174,1.5461394286817,1.67017343489546));
#262193=CARTESIAN_POINT('Ctrl Pts',(0.130503759600618,1.55037753216908,
1.67302471411423));
#262194=CARTESIAN_POINT('Ctrl Pts',(0.0970931573111436,1.55282808649424,
1.67534185874847));
#262195=CARTESIAN_POINT('Ctrl Pts',(-0.107253913315879,1.56119373741955,
1.68927255530099));
#262196=CARTESIAN_POINT('Ctrl Pts',(-0.278122108333887,1.53996374451727,
1.70002491625374));
#262197=CARTESIAN_POINT('Ctrl Pts',(-0.443325082000494,1.49098782518629,
1.71187508691197));
#262198=CARTESIAN_POINT('Ctrl Pts',(-0.444527182648,1.49062986923554,1.71196138738509));
#262199=CARTESIAN_POINT('Ctrl Pts',(-0.469993564734121,1.48301306315438,
1.71379120525399));
#262200=CARTESIAN_POINT('Ctrl Pts',(-0.494076136857859,1.47516451321403,
1.71555153770954));
#262201=CARTESIAN_POINT('Ctrl Pts',(-0.52673290763341,1.46363224530571,
1.71798512910616));
#262202=CARTESIAN_POINT('Ctrl Pts',(-0.535482390997831,1.46045387044117,
1.71864176765678));
#262203=CARTESIAN_POINT('Ctrl Pts',(-0.549365279600562,1.45526918801366,
1.71969129137074));
#262204=CARTESIAN_POINT('Ctrl Pts',(-0.554517563422742,1.45331376187195,
1.72008248044149));
#262205=CARTESIAN_POINT('Ctrl Pts',(-0.565074550062345,1.44924279836446,
1.72088754764572));
#262206=CARTESIAN_POINT('Ctrl Pts',(-0.570478014085313,1.44712431031574,
1.72130151920057));
#262207=CARTESIAN_POINT('Ctrl Pts',(-0.582821028996978,1.44220522056503,
1.72225159077979));
#262208=CARTESIAN_POINT('Ctrl Pts',(-0.589752431596045,1.43938470044253,
1.72278835320441));
#262209=CARTESIAN_POINT('Ctrl Pts',(-0.611390071788284,1.43039740297878,
1.72447429107726));
#262210=CARTESIAN_POINT('Ctrl Pts',(-0.626021575923056,1.42405459924818,
1.72562938090733));
#262211=CARTESIAN_POINT('Ctrl Pts',(-0.659917215290968,1.40873740908626,
1.72834156570365));
#262212=CARTESIAN_POINT('Ctrl Pts',(-0.679099671132186,1.39959114535965,
1.72990429881964));
#262213=CARTESIAN_POINT('Ctrl Pts',(-0.746010359930316,1.36598849205803,
1.73545590740555));
#262214=CARTESIAN_POINT('Ctrl Pts',(-0.79265113832465,1.3394622377052,1.7395110802964));
#262215=CARTESIAN_POINT('Ctrl Pts',(-0.904029186446442,1.26826088489775,
1.74964176990572));
#262216=CARTESIAN_POINT('Ctrl Pts',(-0.96692966888749,1.22098343534443,
1.75576913779383));
#262217=CARTESIAN_POINT('Ctrl Pts',(-1.07353906818084,1.12742932829995,
1.76671717593721));
#262218=CARTESIAN_POINT('Ctrl Pts',(-1.11850902213156,1.0828308649186,1.77154788201603));
#262219=CARTESIAN_POINT('Ctrl Pts',(-1.16597338339633,1.02963607527253,
1.77678706172197));
#262220=CARTESIAN_POINT('Ctrl Pts',(-1.17125884182497,1.0236196124858,1.77737257427929));
#262221=CARTESIAN_POINT('Ctrl Pts',(-1.17915976994911,1.01448462097367,
1.77825066547507));
#262222=CARTESIAN_POINT('Ctrl Pts',(-1.18180974435766,1.01139633103077,
1.77854566842986));
#262223=CARTESIAN_POINT('Ctrl Pts',(-1.18653373032254,1.00584706292034,
1.77907238458635));
#262224=CARTESIAN_POINT('Ctrl Pts',(-1.18861224342836,1.00339002517113,
1.77930442209405));
#262225=CARTESIAN_POINT('Ctrl Pts',(-1.19312553998957,0.998021093069249,
1.77980889308389));
#262226=CARTESIAN_POINT('Ctrl Pts',(-1.1955572930282,0.99510673613754,1.78008110723755));
#262227=CARTESIAN_POINT('Ctrl Pts',(-1.20241453719153,0.986827188448362,
1.78084997135814));
#262228=CARTESIAN_POINT('Ctrl Pts',(-1.20681482330775,0.981441086455878,
1.78134484328317));
#262229=CARTESIAN_POINT('Ctrl Pts',(-1.2344088629729,0.947198826155264,
1.78445902357458));
#262230=CARTESIAN_POINT('Ctrl Pts',(-1.25660464510444,0.917549007079306,
1.78701308876241));
#262231=CARTESIAN_POINT('Ctrl Pts',(-1.31058486458874,0.839802122581353,
1.79343686479274));
#262232=CARTESIAN_POINT('Ctrl Pts',(-1.34079371490773,0.790679097576037,
1.79724414685384));
#262233=CARTESIAN_POINT('Ctrl Pts',(-1.39692084927034,0.68690250745392,
1.80501613569411));
#262234=CARTESIAN_POINT('Ctrl Pts',(-1.42251840494302,0.63218985647847,
1.80897367910986));
#262235=CARTESIAN_POINT('Ctrl Pts',(-1.47032488640934,0.512296374354675,
1.81757527571476));
#262236=CARTESIAN_POINT('Ctrl Pts',(-1.49151670245953,0.446854349824916,
1.82223016809479));
#262237=CARTESIAN_POINT('Ctrl Pts',(-1.51114722757016,0.368983563398039,
1.82784170148304));
#262238=CARTESIAN_POINT('Ctrl Pts',(-1.51385682428068,0.357704230111939,
1.82865611756081));
#262239=CARTESIAN_POINT('Ctrl Pts',(-1.51806885680709,0.339264940776269,
1.82999064228205));
#262240=CARTESIAN_POINT('Ctrl Pts',(-1.51964741766889,0.332122683238821,
1.83050831603216));
#262241=CARTESIAN_POINT('Ctrl Pts',(-1.52237946125015,0.319334050182801,
1.83143672332191));
#262242=CARTESIAN_POINT('Ctrl Pts',(-1.52355205904101,0.313691857399968,
1.83184683915886));
#262243=CARTESIAN_POINT('Ctrl Pts',(-1.52576013074415,0.302762772016354,
1.83264229694041));
#262244=CARTESIAN_POINT('Ctrl Pts',(-1.52679954597543,0.297476751611537,
1.83302750693188));
#262245=CARTESIAN_POINT('Ctrl Pts',(-1.52899934045419,0.285974225842405,
1.83386681425304));
#262246=CARTESIAN_POINT('Ctrl Pts',(-1.53014930694245,0.279755852892933,
1.83432123552279));
#262247=CARTESIAN_POINT('Ctrl Pts',(-1.53286352839187,0.264561280920582,
1.83543335865316));
#262248=CARTESIAN_POINT('Ctrl Pts',(-1.53438687724789,0.255578114084439,
1.83609234040411));
#262249=CARTESIAN_POINT('Ctrl Pts',(-1.53996566034564,0.220830808418806,
1.83864734805022));
#262250=CARTESIAN_POINT('Ctrl Pts',(-1.54345157031347,0.194980973357823,
1.84056099832855));
#262251=CARTESIAN_POINT('Ctrl Pts',(-1.55247491780949,0.112448658570735,
1.84671483795149));
#262252=CARTESIAN_POINT('Ctrl Pts',(-1.55554994910745,0.0555504721415419,
1.85102502171189));
#262253=CARTESIAN_POINT('Ctrl Pts',(-1.55549938654046,-0.00138147466141999,
1.85539356957841));
#262254=CARTESIAN_POINT('Ctrl Pts',(-1.55549938776457,-0.0013800956646107,
1.85539346376413));
#262255=CARTESIAN_POINT('Ctrl Pts',(-1.55538499258098,-0.130314373632887,
1.86528695038457));
#262256=CARTESIAN_POINT('Ctrl Pts',(-1.53924107972692,-0.258738026691858,
1.87546978858605));
#262257=CARTESIAN_POINT('Ctrl Pts',(-1.50487644833776,-0.393744166409597,
1.88583137537503));
#262258=CARTESIAN_POINT('Ctrl Pts',(-1.5022203898513,-0.403759220324333,
1.88659759205956));
#262259=CARTESIAN_POINT('Ctrl Pts',(-1.49796387007771,-0.419185301674853,
1.88777327251184));
#262260=CARTESIAN_POINT('Ctrl Pts',(-1.49643376510856,-0.424615193295317,
1.88818623609406));
#262261=CARTESIAN_POINT('Ctrl Pts',(-1.49351459876753,-0.434762666153521,
1.88895620939144));
#262262=CARTESIAN_POINT('Ctrl Pts',(-1.49213264558227,-0.439482198017928,
1.88931359583662));
#262263=CARTESIAN_POINT('Ctrl Pts',(-1.48977183557845,-0.447405125687906,
1.88991225021017));
#262264=CARTESIAN_POINT('Ctrl Pts',(-1.48880498216734,-0.450612022002268,
1.89015420063082));
#262265=CARTESIAN_POINT('Ctrl Pts',(-1.48694934173345,-0.456695708852062,
1.89061247602489));
#262266=CARTESIAN_POINT('Ctrl Pts',(-1.48606255163317,-0.459573071906472,
1.89082891833997));
#262267=CARTESIAN_POINT('Ctrl Pts',(-1.48371393148164,-0.46711574703639,
1.89139554012947));
#262268=CARTESIAN_POINT('Ctrl Pts',(-1.48223843588305,-0.471776824914916,
1.89174492909669));
#262269=CARTESIAN_POINT('Ctrl Pts',(-1.47702516980499,-0.487979585419309,
1.89295707142932));
#262270=CARTESIAN_POINT('Ctrl Pts',(-1.47317424690282,-0.499484824934753,
1.89381354141442));
#262271=CARTESIAN_POINT('Ctrl Pts',(-1.43724840276836,-0.602787383732344,
1.9014752561513));
#262272=CARTESIAN_POINT('Ctrl Pts',(-1.39676087985296,-0.691448179988233,
1.90785665448435));
#262273=CARTESIAN_POINT('Ctrl Pts',(-1.32169692530766,-0.821907808632035,
1.91776334461363));
#262274=CARTESIAN_POINT('Ctrl Pts',(-1.29279161788773,-0.866662986828566,
1.92126556897074));
#262275=CARTESIAN_POINT('Ctrl Pts',(-1.23593806779234,-0.94549963738856,
1.92775448249206));
#262276=CARTESIAN_POINT('Ctrl Pts',(-1.20872877063328,-0.980044252883185,
1.93072127399104));
#262277=CARTESIAN_POINT('Ctrl Pts',(-1.16203011148658,-1.03442503248422,
1.93564591353479));
#262278=CARTESIAN_POINT('Ctrl Pts',(-1.1434070225353,-1.05497362250637,
1.93757086389945));
#262279=CARTESIAN_POINT('Ctrl Pts',(-1.11799061111316,-1.08155404918583,
1.94015469906845));
#262280=CARTESIAN_POINT('Ctrl Pts',(-1.1116786785005,-1.08804075173548,
1.94079297721551));
#262281=CARTESIAN_POINT('Ctrl Pts',(-1.10151978967503,-1.09830024568838,
1.94181512995576));
#262282=CARTESIAN_POINT('Ctrl Pts',(-1.0977091453651,-1.10210884561348,
1.9421974121334));
#262283=CARTESIAN_POINT('Ctrl Pts',(-1.0897821085005,-1.10994973287904,
1.94299037406554));
#262284=CARTESIAN_POINT('Ctrl Pts',(-1.08566294827885,-1.11397909074632,
1.94340117328898));
#262285=CARTESIAN_POINT('Ctrl Pts',(-1.07626796928543,-1.12306764595055,
1.94433536886532));
#262286=CARTESIAN_POINT('Ctrl Pts',(-1.07097872002294,-1.12811269692917,
1.94485936502879));
#262287=CARTESIAN_POINT('Ctrl Pts',(-1.05721632549102,-1.14105567807739,
1.94621792822754));
#262288=CARTESIAN_POINT('Ctrl Pts',(-1.04869030294633,-1.14889645067528,
1.94705489950776));
#262289=CARTESIAN_POINT('Ctrl Pts',(-0.98862738161977,-1.20290638284154,
1.95291996585733));
#262290=CARTESIAN_POINT('Ctrl Pts',(-0.934155516572659,-1.24568001294183,
1.95808678075277));
#262291=CARTESIAN_POINT('Ctrl Pts',(-0.781485943385103,-1.34990435444065,
1.97217863977512));
#262292=CARTESIAN_POINT('Ctrl Pts',(-0.678977632791914,-1.40426095260128,
1.98127493536658));
#262293=CARTESIAN_POINT('Ctrl Pts',(-0.535260017485219,-1.46102239890852,
1.9930455335592));
#262294=CARTESIAN_POINT('Ctrl Pts',(-0.498598212611087,-1.47393696946553,
1.99596535599343));
#262295=CARTESIAN_POINT('Ctrl Pts',(-0.454776574836293,-1.48755097448557,
1.99932984970858));
#262296=CARTESIAN_POINT('Ctrl Pts',(-0.448051324438485,-1.48959043042102,
1.99984275035747));
#262297=CARTESIAN_POINT('Ctrl Pts',(-0.437657738833779,-1.49266556157411,
2.00062987404458));
#262298=CARTESIAN_POINT('Ctrl Pts',(-0.433999148669779,-1.4937334149272,
2.00090589052176));
#262299=CARTESIAN_POINT('Ctrl Pts',(-0.42724509040867,-1.49567785047648,
2.00141345010194));
#262300=CARTESIAN_POINT('Ctrl Pts',(-0.424150845743791,-1.49655827154781,
2.0016452060117));
#262301=CARTESIAN_POINT('Ctrl Pts',(-0.417155450802506,-1.49852526789335,
2.00216742583565));
#262302=CARTESIAN_POINT('Ctrl Pts',(-0.413252780308723,-1.49960621138355,
2.00245756229349));
#262303=CARTESIAN_POINT('Ctrl Pts',(-0.40170970674649,-1.5027548739734,
2.0033122751829));
#262304=CARTESIAN_POINT('Ctrl Pts',(-0.394057538850978,-1.50477957283972,
2.00387444798146));
#262305=CARTESIAN_POINT('Ctrl Pts',(-0.332756678753086,-1.52049957092653,
2.00834506589394));
#262306=CARTESIAN_POINT('Ctrl Pts',(-0.278419906757475,-1.53138170264221,
2.01210734784367));
#262307=CARTESIAN_POINT('Ctrl Pts',(-0.0891465103870856,-1.55887639352212,
2.02488919281763));
#262308=CARTESIAN_POINT('Ctrl Pts',(0.047293221060649,-1.56070725254469,
2.03359773365823));
#262309=CARTESIAN_POINT('Ctrl Pts',(0.205730075032876,-1.5420165184012,
2.04447952219237));
#262310=CARTESIAN_POINT('Ctrl Pts',(0.229154778366163,-1.53870978370918,
2.04610662302219));
#262311=CARTESIAN_POINT('Ctrl Pts',(0.269737219950002,-1.53203376487535,
2.04896359376813));
#262312=CARTESIAN_POINT('Ctrl Pts',(0.286930768307157,-1.5289069022523,
2.05018598565427));
#262313=CARTESIAN_POINT('Ctrl Pts',(0.311710154985867,-1.52396776922958,
2.05196674293335));
#262314=CARTESIAN_POINT('Ctrl Pts',(0.319341223582539,-1.52238699459602,
2.05251777034855));
#262315=CARTESIAN_POINT('Ctrl Pts',(0.332657803918739,-1.51952393910869,
2.05348408439427));
#262316=CARTESIAN_POINT('Ctrl Pts',(0.338348637947812,-1.51826691116625,
2.05389855878551));
#262317=CARTESIAN_POINT('Ctrl Pts',(0.349360875367013,-1.51576946925564,
2.05470361324727));
#262318=CARTESIAN_POINT('Ctrl Pts',(0.354683079283868,-1.51453293692481,
2.05509406349522));
#262319=CARTESIAN_POINT('Ctrl Pts',(0.367361603793998,-1.51151678261298,
2.05602751618959));
#262320=CARTESIAN_POINT('Ctrl Pts',(0.374711606521245,-1.5097114758275,
2.05657133595602));
#262321=CARTESIAN_POINT('Ctrl Pts',(0.401108853599507,-1.50302314578475,
2.05853429542472));
#262322=CARTESIAN_POINT('Ctrl Pts',(0.420075544011653,-1.49783288812394,
2.05996324906894));
#262323=CARTESIAN_POINT('Ctrl Pts',(0.6113186963147,-1.4415809674105,2.07456739024955));
#262324=CARTESIAN_POINT('Ctrl Pts',(0.773595403711356,-1.36139020385998,
2.08881230446037));
#262325=CARTESIAN_POINT('Ctrl Pts',(0.945861485354785,-1.23534332848347,
2.10500840146732));
#262326=CARTESIAN_POINT('Ctrl Pts',(0.97253404260021,-1.21445669426599,
2.10754445494982));
#262327=CARTESIAN_POINT('Ctrl Pts',(1.00369283351676,-1.18837145249997,
2.11052214192413));
#262328=CARTESIAN_POINT('Ctrl Pts',(1.00885167484771,-1.18399506579218,
2.11101565497474));
#262329=CARTESIAN_POINT('Ctrl Pts',(1.01682911972012,-1.17713758241263,
2.11177938428429));
#262330=CARTESIAN_POINT('Ctrl Pts',(1.01966748396584,-1.17467977321128,
2.11205123336971));
#262331=CARTESIAN_POINT('Ctrl Pts',(1.02492535535232,-1.17009343643565,
2.11255498474));
#262332=CARTESIAN_POINT('Ctrl Pts',(1.02734712686369,-1.16796768589668,
2.11278707447444));
#262333=CARTESIAN_POINT('Ctrl Pts',(1.03285384397178,-1.16310369309019,
2.11331497276618));
#262334=CARTESIAN_POINT('Ctrl Pts',(1.03593451372078,-1.16036069746794,
2.11361042268479));
#262335=CARTESIAN_POINT('Ctrl Pts',(1.04394540730739,-1.15317055090816,
2.11437914111468));
#262336=CARTESIAN_POINT('Ctrl Pts',(1.04885820209299,-1.14870396925677,
2.11485100519347));
#262337=CARTESIAN_POINT('Ctrl Pts',(1.08196312978606,-1.11821639460408,
2.11803489272853));
#262338=CARTESIAN_POINT('Ctrl Pts',(1.10921570273056,-1.0911889172588,2.12067694432897));
#262339=CARTESIAN_POINT('Ctrl Pts',(1.23785287999457,-0.953808185164887,
2.13342705634154));
#262340=CARTESIAN_POINT('Ctrl Pts',(1.32392613459265,-0.83021427623846,
2.14293675167309));
#262341=CARTESIAN_POINT('Ctrl Pts',(1.40857223896123,-0.661094844466187,
2.1557981836645));
#262342=CARTESIAN_POINT('Ctrl Pts',(1.42480998331716,-0.625330483879022,
2.15850489772792));
#262343=CARTESIAN_POINT('Ctrl Pts',(1.44366156506559,-0.57925150487408,
2.16199604935914));
#262344=CARTESIAN_POINT('Ctrl Pts',(1.44754772196033,-0.569470458694504,
2.16273728224994));
#262345=CARTESIAN_POINT('Ctrl Pts',(1.45363283673408,-0.553690023419767,
2.16393381203582));
#262346=CARTESIAN_POINT('Ctrl Pts',(1.45589465606157,-0.547715084972244,
2.16438700080556));
#262347=CARTESIAN_POINT('Ctrl Pts',(1.46013036130729,-0.536314193282347,
2.16525210349797));
#262348=CARTESIAN_POINT('Ctrl Pts',(1.4621109745447,-0.530890838489971,
2.16566378517008));
#262349=CARTESIAN_POINT('Ctrl Pts',(1.46656449221328,-0.518482159325499,
2.16660613951145));
#262350=CARTESIAN_POINT('Ctrl Pts',(1.46901775021251,-0.511489985632441,
2.16713745238744));
#262351=CARTESIAN_POINT('Ctrl Pts',(1.47528591587566,-0.493207599844335,
2.16852760986062));
#262352=CARTESIAN_POINT('Ctrl Pts',(1.47902113470459,-0.481890795235131,
2.16938904835694));
#262353=CARTESIAN_POINT('Ctrl Pts',(1.51470066127733,-0.369466273351515,
2.17795781999972));
#262354=CARTESIAN_POINT('Ctrl Pts',(1.53635080533132,-0.265406936443129,
2.18600603168384));
#262355=CARTESIAN_POINT('Ctrl Pts',(1.55578618964926,-0.077432978740626,
2.20062071586958));
#262356=CARTESIAN_POINT('Ctrl Pts',(1.55770196251515,0.00566340668308941,
2.20709852841827));
#262357=CARTESIAN_POINT('Ctrl Pts',(1.55101756352495,0.12293564772127,2.21601557926069));
#262358=CARTESIAN_POINT('Ctrl Pts',(1.54791200045187,0.157281765443562,
2.21859831285309));
#262359=CARTESIAN_POINT('Ctrl Pts',(1.54283022917094,0.198245672491054,
2.22162324447463));
#262360=CARTESIAN_POINT('Ctrl Pts',(1.54194908384755,0.20498656074154,2.22211920424176));
#262361=CARTESIAN_POINT('Ctrl Pts',(1.54051173636375,0.215448348308985,
2.2228858893746));
#262362=CARTESIAN_POINT('Ctrl Pts',(1.5399861958074,0.219173260687879,2.22315826748154));
#262363=CARTESIAN_POINT('Ctrl Pts',(1.53898549879714,0.226084637262817,
2.22366249174206));
#262364=CARTESIAN_POINT('Ctrl Pts',(1.53851396021596,0.229271505604267,
2.22389452858872));
#262365=CARTESIAN_POINT('Ctrl Pts',(1.53741759886222,0.236525490328586,
2.22442165847497));
#262366=CARTESIAN_POINT('Ctrl Pts',(1.53678653743202,0.240591604769501,
2.22471639704041));
#262367=CARTESIAN_POINT('Ctrl Pts',(1.53510031819862,0.251179024854326,
2.22548203696888));
#262368=CARTESIAN_POINT('Ctrl Pts',(1.53401972506342,0.257696287670466,
2.22595155222362));
#262369=CARTESIAN_POINT('Ctrl Pts',(1.52649951879612,0.301327693421585,
2.22908406235724));
#262370=CARTESIAN_POINT('Ctrl Pts',(1.51875445814113,0.338207976083737,
2.23167962899964));
#262371=CARTESIAN_POINT('Ctrl Pts',(1.49045761928223,0.45219417480216,2.23964144827837));
#262372=CARTESIAN_POINT('Ctrl Pts',(1.46533588500121,0.527922725757585,
2.24484847407491));
#262373=CARTESIAN_POINT('Ctrl Pts',(1.43457657517513,0.601307159410884,
2.25008958711186));
#262374=CARTESIAN_POINT('Origin',(0.,0.,-1.29405622560371));
#262375=CARTESIAN_POINT('',(1.43457670182626,0.601306857251191,3.08743730443809));
#262376=CARTESIAN_POINT('',(1.43457668232327,0.601306903780717,2.94872114469929));
#262377=CARTESIAN_POINT('',(1.43457668357355,0.601306900797845,-1.29405622560371));
#262378=CARTESIAN_POINT('Ctrl Pts',(1.43457670182626,0.601306857251181,
3.08743730443809));
#262379=CARTESIAN_POINT('Ctrl Pts',(1.46774209616445,0.522182028637142,
3.08172695245763));
#262380=CARTESIAN_POINT('Ctrl Pts',(1.49431527012455,0.440423298556932,
3.07614889058204));
#262381=CARTESIAN_POINT('Ctrl Pts',(1.52964391206799,0.290538795584047,
3.06591309957777));
#262382=CARTESIAN_POINT('Ctrl Pts',(1.5408998950646,0.223268878613844,3.06131690589896));
#262383=CARTESIAN_POINT('Ctrl Pts',(1.54937676033112,0.138888701868872,
3.05542021869638));
#262384=CARTESIAN_POINT('Ctrl Pts',(1.55077681655962,0.122268739439419,
3.05425275856998));
#262385=CARTESIAN_POINT('Ctrl Pts',(1.55242485109702,0.098055925063515,
3.05254175184623));
#262386=CARTESIAN_POINT('Ctrl Pts',(1.55288491538876,0.090478277050115,
3.05200482820358));
#262387=CARTESIAN_POINT('Ctrl Pts',(1.55359529967532,0.077167501855097,
3.05105899907139));
#262388=CARTESIAN_POINT('Ctrl Pts',(1.55386939980407,0.0714357421323946,
3.05065084429601));
#262389=CARTESIAN_POINT('Ctrl Pts',(1.55434089145987,0.0602832155659266,
3.04985492729094));
#262390=CARTESIAN_POINT('Ctrl Pts',(1.55454165569358,0.0548626674629069,
3.04946727657302));
#262391=CARTESIAN_POINT('Ctrl Pts',(1.55500338651687,0.0403432225422172,
3.04842669971374));
#262392=CARTESIAN_POINT('Ctrl Pts',(1.55521283904623,0.0312430217269055,
3.04777217504043));
#262393=CARTESIAN_POINT('Ctrl Pts',(1.55568968887484,-0.00225329086883831,
3.04535404575373));
#262394=CARTESIAN_POINT('Ctrl Pts',(1.55546296879262,-0.0266516949009347,
3.04357519287758));
#262395=CARTESIAN_POINT('Ctrl Pts',(1.54896109538769,-0.224722200085808,
3.02898273588573));
#262396=CARTESIAN_POINT('Ctrl Pts',(1.5141880028679,-0.396216312241429,
3.01520270121296));
#262397=CARTESIAN_POINT('Ctrl Pts',(1.43978562106666,-0.589682159621664,
2.99947919619744));
#262398=CARTESIAN_POINT('Ctrl Pts',(1.42672036046807,-0.620626397851031,
2.99696533613715));
#262399=CARTESIAN_POINT('Ctrl Pts',(1.40986150927731,-0.657202818956143,
2.99401454272213));
#262400=CARTESIAN_POINT('Ctrl Pts',(1.40702140041963,-0.663261489688012,
2.99352645908383));
#262401=CARTESIAN_POINT('Ctrl Pts',(1.40254588781376,-0.67265076112479,
2.9927713624617));
#262402=CARTESIAN_POINT('Ctrl Pts',(1.40093756073984,-0.675994057337581,
2.9925027481483));
#262403=CARTESIAN_POINT('Ctrl Pts',(1.397928035989,-0.682193209345491,2.99200520516163));
#262404=CARTESIAN_POINT('Ctrl Pts',(1.39653005189859,-0.685050496793545,
2.99177609203497));
#262405=CARTESIAN_POINT('Ctrl Pts',(1.39332576720341,-0.691549041637331,
2.99125546689188));
#262406=CARTESIAN_POINT('Ctrl Pts',(1.39151395467407,-0.695187518231353,
2.99096430163952));
#262407=CARTESIAN_POINT('Ctrl Pts',(1.38675548170837,-0.704650330570732,
2.99020779649077));
#262408=CARTESIAN_POINT('Ctrl Pts',(1.38378634610123,-0.710463374658684,
2.98974381240098));
#262409=CARTESIAN_POINT('Ctrl Pts',(1.36367801113416,-0.749227634954817,
2.98665353206283));
#262410=CARTESIAN_POINT('Ctrl Pts',(1.34539822847524,-0.781577848333375,
2.98409293756511));
#262411=CARTESIAN_POINT('Ctrl Pts',(1.32116138060967,-0.82109539922213,
2.98094856265592));
#262412=CARTESIAN_POINT('Ctrl Pts',(1.31627725142367,-0.828902437897368,
2.98032654045963));
#262413=CARTESIAN_POINT('Ctrl Pts',(1.2525261400118,-0.928820905353651,
2.97234883778091));
#262414=CARTESIAN_POINT('Ctrl Pts',(1.18417591170568,-1.01452448147179,
2.96530066416187));
#262415=CARTESIAN_POINT('Ctrl Pts',(1.0633040219609,-1.13706104320945,2.95382583976959));
#262416=CARTESIAN_POINT('Ctrl Pts',(1.01654568798507,-1.17904903767613,
2.94957586124099));
#262417=CARTESIAN_POINT('Ctrl Pts',(0.954864096200996,-1.22803515713081,
2.9440943431103));
#262418=CARTESIAN_POINT('Ctrl Pts',(0.942193879515839,-1.23778287660688,
2.94297470923135));
#262419=CARTESIAN_POINT('Ctrl Pts',(0.923391289703923,-1.251792506168,2.94132108960339));
#262420=CARTESIAN_POINT('Ctrl Pts',(0.917374572372189,-1.25620851886206,
2.94079310659225));
#262421=CARTESIAN_POINT('Ctrl Pts',(0.90669108507752,-1.26393205593711,
2.93985751731442));
#262422=CARTESIAN_POINT('Ctrl Pts',(0.902037377766745,-1.26725748500327,
2.93945061008496));
#262423=CARTESIAN_POINT('Ctrl Pts',(0.892901035371278,-1.27371027503062,
2.93865292886185));
#262424=CARTESIAN_POINT('Ctrl Pts',(0.888420044164304,-1.27683982840649,
2.93826224643868));
#262425=CARTESIAN_POINT('Ctrl Pts',(0.876256230401911,-1.28524008434027,
2.93720313320042));
#262426=CARTESIAN_POINT('Ctrl Pts',(0.868542501960563,-1.2904654086738,
2.9365329990759));
#262427=CARTESIAN_POINT('Ctrl Pts',(0.839246145170708,-1.30992927153032,
2.93399313329773));
#262428=CARTESIAN_POINT('Ctrl Pts',(0.817357712092558,-1.32369747684409,
2.93210609734005));
#262429=CARTESIAN_POINT('Ctrl Pts',(0.79009169463593,-1.33991411309846,
2.92976665035238));
#262430=CARTESIAN_POINT('Ctrl Pts',(0.785028994360522,-1.3428865152119,
2.92933273525665));
#262431=CARTESIAN_POINT('Ctrl Pts',(0.636043349168608,-1.4292282440149,
2.91657696721538));
#262432=CARTESIAN_POINT('Ctrl Pts',(0.479696703621871,-1.48899749632878,
2.90339088856393));
#262433=CARTESIAN_POINT('Ctrl Pts',(0.284395554843879,-1.52964158812443,
2.88826310779952));
#262434=CARTESIAN_POINT('Ctrl Pts',(0.25165473062136,-1.53536788196153,
2.8857761781118));
#262435=CARTESIAN_POINT('Ctrl Pts',(0.212147366300636,-1.54097964149389,
2.88285268485845));
#262436=CARTESIAN_POINT('Ctrl Pts',(0.205535918879187,-1.54187540057457,
2.88236603748075));
#262437=CARTESIAN_POINT('Ctrl Pts',(0.195243435083639,-1.54320250894074,
2.88161267637891));
#262438=CARTESIAN_POINT('Ctrl Pts',(0.191566382148108,-1.5436632743428,
2.881344372868));
#262439=CARTESIAN_POINT('Ctrl Pts',(0.18472948109058,-1.54449518957619,
2.88084710723366));
#262440=CARTESIAN_POINT('Ctrl Pts',(0.181570168731373,-1.54486978284983,
2.88061796254175));
#262441=CARTESIAN_POINT('Ctrl Pts',(0.174366006877567,-1.5457015606306,
2.8800968837267));
#262442=CARTESIAN_POINT('Ctrl Pts',(0.170320500182812,-1.54615256269456,
2.87980529879377));
#262443=CARTESIAN_POINT('Ctrl Pts',(0.159763775885368,-1.54728751315787,
2.87904697823008));
#262444=CARTESIAN_POINT('Ctrl Pts',(0.153249838935343,-1.54794625337149,
2.87858160908596));
#262445=CARTESIAN_POINT('Ctrl Pts',(0.10934872973357,-1.55210603541351,
2.87546117164698));
#262446=CARTESIAN_POINT('Ctrl Pts',(0.071845772791788,-1.5542937466236,
2.8728732748488));
#262447=CARTESIAN_POINT('Ctrl Pts',(0.0251877133311025,-1.55532274585193,
2.86970903563867));
#262448=CARTESIAN_POINT('Ctrl Pts',(0.0160769427927272,-1.5554436030528,
2.86909379072456));
#262449=CARTESIAN_POINT('Ctrl Pts',(-0.0830404683954157,-1.55588745232811,
2.86242403333929));
#262450=CARTESIAN_POINT('Ctrl Pts',(-0.172915846772297,-1.54847775808896,
2.856578566149));
#262451=CARTESIAN_POINT('Ctrl Pts',(-0.347314940947573,-1.51871813082405,
2.84487518722786));
#262452=CARTESIAN_POINT('Ctrl Pts',(-0.431591415105831,-1.49694951544136,
2.83904396725075));
#262453=CARTESIAN_POINT('Ctrl Pts',(-0.525641819905539,-1.4640504143463,
2.83208050575296));
#262454=CARTESIAN_POINT('Ctrl Pts',(-0.537628837112943,-1.45969111630673,
2.83118444417943));
#262455=CARTESIAN_POINT('Ctrl Pts',(-0.555940981005288,-1.4527754097963,
2.82980174376558));
#262456=CARTESIAN_POINT('Ctrl Pts',(-0.562305369598177,-1.45032390668688,
2.82931860066859));
#262457=CARTESIAN_POINT('Ctrl Pts',(-0.573872816114587,-1.44578064948175,
2.82843565107156));
#262458=CARTESIAN_POINT('Ctrl Pts',(-0.579081105289074,-1.44370245115743,
2.82803630518541));
#262459=CARTESIAN_POINT('Ctrl Pts',(-0.590424061378311,-1.43910515847063,
2.82716259799904));
#262460=CARTESIAN_POINT('Ctrl Pts',(-0.596554058799803,-1.43657491339688,
2.82668786672457));
#262461=CARTESIAN_POINT('Ctrl Pts',(-0.613317280508964,-1.42952985670212,
2.82538250756394));
#262462=CARTESIAN_POINT('Ctrl Pts',(-0.623916494545244,-1.42493575020628,
2.82454920662095));
#262463=CARTESIAN_POINT('Ctrl Pts',(-0.679411582045571,-1.40014417303658,
2.82014334839106));
#262464=CARTESIAN_POINT('Ctrl Pts',(-0.72337615810115,-1.37794402819099,
2.81650283576617));
#262465=CARTESIAN_POINT('Ctrl Pts',(-0.893125605647638,-1.2818637863929,
2.80182550577675));
#262466=CARTESIAN_POINT('Ctrl Pts',(-1.00928541666132,-1.19255241530577,
2.79028406414977));
#262467=CARTESIAN_POINT('Ctrl Pts',(-1.13347603197739,-1.06574694037192,
2.7768422008073));
#262468=CARTESIAN_POINT('Ctrl Pts',(-1.15495411164472,-1.0424326464691,
2.77447296926127));
#262469=CARTESIAN_POINT('Ctrl Pts',(-1.18001709079506,-1.01350049549463,
2.77166915728551));
#262470=CARTESIAN_POINT('Ctrl Pts',(-1.18429598751108,-1.00849720230472,
2.77118903238763));
#262471=CARTESIAN_POINT('Ctrl Pts',(-1.19092129557197,-1.00064994286264,
2.77044355691128));
#262472=CARTESIAN_POINT('Ctrl Pts',(-1.19328951176967,-0.997824625005049,
2.77017666852129));
#262473=CARTESIAN_POINT('Ctrl Pts',(-1.19768432471044,-0.992543523345301,
2.76968065075127));
#262474=CARTESIAN_POINT('Ctrl Pts',(-1.19971340665289,-0.990089960356257,
2.76945134742045));
#262475=CARTESIAN_POINT('Ctrl Pts',(-1.20433711945371,-0.984463888972264,
2.76892813547101));
#262476=CARTESIAN_POINT('Ctrl Pts',(-1.20692675473208,-0.981287346161066,
2.76863458738079));
#262477=CARTESIAN_POINT('Ctrl Pts',(-1.21367878275593,-0.972937893945883,
2.76786775731323));
#262478=CARTESIAN_POINT('Ctrl Pts',(-1.21782072160465,-0.967748431868068,
2.7673958924056));
#262479=CARTESIAN_POINT('Ctrl Pts',(-1.24610217968112,-0.931845285032626,
2.76416253977896));
#262480=CARTESIAN_POINT('Ctrl Pts',(-1.26911296168295,-0.900255079734131,
2.76147376513764));
#262481=CARTESIAN_POINT('Ctrl Pts',(-1.37438254850477,-0.743664530601003,
2.74869960249207));
#262482=CARTESIAN_POINT('Ctrl Pts',(-1.43950589647837,-0.608106265900794,
2.7392028206991));
#262483=CARTESIAN_POINT('Ctrl Pts',(-1.49595404852199,-0.428050970372786,
2.72636753936062));
#262484=CARTESIAN_POINT('Ctrl Pts',(-1.50623046029735,-0.390353060063493,
2.72367439103407));
#262485=CARTESIAN_POINT('Ctrl Pts',(-1.51743733177194,-0.342159066350754,
2.72020430087715));
#262486=CARTESIAN_POINT('Ctrl Pts',(-1.51969585961313,-0.331983986682047,
2.71947019446641));
#262487=CARTESIAN_POINT('Ctrl Pts',(-1.52315831369877,-0.315608747190726,
2.71828604571868));
#262488=CARTESIAN_POINT('Ctrl Pts',(-1.52442705738191,-0.309422485409392,
2.71783807722669));
#262489=CARTESIAN_POINT('Ctrl Pts',(-1.5267690223959,-0.297639177172171,
2.71698354918531));
#262490=CARTESIAN_POINT('Ctrl Pts',(-1.52784922562394,-0.292043609255253,
2.71657721949318));
#262491=CARTESIAN_POINT('Ctrl Pts',(-1.53024325749635,-0.279265356581206,
2.71564801860801));
#262492=CARTESIAN_POINT('Ctrl Pts',(-1.53153729927371,-0.272079150366061,
2.71512452833244));
#262493=CARTESIAN_POINT('Ctrl Pts',(-1.53477574995357,-0.253339510907867,
2.71375685811168));
#262494=CARTESIAN_POINT('Ctrl Pts',(-1.53664027710408,-0.241772941500433,
2.71291017558365));
#262495=CARTESIAN_POINT('Ctrl Pts',(-1.54984432395086,-0.153528220502592,
2.70643007995584));
#262496=CARTESIAN_POINT('Ctrl Pts',(-1.55556693000821,-0.0761328717606003,
2.7006206256036));
#262497=CARTESIAN_POINT('Ctrl Pts',(-1.5554244222916,0.0874127041405672,
2.68809930640455));
#262498=CARTESIAN_POINT('Ctrl Pts',(-1.54820777027417,0.173313721931464,
2.68137810810466));
#262499=CARTESIAN_POINT('Ctrl Pts',(-1.53126018567324,0.27400806299856,
2.67351039372902));
#262500=CARTESIAN_POINT('Ctrl Pts',(-1.52834947844039,0.289803503858001,
2.67227693440786));
#262501=CARTESIAN_POINT('Ctrl Pts',(-1.51673895875536,0.34775873708832,
2.66775939431766));
#262502=CARTESIAN_POINT('Ctrl Pts',(-1.50653393184117,0.389601770587477,
2.66451336604147));
#262503=CARTESIAN_POINT('Ctrl Pts',(-1.4927231447756,0.437497415182287,
2.66085441510424));
#262504=CARTESIAN_POINT('Ctrl Pts',(-1.49079869057939,0.444010860111326,
2.66035806671069));
#262505=CARTESIAN_POINT('Ctrl Pts',(-1.48764426143674,0.454435482371629,
2.6595658926794));
#262506=CARTESIAN_POINT('Ctrl Pts',(-1.48644140658161,0.458354668425679,
2.65926857659677));
#262507=CARTESIAN_POINT('Ctrl Pts',(-1.48427470715647,0.465316050527937,
2.65874143026232));
#262508=CARTESIAN_POINT('Ctrl Pts',(-1.48331698031487,0.468360085662373,
2.65851125116392));
#262509=CARTESIAN_POINT('Ctrl Pts',(-1.48124634835806,0.474871313764481,
2.65801961268047));
#262510=CARTESIAN_POINT('Ctrl Pts',(-1.48013063539409,0.47833755034198,
2.65775831998459));
#262511=CARTESIAN_POINT('Ctrl Pts',(-1.47702761955545,0.487863017417177,
2.65704136931015));
#262512=CARTESIAN_POINT('Ctrl Pts',(-1.47501518342424,0.493914086777181,
2.6565871531279));
#262513=CARTESIAN_POINT('Ctrl Pts',(-1.46382750705937,0.52687532536351,
2.6541187831204));
#262514=CARTESIAN_POINT('Ctrl Pts',(-1.45395228286217,0.553544585872945,
2.65214284052181));
#262515=CARTESIAN_POINT('Ctrl Pts',(-1.38832521458323,0.716879516271307,
2.64008496955723));
#262516=CARTESIAN_POINT('Ctrl Pts',(-1.31408591333191,0.84531122344867,
2.63072916912009));
#262517=CARTESIAN_POINT('Ctrl Pts',(-1.19140830038867,1.00135625400519,
2.61735628775353));
#262518=CARTESIAN_POINT('Ctrl Pts',(-1.15802832559165,1.03977765962633,
2.61387541394079));
#262519=CARTESIAN_POINT('Ctrl Pts',(-1.11475543628918,1.08491320696422,
2.60949954607314));
#262520=CARTESIAN_POINT('Ctrl Pts',(-1.10658752416475,1.09324305972751,
2.60867920520538));
#262521=CARTESIAN_POINT('Ctrl Pts',(-1.0936124475559,1.10618099299924,2.60738428416947));
#262522=CARTESIAN_POINT('Ctrl Pts',(-1.08886794833194,1.11085154873121,
2.60691246753445));
#262523=CARTESIAN_POINT('Ctrl Pts',(-1.0804399564771,1.11904231773449,2.6060772149358));
#262524=CARTESIAN_POINT('Ctrl Pts',(-1.07676885125618,1.12257518601835,
2.60571433758587));
#262525=CARTESIAN_POINT('Ctrl Pts',(-1.06831381323696,1.13063221259578,
2.6048806936157));
#262526=CARTESIAN_POINT('Ctrl Pts',(-1.06351840707287,1.13514413140526,
2.60440940964866));
#262527=CARTESIAN_POINT('Ctrl Pts',(-1.05015816767556,1.14755558941676,
2.60310048957236));
#262528=CARTESIAN_POINT('Ctrl Pts',(-1.0415331586253,1.15538940348336,2.60226009217872));
#262529=CARTESIAN_POINT('Ctrl Pts',(-0.990213015635063,1.20096018260002,
2.59728537030449));
#262530=CARTESIAN_POINT('Ctrl Pts',(-0.945563734261361,1.23642018763241,
2.59305848426494));
#262531=CARTESIAN_POINT('Ctrl Pts',(-0.768596323846064,1.36176567643758,
2.57666024283518));
#262532=CARTESIAN_POINT('Ctrl Pts',(-0.624669107862679,1.43350152776506,
2.56391299303347));
#262533=CARTESIAN_POINT('Ctrl Pts',(-0.459877410272278,1.48602300904074,
2.55108669900979));
#262534=CARTESIAN_POINT('Ctrl Pts',(-0.447354641892783,1.48984075343229,
2.55012318946272));
#262535=CARTESIAN_POINT('Ctrl Pts',(-0.429974232812458,1.4949005017355,
2.54880270726187));
#262536=CARTESIAN_POINT('Ctrl Pts',(-0.425157012455512,1.49627767062338,
2.54843848806312));
#262537=CARTESIAN_POINT('Ctrl Pts',(-0.417437529773943,1.49844426113464,
2.54785775648594));
#262538=CARTESIAN_POINT('Ctrl Pts',(-0.414539541907525,1.49924856631844,
2.5476403996089));
#262539=CARTESIAN_POINT('Ctrl Pts',(-0.408484178970388,1.50091026691433,
2.54718762740592));
#262540=CARTESIAN_POINT('Ctrl Pts',(-0.405326411272183,1.50176611175629,
2.54695230844253));
#262541=CARTESIAN_POINT('Ctrl Pts',(-0.397648783096102,1.50382098724377,
2.54638204289761));
#262542=CARTESIAN_POINT('Ctrl Pts',(-0.393126118415454,1.50500962552287,
2.54604769207873));
#262543=CARTESIAN_POINT('Ctrl Pts',(-0.377080507556957,1.50914943779184,
2.54486682445075));
#262544=CARTESIAN_POINT('Ctrl Pts',(-0.365528759811657,1.51198891641533,
2.54402643591899));
#262545=CARTESIAN_POINT('Ctrl Pts',(-0.293270803642644,1.52887372718614,
2.53882375712783));
#262546=CARTESIAN_POINT('Ctrl Pts',(-0.231791194904814,1.53939517082956,
2.53463332818678));
#262547=CARTESIAN_POINT('Ctrl Pts',(-0.105269907564111,1.55329261530381,
2.52618638666746));
#262548=CARTESIAN_POINT('Ctrl Pts',(-0.0403193927686453,1.55633361141347,
2.52194200073317));
#262549=CARTESIAN_POINT('Ctrl Pts',(0.113215025401039,1.55390204546577,
2.51179222792609));
#262550=CARTESIAN_POINT('Ctrl Pts',(0.201503106760171,1.54493435817493,
2.50585647253301));
#262551=CARTESIAN_POINT('Ctrl Pts',(0.300241775964519,1.52629516488186,
2.49883861227433));
#262552=CARTESIAN_POINT('Ctrl Pts',(0.311917226452365,1.52395199543456,
2.49800288003116));
#262553=CARTESIAN_POINT('Ctrl Pts',(0.330762786646527,1.51994420623441,
2.49664378160146));
#262554=CARTESIAN_POINT('Ctrl Pts',(0.337950160475337,1.51836230747804,
2.49612304914987));
#262555=CARTESIAN_POINT('Ctrl Pts',(0.350689693844656,1.51546347594091,
2.49519567094962));
#262556=CARTESIAN_POINT('Ctrl Pts',(0.356246382530431,1.51416687377099,
2.49478968259899));
#262557=CARTESIAN_POINT('Ctrl Pts',(0.367907947435551,1.51137800960125,
2.49393446109253));
#262558=CARTESIAN_POINT('Ctrl Pts',(0.3740111515848,1.50987926737252,2.49348502626209));
#262559=CARTESIAN_POINT('Ctrl Pts',(0.390077659837113,1.50583048134034,
2.49229693506263));
#262560=CARTESIAN_POINT('Ctrl Pts',(0.400024897876221,1.50321857721106,
2.4915562987319));
#262561=CARTESIAN_POINT('Ctrl Pts',(0.446125973649888,1.49062356597216,
2.48809961677071));
#262562=CARTESIAN_POINT('Ctrl Pts',(0.481934162274265,1.47943435637402,
2.48534492991948));
#262563=CARTESIAN_POINT('Ctrl Pts',(0.643988906997105,1.42228841929179,
2.47254262700393));
#262564=CARTESIAN_POINT('Ctrl Pts',(0.764343325177799,1.36139405210565,
2.46201572695771));
#262565=CARTESIAN_POINT('Ctrl Pts',(0.920977311222372,1.25476187833795,
2.44743564227172));
#262566=CARTESIAN_POINT('Ctrl Pts',(0.964922439106366,1.22129144378709,
2.44324134478558));
#262567=CARTESIAN_POINT('Ctrl Pts',(1.01297668773709,1.18047447181703,2.43860940188017));
#262568=CARTESIAN_POINT('Ctrl Pts',(1.01891537024943,1.17535238276979,2.43803615902145));
#262569=CARTESIAN_POINT('Ctrl Pts',(1.0278277857804,1.16754714209027,2.43717496063763));
#262570=CARTESIAN_POINT('Ctrl Pts',(1.03083019268011,1.16489716329847,2.43688468280418));
#262571=CARTESIAN_POINT('Ctrl Pts',(1.03619592245224,1.16012428281628,2.43636568290767));
#262572=CARTESIAN_POINT('Ctrl Pts',(1.03856299538568,1.15800571955851,2.43613664977717));
#262573=CARTESIAN_POINT('Ctrl Pts',(1.04371395960431,1.15336703642048,2.43563808555478));
#262574=CARTESIAN_POINT('Ctrl Pts',(1.04649521718309,1.15084408648365,2.43536877190514));
#262575=CARTESIAN_POINT('Ctrl Pts',(1.05436096960117,1.14365676804982,2.43460669806228));
#262576=CARTESIAN_POINT('Ctrl Pts',(1.05942369023692,1.13896852748979,2.4341156942714));
#262577=CARTESIAN_POINT('Ctrl Pts',(1.09192886131023,1.10846343600315,2.4309586078739));
#262578=CARTESIAN_POINT('Ctrl Pts',(1.11845959081112,1.08168782791421,2.42836036331622));
#262579=CARTESIAN_POINT('Ctrl Pts',(1.21694413442665,0.9747915270411,2.41850125243184));
#262580=CARTESIAN_POINT('Ctrl Pts',(1.28148137261592,0.888245829324381,
2.41155201942595));
#262581=CARTESIAN_POINT('Ctrl Pts',(1.37374439069927,0.733272660487642,
2.39958638004565));
#262582=CARTESIAN_POINT('Ctrl Pts',(1.40649269259679,0.668308691645928,
2.39469560923041));
#262583=CARTESIAN_POINT('Ctrl Pts',(1.43457668658422,0.601306893615097,
2.38964409368597));
#262584=CARTESIAN_POINT('Ctrl Pts',(1.43457657517513,0.601307159410884,
2.25008958711186));
#262585=CARTESIAN_POINT('Ctrl Pts',(1.40787999711051,0.66499887657981,2.25463844676208));
#262586=CARTESIAN_POINT('Ctrl Pts',(1.3769368821431,0.726924889666375,2.25921276655968));
#262587=CARTESIAN_POINT('Ctrl Pts',(1.32835359323674,0.809800221634025,
2.26573866177729));
#262588=CARTESIAN_POINT('Ctrl Pts',(1.3141934242662,0.832583434589511,2.26757744870429));
#262589=CARTESIAN_POINT('Ctrl Pts',(1.28886519172717,0.871078496194537,
2.27077179473554));
#262590=CARTESIAN_POINT('Ctrl Pts',(1.27798087916106,0.886970148501126,
2.27211717264022));
#262591=CARTESIAN_POINT('Ctrl Pts',(1.26210337007526,0.909252972981009,
2.2740442368232));
#262592=CARTESIAN_POINT('Ctrl Pts',(1.25735063731273,0.915813985489399,
2.27461676737545));
#262593=CARTESIAN_POINT('Ctrl Pts',(1.24906008264253,0.927072672666492,
2.27560828412533));
#262594=CARTESIAN_POINT('Ctrl Pts',(1.24554643765249,0.931788012572387,
2.27602632922705));
#262595=CARTESIAN_POINT('Ctrl Pts',(1.2387618040858,0.940786098525371,2.276829481103));
#262596=CARTESIAN_POINT('Ctrl Pts',(1.23549512466424,0.945072000444913,
2.27721441512732));
#262597=CARTESIAN_POINT('Ctrl Pts',(1.22776703827887,0.955102746664643,
2.27812099159363));
#262598=CARTESIAN_POINT('Ctrl Pts',(1.22328750921978,0.960833400452387,
2.27864334477606));
#262599=CARTESIAN_POINT('Ctrl Pts',(1.20765321046644,0.980547777970117,
2.28045586327725));
#262600=CARTESIAN_POINT('Ctrl Pts',(1.19629791741044,0.99436988331831,2.28175399212581));
#262601=CARTESIAN_POINT('Ctrl Pts',(1.1033233685304,1.1036441198971,2.29224334566138));
#262602=CARTESIAN_POINT('Ctrl Pts',(1.01067128419277,1.18906819411496,2.30191358507367));
#262603=CARTESIAN_POINT('Ctrl Pts',(0.865672066590175,1.29345064413419,
2.31576709535217));
#262604=CARTESIAN_POINT('Ctrl Pts',(0.820991429587782,1.32226183013476,
2.31988077752487));
#262605=CARTESIAN_POINT('Ctrl Pts',(0.742978329420344,1.36708474471614,
2.32672393845409));
#262606=CARTESIAN_POINT('Ctrl Pts',(0.710389348395907,1.38429946877727,
2.32948868689261));
#262607=CARTESIAN_POINT('Ctrl Pts',(0.67098696973409,1.40335477384006,2.33269700132653));
#262608=CARTESIAN_POINT('Ctrl Pts',(0.664737137268901,1.4063259501083,2.33320196049432));
#262609=CARTESIAN_POINT('Ctrl Pts',(0.655035605193385,1.41085894242009,
2.33397950893901));
#262610=CARTESIAN_POINT('Ctrl Pts',(0.651597784565557,1.41244997343553,
2.33425382509069));
#262611=CARTESIAN_POINT('Ctrl Pts',(0.645227946972664,1.41536974253692,
2.33475980830705));
#262612=CARTESIAN_POINT('Ctrl Pts',(0.642297638311491,1.41670192907245,
2.33499167788606));
#262613=CARTESIAN_POINT('Ctrl Pts',(0.635644518256468,1.41970170656476,
2.33551611289776));
#262614=CARTESIAN_POINT('Ctrl Pts',(0.631919273235037,1.42136375441045,
2.33580833858881));
#262615=CARTESIAN_POINT('Ctrl Pts',(0.622251917433307,1.42563140320678,
2.33656313397546));
#262616=CARTESIAN_POINT('Ctrl Pts',(0.616299885785098,1.42821455014051,
2.33702438121305));
#262617=CARTESIAN_POINT('Ctrl Pts',(0.577848895946942,1.44461691803642,
2.33998293013297));
#262618=CARTESIAN_POINT('Ctrl Pts',(0.544900379448127,1.45736455604692,
2.34242105548473));
#262619=CARTESIAN_POINT('Ctrl Pts',(0.501891423484348,1.47234157218497,
2.34551560285442));
#262620=CARTESIAN_POINT('Ctrl Pts',(0.492206433915786,1.47560751585966,
2.34620679838473));
#262621=CARTESIAN_POINT('Ctrl Pts',(0.392691362852711,1.50807689887382,
2.3532579082713));
#262622=CARTESIAN_POINT('Ctrl Pts',(0.300406549579926,1.52913713562619,
2.35938349736952));
#262623=CARTESIAN_POINT('Ctrl Pts',(0.131635370515287,1.55177324016713,
2.3706616584296));
#262624=CARTESIAN_POINT('Ctrl Pts',(0.0558672381891772,1.55634334883733,
2.37575044688581));
#262625=CARTESIAN_POINT('Ctrl Pts',(-0.0376270146164141,1.55514560233141,
2.382243851419));
#262626=CARTESIAN_POINT('Ctrl Pts',(-0.0553224707870181,1.55461667823798,
2.38348194285182));
#262627=CARTESIAN_POINT('Ctrl Pts',(-0.0808294004021085,1.5534182383694,
2.38528144391646));
#262628=CARTESIAN_POINT('Ctrl Pts',(-0.0886513463083985,1.55299148420934,
2.38583529464545));
#262629=CARTESIAN_POINT('Ctrl Pts',(-0.102292937229947,1.55214382294013,
2.38680489062743));
#262630=CARTESIAN_POINT('Ctrl Pts',(-0.108114110830074,1.55174921602793,
2.3872198069088));
#262631=CARTESIAN_POINT('Ctrl Pts',(-0.119371162576086,1.55092247074394,
2.38802449941711));
#262632=CARTESIAN_POINT('Ctrl Pts',(-0.124807267737676,1.55049447894449,
2.38841413991957));
#262633=CARTESIAN_POINT('Ctrl Pts',(-0.13921462186189,1.54928391020798,
2.38944965329036));
#262634=CARTESIAN_POINT('Ctrl Pts',(-0.148181400589745,1.54845200492632,
2.39009706079054));
#262635=CARTESIAN_POINT('Ctrl Pts',(-0.180373823824945,1.54518312734855,
2.39243224235653));
#262636=CARTESIAN_POINT('Ctrl Pts',(-0.203550054538218,1.54230116346145,
2.39413382220271));
#262637=CARTESIAN_POINT('Ctrl Pts',(-0.399585175939417,1.51342879244656,
2.40870889729388));
#262638=CARTESIAN_POINT('Ctrl Pts',(-0.566976169987425,1.45898741140259,
2.42256666584745));
#262639=CARTESIAN_POINT('Ctrl Pts',(-0.751575039869815,1.36229550207755,
2.43837576876498));
#262640=CARTESIAN_POINT('Ctrl Pts',(-0.780890978319354,1.34570568342085,
2.44089704195184));
#262641=CARTESIAN_POINT('Ctrl Pts',(-0.815414932305842,1.32466009120535,
2.44385975133892));
#262642=CARTESIAN_POINT('Ctrl Pts',(-0.821159231444159,1.32110688066728,
2.44435247750877));
#262643=CARTESIAN_POINT('Ctrl Pts',(-0.830058506708602,1.31552164737929,
2.44511525613897));
#262644=CARTESIAN_POINT('Ctrl Pts',(-0.833229488323259,1.31351549282064,
2.44538693504053));
#262645=CARTESIAN_POINT('Ctrl Pts',(-0.839110402794,1.30976500478088,2.44589053516614));
#262646=CARTESIAN_POINT('Ctrl Pts',(-0.841822150807203,1.30802373930058,
2.44612264279364));
#262647=CARTESIAN_POINT('Ctrl Pts',(-0.847995212652573,1.30403274893734,
2.44665079212162));
#262648=CARTESIAN_POINT('Ctrl Pts',(-0.851452993612248,1.30177766600631,
2.44694647382793));
#262649=CARTESIAN_POINT('Ctrl Pts',(-0.860457754109468,1.29585374614435,
2.44771619587982));
#262650=CARTESIAN_POINT('Ctrl Pts',(-0.865990332165826,1.29216300317849,
2.44818882579668));
#262651=CARTESIAN_POINT('Ctrl Pts',(-0.903461756381395,1.26681731596414,
2.45138915219043));
#262652=CARTESIAN_POINT('Ctrl Pts',(-0.934612153072268,1.24401366517864,
2.45404605446767));
#262653=CARTESIAN_POINT('Ctrl Pts',(-1.08263455729948,1.12695127719115,
2.46682818372891));
#262654=CARTESIAN_POINT('Ctrl Pts',(-1.18628659767463,1.01727438248153,
2.47635589619498));
#262655=CARTESIAN_POINT('Ctrl Pts',(-1.29493883918945,0.862681913000764,
2.48921095800829));
#262656=CARTESIAN_POINT('Ctrl Pts',(-1.31605869328874,0.830105877099318,
2.49188708597596));
#262657=CARTESIAN_POINT('Ctrl Pts',(-1.34130764699851,0.787771526290683,
2.4953438173391));
#262658=CARTESIAN_POINT('Ctrl Pts',(-1.34658700302873,0.778712793810908,
2.49608227432604));
#262659=CARTESIAN_POINT('Ctrl Pts',(-1.35493081692038,0.764057219761254,
2.49727539489196));
#262660=CARTESIAN_POINT('Ctrl Pts',(-1.35805318489658,0.758493571824898,
2.49772797212015));
#262661=CARTESIAN_POINT('Ctrl Pts',(-1.36393683834896,0.747856878170622,
2.49859261336942));
#262662=CARTESIAN_POINT('Ctrl Pts',(-1.3667042744486,0.7427873408882,2.49900444922148));
#262663=CARTESIAN_POINT('Ctrl Pts',(-1.37296548099196,0.731164271938896,
2.49994815346791));
#262664=CARTESIAN_POINT('Ctrl Pts',(-1.37644065568313,0.724600940101763,
2.50048066871829));
#262665=CARTESIAN_POINT('Ctrl Pts',(-1.38539505704458,0.707392482455828,
2.5018760389895));
#262666=CARTESIAN_POINT('Ctrl Pts',(-1.39079852268976,0.69670872156705,
2.50274151984586));
#262667=CARTESIAN_POINT('Ctrl Pts',(-1.44160069586674,0.59331582697167,
2.51111115917462));
#262668=CARTESIAN_POINT('Ctrl Pts',(-1.47777843919311,0.496385912627004,
2.51893711419881));
#262669=CARTESIAN_POINT('Ctrl Pts',(-1.52279333931768,0.325672301892699,
2.53258185991097));
#262670=CARTESIAN_POINT('Ctrl Pts',(-1.53645671527855,0.253501648326342,
2.53830305351554));
#262671=CARTESIAN_POINT('Ctrl Pts',(-1.5503087862466,0.135024752427407,
2.54743274328808));
#262672=CARTESIAN_POINT('Ctrl Pts',(-1.55361973207785,0.089194837883794,
2.55090014149526));
#262673=CARTESIAN_POINT('Ctrl Pts',(-1.55510086053665,0.0359839820638677,
2.55480543319032));
#262674=CARTESIAN_POINT('Ctrl Pts',(-1.55525260587007,0.0286857272568646,
2.55533843638348));
#262675=CARTESIAN_POINT('Ctrl Pts',(-1.55540616765941,0.0175177963063136,
2.55614974754471));
#262676=CARTESIAN_POINT('Ctrl Pts',(-1.55544492957266,0.0136488655404375,
2.55643002229322));
#262677=CARTESIAN_POINT('Ctrl Pts',(-1.55548946381145,0.00656571190506091,
2.55694164937043));
#262678=CARTESIAN_POINT('Ctrl Pts',(-1.55549970995759,0.00335162418207283,
2.5571732400069));
#262679=CARTESIAN_POINT('Ctrl Pts',(-1.55550034567455,-0.00384388205011361,
2.55769045072654));
#262680=CARTESIAN_POINT('Ctrl Pts',(-1.55548541215615,-0.00782523789051597,
2.55797577183294));
#262681=CARTESIAN_POINT('Ctrl Pts',(-1.55539568864849,-0.0196458685768857,
2.55882046094463));
#262682=CARTESIAN_POINT('Ctrl Pts',(-1.55527692028593,-0.0274848409070515,
2.55937745432954));
#262683=CARTESIAN_POINT('Ctrl Pts',(-1.553548405089,-0.10358334601925,2.56475674076048));
#262684=CARTESIAN_POINT('Ctrl Pts',(-1.54750491514884,-0.171678409652982,
2.56935404680753));
#262685=CARTESIAN_POINT('Ctrl Pts',(-1.52736745018196,-0.301092762550527,
2.57804658936515));
#262686=CARTESIAN_POINT('Ctrl Pts',(-1.51399714917435,-0.362382484248962,
2.58214444458106));
#262687=CARTESIAN_POINT('Ctrl Pts',(-1.47235783137446,-0.509845793888468,
2.59226745183739));
#262688=CARTESIAN_POINT('Ctrl Pts',(-1.44019143391049,-0.594663994081574,
2.5983274905965));
#262689=CARTESIAN_POINT('Ctrl Pts',(-1.39561276286524,-0.687014985489912,
2.60548853499373));
#262690=CARTESIAN_POINT('Ctrl Pts',(-1.39026531057886,-0.697772832792645,
2.60633156853736));
#262691=CARTESIAN_POINT('Ctrl Pts',(-1.38140579429891,-0.715089937570975,
2.60770360957363));
#262692=CARTESIAN_POINT('Ctrl Pts',(-1.37797026375547,-0.721687976952016,
2.60822994562417));
#262693=CARTESIAN_POINT('Ctrl Pts',(-1.37178276421229,-0.733365989556275,
2.60916801759704));
#262694=CARTESIAN_POINT('Ctrl Pts',(-1.36904955107434,-0.738455788713131,
2.60957908572664));
#262695=CARTESIAN_POINT('Ctrl Pts',(-1.36324155012157,-0.749128391751868,
2.61044577506964));
#262696=CARTESIAN_POINT('Ctrl Pts',(-1.3601606839041,-0.754707746771307,
2.61090160670166));
#262697=CARTESIAN_POINT('Ctrl Pts',(-1.35193540969707,-0.769389508477288,
2.6121084842876));
#262698=CARTESIAN_POINT('Ctrl Pts',(-1.34673344259631,-0.778459114164683,
2.61286158031631));
#262699=CARTESIAN_POINT('Ctrl Pts',(-1.32195828403722,-0.82066284903708,
2.61640216284323));
#262700=CARTESIAN_POINT('Ctrl Pts',(-1.30125287953495,-0.853112933451776,
2.61923033809146));
#262701=CARTESIAN_POINT('Ctrl Pts',(-1.19384205686457,-1.00842959781245,
2.63331204196824));
#262702=CARTESIAN_POINT('Ctrl Pts',(-1.09083915533347,-1.11903727593352,
2.64518484806637));
#262703=CARTESIAN_POINT('Ctrl Pts',(-0.943393153877153,-1.23737255934958,
2.65959141878237));
#262704=CARTESIAN_POINT('Ctrl Pts',(-0.912276745096169,-1.26048929177823,
2.66250478509144));
#262705=CARTESIAN_POINT('Ctrl Pts',(-0.874836809362642,-1.28619016569747,
2.66583707748606));
#262706=CARTESIAN_POINT('Ctrl Pts',(-0.869322997972508,-1.28992329802167,
2.66632357139289));
#262707=CARTESIAN_POINT('Ctrl Pts',(-0.860350154723142,-1.29591470486006,
2.66710818095526));
#262708=CARTESIAN_POINT('Ctrl Pts',(-0.856905878619585,-1.2981947570607,
2.66740768335076));
#262709=CARTESIAN_POINT('Ctrl Pts',(-0.850758055354086,-1.30222938384827,
2.66793924668592));
#262710=CARTESIAN_POINT('Ctrl Pts',(-0.848058103445263,-1.30398929857616,
2.6681716577564));
#262711=CARTESIAN_POINT('Ctrl Pts',(-0.842204289031549,-1.30777912969043,
2.66867330538221));
#262712=CARTESIAN_POINT('Ctrl Pts',(-0.839048552356202,-1.30980603301041,
2.66894234268938));
#262713=CARTESIAN_POINT('Ctrl Pts',(-0.830195976003729,-1.31544684601059,
2.66969324906925));
#262714=CARTESIAN_POINT('Ctrl Pts',(-0.824482818683226,-1.31903519640998,
2.67017346945639));
#262715=CARTESIAN_POINT('Ctrl Pts',(-0.790235631203481,-1.34023589912645,
2.67302717577542));
#262716=CARTESIAN_POINT('Ctrl Pts',(-0.761158915107036,-1.35696062934189,
2.67534728406832));
#262717=CARTESIAN_POINT('Ctrl Pts',(-0.580179981659949,-1.4534084906595,
2.68931552706292));
#262718=CARTESIAN_POINT('Ctrl Pts',(-0.416494468965732,-1.50849210368012,
2.70009826825702));
#262719=CARTESIAN_POINT('Ctrl Pts',(-0.221557597978971,-1.53985779190144,
2.71368259492742));
#262720=CARTESIAN_POINT('Ctrl Pts',(-0.195913525058172,-1.5433300181157,
2.7154803715659));
#262721=CARTESIAN_POINT('Ctrl Pts',(-0.160863244168044,-1.54718823118976,
2.71795779258158));
#262722=CARTESIAN_POINT('Ctrl Pts',(-0.151521547159138,-1.5481310086368,
2.71862001843417));
#262723=CARTESIAN_POINT('Ctrl Pts',(-0.13666878387214,-1.54949425129131,
2.71967624306559));
#262724=CARTESIAN_POINT('Ctrl Pts',(-0.131162912912977,-1.54997002555289,
2.72006850591722));
#262725=CARTESIAN_POINT('Ctrl Pts',(-0.11987650525895,-1.55088474110086,
2.72087414087667));
#262726=CARTESIAN_POINT('Ctrl Pts',(-0.11409582319336,-1.55132072704217,
2.7212875988703));
#262727=CARTESIAN_POINT('Ctrl Pts',(-0.100743303483416,-1.55225275484565,
2.72224460354692));
#262728=CARTESIAN_POINT('Ctrl Pts',(-0.093170058503897,-1.5527257209637,
2.72278886228998));
#262729=CARTESIAN_POINT('Ctrl Pts',(-0.06926787321072,-1.55404297123155,
2.72451142882781));
#262730=CARTESIAN_POINT('Ctrl Pts',(-0.0529293998675839,-1.55468518852481,
2.7256959923748));
#262731=CARTESIAN_POINT('Ctrl Pts',(0.0283501065787997,-1.55659736144991,
2.73162629913285));
#262732=CARTESIAN_POINT('Ctrl Pts',(0.0933072134609718,-1.5540562042871,
2.73648838369896));
#262733=CARTESIAN_POINT('Ctrl Pts',(0.223011635854469,-1.54082079516736,
2.74643428385114));
#262734=CARTESIAN_POINT('Ctrl Pts',(0.287627980718051,-1.53007584740424,
2.75150974494844));
#262735=CARTESIAN_POINT('Ctrl Pts',(0.375845769790922,-1.50961962402928,
2.75853082719658));
#262736=CARTESIAN_POINT('Ctrl Pts',(0.400179418852243,-1.50335222855512,
2.76047689001292));
#262737=CARTESIAN_POINT('Ctrl Pts',(0.482864518482418,-1.47990582537885,
2.76710497754921));
#262738=CARTESIAN_POINT('Ctrl Pts',(0.540362574835862,-1.45989369333721,
2.77174228132225));
#262739=CARTESIAN_POINT('Ctrl Pts',(0.603913458445661,-1.43350354150583,
2.77679890775196));
#262740=CARTESIAN_POINT('Ctrl Pts',(0.611256296257649,-1.4303879251203,
2.77738206110409));
#262741=CARTESIAN_POINT('Ctrl Pts',(0.622302541884912,-1.42560032987945,
2.77825731767137));
#262742=CARTESIAN_POINT('Ctrl Pts',(0.626023748415112,-1.42397016177547,
2.77855182259394));
#262743=CARTESIAN_POINT('Ctrl Pts',(0.632680925735021,-1.42102267775762,
2.77907800881327));
#262744=CARTESIAN_POINT('Ctrl Pts',(0.635619221716408,-1.41971081919212,
2.77931001154286));
#262745=CARTESIAN_POINT('Ctrl Pts',(0.642019359098197,-1.41682950250657,
2.77981482380017));
#262746=CARTESIAN_POINT('Ctrl Pts',(0.645479521440103,-1.41525647317628,
2.78008741166917));
#262747=CARTESIAN_POINT('Ctrl Pts',(0.655276966453399,-1.41075903661987,
2.78085839519975));
#262748=CARTESIAN_POINT('Ctrl Pts',(0.66160048975873,-1.40780458835677,
2.78135499726987));
#262749=CARTESIAN_POINT('Ctrl Pts',(0.702294004470904,-1.38845719583962,
2.78454559791216));
#262750=CARTESIAN_POINT('Ctrl Pts',(0.736075590181329,-1.37084775988776,
2.78717046325614));
#262751=CARTESIAN_POINT('Ctrl Pts',(0.864663726083719,-1.29769215027956,
2.7972012688602));
#262752=CARTESIAN_POINT('Ctrl Pts',(0.954130363923101,-1.23340472004064,
2.80428568144567));
#262753=CARTESIAN_POINT('Ctrl Pts',(1.0924122186762,-1.10991863187252,2.81660083761174));
#262754=CARTESIAN_POINT('Ctrl Pts',(1.14499703284813,-1.05558663847816,
2.82169748327598));
#262755=CARTESIAN_POINT('Ctrl Pts',(1.20096509202446,-0.988636094904325,
2.82779357805644));
#262756=CARTESIAN_POINT('Ctrl Pts',(1.20840311233166,-0.979530696410439,
2.82861886537459));
#262757=CARTESIAN_POINT('Ctrl Pts',(1.22032954586665,-0.964588123836426,
2.82996765162779));
#262758=CARTESIAN_POINT('Ctrl Pts',(1.22488108698391,-0.958801735787404,
2.83048862698344));
#262759=CARTESIAN_POINT('Ctrl Pts',(1.23292513864038,-0.948424547906283,
2.83142070051063));
#262760=CARTESIAN_POINT('Ctrl Pts',(1.23643353756728,-0.943846187735028,
2.83183116191293));
#262761=CARTESIAN_POINT('Ctrl Pts',(1.24378996623189,-0.934134853196116,
2.83270026469177));
#262762=CARTESIAN_POINT('Ctrl Pts',(1.24763185863574,-0.928997388099676,
2.83315913567376));
#262763=CARTESIAN_POINT('Ctrl Pts',(1.25776375913431,-0.915272572501554,
2.83438273642862));
#262764=CARTESIAN_POINT('Ctrl Pts',(1.26399748739438,-0.906644305757947,
2.83514961951849));
#262765=CARTESIAN_POINT('Ctrl Pts',(1.29361765540512,-0.86474698709582,
2.83886292879876));
#262766=CARTESIAN_POINT('Ctrl Pts',(1.3157798722374,-0.830636352481715,
2.84185504503788));
#262767=CARTESIAN_POINT('Ctrl Pts',(1.41280088785832,-0.66766500870913,
2.85602404337296));
#262768=CARTESIAN_POINT('Ctrl Pts',(1.47022494052532,-0.529346745876509,
2.86779386198882));
#262769=CARTESIAN_POINT('Ctrl Pts',(1.51640914243423,-0.348567405116211,
2.8820002333459));
#262770=CARTESIAN_POINT('Ctrl Pts',(1.52439753028294,-0.311783045213684,
2.88482721174136));
#262771=CARTESIAN_POINT('Ctrl Pts',(1.53221319825499,-0.268228907256127,
2.88807387336371));
#262772=CARTESIAN_POINT('Ctrl Pts',(1.53334035109987,-0.261708623170449,
2.88855728202526));
#262773=CARTESIAN_POINT('Ctrl Pts',(1.53510144267666,-0.251119031949921,
2.88933790610767));
#262774=CARTESIAN_POINT('Ctrl Pts',(1.53576087317674,-0.247054141826135,
2.88963648593991));
#262775=CARTESIAN_POINT('Ctrl Pts',(1.53690744903566,-0.239804343712694,
2.89016704834123));
#262776=CARTESIAN_POINT('Ctrl Pts',(1.53740084834131,-0.236620502888031,
2.89039937575605));
#262777=CARTESIAN_POINT('Ctrl Pts',(1.53844854508629,-0.229718212893933,
2.89090157008159));
#262778=CARTESIAN_POINT('Ctrl Pts',(1.53899925519365,-0.225999284372101,
2.89117123375325));
#262779=CARTESIAN_POINT('Ctrl Pts',(1.54050637653601,-0.215560713225502,
2.89192566935078));
#262780=CARTESIAN_POINT('Ctrl Pts',(1.54143231378084,-0.208836643731767,
2.89240876752484));
#262781=CARTESIAN_POINT('Ctrl Pts',(1.5467676100949,-0.168121967208169,
2.89531776400866));
#262782=CARTESIAN_POINT('Ctrl Pts',(1.5500969398411,-0.133996135898236,
2.89768784641757));
#262783=CARTESIAN_POINT('Ctrl Pts',(1.55755985801762,-0.0178999546183899,
2.90560569119024));
#262784=CARTESIAN_POINT('Ctrl Pts',(1.55633654998758,0.0642802138626112,
2.91097104270541));
#262785=CARTESIAN_POINT('Ctrl Pts',(1.53857498879349,0.25269671574714,2.92343378259378));
#262786=CARTESIAN_POINT('Ctrl Pts',(1.51751547903197,0.35806481569268,2.93053979639105));
#262787=CARTESIAN_POINT('Ctrl Pts',(1.482271045949,0.471799359505524,2.93885597595728));
#262788=CARTESIAN_POINT('Ctrl Pts',(1.47861538631174,0.483134158211466,
2.9396918199761));
#262789=CARTESIAN_POINT('Ctrl Pts',(1.47247539816963,0.501449227225489,
2.94105444354732));
#262790=CARTESIAN_POINT('Ctrl Pts',(1.47007067159434,0.508455841538123,
2.94157861202159));
#262791=CARTESIAN_POINT('Ctrl Pts',(1.46570288103446,0.5208921647549,2.94251425181334));
#262792=CARTESIAN_POINT('Ctrl Pts',(1.46375944703422,0.52632866381182,2.94292506789212));
#262793=CARTESIAN_POINT('Ctrl Pts',(1.45960137890462,0.537759143482083,
2.94379270033739));
#262794=CARTESIAN_POINT('Ctrl Pts',(1.45737999025646,0.543750534206534,
2.94424973476265));
#262795=CARTESIAN_POINT('Ctrl Pts',(1.45140027483632,0.559578751723736,
2.94546322940269));
#262796=CARTESIAN_POINT('Ctrl Pts',(1.44757892383351,0.569391241871289,
2.94622178030161));
#262797=CARTESIAN_POINT('Ctrl Pts',(1.44068771213679,0.586568683636156,
2.94756096891561));
#262798=CARTESIAN_POINT('Ctrl Pts',(1.43766040000972,0.593949879505714,
2.94814012489374));
#262799=CARTESIAN_POINT('Ctrl Pts',(1.43457668232327,0.601306903780717,
2.94872114469929));
#262800=CARTESIAN_POINT('Origin',(0.,0.,-1.29405622560371));
#262801=CARTESIAN_POINT('',(1.43457681153698,0.601306595507149,3.78763867041446));
#262802=CARTESIAN_POINT('',(1.43457668196675,0.601306904631308,3.65081500619461));
#262803=CARTESIAN_POINT('',(1.43457668357355,0.601306900797845,-1.29405622560371));
#262804=CARTESIAN_POINT('',(-1.55549981857965,-0.000751264718236687,3.39526827503829));
#262805=CARTESIAN_POINT('Ctrl Pts',(1.43457681153698,0.601306595507149,
3.78763867041446));
#262806=CARTESIAN_POINT('Ctrl Pts',(1.45228495682761,0.559059105126902,
3.78410173349879));
#262807=CARTESIAN_POINT('Ctrl Pts',(1.46812981601876,0.516022379834169,
3.78058974358071));
#262808=CARTESIAN_POINT('Ctrl Pts',(1.48860755329112,0.451766629824114,
3.77553199083611));
#262809=CARTESIAN_POINT('Ctrl Pts',(1.4947295481773,0.43107915613783,3.7739312732006));
#262810=CARTESIAN_POINT('Ctrl Pts',(1.5020235734551,0.404403778784375,3.77190807115718));
#262811=CARTESIAN_POINT('Ctrl Pts',(1.50359314973623,0.398528386534485,
3.77146496846811));
#262812=CARTESIAN_POINT('Ctrl Pts',(1.50603094392167,0.38918354821158,3.77076436611229));
#262813=CARTESIAN_POINT('Ctrl Pts',(1.50692170200068,0.385720135578987,
3.77050560992117));
#262814=CARTESIAN_POINT('Ctrl Pts',(1.50858835203985,0.379146029881205,
3.77001620077042));
#262815=CARTESIAN_POINT('Ctrl Pts',(1.50936656214683,0.376036047720497,
3.76978542472547));
#262816=CARTESIAN_POINT('Ctrl Pts',(1.51116273365963,0.36876254236952,3.76924740410533));
#262817=CARTESIAN_POINT('Ctrl Pts',(1.51217310828068,0.364597191476883,
3.76894059650567));
#262818=CARTESIAN_POINT('Ctrl Pts',(1.51538571844277,0.351109842973347,
3.76795120853024));
#262819=CARTESIAN_POINT('Ctrl Pts',(1.5175191280994,0.341771422989115,3.7672724200373));
#262820=CARTESIAN_POINT('Ctrl Pts',(1.53684926574886,0.253407332177902,
3.76090308475515));
#262821=CARTESIAN_POINT('Ctrl Pts',(1.54794717545517,0.173160517748061,
3.7555198102427));
#262822=CARTESIAN_POINT('Ctrl Pts',(1.56056567214749,-0.0388810575686845,
3.74150111489887));
#262823=CARTESIAN_POINT('Ctrl Pts',(1.55169748158616,-0.170609119704074,
3.73295215226419));
#262824=CARTESIAN_POINT('Ctrl Pts',(1.52296156721753,-0.316986740024555,
3.722592210792));
#262825=CARTESIAN_POINT('Ctrl Pts',(1.51926228542067,-0.334267246674258,
3.72135625840327));
#262826=CARTESIAN_POINT('Ctrl Pts',(1.51368930793458,-0.358292948888097,
3.7196181087253));
#262827=CARTESIAN_POINT('Ctrl Pts',(1.51206317070268,-0.365094676910799,
3.71912381141409));
#262828=CARTESIAN_POINT('Ctrl Pts',(1.5090039472547,-0.377519547388339,
3.71821667831772));
#262829=CARTESIAN_POINT('Ctrl Pts',(1.50758514848097,-0.383146107776329,
3.71780430742775));
#262830=CARTESIAN_POINT('Ctrl Pts',(1.50464970696429,-0.394518469808338,
3.7169675612951));
#262831=CARTESIAN_POINT('Ctrl Pts',(1.50313155450186,-0.4002637777037,3.71654314349472));
#262832=CARTESIAN_POINT('Ctrl Pts',(1.49930956471333,-0.414399302433667,
3.71549466496931));
#262833=CARTESIAN_POINT('Ctrl Pts',(1.4969682048874,-0.42277906824087,3.71486939913729));
#262834=CARTESIAN_POINT('Ctrl Pts',(1.48802499017834,-0.453781028454427,
3.71254204715143));
#262835=CARTESIAN_POINT('Ctrl Pts',(1.48097992077509,-0.476270883424295,
3.7108256743585));
#262836=CARTESIAN_POINT('Ctrl Pts',(1.42411971780435,-0.644303145615583,
3.69778134956352));
#262837=CARTESIAN_POINT('Ctrl Pts',(1.35347502552335,-0.781874651013664,
3.68571967058551));
#262838=CARTESIAN_POINT('Ctrl Pts',(1.25215522599585,-0.923086737694484,
3.672359514497));
#262839=CARTESIAN_POINT('Ctrl Pts',(1.24015883741703,-0.939142134830813,
3.67082634275174));
#262840=CARTESIAN_POINT('Ctrl Pts',(1.20673646821736,-0.982115403112518,
3.66669195004829));
#262841=CARTESIAN_POINT('Ctrl Pts',(1.18472075176358,-1.00856371279372,
3.66411343206859));
#262842=CARTESIAN_POINT('Ctrl Pts',(1.15759680630836,-1.03903353441394,
3.66112193902722));
#262843=CARTESIAN_POINT('Ctrl Pts',(1.15332019217965,-1.04377851562435,
3.66065546216106));
#262844=CARTESIAN_POINT('Ctrl Pts',(1.14630307427229,-1.05146835008178,
3.65989865350859));
#262845=CARTESIAN_POINT('Ctrl Pts',(1.14358022018729,-1.05442909211347,
3.65960706512636));
#262846=CARTESIAN_POINT('Ctrl Pts',(1.13868569475551,-1.05970997780205,
3.65908666829663));
#262847=CARTESIAN_POINT('Ctrl Pts',(1.13651837895164,-1.06203405003917,
3.65885754132213));
#262848=CARTESIAN_POINT('Ctrl Pts',(1.13178399489142,-1.06707976985674,
3.65835986677598));
#262849=CARTESIAN_POINT('Ctrl Pts',(1.12921422906795,-1.06979879977451,
3.65809153060942));
#262850=CARTESIAN_POINT('Ctrl Pts',(1.12192167289263,-1.07745938789422,
3.65733500208633));
#262851=CARTESIAN_POINT('Ctrl Pts',(1.11717600594268,-1.08237920758373,
3.65684852594792));
#262852=CARTESIAN_POINT('Ctrl Pts',(1.08699520392428,-1.11325758465683,
3.65379006558649));
#262853=CARTESIAN_POINT('Ctrl Pts',(1.06068682475235,-1.1383518851365,3.65128112577189));
#262854=CARTESIAN_POINT('Ctrl Pts',(0.964226133867791,-1.22411000159353,
3.64251465889047));
#262855=CARTESIAN_POINT('Ctrl Pts',(0.889556521303112,-1.27940194143842,
3.63648742405289));
#262856=CARTESIAN_POINT('Ctrl Pts',(0.729795156973847,-1.37691581603811,
3.62413543362215));
#262857=CARTESIAN_POINT('Ctrl Pts',(0.644889292852592,-1.41866554003948,
3.61782900111829));
#262858=CARTESIAN_POINT('Ctrl Pts',(0.545593974309176,-1.45672567951637,
3.61040227455098));
#262859=CARTESIAN_POINT('Ctrl Pts',(0.534409140939756,-1.4608659576953,
3.60956527654516));
#262860=CARTESIAN_POINT('Ctrl Pts',(0.516316624485444,-1.46732766550339,
3.60821009075901));
#262861=CARTESIAN_POINT('Ctrl Pts',(0.509438151575961,-1.46972994156417,
3.60769458138776));
#262862=CARTESIAN_POINT('Ctrl Pts',(0.497137138509152,-1.47392928816994,
3.60677203736411));
#262863=CARTESIAN_POINT('Ctrl Pts',(0.491721058912517,-1.47574499139884,
3.6063656254041));
#262864=CARTESIAN_POINT('Ctrl Pts',(0.480349156264552,-1.47948779073394,
3.60551177679746));
#262865=CARTESIAN_POINT('Ctrl Pts',(0.47439146861482,-1.48140884540511,
3.6050641500061));
#262866=CARTESIAN_POINT('Ctrl Pts',(0.458722597262361,-1.48635705623752,
3.60388600257941));
#262867=CARTESIAN_POINT('Ctrl Pts',(0.448993173344979,-1.48932496152393,
3.60315356147507));
#262868=CARTESIAN_POINT('Ctrl Pts',(0.404420976842879,-1.50244500610665,
3.59979351815833));
#262869=CARTESIAN_POINT('Ctrl Pts',(0.369261360520735,-1.51147046407328,
3.59712986563063));
#262870=CARTESIAN_POINT('Ctrl Pts',(0.201730177319029,-1.5482814758348,
3.58436385052272));
#262871=CARTESIAN_POINT('Ctrl Pts',(0.066432027133175,-1.55995042232364,
3.57376843586547));
#262872=CARTESIAN_POINT('Ctrl Pts',(-0.124291199208441,-1.55152691528764,
3.55907537328113));
#262873=CARTESIAN_POINT('Ctrl Pts',(-0.179783991445488,-1.54607999382093,
3.55484037053534));
#262874=CARTESIAN_POINT('Ctrl Pts',(-0.242631479585287,-1.53648034316866,
3.55016963475518));
#262875=CARTESIAN_POINT('Ctrl Pts',(-0.250383073118482,-1.53523620444844,
3.5495957727605));
#262876=CARTESIAN_POINT('Ctrl Pts',(-0.262075895247744,-1.53326857584135,
3.54873382976801));
#262877=CARTESIAN_POINT('Ctrl Pts',(-0.26602413752954,-1.5325884835016,
3.54844342062868));
#262878=CARTESIAN_POINT('Ctrl Pts',(-0.273098342554592,-1.53134177676573,
3.54792428115634));
#262879=CARTESIAN_POINT('Ctrl Pts',(-0.276225222729987,-1.5307808363484,
3.54769523900785));
#262880=CARTESIAN_POINT('Ctrl Pts',(-0.283043043753944,-1.52953619603863,
3.54719676566028));
#262881=CARTESIAN_POINT('Ctrl Pts',(-0.286733230157128,-1.528848715583,
3.54692755129187));
#262882=CARTESIAN_POINT('Ctrl Pts',(-0.297192987953784,-1.5268608629737,
3.54616604130273));
#262883=CARTESIAN_POINT('Ctrl Pts',(-0.303956569229325,-1.52552881837807,
3.54567549797882));
#262884=CARTESIAN_POINT('Ctrl Pts',(-0.347493136481235,-1.51665352095195,
3.5425286608509));
#262885=CARTESIAN_POINT('Ctrl Pts',(-0.383995410676809,-1.50782541677269,
3.539939698296));
#262886=CARTESIAN_POINT('Ctrl Pts',(-0.522902388275454,-1.4688577774429,
3.53015243409652));
#262887=CARTESIAN_POINT('Ctrl Pts',(-0.622426285678056,-1.42953110078364,
3.52326086316968));
#262888=CARTESIAN_POINT('Ctrl Pts',(-0.787591802583994,-1.34371936694108,
3.51091781051548));
#262889=CARTESIAN_POINT('Ctrl Pts',(-0.855123298424616,-1.30178490941716,
3.5055716927596));
#262890=CARTESIAN_POINT('Ctrl Pts',(-0.928667192730548,-1.24791688309828,
3.49920368167366));
#262891=CARTESIAN_POINT('Ctrl Pts',(-0.938100521604567,-1.24084112597254,
3.49837598998781));
#262892=CARTESIAN_POINT('Ctrl Pts',(-0.953261431373565,-1.22919752048136,
3.49702742177383));
#262893=CARTESIAN_POINT('Ctrl Pts',(-0.959038918513254,-1.22469516630268,
3.49650911200703));
#262894=CARTESIAN_POINT('Ctrl Pts',(-0.969093940758407,-1.2167445784329,
3.49559919038582));
#262895=CARTESIAN_POINT('Ctrl Pts',(-0.973385442714616,-1.21331414466905,
3.49520829137425));
#262896=CARTESIAN_POINT('Ctrl Pts',(-0.982343395788234,-1.20607544575574,
3.49438693171287));
#262897=CARTESIAN_POINT('Ctrl Pts',(-0.987006071298748,-1.20226267572384,
3.49395629401762));
#262898=CARTESIAN_POINT('Ctrl Pts',(-0.999035001351912,-1.19230922374725,
3.49283712703259));
#262899=CARTESIAN_POINT('Ctrl Pts',(-1.00636672256549,-1.18612740926773,
3.49214693384171));
#262900=CARTESIAN_POINT('Ctrl Pts',(-1.02225315382704,-1.17247927927087,
3.49063345945227));
#262901=CARTESIAN_POINT('Ctrl Pts',(-1.03078415404837,-1.16498634579644,
3.48980910496562));
#262902=CARTESIAN_POINT('Ctrl Pts',(-1.05551298293407,-1.1427822894922,
3.4873848137032));
#262903=CARTESIAN_POINT('Ctrl Pts',(-1.07148275069573,-1.12782252353667,
3.48577467467052));
#262904=CARTESIAN_POINT('Ctrl Pts',(-1.12740088558028,-1.07318107590871,
3.47997283705036));
#262905=CARTESIAN_POINT('Ctrl Pts',(-1.16550020470256,-1.03167746573578,
3.47570772852948));
#262906=CARTESIAN_POINT('Ctrl Pts',(-1.2609046484283,-0.915703676367821,
3.46417932460461));
#262907=CARTESIAN_POINT('Ctrl Pts',(-1.31385835809563,-0.837955433560799,
3.4568287418661));
#262908=CARTESIAN_POINT('Ctrl Pts',(-1.3641631101764,-0.747483901960602,
3.44890655835622));
#262909=CARTESIAN_POINT('Ctrl Pts',(-1.36876930105928,-0.73901541395515,
3.44817089410334));
#262910=CARTESIAN_POINT('Ctrl Pts',(-1.39028693681688,-0.69856378795933,
3.44468628528528));
#262911=CARTESIAN_POINT('Ctrl Pts',(-1.40615955824313,-0.666036747091945,
3.44197096923252));
#262912=CARTESIAN_POINT('Ctrl Pts',(-1.42352145684948,-0.627063711645005,
3.43884151283026));
#262913=CARTESIAN_POINT('Ctrl Pts',(-1.42612130725718,-0.621128213395096,
3.43836822817792));
#262914=CARTESIAN_POINT('Ctrl Pts',(-1.43028585119029,-0.611456489184943,
3.43760261065442));
#262915=CARTESIAN_POINT('Ctrl Pts',(-1.4318731406569,-0.607730173971907,
3.43730897340904));
#262916=CARTESIAN_POINT('Ctrl Pts',(-1.43468059831586,-0.601067335704458,
3.43678637632814));
#262917=CARTESIAN_POINT('Ctrl Pts',(-1.43590633025794,-0.598133239860774,
3.43655708633019));
#262918=CARTESIAN_POINT('Ctrl Pts',(-1.43854663313726,-0.591758122095598,
3.43606072880717));
#262919=CARTESIAN_POINT('Ctrl Pts',(-1.43995785769421,-0.588315782235392,
3.43579386353481));
#262920=CARTESIAN_POINT('Ctrl Pts',(-1.44389054899149,-0.578624009771287,
3.43504565321599));
#262921=CARTESIAN_POINT('Ctrl Pts',(-1.44638381597577,-0.572363104544709,
3.43456596491598));
#262922=CARTESIAN_POINT('Ctrl Pts',(-1.46137739088142,-0.533988661253052,
3.43164697466891));
#262923=CARTESIAN_POINT('Ctrl Pts',(-1.47284955156609,-0.501480235914487,
3.42926425445776));
#262924=CARTESIAN_POINT('Ctrl Pts',(-1.53105158791671,-0.317262296235985,
3.41611746690408));
#262925=CARTESIAN_POINT('Ctrl Pts',(-1.55542315334262,-0.159487272665282,
3.4060917948684));
#262926=CARTESIAN_POINT('Ctrl Pts',(-1.55549981857965,-0.000751264718236687,
3.39526827503829));
#262927=CARTESIAN_POINT('Ctrl Pts',(-1.55549981945131,-0.000749457767515238,
3.39526815183013));
#262928=CARTESIAN_POINT('Ctrl Pts',(-1.55551551317976,0.031822880291549,
3.39304718442064));
#262929=CARTESIAN_POINT('Ctrl Pts',(-1.55450810755596,0.0643860290742983,
3.39080044892672));
#262930=CARTESIAN_POINT('Ctrl Pts',(-1.55193830940151,0.105561257287131,
3.38791462042648));
#262931=CARTESIAN_POINT('Ctrl Pts',(-1.55132467008113,0.114225469361474,
3.38730486765438));
#262932=CARTESIAN_POINT('Ctrl Pts',(-1.55015512784323,0.128983600474185,
3.38626174224459));
#262933=CARTESIAN_POINT('Ctrl Pts',(-1.54963576541783,0.135080280521943,
3.38582950756042));
#262934=CARTESIAN_POINT('Ctrl Pts',(-1.54859869653279,0.146459904282944,
3.38502019759924));
#262935=CARTESIAN_POINT('Ctrl Pts',(-1.5480898904487,0.151743587292015,
3.38464340535572));
#262936=CARTESIAN_POINT('Ctrl Pts',(-1.54697665844573,0.162715038651089,
3.38385883031495));
#262937=CARTESIAN_POINT('Ctrl Pts',(-1.54636788564916,0.168402274939897,
3.3834509167941));
#262938=CARTESIAN_POINT('Ctrl Pts',(-1.54490645612242,0.18137846361503,
3.38251736478529));
#262939=CARTESIAN_POINT('Ctrl Pts',(-1.54403356124884,0.188664950502778,
3.38199109819578));
#262940=CARTESIAN_POINT('Ctrl Pts',(-1.54112563059196,0.211565546626314,
3.38033047644349));
#262941=CARTESIAN_POINT('Ctrl Pts',(-1.53890510533234,0.227154644840348,
3.37919032517134));
#262942=CARTESIAN_POINT('Ctrl Pts',(-1.53053872248536,0.280117783514749,
3.37528220642439));
#262943=CARTESIAN_POINT('Ctrl Pts',(-1.52326517167634,0.317297210056309,
3.37247956685669));
#262944=CARTESIAN_POINT('Ctrl Pts',(-1.48094035748025,0.498302709708821,
3.35853604265877));
#262945=CARTESIAN_POINT('Ctrl Pts',(-1.4268472150639,0.636855835611352,
3.34682716900537));
#262946=CARTESIAN_POINT('Ctrl Pts',(-1.33727291321783,0.79525914961694,
3.33301825889263));
#262947=CARTESIAN_POINT('Ctrl Pts',(-1.31957184442428,0.824297610163576,
3.33047230154255));
#262948=CARTESIAN_POINT('Ctrl Pts',(-1.29725097816734,0.858350293523376,
3.32748900978086));
#262949=CARTESIAN_POINT('Ctrl Pts',(-1.2935339564547,0.863941684748613,
3.32699924052793));
#262950=CARTESIAN_POINT('Ctrl Pts',(-1.28770415471284,0.872589285154732,
3.32624210750205));
#262951=CARTESIAN_POINT('Ctrl Pts',(-1.28561649363749,0.87566219668557,
3.32597312880769));
#262952=CARTESIAN_POINT('Ctrl Pts',(-1.28172113572727,0.881351970200548,
3.32547525920051));
#262953=CARTESIAN_POINT('Ctrl Pts',(-1.27991643736251,0.883970745473139,
3.32524618162784));
#262954=CARTESIAN_POINT('Ctrl Pts',(-1.27579093688326,0.88991808606258,
3.32472608179312));
#262955=CARTESIAN_POINT('Ctrl Pts',(-1.27346513623701,0.893243114909643,
3.324435403479));
#262956=CARTESIAN_POINT('Ctrl Pts',(-1.26737734971728,0.901874276014599,
3.32368100305429));
#262957=CARTESIAN_POINT('Ctrl Pts',(-1.2635949954457,0.907166053004247,
3.3232186244172));
#262958=CARTESIAN_POINT('Ctrl Pts',(-1.2382670172783,0.942135885849864,
3.32016289002876));
#262959=CARTESIAN_POINT('Ctrl Pts',(-1.21570866804082,0.971070650456909,
3.31763357307961));
#262960=CARTESIAN_POINT('Ctrl Pts',(-1.16144304584891,1.03581606862865,
3.31190087639963));
#262961=CARTESIAN_POINT('Ctrl Pts',(-1.12906569480635,1.07101639464612,
3.30872835986349));
#262962=CARTESIAN_POINT('Ctrl Pts',(-1.02654759999703,1.17264775015576,
3.29920115594701));
#262963=CARTESIAN_POINT('Ctrl Pts',(-0.951802795982941,1.23408789430428,
3.29290931757748));
#262964=CARTESIAN_POINT('Ctrl Pts',(-0.846841718172696,1.3051249021125,
3.28433399908301));
#262965=CARTESIAN_POINT('Ctrl Pts',(-0.82135053929949,1.32131563591338,
3.28227091451346));
#262966=CARTESIAN_POINT('Ctrl Pts',(-0.783146223420403,1.34404826863669,
3.27919519350072));
#262967=CARTESIAN_POINT('Ctrl Pts',(-0.770787399388576,1.35117375560407,
3.27820267659231));
#262968=CARTESIAN_POINT('Ctrl Pts',(-0.748224082938496,1.3637723464734,
3.27639383215283));
#262969=CARTESIAN_POINT('Ctrl Pts',(-0.738053054623798,1.36930346053753,
3.27557959528765));
#262970=CARTESIAN_POINT('Ctrl Pts',(-0.722072087278263,1.37776430188822,
3.27430154645416));
#262971=CARTESIAN_POINT('Ctrl Pts',(-0.716303746362942,1.38077207076284,
3.2738404960097));
#262972=CARTESIAN_POINT('Ctrl Pts',(-0.710458372943106,1.38377351999047,
3.27337350397857));
#262973=CARTESIAN_POINT('Ctrl Pts',(-0.710399957552157,1.38380351012044,
3.27336883714324));
#262974=CARTESIAN_POINT('Ctrl Pts',(-0.710281781006218,1.38386417183291,
3.27335939600262));
#262975=CARTESIAN_POINT('Ctrl Pts',(-0.7102220197613,1.38389484324436,3.27335462169115));
#262976=CARTESIAN_POINT('Ctrl Pts',(-0.710119845631572,1.38394727396405,
3.27334645906318));
#262977=CARTESIAN_POINT('Ctrl Pts',(-0.710077433730436,1.3839690351952,
3.27334307081405));
#262978=CARTESIAN_POINT('Ctrl Pts',(-0.709988068657457,1.38401488256044,
3.27333593154164));
#262979=CARTESIAN_POINT('Ctrl Pts',(-0.709941115259242,1.3840389682553,
3.27333218050285));
#262980=CARTESIAN_POINT('Ctrl Pts',(-0.709842180129513,1.38408971267103,
3.27332427674834));
#262981=CARTESIAN_POINT('Ctrl Pts',(-0.709790198117694,1.38411637085501,
3.27332012401335));
#262982=CARTESIAN_POINT('Ctrl Pts',(-0.709680666593918,1.38417253463769,
3.2733113738032));
#262983=CARTESIAN_POINT('Ctrl Pts',(-0.709623116746646,1.38420203957417,
3.27330677630508));
#262984=CARTESIAN_POINT('Ctrl Pts',(-0.70950185288945,1.38426420017001,
3.27329708891478));
#262985=CARTESIAN_POINT('Ctrl Pts',(-0.709438138467444,1.38429685501836,
3.27329199899436));
#262986=CARTESIAN_POINT('Ctrl Pts',(-0.709303885421847,1.38436565054444,
3.27328127404572));
#262987=CARTESIAN_POINT('Ctrl Pts',(-0.709233346282192,1.38440179023404,
3.273275638982));
#262988=CARTESIAN_POINT('Ctrl Pts',(-0.709084713923514,1.38447792549329,
3.27326376545767));
#262989=CARTESIAN_POINT('Ctrl Pts',(-0.709006620095092,1.38451791984052,
3.27325752695537));
#262990=CARTESIAN_POINT('Ctrl Pts',(-0.708842071856696,1.38460217268322,
3.27324438214823));
#262991=CARTESIAN_POINT('Ctrl Pts',(-0.708755616693444,1.38464642968473,
3.27323747579176));
#262992=CARTESIAN_POINT('Ctrl Pts',(-0.708573453953337,1.38473965853182,
3.27322292405972));
#262993=CARTESIAN_POINT('Ctrl Pts',(-0.708477745443298,1.38478862855231,
3.27321527861989));
#262994=CARTESIAN_POINT('Ctrl Pts',(-0.708276101185557,1.38489177506655,
3.27319917088203));
#262995=CARTESIAN_POINT('Ctrl Pts',(-0.708170160205065,1.38494595141957,
3.27319070817865));
#262996=CARTESIAN_POINT('Ctrl Pts',(-0.707946962568743,1.38506005845577,
3.27317287900641));
#262997=CARTESIAN_POINT('Ctrl Pts',(-0.707829705892194,1.38511998570453,
3.27316351255163));
#262998=CARTESIAN_POINT('Ctrl Pts',(-0.707588120153607,1.38524341604903,
3.27314421487366));
#262999=CARTESIAN_POINT('Ctrl Pts',(-0.70746379316258,1.38530691576024,
3.27313428382644));
#263000=CARTESIAN_POINT('Ctrl Pts',(-0.702461597832995,1.38786092596588,
3.27273472001348));
#263001=CARTESIAN_POINT('Ctrl Pts',(-0.697570675714839,1.39032564430966,
3.27234418922685));
#263002=CARTESIAN_POINT('Ctrl Pts',(-0.686137757793286,1.39601160488472,
3.27143157018871));
#263003=CARTESIAN_POINT('Ctrl Pts',(-0.679585971804953,1.39921275266236,
3.27090879192916));
#263004=CARTESIAN_POINT('Ctrl Pts',(-0.662478951758425,1.40742260407319,
3.26954420132373));
#263005=CARTESIAN_POINT('Ctrl Pts',(-0.651889540458947,1.41235858094296,
3.26869990486133));
#263006=CARTESIAN_POINT('Ctrl Pts',(-0.571842095188852,1.44857859561112,
3.26231937269221));
#263007=CARTESIAN_POINT('Ctrl Pts',(-0.500237121934826,1.47483648988481,
3.25661335849307));
#263008=CARTESIAN_POINT('Ctrl Pts',(-0.321533724486945,1.52585311757628,
3.2423942515112));
#263009=CARTESIAN_POINT('Ctrl Pts',(-0.21317716024154,1.54472190463823,
3.23377630413257));
#263010=CARTESIAN_POINT('Ctrl Pts',(-0.0658559685848307,1.55456902334545,
3.22253667813031));
#263011=CARTESIAN_POINT('Ctrl Pts',(-0.0278879192548577,1.55571357150846,
3.21968519758869));
#263012=CARTESIAN_POINT('Ctrl Pts',(0.017000911691727,1.55542245532995,
3.21639460841116));
#263013=CARTESIAN_POINT('Ctrl Pts',(0.0239139970512186,1.55533153092179,
3.21589011161483));
#263014=CARTESIAN_POINT('Ctrl Pts',(0.0345836246196253,1.55512004200872,
3.21511520627182));
#263015=CARTESIAN_POINT('Ctrl Pts',(0.0383406033473937,1.55503195179263,
3.21484306197811));
#263016=CARTESIAN_POINT('Ctrl Pts',(0.0452726000767095,1.55484427893354,
3.21434229237984));
#263017=CARTESIAN_POINT('Ctrl Pts',(0.0484476123790022,1.55474858716306,
3.21411346139317));
#263018=CARTESIAN_POINT('Ctrl Pts',(0.0556210320237971,1.55451039154857,
3.21359764379745));
#263019=CARTESIAN_POINT('Ctrl Pts',(0.0596191909802766,1.55436218741715,
3.21331097787211));
#263020=CARTESIAN_POINT('Ctrl Pts',(0.0716935259977487,1.55386795810465,
3.21244763651832));
#263021=CARTESIAN_POINT('Ctrl Pts',(0.0797677893749526,1.55347439636167,
3.21187352897399));
#263022=CARTESIAN_POINT('Ctrl Pts',(0.15507294591503,1.54921512917367,3.20654602932862));
#263023=CARTESIAN_POINT('Ctrl Pts',(0.221999508046671,1.54104965111159,
3.20201055650979));
#263024=CARTESIAN_POINT('Ctrl Pts',(0.382992674229787,1.51069618754045,
3.19113545704856));
#263025=CARTESIAN_POINT('Ctrl Pts',(0.475920657562925,1.48404378345445,
3.18487707321645));
#263026=CARTESIAN_POINT('Ctrl Pts',(0.602760507023185,1.43451593337269,
3.17575331840211));
#263027=CARTESIAN_POINT('Ctrl Pts',(0.639170658572096,1.41866721852994,
3.17306421684574));
#263028=CARTESIAN_POINT('Ctrl Pts',(0.69050082763851,1.39394671175148,3.16914203717298));
#263029=CARTESIAN_POINT('Ctrl Pts',(0.70594234865254,1.38619053128106,3.16794459084792));
#263030=CARTESIAN_POINT('Ctrl Pts',(0.73331232641578,1.37186683086779,3.16578821511187));
#263031=CARTESIAN_POINT('Ctrl Pts',(0.745289958969322,1.3653968017026,3.16483267165329));
#263032=CARTESIAN_POINT('Ctrl Pts',(0.76329403627544,1.35536395145273,3.1633774712189));
#263033=CARTESIAN_POINT('Ctrl Pts',(0.76938411724057,1.35191616010507,3.16288191445814));
#263034=CARTESIAN_POINT('Ctrl Pts',(0.780365669575825,1.34560091355362,
3.16198219316066));
#263035=CARTESIAN_POINT('Ctrl Pts',(0.785265151926864,1.34274756987973,
3.16157854236464));
#263036=CARTESIAN_POINT('Ctrl Pts',(0.795754259779842,1.33656191611745,
3.1607095048516));
#263037=CARTESIAN_POINT('Ctrl Pts',(0.801338774282202,1.33322119846095,
3.16024381839727));
#263038=CARTESIAN_POINT('Ctrl Pts',(0.816314566616588,1.32413443064572,
3.15898678914332));
#263039=CARTESIAN_POINT('Ctrl Pts',(0.825665917885608,1.31832364863173,
3.15819309019915));
#263040=CARTESIAN_POINT('Ctrl Pts',(0.870280228598846,1.28994013809138,
3.15436328859284));
#263041=CARTESIAN_POINT('Ctrl Pts',(0.904680668575205,1.26605114664814,
3.15127878231632));
#263042=CARTESIAN_POINT('Ctrl Pts',(1.06041827369226,1.14831054178011,3.13667091107057));
#263043=CARTESIAN_POINT('Ctrl Pts',(1.16838432729194,1.03825254450101,3.12452442670456));
#263044=CARTESIAN_POINT('Ctrl Pts',(1.27758068440472,0.887931263723227,
3.11044394375497));
#263045=CARTESIAN_POINT('Ctrl Pts',(1.29583675966283,0.861070158552939,
3.10801519796255));
#263046=CARTESIAN_POINT('Ctrl Pts',(1.31679272047913,0.82805864518375,3.10515079325348));
#263047=CARTESIAN_POINT('Ctrl Pts',(1.32030954079294,0.822439608299907,
3.10466731934354));
#263048=CARTESIAN_POINT('Ctrl Pts',(1.32573140848259,0.813652349549277,
3.10391779410263));
#263049=CARTESIAN_POINT('Ctrl Pts',(1.32766120782145,0.810499618374063,
3.10365017836393));
#263050=CARTESIAN_POINT('Ctrl Pts',(1.33123163248425,0.80461961185084,3.10315352232265));
#263051=CARTESIAN_POINT('Ctrl Pts',(1.33287511131194,0.801894205656458,
3.10292430363258));
#263052=CARTESIAN_POINT('Ctrl Pts',(1.33660840669026,0.795660037311968,
3.10240220212653));
#263053=CARTESIAN_POINT('Ctrl Pts',(1.33869277680272,0.792148078439551,
3.10210967395048));
#263054=CARTESIAN_POINT('Ctrl Pts',(1.34410510315408,0.782946465496307,
3.1013472684211));
#263055=CARTESIAN_POINT('Ctrl Pts',(1.34741081520692,0.777243716799086,
3.10087878172937));
#263056=CARTESIAN_POINT('Ctrl Pts',(1.3697572451804,0.738122395296404,3.09769105710446));
#263057=CARTESIAN_POINT('Ctrl Pts',(1.38759098388224,0.704025182244774,
3.09504232460242));
#263058=CARTESIAN_POINT('Ctrl Pts',(1.40850880864417,0.660140968020444,
3.09174909346945));
#263059=CARTESIAN_POINT('Ctrl Pts',(1.41278418143391,0.650940877528165,
3.09106494698954));
#263060=CARTESIAN_POINT('Ctrl Pts',(1.42303060888839,0.628315217936988,
3.08939615253733));
#263061=CARTESIAN_POINT('Ctrl Pts',(1.428900212522,0.614849625316866,3.08841467113574));
#263062=CARTESIAN_POINT('Ctrl Pts',(1.43457670182626,0.601306857251181,
3.08743730443809));
#263063=CARTESIAN_POINT('',(-1.55549947507011,0.00127791103983615,3.25533765336848));
#263064=CARTESIAN_POINT('Ctrl Pts',(1.43457668232327,0.601306903780717,
2.94872114469929));
#263065=CARTESIAN_POINT('Ctrl Pts',(1.42245865255591,0.630217669365907,
2.95100436774854));
#263066=CARTESIAN_POINT('Ctrl Pts',(1.40946959757188,0.658755155633724,
2.95331658692606));
#263067=CARTESIAN_POINT('Ctrl Pts',(1.32947041243761,0.821300206040414,
2.96683563098988));
#263068=CARTESIAN_POINT('Ctrl Pts',(1.24424164167907,0.94544917436953,2.97866702762622));
#263069=CARTESIAN_POINT('Ctrl Pts',(1.11660624355328,1.08362363781819,2.9929963563998));
#263070=CARTESIAN_POINT('Ctrl Pts',(1.08956087377236,1.11081384470458,2.99587787148548));
#263071=CARTESIAN_POINT('Ctrl Pts',(1.05668376036441,1.14150941440539,2.99917821109605));
#263072=CARTESIAN_POINT('Ctrl Pts',(1.05180273231258,1.14600843325333,2.99966318772031));
#263073=CARTESIAN_POINT('Ctrl Pts',(1.04384250819401,1.1532519578066,3.00044583753614));
#263074=CARTESIAN_POINT('Ctrl Pts',(1.04078100297414,1.15601564219912,3.0007448864676));
#263075=CARTESIAN_POINT('Ctrl Pts',(1.0353080083478,1.16091686239938,3.00127595736976));
#263076=CARTESIAN_POINT('Ctrl Pts',(1.0329008396858,1.16305910840185,3.00150832687416));
#263077=CARTESIAN_POINT('Ctrl Pts',(1.02767425360739,1.16768145381597,3.00201024118986));
#263078=CARTESIAN_POINT('Ctrl Pts',(1.02485251105918,1.17015882703852,3.00227958479922));
#263079=CARTESIAN_POINT('Ctrl Pts',(1.01692091170457,1.17707174503205,3.00303221637908));
#263080=CARTESIAN_POINT('Ctrl Pts',(1.01179096021632,1.18148427450294,3.00351384343232));
#263081=CARTESIAN_POINT('Ctrl Pts',(0.980793807567881,1.20779652631221,
3.00639438651572));
#263082=CARTESIAN_POINT('Ctrl Pts',(0.954242911156409,1.22888154295084,
3.00873874862865));
#263083=CARTESIAN_POINT('Ctrl Pts',(0.782171907016893,1.35658597745834,
3.02332864685264));
#263084=CARTESIAN_POINT('Ctrl Pts',(0.6197277517959,1.43807792081024,3.03463511473062));
#263085=CARTESIAN_POINT('Ctrl Pts',(0.428601843589367,1.49540842706723,
3.04846325505601));
#263086=CARTESIAN_POINT('Ctrl Pts',(0.410187001979165,1.50056405116865,
3.04979845186935));
#263087=CARTESIAN_POINT('Ctrl Pts',(0.384441582809637,1.5072627174754,3.05167129474415));
#263088=CARTESIAN_POINT('Ctrl Pts',(0.377187299924965,1.50909441962825,
3.05219967290755));
#263089=CARTESIAN_POINT('Ctrl Pts',(0.364634735537623,1.51216777190815,
3.0531152458029));
#263090=CARTESIAN_POINT('Ctrl Pts',(0.359342581925982,1.51343409774031,
3.05350164352768));
#263091=CARTESIAN_POINT('Ctrl Pts',(0.348355610294849,1.5160022242349,3.05430470821913));
#263092=CARTESIAN_POINT('Ctrl Pts',(0.342659894783035,1.51729976270497,
3.05472150468727));
#263093=CARTESIAN_POINT('Ctrl Pts',(0.329267193135695,1.52027149264878,
3.05570274809804));
#263094=CARTESIAN_POINT('Ctrl Pts',(0.321564593725083,1.52191934860861,
3.05626802540339));
#263095=CARTESIAN_POINT('Ctrl Pts',(0.296270532187378,1.52713004429368,
3.05812756139498));
#263096=CARTESIAN_POINT('Ctrl Pts',(0.278630476160886,1.53044680014764,
3.05942957310171));
#263097=CARTESIAN_POINT('Ctrl Pts',(0.236802024620758,1.53756445286809,
3.06253042528793));
#263098=CARTESIAN_POINT('Ctrl Pts',(0.212574118963641,1.54110082946908,
3.0643371345177));
#263099=CARTESIAN_POINT('Ctrl Pts',(0.0543418606711603,1.56039473933996,
3.07620905396344));
#263100=CARTESIAN_POINT('Ctrl Pts',(-0.0811324640171465,1.55922754567866,
3.08678189113481));
#263101=CARTESIAN_POINT('Ctrl Pts',(-0.269041554539805,1.53303778457616,
3.10137761908434));
#263102=CARTESIAN_POINT('Ctrl Pts',(-0.322930037961329,1.52259840227671,
3.10554464299519));
#263103=CARTESIAN_POINT('Ctrl Pts',(-0.383823573167472,1.5074223322848,
3.11015547717816));
#263104=CARTESIAN_POINT('Ctrl Pts',(-0.391472398761162,1.50545408141071,
3.1107328234122));
#263105=CARTESIAN_POINT('Ctrl Pts',(-0.403016460707738,1.50238954694443,
3.11160109628738));
#263106=CARTESIAN_POINT('Ctrl Pts',(-0.406922802407952,1.50133622225514,
3.11189436942759));
#263107=CARTESIAN_POINT('Ctrl Pts',(-0.413927678720256,1.49941804541915,
3.11241924823709));
#263108=CARTESIAN_POINT('Ctrl Pts',(-0.417027664726775,1.49855881620741,
3.11265116823625));
#263109=CARTESIAN_POINT('Ctrl Pts',(-0.423797474038313,1.49665978060452,
3.11315684161599));
#263110=CARTESIAN_POINT('Ctrl Pts',(-0.427466140915138,1.49561609281795,
3.11343036749624));
#263111=CARTESIAN_POINT('Ctrl Pts',(-0.437896536184823,1.49260726756071,
3.11420668572888));
#263112=CARTESIAN_POINT('Ctrl Pts',(-0.444648928289597,1.49060966290774,
3.11470764503976));
#263113=CARTESIAN_POINT('Ctrl Pts',(-0.488890511746678,1.47719399759256,
3.11798076965843));
#263114=CARTESIAN_POINT('Ctrl Pts',(-0.525954224242145,1.46440733520357,
3.12067966989121));
#263115=CARTESIAN_POINT('Ctrl Pts',(-0.672773715273248,1.40746074047854,
3.13134555018392));
#263116=CARTESIAN_POINT('Ctrl Pts',(-0.777815979175703,1.35224870075751,
3.13894557828339));
#263117=CARTESIAN_POINT('Ctrl Pts',(-0.930490623375034,1.24827056208346,
3.15127083069428));
#263118=CARTESIAN_POINT('Ctrl Pts',(-0.982932447592461,1.20740804818085,
3.1557760286771));
#263119=CARTESIAN_POINT('Ctrl Pts',(-1.0411808964787,1.15570510607355,3.16121937653398));
#263120=CARTESIAN_POINT('Ctrl Pts',(-1.04967885035192,1.147992269194,3.16202520269222));
#263121=CARTESIAN_POINT('Ctrl Pts',(-1.06342463163254,1.13523621293507,
3.16334845187816));
#263122=CARTESIAN_POINT('Ctrl Pts',(-1.06872388923758,1.13024884501007,
3.16386350909661));
#263123=CARTESIAN_POINT('Ctrl Pts',(-1.07815373615492,1.12124838262156,
3.16478902937418));
#263124=CARTESIAN_POINT('Ctrl Pts',(-1.08229743121077,1.11724915890713,
3.16519888983791));
#263125=CARTESIAN_POINT('Ctrl Pts',(-1.09027623244304,1.10946250000858,
3.16599430707404));
#263126=CARTESIAN_POINT('Ctrl Pts',(-1.09411405392934,1.10567795383662,
3.16637973413627));
#263127=CARTESIAN_POINT('Ctrl Pts',(-1.10438290736315,1.0954458329791,3.16741873040797));
#263128=CARTESIAN_POINT('Ctrl Pts',(-1.11077702985881,1.08896169007784,
3.16807391007661));
#263129=CARTESIAN_POINT('Ctrl Pts',(-1.13673711391532,1.06216958053223,
3.17076831420438));
#263130=CARTESIAN_POINT('Ctrl Pts',(-1.15580486766016,1.04138868791256,
3.17282870520902));
#263131=CARTESIAN_POINT('Ctrl Pts',(-1.20380218345447,0.986136319789469,
3.17823646081524));
#263132=CARTESIAN_POINT('Ctrl Pts',(-1.23181784886212,0.950909373012751,
3.18161740428921));
#263133=CARTESIAN_POINT('Ctrl Pts',(-1.28895833107738,0.872291271880543,
3.18901705356084));
#263134=CARTESIAN_POINT('Ctrl Pts',(-1.31750405972983,0.828545764783225,
3.19304683850954));
#263135=CARTESIAN_POINT('Ctrl Pts',(-1.39245855187102,0.699981865965765,
3.20458025825976));
#263136=CARTESIAN_POINT('Ctrl Pts',(-1.43324406485111,0.612152428725425,
3.21210845457625));
#263137=CARTESIAN_POINT('Ctrl Pts',(-1.46969263819697,0.5096388186464,3.22016516025574));
#263138=CARTESIAN_POINT('Ctrl Pts',(-1.47363274563239,0.49813123949159,
3.22105942646282));
#263139=CARTESIAN_POINT('Ctrl Pts',(-1.47896855035198,0.481929693052078,
3.22230319042214));
#263140=CARTESIAN_POINT('Ctrl Pts',(-1.48047755438171,0.47727394093664,
3.22265884746795));
#263141=CARTESIAN_POINT('Ctrl Pts',(-1.48287967441495,0.469741622874787,
3.22323132831454));
#263142=CARTESIAN_POINT('Ctrl Pts',(-1.48378643707873,0.466869500630587,
3.22344893560381));
#263143=CARTESIAN_POINT('Ctrl Pts',(-1.48568365230811,0.460798813716566,
3.22390741490636));
#263144=CARTESIAN_POINT('Ctrl Pts',(-1.48667212963436,0.457599651293138,
3.22414816644432));
#263145=CARTESIAN_POINT('Ctrl Pts',(-1.48908526833037,0.449699281870232,
3.22474064249161));
#263146=CARTESIAN_POINT('Ctrl Pts',(-1.4904980211127,0.444994417144961,
3.22509167906687));
#263147=CARTESIAN_POINT('Ctrl Pts',(-1.4934830516549,0.434879708684663,
3.22584265824799));
#263148=CARTESIAN_POINT('Ctrl Pts',(-1.49504828275043,0.429467835059389,
3.22624221020648));
#263149=CARTESIAN_POINT('Ctrl Pts',(-1.49940305727876,0.414098597418418,
3.22737082452772));
#263150=CARTESIAN_POINT('Ctrl Pts',(-1.50212282341242,0.404121533713502,
3.22809626407978));
#263151=CARTESIAN_POINT('Ctrl Pts',(-1.53832983940184,0.265883022023333,
3.23805792544598));
#263152=CARTESIAN_POINT('Ctrl Pts',(-1.55539054677746,0.13386765848789,
3.24654259388127));
#263153=CARTESIAN_POINT('Ctrl Pts',(-1.55549947507011,0.00127791103983615,
3.25533765336848));
#263154=CARTESIAN_POINT('Ctrl Pts',(-1.5554994762935,0.00127642103556679,
3.25533775220476));
#263155=CARTESIAN_POINT('Ctrl Pts',(-1.55556457573093,-0.0780564464206632,
3.26060013061482));
#263156=CARTESIAN_POINT('Ctrl Pts',(-1.5495606928194,-0.157269483732473,
3.26594478189099));
#263157=CARTESIAN_POINT('Ctrl Pts',(-1.53615483445118,-0.244729426438979,
3.2721277023867));
#263158=CARTESIAN_POINT('Ctrl Pts',(-1.53468696410739,-0.253771715318804,
3.2727702323005));
#263159=CARTESIAN_POINT('Ctrl Pts',(-1.53206754625742,-0.269053021556787,
3.27386194570828));
#263160=CARTESIAN_POINT('Ctrl Pts',(-1.53095752842476,-0.275298998777278,
3.27430982484675));
#263161=CARTESIAN_POINT('Ctrl Pts',(-1.52883382825815,-0.286838674369593,
3.27514045922882));
#263162=CARTESIAN_POINT('Ctrl Pts',(-1.52783077498162,-0.292134252067406,
3.27552287379926));
#263163=CARTESIAN_POINT('Ctrl Pts',(-1.5256990345478,-0.303077339597831,
3.27631572950416));
#263164=CARTESIAN_POINT('Ctrl Pts',(-1.52456646572806,-0.308723999289791,
3.27672628834616));
#263165=CARTESIAN_POINT('Ctrl Pts',(-1.52193129050685,-0.321494006526159,
3.2776581117536));
#263166=CARTESIAN_POINT('Ctrl Pts',(-1.52040998986305,-0.328613311729287,
3.2781799643184));
#263167=CARTESIAN_POINT('Ctrl Pts',(-1.51635981562754,-0.346936715384596,
3.27952931444606));
#263168=CARTESIAN_POINT('Ctrl Pts',(-1.51375675800904,-0.358123776593075,
3.28035916222648));
#263169=CARTESIAN_POINT('Ctrl Pts',(-1.49519692997988,-0.434067247794134,
3.28603482323786));
#263170=CARTESIAN_POINT('Ctrl Pts',(-1.47521598446976,-0.497758631914721,
3.29100915833726));
#263171=CARTESIAN_POINT('Ctrl Pts',(-1.42828360251659,-0.619389533929868,
3.3009335133554));
#263172=CARTESIAN_POINT('Ctrl Pts',(-1.40172659660111,-0.677347023317625,
3.30586499761823));
#263173=CARTESIAN_POINT('Ctrl Pts',(-1.34198748279839,-0.789061695121617,
3.31568894214456));
#263174=CARTESIAN_POINT('Ctrl Pts',(-1.30893197931883,-0.842761422371147,
3.3205721331193));
#263175=CARTESIAN_POINT('Ctrl Pts',(-1.25481325262656,-0.919778667336661,
3.3276976380773));
#263176=CARTESIAN_POINT('Ctrl Pts',(-1.23615560748826,-0.94470564615604,
3.33002403423597));
#263177=CARTESIAN_POINT('Ctrl Pts',(-1.21263038331133,-0.974244199820357,
3.33279022888197));
#263178=CARTESIAN_POINT('Ctrl Pts',(-1.20846673216654,-0.979404088667083,
3.33327379190739));
#263179=CARTESIAN_POINT('Ctrl Pts',(-1.20191228281821,-0.987421385032341,
3.33402549165318));
#263180=CARTESIAN_POINT('Ctrl Pts',(-1.19954406228006,-0.99029701132986,
3.33429518125567));
#263181=CARTESIAN_POINT('Ctrl Pts',(-1.19510555140728,-0.995647216658856,
3.33479703837405));
#263182=CARTESIAN_POINT('Ctrl Pts',(-1.19303791325238,-0.998123838458429,
3.3350293800104));
#263183=CARTESIAN_POINT('Ctrl Pts',(-1.18828160088191,-1.00378506499656,
3.33556057724508));
#263184=CARTESIAN_POINT('Ctrl Pts',(-1.18558782337883,-1.00696530915993,
3.33585905649905));
#263185=CARTESIAN_POINT('Ctrl Pts',(-1.17847662411039,-1.01529261837258,
3.33664092555214));
#263186=CARTESIAN_POINT('Ctrl Pts',(-1.1740381993345,-1.02042175860083,
3.33712283138497));
#263187=CARTESIAN_POINT('Ctrl Pts',(-1.14227753536441,-1.05664351425257,
3.3405297083049));
#263188=CARTESIAN_POINT('Ctrl Pts',(-1.11375443117199,-1.08666705944277,
3.3433731285709));
#263189=CARTESIAN_POINT('Ctrl Pts',(-1.05464705106878,-1.14410772890806,
3.34894111057736));
#263190=CARTESIAN_POINT('Ctrl Pts',(-1.02410877252334,-1.17152228698045,
3.35166435486929));
#263191=CARTESIAN_POINT('Ctrl Pts',(-0.921728772019352,-1.25636356849182,
3.36044439132946));
#263192=CARTESIAN_POINT('Ctrl Pts',(-0.845878469305043,-1.30863366995126,
3.36643636751983));
#263193=CARTESIAN_POINT('Ctrl Pts',(-0.73656342221112,-1.37046975170061,
3.37490143682063));
#263194=CARTESIAN_POINT('Ctrl Pts',(-0.70674059524315,-1.38608459200649,
3.37719346706223));
#263195=CARTESIAN_POINT('Ctrl Pts',(-0.662526312616567,-1.40743658802385,
3.38058367841519));
#263196=CARTESIAN_POINT('Ctrl Pts',(-0.648517389898912,-1.41394626156147,
3.38165667290346));
#263197=CARTESIAN_POINT('Ctrl Pts',(-0.623139855817195,-1.42528223361025,
3.38359994329796));
#263198=CARTESIAN_POINT('Ctrl Pts',(-0.611806183874596,-1.43018387043294,
3.38446763794292));
#263199=CARTESIAN_POINT('Ctrl Pts',(-0.594182710133811,-1.43755793206207,
3.38581719334363));
#263200=CARTESIAN_POINT('Ctrl Pts',(-0.587932945936292,-1.4401252548069,
3.38629584293086));
#263201=CARTESIAN_POINT('Ctrl Pts',(-0.581612273954868,-1.4426737040073,
3.38678003856248));
#263202=CARTESIAN_POINT('Ctrl Pts',(-0.581557804409939,-1.44269566214742,
3.38678421121533));
#263203=CARTESIAN_POINT('Ctrl Pts',(-0.581447687413543,-1.44274004602388,
3.38679264677229));
#263204=CARTESIAN_POINT('Ctrl Pts',(-0.581392039911287,-1.44276247162426,
3.38679690968066));
#263205=CARTESIAN_POINT('Ctrl Pts',(-0.581279534917941,-1.44280780287709,
3.38680552820755));
#263206=CARTESIAN_POINT('Ctrl Pts',(-0.581222677358193,-1.44283070839306,
3.38680988383171));
#263207=CARTESIAN_POINT('Ctrl Pts',(-0.58110771909995,-1.4428770123353,
3.38681869033094));
#263208=CARTESIAN_POINT('Ctrl Pts',(-0.581049618345017,-1.442900410612,
3.38682314121074));
#263209=CARTESIAN_POINT('Ctrl Pts',(-0.580932139514336,-1.44294771332037,
3.38683214084115));
#263210=CARTESIAN_POINT('Ctrl Pts',(-0.580872761377508,-1.44297161759573,
3.38683668959687));
#263211=CARTESIAN_POINT('Ctrl Pts',(-0.580752692522672,-1.44301994594932,
3.3868458876817));
#263212=CARTESIAN_POINT('Ctrl Pts',(-0.580692001736192,-1.44304436986515,
3.38685053701653));
#263213=CARTESIAN_POINT('Ctrl Pts',(-0.580569271179736,-1.4430937515746,
3.38685993904974));
#263214=CARTESIAN_POINT('Ctrl Pts',(-0.580507231346287,-1.44311870919425,
3.38686469175348));
#263215=CARTESIAN_POINT('Ctrl Pts',(-0.580381765175071,-1.4431691728019,
3.38687430340046));
#263216=CARTESIAN_POINT('Ctrl Pts',(-0.580318338759307,-1.44319467861169,
3.3868791623502));
#263217=CARTESIAN_POINT('Ctrl Pts',(-0.58020870096192,-1.44323875911389,
3.38688756146686));
#263218=CARTESIAN_POINT('Ctrl Pts',(-0.580162490370144,-1.44325733576796,
3.38689110156763));
#263219=CARTESIAN_POINT('Ctrl Pts',(-0.580065254054557,-1.44329641933415,
3.38689855066025));
#263220=CARTESIAN_POINT('Ctrl Pts',(-0.580014228133236,-1.44331692576065,
3.38690245966864));
#263221=CARTESIAN_POINT('Ctrl Pts',(-0.579906847384672,-1.44336007359386,
3.38691068594024));
#263222=CARTESIAN_POINT('Ctrl Pts',(-0.579850492318087,-1.44338271440633,
3.38691500322352));
#263223=CARTESIAN_POINT('Ctrl Pts',(-0.579731882508308,-1.44343035817603,
3.38692408977627));
#263224=CARTESIAN_POINT('Ctrl Pts',(-0.579669627474473,-1.44345536040586,
3.38692885907012));
#263225=CARTESIAN_POINT('Ctrl Pts',(-0.579538583315963,-1.4435079791753,
3.38693889825251));
#263226=CARTESIAN_POINT('Ctrl Pts',(-0.579469793839462,-1.44353559482344,
3.38694416817059));
#263227=CARTESIAN_POINT('Ctrl Pts',(-0.579324975309748,-1.44359372043994,
3.38695526265647));
#263228=CARTESIAN_POINT('Ctrl Pts',(-0.579248945826049,-1.44362422931685,
3.38696108726044));
#263229=CARTESIAN_POINT('Ctrl Pts',(-0.579088862447392,-1.4436884523993,
3.3869733512542));
#263230=CARTESIAN_POINT('Ctrl Pts',(-0.579004808014012,-1.44372216527224,
3.38697979068918));
#263231=CARTESIAN_POINT('Ctrl Pts',(-0.578827801267903,-1.44379314186904,
3.38699335127407));
#263232=CARTESIAN_POINT('Ctrl Pts',(-0.578734848304132,-1.44383040395578,
3.38700047247871));
#263233=CARTESIAN_POINT('Ctrl Pts',(-0.573298418678159,-1.44600909804026,
3.38741696348327));
#263234=CARTESIAN_POINT('Ctrl Pts',(-0.56794316612072,-1.44812083297473,
3.38782732404715));
#263235=CARTESIAN_POINT('Ctrl Pts',(-0.55581269380091,-1.45282660058535,
3.38875712065688));
#263236=CARTESIAN_POINT('Ctrl Pts',(-0.549030841810344,-1.45540304156594,
3.38927713457183));
#263237=CARTESIAN_POINT('Ctrl Pts',(-0.5315439608046,-1.46190672978584,
3.39061859530969));
#263238=CARTESIAN_POINT('Ctrl Pts',(-0.520813491094521,-1.46576381572419,
3.39144234652724));
#263239=CARTESIAN_POINT('Ctrl Pts',(-0.449184255053168,-1.49062522843342,
3.39694614317823));
#263240=CARTESIAN_POINT('Ctrl Pts',(-0.387082251491503,-1.50794404522555,
3.40174577732764));
#263241=CARTESIAN_POINT('Ctrl Pts',(-0.200863419202999,-1.54761393051519,
3.41622013688214));
#263242=CARTESIAN_POINT('Ctrl Pts',(-0.0749139098115009,-1.55879411021227,
3.42615277500801));
#263243=CARTESIAN_POINT('Ctrl Pts',(0.0850777475656494,-1.55354584464973,
3.43830130569816));
#263244=CARTESIAN_POINT('Ctrl Pts',(0.119114695138189,-1.55130752900714,
3.440855275023));
#263245=CARTESIAN_POINT('Ctrl Pts',(0.159809111012734,-1.54728387217716,
3.44385192284407));
#263246=CARTESIAN_POINT('Ctrl Pts',(0.166560342685347,-1.54657168920358,
3.44434717820296));
#263247=CARTESIAN_POINT('Ctrl Pts',(0.177043121451004,-1.54539642754252,
3.44511301251469));
#263248=CARTESIAN_POINT('Ctrl Pts',(0.180777905784097,-1.54496399139518,
3.44538523846394));
#263249=CARTESIAN_POINT('Ctrl Pts',(0.187710226967688,-1.54413584276426,
3.44588932641909));
#263250=CARTESIAN_POINT('Ctrl Pts',(0.190908075665918,-1.54374374078353,
3.44612137818574));
#263251=CARTESIAN_POINT('Ctrl Pts',(0.198190192746293,-1.54282787507327,
3.44664872775242));
#263252=CARTESIAN_POINT('Ctrl Pts',(0.202273612220895,-1.54229782839002,
3.44694366988646));
#263253=CARTESIAN_POINT('Ctrl Pts',(0.212912062093942,-1.54087393056,3.44771019041575));
#263254=CARTESIAN_POINT('Ctrl Pts',(0.219463670693843,-1.53995445303672,
3.44818037747277));
#263255=CARTESIAN_POINT('Ctrl Pts',(0.263209983521974,-1.53353007339282,
3.4513086209682));
#263256=CARTESIAN_POINT('Ctrl Pts',(0.300204156182742,-1.52671936599132,
3.45389952253976));
#263257=CARTESIAN_POINT('Ctrl Pts',(0.482334447487755,-1.48631099021652,
3.46654717759309));
#263258=CARTESIAN_POINT('Ctrl Pts',(0.622366138452038,-1.43332961786917,
3.47600213656755));
#263259=CARTESIAN_POINT('Ctrl Pts',(0.788364511324682,-1.34153617000343,
3.48888698906256));
#263260=CARTESIAN_POINT('Ctrl Pts',(0.823203841668285,-1.32044418391014,
3.49169105915656));
#263261=CARTESIAN_POINT('Ctrl Pts',(0.866059315765286,-1.29214353062344,
3.49529163781995));
#263262=CARTESIAN_POINT('Ctrl Pts',(0.874884495245487,-1.28618457156308,
3.49604147917818));
#263263=CARTESIAN_POINT('Ctrl Pts',(0.888927836291067,-1.27649078234281,
3.49724858264547));
#263264=CARTESIAN_POINT('Ctrl Pts',(0.894185392106557,-1.27281337903213,
3.49770366852515));
#263265=CARTESIAN_POINT('Ctrl Pts',(0.904125883549563,-1.26576850377727,
3.49857023271642));
#263266=CARTESIAN_POINT('Ctrl Pts',(0.908813145639846,-1.26240729684418,
3.49898146623335));
#263267=CARTESIAN_POINT('Ctrl Pts',(0.919439060930761,-1.25469766834677,
3.49991977866266));
#263268=CARTESIAN_POINT('Ctrl Pts',(0.925365722378492,-1.25033303648256,
3.50044747781748));
#263269=CARTESIAN_POINT('Ctrl Pts',(0.940674112759945,-1.23889086275214,
3.50182200395248));
#263270=CARTESIAN_POINT('Ctrl Pts',(0.950006852292963,-1.23174888785683,
3.5026713301628));
#263271=CARTESIAN_POINT('Ctrl Pts',(1.01856377937654,-1.17804236267732,
3.50899647575765));
#263272=CARTESIAN_POINT('Ctrl Pts',(1.07440649729285,-1.12734346779031,
3.51463791465493));
#263273=CARTESIAN_POINT('Ctrl Pts',(1.2052041757994,-0.990017760278477,
3.52914230118053));
#263274=CARTESIAN_POINT('Ctrl Pts',(1.2746855521503,-0.898792283161244,
3.53813530052346));
#263275=CARTESIAN_POINT('Ctrl Pts',(1.35113078869099,-0.771487668291091,
3.54940517824461));
#263276=CARTESIAN_POINT('Ctrl Pts',(1.36775198189399,-0.741621598017589,
3.55196439986789));
#263277=CARTESIAN_POINT('Ctrl Pts',(1.3864780124704,-0.705198524059447,
3.55496554660474));
#263278=CARTESIAN_POINT('Ctrl Pts',(1.38953931266988,-0.699147152229028,
3.55546028155649));
#263279=CARTESIAN_POINT('Ctrl Pts',(1.39423550872059,-0.689711330810145,
3.55622548721787));
#263280=CARTESIAN_POINT('Ctrl Pts',(1.3958978291903,-0.686340749846035,
3.55649760068546));
#263281=CARTESIAN_POINT('Ctrl Pts',(1.39896260984374,-0.680069296178067,
3.55700158805259));
#263282=CARTESIAN_POINT('Ctrl Pts',(1.40036826116462,-0.677170115119824,
3.55723365102325));
#263283=CARTESIAN_POINT('Ctrl Pts',(1.40355072950968,-0.670553929169158,
3.55776116375599));
#263284=CARTESIAN_POINT('Ctrl Pts',(1.40532179379059,-0.666834221665083,
3.55805625696772));
#263285=CARTESIAN_POINT('Ctrl Pts',(1.40990133448869,-0.657116684596081,
3.55882343116313));
#263286=CARTESIAN_POINT('Ctrl Pts',(1.41268636073715,-0.65110779482949,
3.55929411692055));
#263287=CARTESIAN_POINT('Ctrl Pts',(1.43119848023104,-0.610488619647277,
3.56245224463541));
#263288=CARTESIAN_POINT('Ctrl Pts',(1.44569218371073,-0.575326123662344,
3.56507099572242));
#263289=CARTESIAN_POINT('Ctrl Pts',(1.51071781923886,-0.399541183608317,
3.57777263425468));
#263290=CARTESIAN_POINT('Ctrl Pts',(1.54209641145772,-0.252678798261506,
3.58725566517923));
#263291=CARTESIAN_POINT('Ctrl Pts',(1.55470808556724,-0.0637159556006852,
3.60012770876487));
#263292=CARTESIAN_POINT('Ctrl Pts',(1.55583157354864,-0.0237613914067299,
3.60288097891822));
#263293=CARTESIAN_POINT('Ctrl Pts',(1.55530558667639,0.0267734064996201,
3.60642448385329));
#263294=CARTESIAN_POINT('Ctrl Pts',(1.55508739942901,0.0373557699431689,
3.60716987608417));
#263295=CARTESIAN_POINT('Ctrl Pts',(1.55456395130295,0.0543337469354434,
3.60837151464195));
#263296=CARTESIAN_POINT('Ctrl Pts',(1.55432716797192,0.0607312722262737,
3.60882562004844));
#263297=CARTESIAN_POINT('Ctrl Pts',(1.55380186411863,0.0728925203749078,
3.60969142353515));
#263298=CARTESIAN_POINT('Ctrl Pts',(1.55352074673013,0.0786564701469008,
3.61010288328317));
#263299=CARTESIAN_POINT('Ctrl Pts',(1.55280673027343,0.0917935641681788,
3.61104325842404));
#263300=CARTESIAN_POINT('Ctrl Pts',(1.55235338061458,0.0991654083658013,
3.61157280425712));
#263301=CARTESIAN_POINT('Ctrl Pts',(1.55103690918677,0.118342104049182,
3.61295531133463));
#263302=CARTESIAN_POINT('Ctrl Pts',(1.55009152933668,0.130140629844021,
3.61381081993734));
#263303=CARTESIAN_POINT('Ctrl Pts',(1.54185007546671,0.220089088830683,
3.62037188301625));
#263304=CARTESIAN_POINT('Ctrl Pts',(1.52878420515685,0.297583496632999,
3.62625784230878));
#263305=CARTESIAN_POINT('Ctrl Pts',(1.50511088588568,0.393222412612422,
3.633804783071));
#263306=CARTESIAN_POINT('Ctrl Pts',(1.49991488516801,0.412599013088281,
3.63534823479072));
#263307=CARTESIAN_POINT('Ctrl Pts',(1.47933721737735,0.483801462586178,
3.64106872112974));
#263308=CARTESIAN_POINT('Ctrl Pts',(1.46163180323961,0.53491570248639,3.6452733433651));
#263309=CARTESIAN_POINT('Ctrl Pts',(1.43909084970007,0.59045096367321,3.64990718000055));
#263310=CARTESIAN_POINT('Ctrl Pts',(1.43684906500452,0.595885533791599,
3.65036133090783));
#263311=CARTESIAN_POINT('Ctrl Pts',(1.43457668196674,0.601306904631308,
3.65081500619461));
#263312=CARTESIAN_POINT('Origin',(0.,0.,-1.29405622560371));
#263313=CARTESIAN_POINT('',(1.43457668488586,0.601306897666988,4.48971815675999));
#263314=CARTESIAN_POINT('',(1.43457657355106,0.601307163285539,4.35096339883543));
#263315=CARTESIAN_POINT('',(1.43457668357355,0.601306900797845,-1.29405622560371));
#263316=CARTESIAN_POINT('Ctrl Pts',(1.43457668488586,0.601306897666987,
4.48971815675999));
#263317=CARTESIAN_POINT('Ctrl Pts',(1.4496294055982,0.565394650091241,4.48688128567671));
#263318=CARTESIAN_POINT('Ctrl Pts',(1.46332789596575,0.528930871216676,
4.48399969080137));
#263319=CARTESIAN_POINT('Ctrl Pts',(1.52292031548538,0.350193919453911,
4.46986194584548));
#263320=CARTESIAN_POINT('Ctrl Pts',(1.54950444596061,0.202352133044675,
4.45802888519858));
#263321=CARTESIAN_POINT('Ctrl Pts',(1.55569384384153,0.0208255808088899,
4.44426720952001));
#263322=CARTESIAN_POINT('Ctrl Pts',(1.55579170206273,-0.0113843345359859,
4.44185894189328));
#263323=CARTESIAN_POINT('Ctrl Pts',(1.5547042178844,-0.0501874368977438,
4.43901536873532));
#263324=CARTESIAN_POINT('Ctrl Pts',(1.55447679251389,-0.0567969160773385,
4.43853303521036));
#263325=CARTESIAN_POINT('Ctrl Pts',(1.55405668083049,-0.0670948677577418,
4.437784888774));
#263326=CARTESIAN_POINT('Ctrl Pts',(1.55389300360795,-0.0707843388302729,
4.43751752053279));
#263327=CARTESIAN_POINT('Ctrl Pts',(1.55356378936395,-0.07765265115957,
4.43702108242808));
#263328=CARTESIAN_POINT('Ctrl Pts',(1.55340163663461,-0.0808315376028501,
4.43679183568499));
#263329=CARTESIAN_POINT('Ctrl Pts',(1.55300889694254,-0.0880927561640625,
4.43626935971131));
#263330=CARTESIAN_POINT('Ctrl Pts',(1.55277197142233,-0.0921746899584727,
4.43597648710965));
#263331=CARTESIAN_POINT('Ctrl Pts',(1.55211006461084,-0.102850658388751,
4.43521258828929));
#263332=CARTESIAN_POINT('Ctrl Pts',(1.55165915192597,-0.109443094599776,
4.43474296161927));
#263333=CARTESIAN_POINT('Ctrl Pts',(1.54827591980018,-0.154671374342359,
4.43153408075855));
#263334=CARTESIAN_POINT('Ctrl Pts',(1.5439425954447,-0.193192771068081,
4.42886638416777));
#263335=CARTESIAN_POINT('Ctrl Pts',(1.53652738683792,-0.242458863410164,
4.42549235834147));
#263336=CARTESIAN_POINT('Ctrl Pts',(1.53476356330938,-0.253384146084462,
4.42474654763777));
#263337=CARTESIAN_POINT('Ctrl Pts',(1.51650866915956,-0.35926266401958,
4.41753434534373));
#263338=CARTESIAN_POINT('Ctrl Pts',(1.49134280153566,-0.452511390464715,
4.41129165747051));
#263339=CARTESIAN_POINT('Ctrl Pts',(1.43963174351419,-0.591374246483627,
4.40145451822027));
#263340=CARTESIAN_POINT('Ctrl Pts',(1.41914447914593,-0.638976743083573,
4.39797998350777));
#263341=CARTESIAN_POINT('Ctrl Pts',(1.38258539116952,-0.713449127435685,
4.39229793029168));
#263342=CARTESIAN_POINT('Ctrl Pts',(1.36801099680807,-0.741011270646466,
4.39013831339894));
#263343=CARTESIAN_POINT('Ctrl Pts',(1.34785359972908,-0.776507607160127,
4.3872718485655));
#263344=CARTESIAN_POINT('Ctrl Pts',(1.34301001484466,-0.784855071217839,
4.38659143755161));
#263345=CARTESIAN_POINT('Ctrl Pts',(1.33495563597446,-0.798443150711165,
4.38547317573753));
#263346=CARTESIAN_POINT('Ctrl Pts',(1.33179085095163,-0.803710857389672,
4.3850369973022));
#263347=CARTESIAN_POINT('Ctrl Pts',(1.32560444073762,-0.813871109499376,
4.38419046054938));
#263348=CARTESIAN_POINT('Ctrl Pts',(1.32258673155626,-0.818765932399785,
4.38378025067284));
#263349=CARTESIAN_POINT('Ctrl Pts',(1.31555102040395,-0.830037692975204,
4.38283003593794));
#263350=CARTESIAN_POINT('Ctrl Pts',(1.31151370000568,-0.836402337416092,
4.38228932491039));
#263351=CARTESIAN_POINT('Ctrl Pts',(1.29831131991099,-0.8568846308752,4.38053551968538));
#263352=CARTESIAN_POINT('Ctrl Pts',(1.28896361348408,-0.870882492515712,
4.37931566375303));
#263353=CARTESIAN_POINT('Ctrl Pts',(1.20048636909602,-0.998828386910547,
4.36796256639652));
#263354=CARTESIAN_POINT('Ctrl Pts',(1.1066874867825,-1.10183978589384,4.35722733646156));
#263355=CARTESIAN_POINT('Ctrl Pts',(0.946422225887876,-1.23646907425629,
4.34101417006435));
#263356=CARTESIAN_POINT('Ctrl Pts',(0.889291785282419,-1.27817574512089,
4.33557555991543));
#263357=CARTESIAN_POINT('Ctrl Pts',(0.818822832638556,-1.32259942951951,
4.32940468565497));
#263358=CARTESIAN_POINT('Ctrl Pts',(0.808045810486581,-1.32921107350094,
4.32847502440679));
#263359=CARTESIAN_POINT('Ctrl Pts',(0.793075598681423,-1.3381458407426,
4.32720413967129));
#263360=CARTESIAN_POINT('Ctrl Pts',(0.788950886555265,-1.34058185000729,
4.3268560934979));
#263361=CARTESIAN_POINT('Ctrl Pts',(0.781970868843404,-1.34466079777616,
4.32627076394256));
#263362=CARTESIAN_POINT('Ctrl Pts',(0.779121505342163,-1.34631377525703,
4.32603284219349));
#263363=CARTESIAN_POINT('Ctrl Pts',(0.773681239626328,-1.34944673554357,
4.32558055065654));
#263364=CARTESIAN_POINT('Ctrl Pts',(0.771091308150122,-1.35092832804917,
4.32536607441216));
#263365=CARTESIAN_POINT('Ctrl Pts',(0.764249913284072,-1.35481592231552,
4.32480170832947));
#263366=CARTESIAN_POINT('Ctrl Pts',(0.759991304406713,-1.35720939146146,
4.32445261608534));
#263367=CARTESIAN_POINT('Ctrl Pts',(0.744957158128021,-1.36556609195917,
4.32322772896582));
#263368=CARTESIAN_POINT('Ctrl Pts',(0.734121777711956,-1.37142158346597,
4.32235845288608));
#263369=CARTESIAN_POINT('Ctrl Pts',(0.65240973054253,-1.41433315597924,
4.31589492371475));
#263370=CARTESIAN_POINT('Ctrl Pts',(0.578828674008771,-1.44600753949109,
4.31058501428635));
#263371=CARTESIAN_POINT('Ctrl Pts',(0.427674721716568,-1.49767586447515,
4.30005117247523));
#263372=CARTESIAN_POINT('Ctrl Pts',(0.350353179279664,-1.51762665615863,
4.29484049618524));
#263373=CARTESIAN_POINT('Ctrl Pts',(0.214871896188,-1.54167391977124,4.28560815878372));
#263374=CARTESIAN_POINT('Ctrl Pts',(0.15738570946834,-1.54859835510715,
4.281661533238));
#263375=CARTESIAN_POINT('Ctrl Pts',(0.0879781719606484,-1.5530540684106,
4.27679344498549));
#263376=CARTESIAN_POINT('Ctrl Pts',(0.0762961996199487,-1.55367177191675,
4.27597070638206));
#263377=CARTESIAN_POINT('Ctrl Pts',(0.0580198643052897,-1.55443154639989,
4.27467774170055));
#263378=CARTESIAN_POINT('Ctrl Pts',(0.0514294988808367,-1.5546635460165,
4.27421032753634));
#263379=CARTESIAN_POINT('Ctrl Pts',(0.039744854766824,-1.55500050086644,
4.27337943361898));
#263380=CARTESIAN_POINT('Ctrl Pts',(0.034651126462614,-1.55512234550101,
4.27301648719875));
#263381=CARTESIAN_POINT('Ctrl Pts',(0.0229108768374192,-1.55534546899381,
4.27217821786568));
#263382=CARTESIAN_POINT('Ctrl Pts',(0.0162641628112747,-1.55542917250117,
4.27170235267692));
#263383=CARTESIAN_POINT('Ctrl Pts',(-0.00200294249263999,-1.55554211493817,
4.27039090302117));
#263384=CARTESIAN_POINT('Ctrl Pts',(-0.013623233797216,-1.55548374372541,
4.26955260430709));
#263385=CARTESIAN_POINT('Ctrl Pts',(-0.0754543521291461,-1.55448026236994,
4.26506957355809));
#263386=CARTESIAN_POINT('Ctrl Pts',(-0.12559244726126,-1.55123426058943,
4.26135400405865));
#263387=CARTESIAN_POINT('Ctrl Pts',(-0.321357330760294,-1.52900750748695,
4.24651777380385));
#263388=CARTESIAN_POINT('Ctrl Pts',(-0.464127891150248,-1.49188144309349,
4.23489079933847));
#263389=CARTESIAN_POINT('Ctrl Pts',(-0.617902306033279,-1.42764555644481,
4.22229129623412));
#263390=CARTESIAN_POINT('Ctrl Pts',(-0.636090150108855,-1.41963534111109,
4.22080146125937));
#263391=CARTESIAN_POINT('Ctrl Pts',(-0.666027906535529,-1.40575934101143,
4.21835529105081));
#263392=CARTESIAN_POINT('Ctrl Pts',(-0.677865564961396,-1.40008956986362,
4.21738968682946));
#263393=CARTESIAN_POINT('Ctrl Pts',(-0.693987705959558,-1.39211527657428,
4.2160782237036));
#263394=CARTESIAN_POINT('Ctrl Pts',(-0.698334807808633,-1.38993970272594,
4.21572497244544));
#263395=CARTESIAN_POINT('Ctrl Pts',(-0.705623365473424,-1.38624920630204,
4.21513339842743));
#263396=CARTESIAN_POINT('Ctrl Pts',(-0.708570283326058,-1.38474522933057,
4.21489440707879));
#263397=CARTESIAN_POINT('Ctrl Pts',(-0.71415413900671,-1.38187298289882,
4.21444196425293));
#263398=CARTESIAN_POINT('Ctrl Pts',(-0.716791982960632,-1.3805065478642,
4.21422839713211));
#263399=CARTESIAN_POINT('Ctrl Pts',(-0.723694699294365,-1.37690573871875,
4.21366993542193));
#263400=CARTESIAN_POINT('Ctrl Pts',(-0.72795318665476,-1.37465908166417,
4.21332580682127));
#263401=CARTESIAN_POINT('Ctrl Pts',(-0.742699123595152,-1.3667918044138,
4.21213534435835));
#263402=CARTESIAN_POINT('Ctrl Pts',(-0.753132810915957,-1.36107046720772,
4.21129505779315));
#263403=CARTESIAN_POINT('Ctrl Pts',(-0.851752753088455,-1.30551062607219,
4.20336206317367));
#263404=CARTESIAN_POINT('Ctrl Pts',(-0.934952469340575,-1.24728153121076,
4.19673216721475));
#263405=CARTESIAN_POINT('Ctrl Pts',(-1.09850602031394,-1.10718842834496,
4.18255932922575));
#263406=CARTESIAN_POINT('Ctrl Pts',(-1.17667246754693,-1.02372761708732,
4.17503308528831));
#263407=CARTESIAN_POINT('Ctrl Pts',(-1.25305610327961,-0.921743281344272,
4.16613635260185));
#263408=CARTESIAN_POINT('Ctrl Pts',(-1.26095993217026,-0.910900820246568,
4.16519437960877));
#263409=CARTESIAN_POINT('Ctrl Pts',(-1.27274803285324,-0.894282455660537,
4.16375569395895));
#263410=CARTESIAN_POINT('Ctrl Pts',(-1.27673557929078,-0.888580285264104,
4.16326293965605));
#263411=CARTESIAN_POINT('Ctrl Pts',(-1.28359206471301,-0.878634111464093,
4.16240488055949));
#263412=CARTESIAN_POINT('Ctrl Pts',(-1.28647856994604,-0.874402297767903,
4.162040248974));
#263413=CARTESIAN_POINT('Ctrl Pts',(-1.29289620856387,-0.864893036107552,
4.16122184143734));
#263414=CARTESIAN_POINT('Ctrl Pts',(-1.29641601765793,-0.859608094992573,
4.16076764782077));
#263415=CARTESIAN_POINT('Ctrl Pts',(-1.30571418159077,-0.845460034128013,
4.15955337822951));
#263416=CARTESIAN_POINT('Ctrl Pts',(-1.31143454184425,-0.836559397465484,
4.15879116226563));
#263417=CARTESIAN_POINT('Ctrl Pts',(-1.3363162870448,-0.796962022263645,
4.15540698539514));
#263418=CARTESIAN_POINT('Ctrl Pts',(-1.3544924211383,-0.765662825511044,
4.15274948624549));
#263419=CARTESIAN_POINT('Ctrl Pts',(-1.44689764714555,-0.592937212205354,
4.13816300746388));
#263420=CARTESIAN_POINT('Ctrl Pts',(-1.50008148799625,-0.441390248115223,
4.12550887901513));
#263421=CARTESIAN_POINT('Ctrl Pts',(-1.53528366002654,-0.252119500937636,
4.11091413652309));
#263422=CARTESIAN_POINT('Ctrl Pts',(-1.54026781020884,-0.219626129507415,
4.10845510820709));
#263423=CARTESIAN_POINT('Ctrl Pts',(-1.54501867130841,-0.180393440283004,
4.10555993194058));
#263424=CARTESIAN_POINT('Ctrl Pts',(-1.54577591035135,-0.173785290652867,
4.10507479419847));
#263425=CARTESIAN_POINT('Ctrl Pts',(-1.54688854268592,-0.163492465079236,
4.1043232576365));
#263426=CARTESIAN_POINT('Ctrl Pts',(-1.54727319813199,-0.159811140882374,
4.1040552811243));
#263427=CARTESIAN_POINT('Ctrl Pts',(-1.5479640997769,-0.152962482369794,
4.10355830603934));
#263428=CARTESIAN_POINT('Ctrl Pts',(-1.54827376481576,-0.149795609806687,
4.10332912688423));
#263429=CARTESIAN_POINT('Ctrl Pts',(-1.54895801519293,-0.142569062247267,
4.10280756508848));
#263430=CARTESIAN_POINT('Ctrl Pts',(-1.54932635978687,-0.138508852546755,
4.10251553421505));
#263431=CARTESIAN_POINT('Ctrl Pts',(-1.55024643188225,-0.127903824039332,
4.10175528321589));
#263432=CARTESIAN_POINT('Ctrl Pts',(-1.55077268557221,-0.121356785923434,
4.10128844097641));
#263433=CARTESIAN_POINT('Ctrl Pts',(-1.55406118177974,-0.0769228370596933,
4.09813578325049));
#263434=CARTESIAN_POINT('Ctrl Pts',(-1.55547649964676,-0.0389452410474964,
4.09551872723645));
#263435=CARTESIAN_POINT('Ctrl Pts',(-1.55556939098356,0.113117882334024,
4.08521302295828));
#263436=CARTESIAN_POINT('Ctrl Pts',(-1.54309197620292,0.226854212899771,
4.07787141785222));
#263437=CARTESIAN_POINT('Ctrl Pts',(-1.50276449358015,0.407891633369894,
4.06552717888365));
#263438=CARTESIAN_POINT('Ctrl Pts',(-1.4824659799087,0.476412806834417,
4.06069798505634));
#263439=CARTESIAN_POINT('Ctrl Pts',(-1.45350419185649,0.554111115996123,
4.05490346341675));
#263440=CARTESIAN_POINT('Ctrl Pts',(-1.44935119513,0.564884647659886,4.05409279664466));
#263441=CARTESIAN_POINT('Ctrl Pts',(-1.44239560745538,0.582346748246318,
4.0527665462406));
#263442=CARTESIAN_POINT('Ctrl Pts',(-1.43966544716021,0.589063851069534,
4.0522533901517));
#263443=CARTESIAN_POINT('Ctrl Pts',(-1.43470802870151,0.601020409480702,
4.05133448841096));
#263444=CARTESIAN_POINT('Ctrl Pts',(-1.43249876461341,0.606267224939563,
4.05092935683803));
#263445=CARTESIAN_POINT('Ctrl Pts',(-1.42776700186372,0.617334494761621,
4.05007071967775));
#263446=CARTESIAN_POINT('Ctrl Pts',(-1.42523760735243,0.623151867861369,
4.04961698559424));
#263447=CARTESIAN_POINT('Ctrl Pts',(-1.41840622783767,0.638604229514652,
4.04840524524267));
#263448=CARTESIAN_POINT('Ctrl Pts',(-1.41404173374574,0.648211041364376,
4.04764511466429));
#263449=CARTESIAN_POINT('Ctrl Pts',(-1.39241945760784,0.694546707755396,
4.04394513519803));
#263450=CARTESIAN_POINT('Ctrl Pts',(-1.37382809364769,0.730631835584284,
4.04095968849643));
#263451=CARTESIAN_POINT('Ctrl Pts',(-1.28062769438369,0.895368323678686,
4.02682178739395));
#263452=CARTESIAN_POINT('Ctrl Pts',(-1.18922762977399,1.01361519780563,
4.01507769280092));
#263453=CARTESIAN_POINT('Ctrl Pts',(-1.0549445414778,1.14374026281844,4.00083332591914));
#263454=CARTESIAN_POINT('Ctrl Pts',(-1.02643547462342,1.16939325983568,
3.99795185372611));
#263455=CARTESIAN_POINT('Ctrl Pts',(-0.991950346270438,1.19818951803847,
3.99465566098604));
#263456=CARTESIAN_POINT('Ctrl Pts',(-0.986869064260426,1.20237808725454,
3.99417459983979));
#263457=CARTESIAN_POINT('Ctrl Pts',(-0.978595065489628,1.20911066891497,
3.99339893251544));
#263458=CARTESIAN_POINT('Ctrl Pts',(-0.975418735680899,1.2116745449994,
3.99310296646358));
#263459=CARTESIAN_POINT('Ctrl Pts',(-0.969748102419786,1.21621502852914,
3.99257784581393));
#263460=CARTESIAN_POINT('Ctrl Pts',(-0.96725779501266,1.21819650978198,
3.99234834786266));
#263461=CARTESIAN_POINT('Ctrl Pts',(-0.961860747412773,1.22246383420884,
3.99185338451835));
#263462=CARTESIAN_POINT('Ctrl Pts',(-0.958951935834489,1.22474695708687,
3.99158811137077));
#263463=CARTESIAN_POINT('Ctrl Pts',(-0.950801235675756,1.23109759209628,
3.99084887112872));
#263464=CARTESIAN_POINT('Ctrl Pts',(-0.945541339666491,1.23514203645756,
3.99037649772629));
#263465=CARTESIAN_POINT('Ctrl Pts',(-0.914305448458741,1.25884348934004,
3.98759774920589));
#263466=CARTESIAN_POINT('Ctrl Pts',(-0.887740714003841,1.27771601005347,
3.98534182920958));
#263467=CARTESIAN_POINT('Ctrl Pts',(-0.731486775138291,1.38149609712096,
3.97255183732372));
#263468=CARTESIAN_POINT('Ctrl Pts',(-0.590276034206814,1.44747635458024,
3.96275163431774));
#263469=CARTESIAN_POINT('Ctrl Pts',(-0.402911855832,1.50295465313333,3.94948220288578));
#263470=CARTESIAN_POINT('Ctrl Pts',(-0.363766666040113,1.51290580938595,
3.94670242458542));
#263471=CARTESIAN_POINT('Ctrl Pts',(-0.31353502297122,1.52361306475423,
3.94310367541299));
#263472=CARTESIAN_POINT('Ctrl Pts',(-0.302764931428852,1.52578975190809,
3.9423302841545));
#263473=CARTESIAN_POINT('Ctrl Pts',(-0.285647918992407,1.52906081731417,
3.94109788132783));
#263474=CARTESIAN_POINT('Ctrl Pts',(-0.279315556943456,1.53023022256615,
3.94064125896278));
#263475=CARTESIAN_POINT('Ctrl Pts',(-0.267945873538773,1.53225695205301,
3.93982006144905));
#263476=CARTESIAN_POINT('Ctrl Pts',(-0.262911213324307,1.53312884358279,
3.93945595443612));
#263477=CARTESIAN_POINT('Ctrl Pts',(-0.25113618520361,1.53510831066129,
3.93860324010663));
#263478=CARTESIAN_POINT('Ctrl Pts',(-0.244392682199628,1.53619631659251,
3.93811402067429));
#263479=CARTESIAN_POINT('Ctrl Pts',(-0.224987760607153,1.53919612873552,
3.93670361899967));
#263480=CARTESIAN_POINT('Ctrl Pts',(-0.212309881224785,1.54099601272446,
3.93577893158095));
#263481=CARTESIAN_POINT('Ctrl Pts',(-0.111220825004964,1.55407654789613,
3.92837830418685));
#263482=CARTESIAN_POINT('Ctrl Pts',(-0.0220277197653859,1.55789387736974,
3.92166687004201));
#263483=CARTESIAN_POINT('Ctrl Pts',(0.162991155967391,1.54991873904261,
3.90742065816221));
#263484=CARTESIAN_POINT('Ctrl Pts',(0.258403588082749,1.53689353713582,
3.89989188140377));
#263485=CARTESIAN_POINT('Ctrl Pts',(0.389244266044576,1.50649621335559,
3.88966003358217));
#263486=CARTESIAN_POINT('Ctrl Pts',(0.426156866801691,1.49647347636279,
3.88678645844192));
#263487=CARTESIAN_POINT('Ctrl Pts',(0.468948085682516,1.48314235218931,
3.88349818738217));
#263488=CARTESIAN_POINT('Ctrl Pts',(0.475217769165342,1.48114537432502,
3.88301750079174));
#263489=CARTESIAN_POINT('Ctrl Pts',(0.485354724867895,1.47784562472242,
3.88224231720864));
#263490=CARTESIAN_POINT('Ctrl Pts',(0.48922978656204,1.4765673423296,3.88194646303792));
#263491=CARTESIAN_POINT('Ctrl Pts',(0.496117987115583,1.47426501002547,
3.88142146415251));
#263492=CARTESIAN_POINT('Ctrl Pts',(0.499133050812023,1.47324694983624,
3.88119197671732));
#263493=CARTESIAN_POINT('Ctrl Pts',(0.505645836467736,1.47102556716418,
3.88069694878178));
#263494=CARTESIAN_POINT('Ctrl Pts',(0.509142393101847,1.46981902134488,
3.88043160099852));
#263495=CARTESIAN_POINT('Ctrl Pts',(0.518903426597858,1.46641180078459,
3.87969194100505));
#263496=CARTESIAN_POINT('Ctrl Pts',(0.525158266509693,1.46418343623874,
3.87921922541267));
#263497=CARTESIAN_POINT('Ctrl Pts',(0.562094027811293,1.45075747195474,
3.87643413088317));
#263498=CARTESIAN_POINT('Ctrl Pts',(0.592433138159572,1.43863487796326,
3.87417247627393));
#263499=CARTESIAN_POINT('Ctrl Pts',(0.765650759609296,1.36301181653492,
3.86128632071859));
#263500=CARTESIAN_POINT('Ctrl Pts',(0.898688880043385,1.279214587416,3.851406447969));
#263501=CARTESIAN_POINT('Ctrl Pts',(1.04663740270753,1.15137478840919,3.83811531485476));
#263502=CARTESIAN_POINT('Ctrl Pts',(1.07528827803231,1.1246636994786,3.83541743835888));
#263503=CARTESIAN_POINT('Ctrl Pts',(1.11056752652789,1.08919156946057,3.83191134638785));
#263504=CARTESIAN_POINT('Ctrl Pts',(1.11815476297379,1.08140113803515,3.83114582533601));
#263505=CARTESIAN_POINT('Ctrl Pts',(1.1300865642747,1.06888996352268,3.82992308858041));
#263506=CARTESIAN_POINT('Ctrl Pts',(1.13448478598546,1.06422068435184,3.82946819741248));
#263507=CARTESIAN_POINT('Ctrl Pts',(1.14233646183328,1.05578113165068,3.82864849753494));
#263508=CARTESIAN_POINT('Ctrl Pts',(1.14580046636822,1.05202076030249,3.82828414638647));
#263509=CARTESIAN_POINT('Ctrl Pts',(1.15387161754523,1.0431719216984,3.82742876172132));
#263510=CARTESIAN_POINT('Ctrl Pts',(1.15846371303028,1.03806993540541,3.82693710325898));
#263511=CARTESIAN_POINT('Ctrl Pts',(1.17163119133005,1.0232441979354,3.82551267313542));
#263512=CARTESIAN_POINT('Ctrl Pts',(1.18011878204187,1.01344362371414,3.82457628692552));
#263513=CARTESIAN_POINT('Ctrl Pts',(1.25152779253115,0.928874491273502,
3.81653835031673));
#263514=CARTESIAN_POINT('Ctrl Pts',(1.30738406671698,0.84845124364151,3.80915069464098));
#263515=CARTESIAN_POINT('Ctrl Pts',(1.38487019825216,0.710873001728965,
3.79696702009401));
#263516=CARTESIAN_POINT('Ctrl Pts',(1.41132923121526,0.656769881463216,
3.79228202654749));
#263517=CARTESIAN_POINT('Ctrl Pts',(1.43457681153698,0.601306595507149,
3.78763867041446));
#263518=CARTESIAN_POINT('Ctrl Pts',(1.43457668196674,0.601306904631308,
3.65081500619461));
#263519=CARTESIAN_POINT('Ctrl Pts',(1.41248223415038,0.654019054440599,
3.65522610449217));
#263520=CARTESIAN_POINT('Ctrl Pts',(1.38749513607011,0.705483256301638,
3.6595938904266));
#263521=CARTESIAN_POINT('Ctrl Pts',(1.3538881908303,0.765970957718364,3.66471482813885));
#263522=CARTESIAN_POINT('Ctrl Pts',(1.34792834150311,0.776410942282884,
3.66559814297501));
#263523=CARTESIAN_POINT('Ctrl Pts',(1.33945480041942,0.790862485526851,
3.66681903248342));
#263524=CARTESIAN_POINT('Ctrl Pts',(1.3370431276979,0.794932896313606,3.66716270131296));
#263525=CARTESIAN_POINT('Ctrl Pts',(1.33291145681734,0.80183431587057,3.66774496213212));
#263526=CARTESIAN_POINT('Ctrl Pts',(1.33120093211004,0.804670927149445,
3.66798415655261));
#263527=CARTESIAN_POINT('Ctrl Pts',(1.32789880561523,0.810107588488455,
3.668442326523));
#263528=CARTESIAN_POINT('Ctrl Pts',(1.32630861255695,0.812708439463858,
3.66866139408254));
#263529=CARTESIAN_POINT('Ctrl Pts',(1.32204398440995,0.819637627171099,
3.66924476884178));
#263530=CARTESIAN_POINT('Ctrl Pts',(1.31935591039348,0.823957596145479,
3.66960819389876));
#263531=CARTESIAN_POINT('Ctrl Pts',(1.30953576221684,0.839568149258955,
3.67092075227493));
#263532=CARTESIAN_POINT('Ctrl Pts',(1.30227929595905,0.850780381050817,
3.67186214561297));
#263533=CARTESIAN_POINT('Ctrl Pts',(1.19831733338818,1.00696837842723,3.68497784886838));
#263534=CARTESIAN_POINT('Ctrl Pts',(1.07805144237437,1.13480284649737,3.69585901537796));
#263535=CARTESIAN_POINT('Ctrl Pts',(0.904337337247798,1.26635407895836,
3.71062707569195));
#263536=CARTESIAN_POINT('Ctrl Pts',(0.868515681298962,1.29118495651451,
3.71362287655073));
#263537=CARTESIAN_POINT('Ctrl Pts',(0.822508707573054,1.32029467236599,
3.71743842292436));
#263538=CARTESIAN_POINT('Ctrl Pts',(0.813255097019537,1.32601460490569,
3.71820425857743));
#263539=CARTESIAN_POINT('Ctrl Pts',(0.798406411914479,1.33497912710978,
3.7194310089638));
#263540=CARTESIAN_POINT('Ctrl Pts',(0.792849656737897,1.33828677342476,
3.71988961857966));
#263541=CARTESIAN_POINT('Ctrl Pts',(0.782306001615559,1.34447414645509,
3.72075900646976));
#263542=CARTESIAN_POINT('Ctrl Pts',(0.777323405731917,1.34736102508348,
3.72116951706343));
#263543=CARTESIAN_POINT('Ctrl Pts',(0.766010916427692,1.35383176090927,
3.7221008531065));
#263544=CARTESIAN_POINT('Ctrl Pts',(0.759671722474857,1.35739899501897,
3.72262226412219));
#263545=CARTESIAN_POINT('Ctrl Pts',(0.743276266197914,1.36647433479872,
3.72396971842492));
#263546=CARTESIAN_POINT('Ctrl Pts',(0.733183860748704,1.37191586068914,
3.72479810088033));
#263547=CARTESIAN_POINT('Ctrl Pts',(0.664473441948673,1.40798777019503,
3.73043184144804));
#263548=CARTESIAN_POINT('Ctrl Pts',(0.604022176256144,1.43495972218187,
3.73536351028652));
#263549=CARTESIAN_POINT('Ctrl Pts',(0.430912554946466,1.49931727905603,
3.74941793161595));
#263550=CARTESIAN_POINT('Ctrl Pts',(0.315431020303203,1.52778858303827,
3.75874492849165));
#263551=CARTESIAN_POINT('Ctrl Pts',(0.158920749501713,1.54785795632627,
3.77076796451315));
#263552=CARTESIAN_POINT('Ctrl Pts',(0.11981987160918,1.5513748431871,3.77371769432799));
#263553=CARTESIAN_POINT('Ctrl Pts',(0.0736006353177334,1.55377368263397,
3.77711110179891));
#263554=CARTESIAN_POINT('Ctrl Pts',(0.0665747110034731,1.55409057755694,
3.77762439984716));
#263555=CARTESIAN_POINT('Ctrl Pts',(0.0557371723841911,1.55450575792803,
3.77841200200046));
#263556=CARTESIAN_POINT('Ctrl Pts',(0.0519270631922611,1.55463769566144,
3.77868810291033));
#263557=CARTESIAN_POINT('Ctrl Pts',(0.04490098527156,1.55485513815668,3.77919574121096));
#263558=CARTESIAN_POINT('Ctrl Pts',(0.0416852548692331,1.55494467395382,
3.77942749191928));
#263559=CARTESIAN_POINT('Ctrl Pts',(0.0344223289403372,1.55512434879558,
3.77994960392184));
#263560=CARTESIAN_POINT('Ctrl Pts',(0.0303750504421464,1.55520866582593,
3.78023963835893));
#263561=CARTESIAN_POINT('Ctrl Pts',(0.0181593010589105,1.55541545163537,
3.78111240783904));
#263562=CARTESIAN_POINT('Ctrl Pts',(0.00998997673869821,1.55548937491343,
3.78169252610975));
#263563=CARTESIAN_POINT('Ctrl Pts',(-0.0685451418059095,1.55558127518474,
3.78723862509665));
#263564=CARTESIAN_POINT('Ctrl Pts',(-0.138846094609719,1.55088886811156,
3.79196697433598));
#263565=CARTESIAN_POINT('Ctrl Pts',(-0.266743725079774,1.53358110516601,
3.8005228848376));
#263566=CARTESIAN_POINT('Ctrl Pts',(-0.324399319969653,1.52242848288096,
3.80436256999112));
#263567=CARTESIAN_POINT('Ctrl Pts',(-0.470997861812928,1.48536314494387,
3.81434851175503));
#263568=CARTESIAN_POINT('Ctrl Pts',(-0.558491506946601,1.45472540837135,
3.82053688684906));
#263569=CARTESIAN_POINT('Ctrl Pts',(-0.654563695136473,1.41113262753592,
3.82790772914782));
#263570=CARTESIAN_POINT('Ctrl Pts',(-0.666322562000888,1.40561842221868,
3.82881992215711));
#263571=CARTESIAN_POINT('Ctrl Pts',(-0.684240171225715,1.39694078136309,
3.83022602558785));
#263572=CARTESIAN_POINT('Ctrl Pts',(-0.690449346872053,1.39388229601962,
3.83071630599239));
#263573=CARTESIAN_POINT('Ctrl Pts',(-0.701265216818251,1.38846466680611,
3.83157571112684));
#263574=CARTESIAN_POINT('Ctrl Pts',(-0.705880971661034,1.38612376357573,
3.83194419468438));
#263575=CARTESIAN_POINT('Ctrl Pts',(-0.716285244587605,1.38078173934341,
3.83277874513233));
#263576=CARTESIAN_POINT('Ctrl Pts',(-0.722066715881598,1.3777671859728,
3.83324527855689));
#263577=CARTESIAN_POINT('Ctrl Pts',(-0.737658513367,1.36951227464327,3.83451112815336));
#263578=CARTESIAN_POINT('Ctrl Pts',(-0.747431700709627,1.3642029884067,
3.83531286761553));
#263579=CARTESIAN_POINT('Ctrl Pts',(-0.792894886804613,1.33886991800512,
3.83908216576555));
#263580=CARTESIAN_POINT('Ctrl Pts',(-0.827839502350788,1.31754929315272,
3.84209567848846));
#263581=CARTESIAN_POINT('Ctrl Pts',(-0.964941933419628,1.2262907817828,
3.85440952449655));
#263582=CARTESIAN_POINT('Ctrl Pts',(-1.05941783009147,1.14565578102305,
3.8640860672503));
#263583=CARTESIAN_POINT('Ctrl Pts',(-1.18102815281365,1.01382692200413,
3.87791569442675));
#263584=CARTESIAN_POINT('Ctrl Pts',(-1.21651868233831,0.970956351383092,
3.8821584403891));
#263585=CARTESIAN_POINT('Ctrl Pts',(-1.25636712957263,0.91719654836222,
3.88710489124932));
#263586=CARTESIAN_POINT('Ctrl Pts',(-1.2629954953069,0.908047504990818,
3.88793434034297));
#263587=CARTESIAN_POINT('Ctrl Pts',(-1.27219080253282,0.895059838170542,
3.88909362383332));
#263588=CARTESIAN_POINT('Ctrl Pts',(-1.27484102535098,0.891281051920285,
3.88942878277673));
#263589=CARTESIAN_POINT('Ctrl Pts',(-1.27935206517222,0.88478775615689,
3.890000979148));
#263590=CARTESIAN_POINT('Ctrl Pts',(-1.28122114532435,0.882079054132552,
3.89023856997621));
#263591=CARTESIAN_POINT('Ctrl Pts',(-1.2848209877176,0.876826519626964,
3.89069713366457));
#263592=CARTESIAN_POINT('Ctrl Pts',(-1.28655280544414,0.874283475340645,
3.8909181815385));
#263593=CARTESIAN_POINT('Ctrl Pts',(-1.29071748419781,0.868128785562189,
3.8914508728641));
#263594=CARTESIAN_POINT('Ctrl Pts',(-1.29314276559258,0.864512001856784,
3.8917620119057));
#263595=CARTESIAN_POINT('Ctrl Pts',(-1.30208644392789,0.851052587662169,
3.892913056396));
#263596=CARTESIAN_POINT('Ctrl Pts',(-1.30850813862925,0.841145699512007,
3.89374681983822));
#263597=CARTESIAN_POINT('Ctrl Pts',(-1.3703013348674,0.743395432380443,
3.90185263972659));
#263598=CARTESIAN_POINT('Ctrl Pts',(-1.41686716636135,0.650274509475742,
3.90863816772539));
#263599=CARTESIAN_POINT('Ctrl Pts',(-1.49233389381873,0.451946009021947,
3.92260693563284));
#263600=CARTESIAN_POINT('Ctrl Pts',(-1.52017276594882,0.346966380250798,
3.9297670519908));
#263601=CARTESIAN_POINT('Ctrl Pts',(-1.5392498347612,0.224780066138408,
3.9383799795859));
#263602=CARTESIAN_POINT('Ctrl Pts',(-1.541394111577,0.209571694903565,3.93945627755315));
#263603=CARTESIAN_POINT('Ctrl Pts',(-1.54423725939253,0.186992761666482,
3.94106161821623));
#263604=CARTESIAN_POINT('Ctrl Pts',(-1.54510932229686,0.179644607351197,
3.94158522416555));
#263605=CARTESIAN_POINT('Ctrl Pts',(-1.546568281975,0.166553657327033,3.94252023423077));
#263606=CARTESIAN_POINT('Ctrl Pts',(-1.54717570725876,0.160813248227054,
3.94293098636375));
#263607=CARTESIAN_POINT('Ctrl Pts',(-1.54838861694445,0.14870718984261,
3.943798870711));
#263608=CARTESIAN_POINT('Ctrl Pts',(-1.54898682778632,0.142340937487493,
3.94425622299247));
#263609=CARTESIAN_POINT('Ctrl Pts',(-1.55046797591417,0.125461585725873,
3.94547146644935));
#263610=CARTESIAN_POINT('Ctrl Pts',(-1.55128322375806,0.114943043846042,
3.94623145909429));
#263611=CARTESIAN_POINT('Ctrl Pts',(-1.55435043694713,0.0693539477777701,
3.94953768983712));
#263612=CARTESIAN_POINT('Ctrl Pts',(-1.55552037157283,0.034223609396336,
3.95211724177831));
#263613=CARTESIAN_POINT('Ctrl Pts',(-1.55541993858913,-0.136754236632592,
3.96483779332785));
#263614=CARTESIAN_POINT('Ctrl Pts',(-1.53754511327777,-0.271984690434862,
3.97547988788291));
#263615=CARTESIAN_POINT('Ctrl Pts',(-1.48800799561479,-0.456590779125059,
3.99018758041753));
#263616=CARTESIAN_POINT('Ctrl Pts',(-1.47082090478669,-0.509244862790918,
3.99439363263666));
#263617=CARTESIAN_POINT('Ctrl Pts',(-1.44800754874389,-0.568257879032682,
3.99904231310736));
#263618=CARTESIAN_POINT('Ctrl Pts',(-1.44509764761657,-0.575617645868236,
3.99962085330804));
#263619=CARTESIAN_POINT('Ctrl Pts',(-1.44061408907592,-0.58670920621473,
4.00049056258533));
#263620=CARTESIAN_POINT('Ctrl Pts',(-1.43908187994513,-0.590457441415419,
4.00078408946524));
#263621=CARTESIAN_POINT('Ctrl Pts',(-1.43630611885773,-0.597172782637498,
4.00130923697414));
#263622=CARTESIAN_POINT('Ctrl Pts',(-1.43506798932785,-0.600142038222562,
4.00154117339725));
#263623=CARTESIAN_POINT('Ctrl Pts',(-1.43234284054855,-0.606620774364344,
4.00204666659691));
#263624=CARTESIAN_POINT('Ctrl Pts',(-1.4308521337207,-0.610128633183781,
4.0023199970875));
#263625=CARTESIAN_POINT('Ctrl Pts',(-1.42657585102065,-0.620089502334404,
4.00309520297843));
#263626=CARTESIAN_POINT('Ctrl Pts',(-1.42375936345784,-0.626529272712305,
4.00359525359604));
#263627=CARTESIAN_POINT('Ctrl Pts',(-1.40497093270187,-0.668707125197741,
4.00686440131286));
#263628=CARTESIAN_POINT('Ctrl Pts',(-1.38769680705483,-0.703854218763706,
4.00956038134491));
#263629=CARTESIAN_POINT('Ctrl Pts',(-1.31320564274172,-0.841988685470106,
4.02019051734059));
#263630=CARTESIAN_POINT('Ctrl Pts',(-1.24570103455101,-0.938981872534296,
4.02776046557674));
#263631=CARTESIAN_POINT('Ctrl Pts',(-1.12367153420295,-1.07769391969544,
4.04008430254892));
#263632=CARTESIAN_POINT('Ctrl Pts',(-1.07626024052109,-1.12504397923258,
4.04462363752967));
#263633=CARTESIAN_POINT('Ctrl Pts',(-1.01731124870653,-1.17677109299921,
4.05010465158792));
#263634=CARTESIAN_POINT('Ctrl Pts',(-1.00858757953179,-1.18425650263217,
4.05091177634744));
#263635=CARTESIAN_POINT('Ctrl Pts',(-0.994202718114478,-1.19632530875286,
4.05223673067819));
#263636=CARTESIAN_POINT('Ctrl Pts',(-0.98859076599963,-1.2009669367611,
4.05275218405477));
#263637=CARTESIAN_POINT('Ctrl Pts',(-0.978482743262037,-1.20920839485114,
4.05367814057749));
#263638=CARTESIAN_POINT('Ctrl Pts',(-0.973998852478831,-1.21282301049138,
4.05408803884237));
#263639=CARTESIAN_POINT('Ctrl Pts',(-0.964442216133727,-1.22043976126517,
4.05495992825379));
#263640=CARTESIAN_POINT('Ctrl Pts',(-0.959364414684744,-1.22443534604672,
4.05542216985932));
#263641=CARTESIAN_POINT('Ctrl Pts',(-0.945690112324847,-1.23505800606424,
4.05666433401356));
#263642=CARTESIAN_POINT('Ctrl Pts',(-0.937049031460018,-1.24162682334011,
4.05744652687098));
#263643=CARTESIAN_POINT('Ctrl Pts',(-0.893630544478683,-1.27392149298274,
4.06136390295115));
#263644=CARTESIAN_POINT('Ctrl Pts',(-0.85786263575134,-1.29827675702903,
4.06455109272063));
#263645=CARTESIAN_POINT('Ctrl Pts',(-0.677790454380509,-1.41019991428294,
4.08042346862211));
#263646=CARTESIAN_POINT('Ctrl Pts',(-0.520943356939866,-1.47535267949552,
4.09388503637533));
#263647=CARTESIAN_POINT('Ctrl Pts',(-0.33926571652047,-1.51815693950149,
4.10782140738633));
#263648=CARTESIAN_POINT('Ctrl Pts',(-0.32174316597514,-1.52196686194536,
4.10914762114653));
#263649=CARTESIAN_POINT('Ctrl Pts',(-0.298549639874176,-1.52659132148868,
4.1108761528686));
#263650=CARTESIAN_POINT('Ctrl Pts',(-0.29293536543642,-1.5276785737662,
4.11129249747033));
#263651=CARTESIAN_POINT('Ctrl Pts',(-0.283852127923382,-1.5293857052043,
4.11196261942163));
#263652=CARTESIAN_POINT('Ctrl Pts',(-0.280386901669633,-1.53002478798759,
4.11221745340248));
#263653=CARTESIAN_POINT('Ctrl Pts',(-0.273689173249273,-1.5312365143614,
4.11270839398404));
#263654=CARTESIAN_POINT('Ctrl Pts',(-0.270457011655737,-1.53181070356316,
4.11294458134071));
#263655=CARTESIAN_POINT('Ctrl Pts',(-0.262721997262527,-1.53315957340096,
4.11350811502675));
#263656=CARTESIAN_POINT('Ctrl Pts',(-0.258217454185146,-1.53392466344834,
4.11383492228367));
#263657=CARTESIAN_POINT('Ctrl Pts',(-0.242841356666374,-1.53646661884572,
4.11494599965505));
#263658=CARTESIAN_POINT('Ctrl Pts',(-0.23195399546229,-1.53814789848327,
4.11572511347373));
#263659=CARTESIAN_POINT('Ctrl Pts',(-0.168706260736674,-1.54722807288897,
4.1202120300487));
#263660=CARTESIAN_POINT('Ctrl Pts',(-0.116007606723696,-1.55206961291846,
4.12379566224567));
#263661=CARTESIAN_POINT('Ctrl Pts',(0.0777742173168805,-1.5599443465302,
4.13674072016949));
#263662=CARTESIAN_POINT('Ctrl Pts',(0.218823709911104,-1.54647724371604,
4.14577731547206));
#263663=CARTESIAN_POINT('Ctrl Pts',(0.361642554461439,-1.5128869756134,
4.1558377876486));
#263664=CARTESIAN_POINT('Ctrl Pts',(0.367149554280194,-1.51155996958776,
4.15622704356669));
#263665=CARTESIAN_POINT('Ctrl Pts',(0.396818803031542,-1.50423895367792,
4.15833164093067));
#263666=CARTESIAN_POINT('Ctrl Pts',(0.420840569521701,-1.49769592609991,
4.16006246247689));
#263667=CARTESIAN_POINT('Ctrl Pts',(0.453552730883087,-1.48793670384046,
4.16246145737352));
#263668=CARTESIAN_POINT('Ctrl Pts',(0.462387673820956,-1.4852149160423,
4.16311362580804));
#263669=CARTESIAN_POINT('Ctrl Pts',(0.476437860270363,-1.48074894878524,
4.164157793315));
#263670=CARTESIAN_POINT('Ctrl Pts',(0.481669127153877,-1.4790555549275,
4.16454812791854));
#263671=CARTESIAN_POINT('Ctrl Pts',(0.492409067032947,-1.47551594844627,
4.16535277266688));
#263672=CARTESIAN_POINT('Ctrl Pts',(0.497916587541557,-1.47366654083732,
4.16576718236396));
#263673=CARTESIAN_POINT('Ctrl Pts',(0.510675431126764,-1.46930247348155,
4.16673142601889));
#263674=CARTESIAN_POINT('Ctrl Pts',(0.517918706230046,-1.46676493152849,
4.1672820073791));
#263675=CARTESIAN_POINT('Ctrl Pts',(0.540976526368626,-1.45849497966674,
4.16904504567866));
#263676=CARTESIAN_POINT('Ctrl Pts',(0.55671650194667,-1.45255977604736,
4.17026418346186));
#263677=CARTESIAN_POINT('Ctrl Pts',(0.636160456066184,-1.421122282574,4.17649976708454));
#263678=CARTESIAN_POINT('Ctrl Pts',(0.698214194750551,-1.39168354780934,
4.18164658268046));
#263679=CARTESIAN_POINT('Ctrl Pts',(0.836049938356933,-1.31474973943011,
4.19371478994464));
#263680=CARTESIAN_POINT('Ctrl Pts',(0.91009460993814,-1.26462355798037,
4.20068731267486));
#263681=CARTESIAN_POINT('Ctrl Pts',(0.988398205587733,-1.20115885285792,
4.20845147774913));
#263682=CARTESIAN_POINT('Ctrl Pts',(0.997288339773477,-1.19378791188782,
4.20933894142703));
#263683=CARTESIAN_POINT('Ctrl Pts',(1.01323283366311,-1.18026566950767,
4.21094050999283));
#263684=CARTESIAN_POINT('Ctrl Pts',(1.02031531446666,-1.17414841088826,
4.21165554394833));
#263685=CARTESIAN_POINT('Ctrl Pts',(1.05592503856544,-1.14282615689047,
4.21526756329304));
#263686=CARTESIAN_POINT('Ctrl Pts',(1.08357830840925,-1.11664137220616,
4.21812849655396));
#263687=CARTESIAN_POINT('Ctrl Pts',(1.1148856267033,-1.0847369182519,4.22140821448593));
#263688=CARTESIAN_POINT('Ctrl Pts',(1.11949569800391,-1.07997848532729,
4.221892242288));
#263689=CARTESIAN_POINT('Ctrl Pts',(1.12692348029859,-1.07221299088711,
4.22267366633463));
#263690=CARTESIAN_POINT('Ctrl Pts',(1.12975982814149,-1.0692239990075,4.22297243145923));
#263691=CARTESIAN_POINT('Ctrl Pts',(1.13479286430116,-1.0638777122507,4.22350319460486));
#263692=CARTESIAN_POINT('Ctrl Pts',(1.13699413265376,-1.06152483461684,
4.22373553853354));
#263693=CARTESIAN_POINT('Ctrl Pts',(1.14174676413533,-1.05641312765597,
4.22423762175113));
#263694=CARTESIAN_POINT('Ctrl Pts',(1.14429544374883,-1.05365189124394,
4.2245071586076));
#263695=CARTESIAN_POINT('Ctrl Pts',(1.15141395257934,-1.04588341344925,
4.22526087925594));
#263696=CARTESIAN_POINT('Ctrl Pts',(1.15596116663405,-1.04085541284043,
4.22574339438784));
#263697=CARTESIAN_POINT('Ctrl Pts',(1.18319760407226,-1.01034055750956,
4.22864106613245));
#263698=CARTESIAN_POINT('Ctrl Pts',(1.20507811896355,-0.984140125181842,
4.23100091095797));
#263699=CARTESIAN_POINT('Ctrl Pts',(1.30251310311015,-0.85934033870235,
4.24177863056146));
#263700=CARTESIAN_POINT('Ctrl Pts',(1.36695060340608,-0.752633848788471,
4.24973944472308));
#263701=CARTESIAN_POINT('Ctrl Pts',(1.44516833388122,-0.579165914038873,
4.26243869235881));
#263702=CARTESIAN_POINT('Ctrl Pts',(1.46845638987722,-0.517280117187117,
4.26692044781474));
#263703=CARTESIAN_POINT('Ctrl Pts',(1.49108537513476,-0.443143382239921,
4.27233793344677));
#263704=CARTESIAN_POINT('Ctrl Pts',(1.49431050029174,-0.432143228029316,
4.2731428590699));
#263705=CARTESIAN_POINT('Ctrl Pts',(1.49938268743468,-0.414107118481615,
4.27446492570531));
#263706=CARTESIAN_POINT('Ctrl Pts',(1.50130253499648,-0.40709193571732,
4.27497970809834));
#263707=CARTESIAN_POINT('Ctrl Pts',(1.50465411644762,-0.394498922106461,
4.27590492595451));
#263708=CARTESIAN_POINT('Ctrl Pts',(1.50610421713621,-0.388926079324327,
4.27631476040796));
#263709=CARTESIAN_POINT('Ctrl Pts',(1.50911713722793,-0.377077632642883,
4.27718701079093));
#263710=CARTESIAN_POINT('Ctrl Pts',(1.51067182493599,-0.370800094291751,
4.27764967979514));
#263711=CARTESIAN_POINT('Ctrl Pts',(1.51473712958283,-0.353935126891896,
4.27889419984797));
#263712=CARTESIAN_POINT('Ctrl Pts',(1.5171758355512,-0.343330917087015,
4.27967833623452));
#263713=CARTESIAN_POINT('Ctrl Pts',(1.52882873833049,-0.290110292316033,
4.28362261958471));
#263714=CARTESIAN_POINT('Ctrl Pts',(1.53635860865336,-0.247149391869968,
4.28683563920812));
#263715=CARTESIAN_POINT('Ctrl Pts',(1.56500597751739,-0.0305271532176449,
4.30319814874146));
#263716=CARTESIAN_POINT('Ctrl Pts',(1.5585246537258,0.145462889455811,4.31719136789475));
#263717=CARTESIAN_POINT('Ctrl Pts',(1.52030008014965,0.32929352736384,4.33111142013338));
#263718=CARTESIAN_POINT('Ctrl Pts',(1.5175176579023,0.341887039580946,4.33206042734252));
#263719=CARTESIAN_POINT('Ctrl Pts',(1.51343593795752,0.359328634364998,
4.33336704067547));
#263720=CARTESIAN_POINT('Ctrl Pts',(1.5122694307825,0.364206776949679,4.33373163565615));
#263721=CARTESIAN_POINT('Ctrl Pts',(1.5103593067695,0.372027180441728,4.33431468798085));
#263722=CARTESIAN_POINT('Ctrl Pts',(1.50963065292883,0.374972999965682,
4.33453398355718));
#263723=CARTESIAN_POINT('Ctrl Pts',(1.50808561069267,0.381141830230326,
4.33499248910738));
#263724=CARTESIAN_POINT('Ctrl Pts',(1.50726750335325,0.384364381294637,
4.33523159311462));
#263725=CARTESIAN_POINT('Ctrl Pts',(1.50524435844471,0.392227817504962,
4.33581407538145));
#263726=CARTESIAN_POINT('Ctrl Pts',(1.50402816905935,0.396865856138813,
4.33615681765806));
#263727=CARTESIAN_POINT('Ctrl Pts',(1.49958146602152,0.413509671475075,
4.33738406569791));
#263728=CARTESIAN_POINT('Ctrl Pts',(1.49622837548985,0.425482662310641,
4.33826185065595));
#263729=CARTESIAN_POINT('Ctrl Pts',(1.4875503041076,0.455097660655022,4.34042344894152));
#263730=CARTESIAN_POINT('Ctrl Pts',(1.48205459103537,0.472688107251331,
4.34169886508878));
#263731=CARTESIAN_POINT('Ctrl Pts',(1.46376367029956,0.527774103569199,
4.34567828967784));
#263732=CARTESIAN_POINT('Ctrl Pts',(1.44986059937387,0.564843095112567,
4.34833476639215));
#263733=CARTESIAN_POINT('Ctrl Pts',(1.43457657355089,0.601307163285946,
4.35096339883546));
#263734=CARTESIAN_POINT('Origin',(0.,0.,-1.29405622560371));
#263735=CARTESIAN_POINT('',(1.43457674133487,0.601306762992916,5.18837549714138));
#263736=CARTESIAN_POINT('',(1.43231908414271,0.600352779935808,5.05019128547067));
#263737=CARTESIAN_POINT('',(1.43457668357355,0.601306900797845,-1.29405622560371));
#263738=CARTESIAN_POINT('',(-1.55549950191149,0.00135080560319381,4.79375124639878));
#263739=CARTESIAN_POINT('Ctrl Pts',(1.43457674133486,0.601306762992946,
5.18837549714138));
#263740=CARTESIAN_POINT('Ctrl Pts',(1.44511665628854,0.576161000831655,
5.18657941512783));
#263741=CARTESIAN_POINT('Ctrl Pts',(1.45499927553352,0.550728945127526,
5.18477898999173));
#263742=CARTESIAN_POINT('Ctrl Pts',(1.49012990958986,0.452757154467981,
5.17786919516953));
#263743=CARTESIAN_POINT('Ctrl Pts',(1.5106566959811,0.378668668901701,5.17269057112632));
#263744=CARTESIAN_POINT('Ctrl Pts',(1.52791039167112,0.291902219434232,
5.16651001909783));
#263745=CARTESIAN_POINT('Ctrl Pts',(1.53006217189651,0.280404721248481,
5.16568890524646));
#263746=CARTESIAN_POINT('Ctrl Pts',(1.53334524896578,0.261697977929183,
5.16434895645143));
#263747=CARTESIAN_POINT('Ctrl Pts',(1.53455587125645,0.25450296441266,5.16383263406341));
#263748=CARTESIAN_POINT('Ctrl Pts',(1.53662174083545,0.241674048030772,
5.16291020372617));
#263749=CARTESIAN_POINT('Ctrl Pts',(1.5374967388295,0.236043420595086,5.16250472794051));
#263750=CARTESIAN_POINT('Ctrl Pts',(1.53927664022648,0.224159750156223,
5.16164758571647));
#263751=CARTESIAN_POINT('Ctrl Pts',(1.54017442039981,0.217905762445593,
5.16119570223162));
#263752=CARTESIAN_POINT('Ctrl Pts',(1.54245410721025,0.201306981085136,
5.15999414384703));
#263753=CARTESIAN_POINT('Ctrl Pts',(1.54377002253141,0.190953609932005,
5.15924240728233));
#263754=CARTESIAN_POINT('Ctrl Pts',(1.54953539191411,0.141629240685879,
5.15564961722445));
#263755=CARTESIAN_POINT('Ctrl Pts',(1.55261353490029,0.102515718359522,
5.15276610768367));
#263756=CARTESIAN_POINT('Ctrl Pts',(1.56029845675663,-0.0860812013401728,
5.13868291784823));
#263757=CARTESIAN_POINT('Ctrl Pts',(1.54480671724319,-0.235582682449016,
5.12687535157839));
#263758=CARTESIAN_POINT('Ctrl Pts',(1.49869668795058,-0.41834109111477,
5.11250962193625));
#263759=CARTESIAN_POINT('Ctrl Pts',(1.48773700552715,-0.455785329332024,
5.10957691072483));
#263760=CARTESIAN_POINT('Ctrl Pts',(1.47327985518892,-0.499069806126764,
5.10622842352198));
#263761=CARTESIAN_POINT('Ctrl Pts',(1.47113933508363,-0.505344698249422,
5.10574404660611));
#263762=CARTESIAN_POINT('Ctrl Pts',(1.46761174412288,-0.515473365386924,
5.10496409831294));
#263763=CARTESIAN_POINT('Ctrl Pts',(1.46624948829557,-0.519335595762319,
5.10466714309885));
#263764=CARTESIAN_POINT('Ctrl Pts',(1.46380116425743,-0.526190589930062,
5.10414094368091));
#263765=CARTESIAN_POINT('Ctrl Pts',(1.46272114810832,-0.529185439132385,
5.10391135053028));
#263766=CARTESIAN_POINT('Ctrl Pts',(1.46036997794362,-0.535642961879161,
5.10341694812502));
#263767=CARTESIAN_POINT('Ctrl Pts',(1.45909570169352,-0.539104432513673,
5.10315232698491));
#263768=CARTESIAN_POINT('Ctrl Pts',(1.45550967446661,-0.54873973513554,
5.10241675061996));
#263769=CARTESIAN_POINT('Ctrl Pts',(1.45317093385964,-0.554903550633025,
5.10194736365208));
#263770=CARTESIAN_POINT('Ctrl Pts',(1.43930726854894,-0.590752798997594,
5.09922315618627));
#263771=CARTESIAN_POINT('Ctrl Pts',(1.42691113019264,-0.620096185616808,
5.09701650839229));
#263772=CARTESIAN_POINT('Ctrl Pts',(1.35281569164905,-0.781477274138088,
5.08489882734599));
#263773=CARTESIAN_POINT('Ctrl Pts',(1.27369802629424,-0.904720226578485,
5.0756496725934));
#263774=CARTESIAN_POINT('Ctrl Pts',(1.14650171308311,-1.05239207209561,
5.06250280738294));
#263775=CARTESIAN_POINT('Ctrl Pts',(1.1126866684412,-1.08808216994098,5.05913685044029));
#263776=CARTESIAN_POINT('Ctrl Pts',(1.06891311172136,-1.13010544455532,
5.05488953970839));
#263777=CARTESIAN_POINT('Ctrl Pts',(1.06049559540173,-1.13800818786546,
5.05407755197911));
#263778=CARTESIAN_POINT('Ctrl Pts',(1.04710705239501,-1.15030040933622,
5.05279296410192));
#263779=CARTESIAN_POINT('Ctrl Pts',(1.04219447285095,-1.15475317240732,
5.05232305467617));
#263780=CARTESIAN_POINT('Ctrl Pts',(1.03307474280039,-1.16291369924173,
5.05145325598756));
#263781=CARTESIAN_POINT('Ctrl Pts',(1.02887570206087,-1.16663039746671,
5.05105375039945));
#263782=CARTESIAN_POINT('Ctrl Pts',(1.01952412232708,-1.17481800766422,
5.05016612159405));
#263783=CARTESIAN_POINT('Ctrl Pts',(1.01436210958863,-1.17927787015013,
5.0496775516157));
#263784=CARTESIAN_POINT('Ctrl Pts',(0.999459053284507,-1.19198352777962,
5.04827087530776));
#263785=CARTESIAN_POINT('Ctrl Pts',(0.98964584809316,-1.20014341100722,
5.04734929257613));
#263786=CARTESIAN_POINT('Ctrl Pts',(0.911981033914877,-1.26312305061513,
5.04008998686995));
#263787=CARTESIAN_POINT('Ctrl Pts',(0.839740027161673,-1.31225790795481,
5.03352720670584));
#263788=CARTESIAN_POINT('Ctrl Pts',(0.691906041537649,-1.39558319102782,
5.0204826246957));
#263789=CARTESIAN_POINT('Ctrl Pts',(0.616930312737117,-1.43030867292629,
5.01403793598719));
#263790=CARTESIAN_POINT('Ctrl Pts',(0.521606335950648,-1.46556246225637,
5.00622639805155));
#263791=CARTESIAN_POINT('Ctrl Pts',(0.503535264990488,-1.47186914709442,
5.00476218649622));
#263792=CARTESIAN_POINT('Ctrl Pts',(0.452160624595348,-1.4887415827988,
5.00065379415605));
#263793=CARTESIAN_POINT('Ctrl Pts',(0.418608262441636,-1.49852204731149,
4.99803409329177));
#263794=CARTESIAN_POINT('Ctrl Pts',(0.378535284889602,-1.5087519520649,
4.9950009921966));
#263795=CARTESIAN_POINT('Ctrl Pts',(0.372308771431782,-1.51030049900207,
4.99453241871477));
#263796=CARTESIAN_POINT('Ctrl Pts',(0.362154982095782,-1.5127591571304,
4.99377289608467));
#263797=CARTESIAN_POINT('Ctrl Pts',(0.358233519220936,-1.5136925861087,
4.99348067570635));
#263798=CARTESIAN_POINT('Ctrl Pts',(0.351213561048297,-1.5153347441316,
4.99295960226092));
#263799=CARTESIAN_POINT('Ctrl Pts',(0.348116492459623,-1.51604922761923,
4.99273042707443));
#263800=CARTESIAN_POINT('Ctrl Pts',(0.341375553850311,-1.51758259370568,
4.99223316818022));
#263801=CARTESIAN_POINT('Ctrl Pts',(0.337730922926314,-1.51839784706743,
4.99196529301813));
#263802=CARTESIAN_POINT('Ctrl Pts',(0.32743705508155,-1.5206615449312,4.9912113749073));
#263803=CARTESIAN_POINT('Ctrl Pts',(0.320781088372202,-1.5220795173554,
4.99072702940935));
#263804=CARTESIAN_POINT('Ctrl Pts',(0.279115178601945,-1.53067047261114,
4.98771338608054));
#263805=CARTESIAN_POINT('Ctrl Pts',(0.243872642686833,-1.53667954383986,
4.98524501563371));
#263806=CARTESIAN_POINT('Ctrl Pts',(0.119716552090874,-1.55346901745102,
4.9767304014672));
#263807=CARTESIAN_POINT('Ctrl Pts',(0.0301045339338664,-1.55778509748695,
4.97090001568472));
#263808=CARTESIAN_POINT('Ctrl Pts',(-0.079524991373503,-1.55359652177789,
4.96366612663505));
#263809=CARTESIAN_POINT('Ctrl Pts',(-0.0996457580148266,-1.55243585318808,
4.9623347078501));
#263810=CARTESIAN_POINT('Ctrl Pts',(-0.197933206649732,-1.54484744562266,
4.95579463698577));
#263811=CARTESIAN_POINT('Ctrl Pts',(-0.275548843800916,-1.53290616649866,
4.95051007562073));
#263812=CARTESIAN_POINT('Ctrl Pts',(-0.363361780290477,-1.51250993099005,
4.94421220008269));
#263813=CARTESIAN_POINT('Ctrl Pts',(-0.374766523701754,-1.50972451598622,
4.9433881196476));
#263814=CARTESIAN_POINT('Ctrl Pts',(-0.393218630615451,-1.50499594038704,
4.94204428298487));
#263815=CARTESIAN_POINT('Ctrl Pts',(-0.400285896940939,-1.50313168733213,
4.94152706369445));
#263816=CARTESIAN_POINT('Ctrl Pts',(-0.412840520722027,-1.49972512209381,
4.94060363012479));
#263817=CARTESIAN_POINT('Ctrl Pts',(-0.418333073292665,-1.49820231464093,
4.94019805313648));
#263818=CARTESIAN_POINT('Ctrl Pts',(-0.429889428686015,-1.49492981760381,
4.93934131637627));
#263819=CARTESIAN_POINT('Ctrl Pts',(-0.435951185867858,-1.49317334620884,
4.93888994273688));
#263820=CARTESIAN_POINT('Ctrl Pts',(-0.451141461550569,-1.48867138692364,
4.93775376196994));
#263821=CARTESIAN_POINT('Ctrl Pts',(-0.460255632774021,-1.48587881792385,
4.93706743178289));
#263822=CARTESIAN_POINT('Ctrl Pts',(-0.501373085326017,-1.47286589230966,
4.93394969732927));
#263823=CARTESIAN_POINT('Ctrl Pts',(-0.533063498035386,-1.46169486921233,
4.93148745237136));
#263824=CARTESIAN_POINT('Ctrl Pts',(-0.618453142547712,-1.42844843843008,
4.92468325954966));
#263825=CARTESIAN_POINT('Ctrl Pts',(-0.671313888997831,-1.40438083582509,
4.92028129313621));
#263826=CARTESIAN_POINT('Ctrl Pts',(-0.812122273003252,-1.33050177653107,
4.90806142300212));
#263827=CARTESIAN_POINT('Ctrl Pts',(-0.896759722897099,-1.27498994923714,
4.90014119504225));
#263828=CARTESIAN_POINT('Ctrl Pts',(-1.00359603224231,-1.18898430943612,
4.88971043858193));
#263829=CARTESIAN_POINT('Ctrl Pts',(-1.03097578303879,-1.16532319025755,
4.88699559969048));
#263830=CARTESIAN_POINT('Ctrl Pts',(-1.06225966717474,-1.1363215354992,
4.88386662329599));
#263831=CARTESIAN_POINT('Ctrl Pts',(-1.0669838748675,-1.13188676431571,
4.88339336162019));
#263832=CARTESIAN_POINT('Ctrl Pts',(-1.07461586352522,-1.12463211735273,
4.88262777380986));
#263833=CARTESIAN_POINT('Ctrl Pts',(-1.07754052069459,-1.12183023706423,
4.8823341434636));
#263834=CARTESIAN_POINT('Ctrl Pts',(-1.08274178058477,-1.11680821888323,
4.8818115538238));
#263835=CARTESIAN_POINT('Ctrl Pts',(-1.08502254388912,-1.11459250002306,
4.88158226440692));
#263836=CARTESIAN_POINT('Ctrl Pts',(-1.08944696822507,-1.11026780362926,
4.88113721537358));
#263837=CARTESIAN_POINT('Ctrl Pts',(-1.09159129617159,-1.10815961616078,
4.88092139794605));
#263838=CARTESIAN_POINT('Ctrl Pts',(-1.09777911380515,-1.10204069911733,
4.88029821893327));
#263839=CARTESIAN_POINT('Ctrl Pts',(-1.10180676680968,-1.09801390543519,
4.87989209220409));
#263840=CARTESIAN_POINT('Ctrl Pts',(-1.12013114783766,-1.07949107710251,
4.87804153174208));
#263841=CARTESIAN_POINT('Ctrl Pts',(-1.13416536724222,-1.06473649301567,
4.87661628095115));
#263842=CARTESIAN_POINT('Ctrl Pts',(-1.17284360760615,-1.02244002497955,
4.87265053641538));
#263843=CARTESIAN_POINT('Ctrl Pts',(-1.19680284400498,-0.994288242983664,
4.87014872059939));
#263844=CARTESIAN_POINT('Ctrl Pts',(-1.25768183783196,-0.917363091393411,
4.8635849916298));
#263845=CARTESIAN_POINT('Ctrl Pts',(-1.29276707498899,-0.867221158893708,
4.85957802836032));
#263846=CARTESIAN_POINT('Ctrl Pts',(-1.38099410670971,-0.723830107117304,
4.84849212400466));
#263847=CARTESIAN_POINT('Ctrl Pts',(-1.42757813784364,-0.62696921113851,
4.84138372230398));
#263848=CARTESIAN_POINT('Ctrl Pts',(-1.46781896986126,-0.515001680400421,
4.83307252974104));
#263849=CARTESIAN_POINT('Ctrl Pts',(-1.47168024637885,-0.503861586239718,
4.83224496394543));
#263850=CARTESIAN_POINT('Ctrl Pts',(-1.47773421905505,-0.485731891844201,
4.83089656065398));
#263851=CARTESIAN_POINT('Ctrl Pts',(-1.48000488606757,-0.478768656893854,
4.83037828887711));
#263852=CARTESIAN_POINT('Ctrl Pts',(-1.48395557725663,-0.466356733587377,
4.82945367603051));
#263853=CARTESIAN_POINT('Ctrl Pts',(-1.48565499038759,-0.460914315448052,
4.82904797827144));
#263854=CARTESIAN_POINT('Ctrl Pts',(-1.48917000411102,-0.44943595450738,
4.82819170750025));
#263855=CARTESIAN_POINT('Ctrl Pts',(-1.49097891076522,-0.443398087322087,
4.82774092431618));
#263856=CARTESIAN_POINT('Ctrl Pts',(-1.49457898433125,-0.431110400010262,
4.82682271794426));
#263857=CARTESIAN_POINT('Ctrl Pts',(-1.49636776269077,-0.424860016707826,
4.82635522700537));
#263858=CARTESIAN_POINT('Ctrl Pts',(-1.50070702967631,-0.409330271867054,
4.82519255412897));
#263859=CARTESIAN_POINT('Ctrl Pts',(-1.50321065606974,-0.400038218326202,
4.82449587349808));
#263860=CARTESIAN_POINT('Ctrl Pts',(-1.5099754364029,-0.373970587772576,
4.82253835731351));
#263861=CARTESIAN_POINT('Ctrl Pts',(-1.51404293375601,-0.357146705601624,
4.82127143326522));
#263862=CARTESIAN_POINT('Ctrl Pts',(-1.54297058110204,-0.228106164304975,
4.81152441339957));
#263863=CARTESIAN_POINT('Ctrl Pts',(-1.55559911830794,-0.113535921865477,
4.80266052462882));
#263864=CARTESIAN_POINT('Ctrl Pts',(-1.5554994142228,0.00134994538273571,
4.79375115972409));
#263865=CARTESIAN_POINT('Ctrl Pts',(-1.55549941348635,0.00135079370216905,
4.79375109393717));
#263866=CARTESIAN_POINT('Ctrl Pts',(-1.55543982818356,0.069965937072524,
4.78843000999));
#263867=CARTESIAN_POINT('Ctrl Pts',(-1.55084024178991,0.138509195077084,
4.78311715906412));
#263868=CARTESIAN_POINT('Ctrl Pts',(-1.53903776772294,0.226613171187347,
4.77643903602023));
#263869=CARTESIAN_POINT('Ctrl Pts',(-1.53595525860854,0.246642097481528,
4.77493141603258));
#263870=CARTESIAN_POINT('Ctrl Pts',(-1.5315242001828,0.272112308381628,
4.77303229281784));
#263871=CARTESIAN_POINT('Ctrl Pts',(-1.53053662561479,0.27761326380552,
4.77262321010403));
#263872=CARTESIAN_POINT('Ctrl Pts',(-1.52884369292503,0.286759474109722,
4.77194497886987));
#263873=CARTESIAN_POINT('Ctrl Pts',(-1.528154904379,0.290407683044102,4.77167496151767));
#263874=CARTESIAN_POINT('Ctrl Pts',(-1.5268831462123,0.297013798197322,
4.77118699127725));
#263875=CARTESIAN_POINT('Ctrl Pts',(-1.52630462953548,0.299972526718701,
4.77096879467688));
#263876=CARTESIAN_POINT('Ctrl Pts',(-1.52509885048197,0.306045483211395,
4.7705216873708));
#263877=CARTESIAN_POINT('Ctrl Pts',(-1.524470656883,0.309159438179908,4.77029284219876));
#263878=CARTESIAN_POINT('Ctrl Pts',(-1.52302894460566,0.316194753018226,
4.76977673267639));
#263879=CARTESIAN_POINT('Ctrl Pts',(-1.52220982034231,0.320114904008777,
4.76948979061479));
#263880=CARTESIAN_POINT('Ctrl Pts',(-1.51968757989683,0.331957179008913,
4.76862478833012));
#263881=CARTESIAN_POINT('Ctrl Pts',(-1.51793765671912,0.339869367601111,
4.76804931055348));
#263882=CARTESIAN_POINT('Ctrl Pts',(-1.49879387502669,0.423328469941545,
4.76200154058142));
#263883=CARTESIAN_POINT('Ctrl Pts',(-1.47583442862184,0.49750037380237,
4.75681921959069));
#263884=CARTESIAN_POINT('Ctrl Pts',(-1.4254014638762,0.625644100516097,
4.74771549031625));
#263885=CARTESIAN_POINT('Ctrl Pts',(-1.40013891305393,0.680302088247146,
4.74377981351629));
#263886=CARTESIAN_POINT('Ctrl Pts',(-1.33827749464894,0.796015985039271,
4.73509304183178));
#263887=CARTESIAN_POINT('Ctrl Pts',(-1.30053147529157,0.856296762508328,
4.73033181777074));
#263888=CARTESIAN_POINT('Ctrl Pts',(-1.24612144789291,0.931250502293052,
4.72392908008005));
#263889=CARTESIAN_POINT('Ctrl Pts',(-1.23307965899597,0.948451704524512,
4.72242432616688));
#263890=CARTESIAN_POINT('Ctrl Pts',(-1.21564741200728,0.970476140085881,
4.72044790699084));
#263891=CARTESIAN_POINT('Ctrl Pts',(-1.21157819230199,0.975551562160408,
4.71998892662598));
#263892=CARTESIAN_POINT('Ctrl Pts',(-1.20350208479432,0.9854961922074,4.71908253682474));
#263893=CARTESIAN_POINT('Ctrl Pts',(-1.19949718490783,0.990366858406006,
4.71863521246902));
#263894=CARTESIAN_POINT('Ctrl Pts',(-1.19181533593243,0.999594395807111,
4.71778117481726));
#263895=CARTESIAN_POINT('Ctrl Pts',(-1.18814382423592,1.00395567752366,
4.71737468714752));
#263896=CARTESIAN_POINT('Ctrl Pts',(-1.17970419424875,1.01386973112551,
4.71644408580829));
#263897=CARTESIAN_POINT('Ctrl Pts',(-1.17492072492786,1.01940919377976,
4.71591934622949));
#263898=CARTESIAN_POINT('Ctrl Pts',(-1.1623411767919,1.03377069205574,4.71454626729671));
#263899=CARTESIAN_POINT('Ctrl Pts',(-1.15448384974252,1.04253819187838,
4.7136953927718));
#263900=CARTESIAN_POINT('Ctrl Pts',(-1.09262295439683,1.11000794484178,
4.70704699132472));
#263901=CARTESIAN_POINT('Ctrl Pts',(-1.03428526917837,1.1645568158285,4.70106257585066));
#263902=CARTESIAN_POINT('Ctrl Pts',(-0.899099408804229,1.27276381111295,
4.68779097043489));
#263903=CARTESIAN_POINT('Ctrl Pts',(-0.82105951223368,1.32444996704154,
4.68047954029265));
#263904=CARTESIAN_POINT('Ctrl Pts',(-0.70923240487482,1.38481150561327,
4.67073174931814));
#263905=CARTESIAN_POINT('Ctrl Pts',(-0.679095037032262,1.39983705104924,
4.66817261701057));
#263906=CARTESIAN_POINT('Ctrl Pts',(-0.631100562305024,1.42185034743603,
4.66422565181814));
#263907=CARTESIAN_POINT('Ctrl Pts',(-0.613562611104443,1.42950597844899,
4.66280947280792));
#263908=CARTESIAN_POINT('Ctrl Pts',(-0.590840131533242,1.43892947658228,
4.66101188555856));
#263909=CARTESIAN_POINT('Ctrl Pts',(-0.58578234729258,1.44099588604967,
4.66061410569835));
#263910=CARTESIAN_POINT('Ctrl Pts',(-0.577928137760229,1.44415661664662,
4.66000013438606));
#263911=CARTESIAN_POINT('Ctrl Pts',(-0.575139324048191,1.44526953339813,
4.65978285730039));
#263912=CARTESIAN_POINT('Ctrl Pts',(-0.569388302008386,1.44754528013879,
4.65933631567059));
#263913=CARTESIAN_POINT('Ctrl Pts',(-0.566425786505574,1.44870708054433,
4.65910712326779));
#263914=CARTESIAN_POINT('Ctrl Pts',(-0.559657483629574,1.45133744897327,
4.6585853789857));
#263915=CARTESIAN_POINT('Ctrl Pts',(-0.555849473156135,1.45280014248085,
4.65829317984575));
#263916=CARTESIAN_POINT('Ctrl Pts',(-0.5458878753069,1.45658158698531,4.65753220005038));
#263917=CARTESIAN_POINT('Ctrl Pts',(-0.539725175582285,1.45887635899957,
4.65706480159645));
#263918=CARTESIAN_POINT('Ctrl Pts',(-0.497711319978021,1.47421816701328,
4.65390004667076));
#263919=CARTESIAN_POINT('Ctrl Pts',(-0.461401588683426,1.48598281862127,
4.65127205055478));
#263920=CARTESIAN_POINT('Ctrl Pts',(-0.41599855517151,1.49886861389726,
4.64807395067595));
#263921=CARTESIAN_POINT('Ctrl Pts',(-0.407283296304176,1.50126021784478,
4.64746401951149));
#263922=CARTESIAN_POINT('Ctrl Pts',(-0.275813348439974,1.53610849487521,
4.63831584352315));
#263923=CARTESIAN_POINT('Ctrl Pts',(-0.149556377549204,1.55349224672585,
4.63017890659324));
#263924=CARTESIAN_POINT('Ctrl Pts',(0.0116176225624342,1.55583269551161,
4.61932043467574));
#263925=CARTESIAN_POINT('Ctrl Pts',(0.0458256458859801,1.55520098190422,
4.61699199032896));
#263926=CARTESIAN_POINT('Ctrl Pts',(0.102804957954734,1.55226724579149,
4.61305335520266));
#263927=CARTESIAN_POINT('Ctrl Pts',(0.125596922893809,1.55058949456994,
4.61146181967363));
#263928=CARTESIAN_POINT('Ctrl Pts',(0.157052910614164,1.54757591020215,
4.60923923700843));
#263929=CARTESIAN_POINT('Ctrl Pts',(0.165755788399802,1.54666797586798,
4.60862155866719));
#263930=CARTESIAN_POINT('Ctrl Pts',(0.180365545238223,1.54501907913603,
4.60757979348178));
#263931=CARTESIAN_POINT('Ctrl Pts',(0.186276747632084,1.54431753739259,
4.60715695116993));
#263932=CARTESIAN_POINT('Ctrl Pts',(0.197933874911923,1.54286616664685,
4.60632037906376));
#263933=CARTESIAN_POINT('Ctrl Pts',(0.203679928295563,1.542118125228,4.60590671204742));
#263934=CARTESIAN_POINT('Ctrl Pts',(0.216320005406149,1.54040071793235,
4.604993800779));
#263935=CARTESIAN_POINT('Ctrl Pts',(0.223211937784856,1.53941714439342,
4.60449411602925));
#263936=CARTESIAN_POINT('Ctrl Pts',(0.247377095126415,1.53580275653071,
4.6027351548794));
#263937=CARTESIAN_POINT('Ctrl Pts',(0.26461179835137,1.53292729248878,4.60146820779354));
#263938=CARTESIAN_POINT('Ctrl Pts',(0.41299061380514,1.50559479240169,4.59044843309601));
#263939=CARTESIAN_POINT('Ctrl Pts',(0.540506912813754,1.46465474421342,
4.58014558056329));
#263940=CARTESIAN_POINT('Ctrl Pts',(0.728697270556073,1.37627768166781,
4.56403096489449));
#263941=CARTESIAN_POINT('Ctrl Pts',(0.793830706540837,1.33976688924317,
4.55827814329));
#263942=CARTESIAN_POINT('Ctrl Pts',(0.866930080054803,1.29158071974666,
4.55178915562403));
#263943=CARTESIAN_POINT('Ctrl Pts',(0.877671321333322,1.28430588283984,
4.55083492530268));
#263944=CARTESIAN_POINT('Ctrl Pts',(0.892292918818326,1.27413382788035,
4.5495362836906));
#263945=CARTESIAN_POINT('Ctrl Pts',(0.896252234757086,1.27135187800589,
4.5491846626269));
#263946=CARTESIAN_POINT('Ctrl Pts',(0.902893000656428,1.2666394100847,4.54859504681989));
#263947=CARTESIAN_POINT('Ctrl Pts',(0.905581370000086,1.26471876274122,
4.54835639297709));
#263948=CARTESIAN_POINT('Ctrl Pts',(0.910678535725685,1.26105261712095,
4.54790400937536));
#263949=CARTESIAN_POINT('Ctrl Pts',(0.913088468273824,1.25930875804642,
4.54769016681631));
#263950=CARTESIAN_POINT('Ctrl Pts',(0.919403244627676,1.25471164502745,
4.54712990411588));
#263951=CARTESIAN_POINT('Ctrl Pts',(0.923299852821414,1.25184704411527,
4.54678425957444));
#263952=CARTESIAN_POINT('Ctrl Pts',(0.936839917069813,1.24179542038698,
4.54558320678598));
#263953=CARTESIAN_POINT('Ctrl Pts',(0.946413652218577,1.23451452753686,
4.54473398944022));
#263954=CARTESIAN_POINT('Ctrl Pts',(1.03376837031311,1.16646708721101,4.5369753672142));
#263955=CARTESIAN_POINT('Ctrl Pts',(1.10569721084739,1.09852736346917,4.53050425029717));
#263956=CARTESIAN_POINT('Ctrl Pts',(1.24760810260063,0.936319330900016,
4.51632054322286));
#263957=CARTESIAN_POINT('Ctrl Pts',(1.3143521250063,0.840055254219469,4.50862303891695));
#263958=CARTESIAN_POINT('Ctrl Pts',(1.37595330447654,0.725608150931165,
4.49954531719119));
#263959=CARTESIAN_POINT('Ctrl Pts',(1.38206446684497,0.713899485485251,
4.49861789230063));
#263960=CARTESIAN_POINT('Ctrl Pts',(1.39114678072451,0.695944464919384,
4.49719692833209));
#263961=CARTESIAN_POINT('Ctrl Pts',(1.39422670555933,0.689753546190524,
4.49670719812811));
#263962=CARTESIAN_POINT('Ctrl Pts',(1.39975453296839,0.678453821338464,
4.49581363122083));
#263963=CARTESIAN_POINT('Ctrl Pts',(1.40221601379396,0.673351757521678,
4.49541027494994));
#263964=CARTESIAN_POINT('Ctrl Pts',(1.40747289066054,0.662301671924632,
4.49453685345166));
#263965=CARTESIAN_POINT('Ctrl Pts',(1.41025855922475,0.656349172514253,
4.49406646140498));
#263966=CARTESIAN_POINT('Ctrl Pts',(1.41772736123915,0.640122541054997,
4.49278434072176));
#263967=CARTESIAN_POINT('Ctrl Pts',(1.42233640257936,0.629814959941075,
4.49197009360227));
#263968=CARTESIAN_POINT('Ctrl Pts',(1.42945258601954,0.613423861039553,
4.49067531280411));
#263969=CARTESIAN_POINT('Ctrl Pts',(1.43203395656596,0.607373248773018,
4.49019736530848));
#263970=CARTESIAN_POINT('Ctrl Pts',(1.43457668488586,0.601306897666987,
4.48971815675999));
#263971=CARTESIAN_POINT('',(-1.55745558960329,-0.000855737989990104,4.65594377439629));
#263972=CARTESIAN_POINT('Ctrl Pts',(1.43457657355089,0.601307163285945,
4.35096339883546));
#263973=CARTESIAN_POINT('Ctrl Pts',(1.3925736165063,0.70151627748767,4.35818730285665));
#263974=CARTESIAN_POINT('Ctrl Pts',(1.34014205752647,0.797155671392286,
4.3652215223073));
#263975=CARTESIAN_POINT('Ctrl Pts',(1.24926110570256,0.928160613025819,
4.37596550768122));
#263976=CARTESIAN_POINT('Ctrl Pts',(1.21844401629644,0.968260671976808,
4.37942473078782));
#263977=CARTESIAN_POINT('Ctrl Pts',(1.17813738289257,1.01573138667639,4.38378252913333));
#263978=CARTESIAN_POINT('Ctrl Pts',(1.17044168169656,1.02458977121553,4.38460761692097));
#263979=CARTESIAN_POINT('Ctrl Pts',(1.15817971255643,1.03838587060438,4.38591200630471));
#263980=CARTESIAN_POINT('Ctrl Pts',(1.15368027067242,1.04338262077613,4.38638852569846));
#263981=CARTESIAN_POINT('Ctrl Pts',(1.14532097352347,1.05254566287716,4.38727004947023));
#263982=CARTESIAN_POINT('Ctrl Pts',(1.14147040807607,1.05672030866841,4.38767465694277));
#263983=CARTESIAN_POINT('Ctrl Pts',(1.13289095749044,1.06592023322632,4.38857303209543));
#263984=CARTESIAN_POINT('Ctrl Pts',(1.12815134461678,1.07093529494876,4.38906725390287));
#263985=CARTESIAN_POINT('Ctrl Pts',(1.11446520717654,1.08522514368831,4.39048859677501));
#263986=CARTESIAN_POINT('Ctrl Pts',(1.10543677678242,1.09442031435196,4.39141925307576));
#263987=CARTESIAN_POINT('Ctrl Pts',(1.03403721774355,1.16535358639662,4.39872727890072));
#263988=CARTESIAN_POINT('Ctrl Pts',(0.966668379230519,1.22181381575873,
4.40533220998903));
#263989=CARTESIAN_POINT('Ctrl Pts',(0.816790833778861,1.3272359643014,4.41942070862936));
#263990=CARTESIAN_POINT('Ctrl Pts',(0.73377697850713,1.37487225366508,4.42690201459907));
#263991=CARTESIAN_POINT('Ctrl Pts',(0.610826736534131,1.43109959018635,
4.43721133966659));
#263992=CARTESIAN_POINT('Ctrl Pts',(0.574112032521799,1.446219684007,4.44019747186926));
#263993=CARTESIAN_POINT('Ctrl Pts',(0.530558407192917,1.46223563137892,
4.44360301920776));
#263994=CARTESIAN_POINT('Ctrl Pts',(0.524246272883247,1.464510537625,4.44409327460879));
#263995=CARTESIAN_POINT('Ctrl Pts',(0.514010261963211,1.46812495650136,
4.44488274036146));
#263996=CARTESIAN_POINT('Ctrl Pts',(0.510095493087323,1.46948971630194,
4.44518336488401));
#263997=CARTESIAN_POINT('Ctrl Pts',(0.503126525789564,1.47188802039723,
4.44571615038264));
#263998=CARTESIAN_POINT('Ctrl Pts',(0.500074529233449,1.47292773464216,
4.44594866791129));
#263999=CARTESIAN_POINT('Ctrl Pts',(0.493475316980536,1.47515299169103,
4.44644967198994));
#264000=CARTESIAN_POINT('Ctrl Pts',(0.489927055354002,1.47633523245712,
4.44671796406293));
#264001=CARTESIAN_POINT('Ctrl Pts',(0.480012605910325,1.47959893482561,
4.44746467807316));
#264002=CARTESIAN_POINT('Ctrl Pts',(0.473637084705325,1.48165212721813,
4.4479414808778));
#264003=CARTESIAN_POINT('Ctrl Pts',(0.436081603369163,1.49347942444672,
4.45073143993949));
#264004=CARTESIAN_POINT('Ctrl Pts',(0.404610380642764,1.50231115028648,
4.45299395824059));
#264005=CARTESIAN_POINT('Ctrl Pts',(0.221670035916833,1.54748233417003,
4.46584043499046));
#264006=CARTESIAN_POINT('Ctrl Pts',(0.0657021567112895,1.56190000766365,
4.47568738531465));
#264007=CARTESIAN_POINT('Ctrl Pts',(-0.129110054987841,1.55063202977053,
4.48894925454823));
#264008=CARTESIAN_POINT('Ctrl Pts',(-0.168296258386443,1.54686942687954,
4.49166008962598));
#264009=CARTESIAN_POINT('Ctrl Pts',(-0.218173429158706,1.5401626809573,
4.49518658248991));
#264010=CARTESIAN_POINT('Ctrl Pts',(-0.229035775078956,1.53858484712221,
4.49595920066771));
#264011=CARTESIAN_POINT('Ctrl Pts',(-0.246290837520988,1.53589165303461,
4.49719428222171));
#264012=CARTESIAN_POINT('Ctrl Pts',(-0.25269499175137,1.53485099776413,
4.49765438489526));
#264013=CARTESIAN_POINT('Ctrl Pts',(-0.264199550809712,1.53290758855465,
4.4984840796035));
#264014=CARTESIAN_POINT('Ctrl Pts',(-0.269302342276915,1.53201936180647,
4.49885320641426));
#264015=CARTESIAN_POINT('Ctrl Pts',(-0.281256462273991,1.52987697731346,
4.4997206244924));
#264016=CARTESIAN_POINT('Ctrl Pts',(-0.288103943261745,1.5286022629328,
4.50021956109151));
#264017=CARTESIAN_POINT('Ctrl Pts',(-0.307898801275203,1.52477955896852,
4.50166802673732));
#264018=CARTESIAN_POINT('Ctrl Pts',(-0.320822325406211,1.52211280490506,
4.50262130475922));
#264019=CARTESIAN_POINT('Ctrl Pts',(-0.438144241765479,1.49634306930411,
4.51134710542526));
#264020=CARTESIAN_POINT('Ctrl Pts',(-0.539912647461299,1.46270239625917,
4.51946572721778));
#264021=CARTESIAN_POINT('Ctrl Pts',(-0.664985955054351,1.40651623139191,
4.53007154407853));
#264022=CARTESIAN_POINT('Ctrl Pts',(-0.692196018374761,1.39332654980192,
4.53241749329191));
#264023=CARTESIAN_POINT('Ctrl Pts',(-0.793746432921847,1.34039216664292,
4.54129509196237));
#264024=CARTESIAN_POINT('Ctrl Pts',(-0.865208618602949,1.29541590314831,
4.54780421116186));
#264025=CARTESIAN_POINT('Ctrl Pts',(-0.93905595959341,1.24008774000993,
4.55458479661798));
#264026=CARTESIAN_POINT('Ctrl Pts',(-0.94539408590019,1.23526261488423,
4.55516715780997));
#264027=CARTESIAN_POINT('Ctrl Pts',(-0.954906675474257,1.22790470998422,
4.55604146210108));
#264028=CARTESIAN_POINT('Ctrl Pts',(-0.958108617332074,1.22540793782187,
4.55633579934273));
#264029=CARTESIAN_POINT('Ctrl Pts',(-0.963688500381046,1.22102168214147,
4.55684875533966));
#264030=CARTESIAN_POINT('Ctrl Pts',(-0.966070711390577,1.21913775071165,
4.55706775694634));
#264031=CARTESIAN_POINT('Ctrl Pts',(-0.971307282633841,1.21497150923385,
4.55754917265716));
#264032=CARTESIAN_POINT('Ctrl Pts',(-0.974159120302818,1.21268611545753,
4.557811362684));
#264033=CARTESIAN_POINT('Ctrl Pts',(-0.981861403890726,1.20646898756828,
4.55851960214041));
#264034=CARTESIAN_POINT('Ctrl Pts',(-0.986696344337618,1.20251800901501,
4.55896430603432));
#264035=CARTESIAN_POINT('Ctrl Pts',(-0.997539627959024,1.19354774915675,
4.55996226191552));
#264036=CARTESIAN_POINT('Ctrl Pts',(-1.0035341827339,1.18851196432758,4.56051440354957));
#264037=CARTESIAN_POINT('Ctrl Pts',(-1.02202353918242,1.17274016877445,
4.56221970549458));
#264038=CARTESIAN_POINT('Ctrl Pts',(-1.03438643712738,1.16185040692115,
4.56336325704867));
#264039=CARTESIAN_POINT('Ctrl Pts',(-1.0828982469832,1.11773089354859,4.56787499274436));
#264040=CARTESIAN_POINT('Ctrl Pts',(-1.11764068087646,1.08299173656077,
4.57116196803684));
#264041=CARTESIAN_POINT('Ctrl Pts',(-1.16510332410368,1.03081215639836,
4.57583795785081));
#264042=CARTESIAN_POINT('Ctrl Pts',(-1.17919363371615,1.01466342053513,
4.57725191187616));
#264043=CARTESIAN_POINT('Ctrl Pts',(-1.27072220942585,0.905281006040948,
4.58664838314353));
#264044=CARTESIAN_POINT('Ctrl Pts',(-1.33735941336891,0.80357571374348,
4.59457211990098));
#264045=CARTESIAN_POINT('Ctrl Pts',(-1.39364965226534,0.690900651535222,
4.60331021588151));
#264046=CARTESIAN_POINT('Ctrl Pts',(-1.39576455578136,0.686618065247832,
4.60364221142822));
#264047=CARTESIAN_POINT('Ctrl Pts',(-1.40460218122327,0.668512697610301,
4.60504536521014));
#264048=CARTESIAN_POINT('Ctrl Pts',(-1.41113934638228,0.654600817253124,
4.60612252326215));
#264049=CARTESIAN_POINT('Ctrl Pts',(-1.42051747353244,0.633849468875813,
4.60772890202038));
#264050=CARTESIAN_POINT('Ctrl Pts',(-1.4235176325813,0.627082600714812,
4.60825267559974));
#264051=CARTESIAN_POINT('Ctrl Pts',(-1.42877137131088,0.615000767014447,
4.60918787325602));
#264052=CARTESIAN_POINT('Ctrl Pts',(-1.43104389260085,0.609694145217382,
4.60959864437981));
#264053=CARTESIAN_POINT('Ctrl Pts',(-1.4357707443131,0.598484327717549,
4.61046645334659));
#264054=CARTESIAN_POINT('Ctrl Pts',(-1.43821831982671,0.592578419292713,
4.61092371065716));
#264055=CARTESIAN_POINT('Ctrl Pts',(-1.44460612035277,0.576892179088964,
4.61213843158502));
#264056=CARTESIAN_POINT('Ctrl Pts',(-1.44848336388064,0.56708673379532,
4.61289799344693));
#264057=CARTESIAN_POINT('Ctrl Pts',(-1.46640752382706,0.520373617331626,
4.61651835272937));
#264058=CARTESIAN_POINT('Ctrl Pts',(-1.47914407698259,0.482982407722027,
4.6194221097683));
#264059=CARTESIAN_POINT('Ctrl Pts',(-1.53366633122595,0.300432004587034,
4.63364103423943));
#264060=CARTESIAN_POINT('Ctrl Pts',(-1.55557443644557,0.150202672118163,
4.64557540615709));
#264061=CARTESIAN_POINT('Ctrl Pts',(-1.55549980996415,-0.000768896282191608,
4.65706502508871));
#264062=CARTESIAN_POINT('Ctrl Pts',(-1.55745558960329,-0.000855737989990104,
4.65594377439629));
#264063=CARTESIAN_POINT('Ctrl Pts',(-1.55778526239128,-0.0506452214687281,
4.6595225162642));
#264064=CARTESIAN_POINT('Ctrl Pts',(-1.53303562869902,-0.615384490639257,
4.70013840098925));
#264065=CARTESIAN_POINT('Ctrl Pts',(-0.844180592856045,-1.63308701924324,
4.77779142857144));
#264066=CARTESIAN_POINT('Ctrl Pts',(0.913832949672081,-1.59515623870176,
4.88890285714287));
#264067=CARTESIAN_POINT('Ctrl Pts',(1.66723696927671,-0.371518783166273,
4.97970280944262));
#264068=CARTESIAN_POINT('Ctrl Pts',(1.52348731929008,0.384421868064892,
5.03346561888522));
#264069=CARTESIAN_POINT('Ctrl Pts',(1.43231908414271,0.600352779935808,
5.05019128547067));
#264070=CARTESIAN_POINT('Origin',(0.,0.,-1.29405622560371));
#264071=CARTESIAN_POINT('',(1.4345766835797,0.601306900783165,5.88690895590303));
#264072=CARTESIAN_POINT('',(1.43457651448711,0.601307304198121,5.74991065382822));
#264073=CARTESIAN_POINT('',(1.43457668357355,0.601306900797845,-1.29405622560371));
#264074=CARTESIAN_POINT('Ctrl Pts',(1.4345766835797,0.601306900783166,5.88690895590303));
#264075=CARTESIAN_POINT('Ctrl Pts',(1.43760164985763,0.594090043492366,
5.88632812774606));
#264076=CARTESIAN_POINT('Ctrl Pts',(1.440572208625,0.586850238760621,5.8857498616395));
#264077=CARTESIAN_POINT('Ctrl Pts',(1.4466166851779,0.571796220422545,5.8845569986114));
#264078=CARTESIAN_POINT('Ctrl Pts',(1.44968222818281,0.563978897874419,
5.8839428497635));
#264079=CARTESIAN_POINT('Ctrl Pts',(1.45413701090922,0.552342566307581,
5.88303688502469));
#264080=CARTESIAN_POINT('Ctrl Pts',(1.45557476325637,0.548542493012787,
5.88274231652757));
#264081=CARTESIAN_POINT('Ctrl Pts',(1.45811155518032,0.541757381345078,
5.88221871311359));
#264082=CARTESIAN_POINT('Ctrl Pts',(1.45921634087792,0.538774571396475,
5.88198934275535));
#264083=CARTESIAN_POINT('Ctrl Pts',(1.46159030083687,0.532304250568302,
5.88149355544579));
#264084=CARTESIAN_POINT('Ctrl Pts',(1.46285614499002,0.528815584602741,
5.88122733669668));
#264085=CARTESIAN_POINT('Ctrl Pts',(1.46631063343231,0.519187688202058,
5.88049557425245));
#264086=CARTESIAN_POINT('Ctrl Pts',(1.46847323072993,0.513039086155522,
5.88003153747311));
#264087=CARTESIAN_POINT('Ctrl Pts',(1.47946873082851,0.4811379472619,5.87764001132807));
#264088=CARTESIAN_POINT('Ctrl Pts',(1.48766374394749,0.455168400565725,
5.87574715491127));
#264089=CARTESIAN_POINT('Ctrl Pts',(1.50015101596917,0.411646602599681,
5.87264297777104));
#264090=CARTESIAN_POINT('Ctrl Pts',(1.50482651389881,0.394212137364547,
5.87141730358523));
#264091=CARTESIAN_POINT('Ctrl Pts',(1.53154543901685,0.287166257390051,
5.86397828661293));
#264092=CARTESIAN_POINT('Ctrl Pts',(1.5458827972227,0.195817085607539,5.85798850949133));
#264093=CARTESIAN_POINT('Ctrl Pts',(1.5573077374083,0.0248757706043105,
5.84665639342991));
#264094=CARTESIAN_POINT('Ctrl Pts',(1.55656029097849,-0.0542562838534247,
5.84136217036904));
#264095=CARTESIAN_POINT('Ctrl Pts',(1.54826686664179,-0.15090961124136,
5.83462749312036));
#264096=CARTESIAN_POINT('Ctrl Pts',(1.54641772477851,-0.168808100256128,
5.83336937149769));
#264097=CARTESIAN_POINT('Ctrl Pts',(1.54331944000417,-0.194439195446802,
5.83155011038271));
#264098=CARTESIAN_POINT('Ctrl Pts',(1.54232167966579,-0.202201204307544,
5.83099685184627));
#264099=CARTESIAN_POINT('Ctrl Pts',(1.5404857944463,-0.215678298501292,
5.83003204468773));
#264100=CARTESIAN_POINT('Ctrl Pts',(1.53967432188042,-0.221396911071885,
5.82962134240612));
#264101=CARTESIAN_POINT('Ctrl Pts',(1.53804843607064,-0.232413399560746,
5.82882755777302));
#264102=CARTESIAN_POINT('Ctrl Pts',(1.5372384501844,-0.237711854863806,
5.82844462077677));
#264103=CARTESIAN_POINT('Ctrl Pts',(1.53525481621018,-0.250253347521404,
5.82753539951784));
#264104=CARTESIAN_POINT('Ctrl Pts',(1.5340572803879,-0.257492418735662,
5.82700836638343));
#264105=CARTESIAN_POINT('Ctrl Pts',(1.52964741552402,-0.283026611572056,
5.82514134001439));
#264106=CARTESIAN_POINT('Ctrl Pts',(1.52615876312676,-0.301271725949632,
5.8237926568179));
#264107=CARTESIAN_POINT('Ctrl Pts',(1.49442911492725,-0.452480240343094,
5.81248832210308));
#264108=CARTESIAN_POINT('Ctrl Pts',(1.44920184131936,-0.581252611122845,
5.80196317095399));
#264109=CARTESIAN_POINT('Ctrl Pts',(1.35606506510378,-0.765257459134564,
5.78598902043888));
#264110=CARTESIAN_POINT('Ctrl Pts',(1.32006059964869,-0.825817019634387,
5.78057275089209));
#264111=CARTESIAN_POINT('Ctrl Pts',(1.27290556863947,-0.894120176361791,
5.77442456487));
#264112=CARTESIAN_POINT('Ctrl Pts',(1.26561013835471,-0.904417205465,5.77349669180073));
#264113=CARTESIAN_POINT('Ctrl Pts',(1.25537537470487,-0.918496505518134,
5.77222783054844));
#264114=CARTESIAN_POINT('Ctrl Pts',(1.25254294299408,-0.922355321804584,
5.77188004746141));
#264115=CARTESIAN_POINT('Ctrl Pts',(1.24773172160197,-0.928846944856834,
5.77129503289012));
#264116=CARTESIAN_POINT('Ctrl Pts',(1.24576231985563,-0.931486628583284,
5.77105716456047));
#264117=CARTESIAN_POINT('Ctrl Pts',(1.24199229107978,-0.936506436518979,
5.77060487766612));
#264118=CARTESIAN_POINT('Ctrl Pts',(1.24019318287166,-0.938887653722996,
5.77039035311786));
#264119=CARTESIAN_POINT('Ctrl Pts',(1.23542896114701,-0.945155770959277,
5.7698256763789));
#264120=CARTESIAN_POINT('Ctrl Pts',(1.23245232504911,-0.949033939137008,
5.76947632345311));
#264121=CARTESIAN_POINT('Ctrl Pts',(1.22190000733758,-0.962648852823616,
5.76824967752111));
#264122=CARTESIAN_POINT('Ctrl Pts',(1.21422656757306,-0.972309780703132,
5.76737892765205));
#264123=CARTESIAN_POINT('Ctrl Pts',(1.15549749332188,-1.04447044640089,
5.76086349709704));
#264124=CARTESIAN_POINT('Ctrl Pts',(1.09975471704661,-1.10301238381767,
5.75550833181416));
#264125=CARTESIAN_POINT('Ctrl Pts',(0.989570970483146,-1.20202913052037,
5.74574124376241));
#264126=CARTESIAN_POINT('Ctrl Pts',(0.936555041376363,-1.24378015919661,
5.74132978626769));
#264127=CARTESIAN_POINT('Ctrl Pts',(0.829494637148359,-1.31735507832076,
5.73266781579023));
#264128=CARTESIAN_POINT('Ctrl Pts',(0.775910055300904,-1.34961026548057,
5.72843729011691));
#264129=CARTESIAN_POINT('Ctrl Pts',(0.70640360875591,-1.38593955883786,
5.72297909695103));
#264130=CARTESIAN_POINT('Ctrl Pts',(0.692159447126213,-1.39310795922849,
5.72186221047449));
#264131=CARTESIAN_POINT('Ctrl Pts',(0.671097198446779,-1.40330481053261,
5.72021189349902));
#264132=CARTESIAN_POINT('Ctrl Pts',(0.664363180544266,-1.40650538636429,
5.71968443101563));
#264133=CARTESIAN_POINT('Ctrl Pts',(0.652423961343773,-1.41207504356847,
5.71874943416538));
#264134=CARTESIAN_POINT('Ctrl Pts',(0.64722817615901,-1.4144640823972,5.71834259583911));
#264135=CARTESIAN_POINT('Ctrl Pts',(0.637038654316781,-1.41908135941536,
5.717544796921));
#264136=CARTESIAN_POINT('Ctrl Pts',(0.632046103469724,-1.42131202535296,
5.71715392670268));
#264137=CARTESIAN_POINT('Ctrl Pts',(0.618503453806651,-1.42727740104034,
5.71609367064213));
#264138=CARTESIAN_POINT('Ctrl Pts',(0.609931465069502,-1.43096153084624,
5.71542257495602));
#264139=CARTESIAN_POINT('Ctrl Pts',(0.577396273525147,-1.44459928553603,
5.71287505596254));
#264140=CARTESIAN_POINT('Ctrl Pts',(0.553219699467053,-1.45402935531549,
5.71098119445812));
#264141=CARTESIAN_POINT('Ctrl Pts',(0.52322110508008,-1.46487384033214,
5.70862865841382));
#264142=CARTESIAN_POINT('Ctrl Pts',(0.517610810543786,-1.46686561754613,
5.70818858513641));
#264143=CARTESIAN_POINT('Ctrl Pts',(0.355113580444933,-1.52350737871315,
5.69543903540739));
#264144=CARTESIAN_POINT('Ctrl Pts',(0.190496349643747,-1.55269753174366,
5.682268353988));
#264145=CARTESIAN_POINT('Ctrl Pts',(-0.00876213502222772,-1.55582993524719,
5.66715605219676));
#264146=CARTESIAN_POINT('Ctrl Pts',(-0.0419856252360379,-1.55528813601466,
5.66466988085725));
#264147=CARTESIAN_POINT('Ctrl Pts',(-0.0818324990848134,-1.55336029151481,
5.66174715680883));
#264148=CARTESIAN_POINT('Ctrl Pts',(-0.0884937939355788,-1.5529950437509,
5.66126055016976));
#264149=CARTESIAN_POINT('Ctrl Pts',(-0.0988513779800285,-1.55236026318874,
5.66050723829953));
#264150=CARTESIAN_POINT('Ctrl Pts',(-0.10254929403598,-1.552120364124,5.66023894360849));
#264151=CARTESIAN_POINT('Ctrl Pts',(-0.109420432661839,-1.55164994145406,
5.65974168582727));
#264152=CARTESIAN_POINT('Ctrl Pts',(-0.112593777416775,-1.5514228996353,
5.65951254022215));
#264153=CARTESIAN_POINT('Ctrl Pts',(-0.119825869056215,-1.55088316174212,
5.65899144845466));
#264154=CARTESIAN_POINT('Ctrl Pts',(-0.123884097077734,-1.55056426883275,
5.65869985155167));
#264155=CARTESIAN_POINT('Ctrl Pts',(-0.134466409555283,-1.54969090612779,
5.65794147919158));
#264156=CARTESIAN_POINT('Ctrl Pts',(-0.140988417253301,-1.54911116129101,
5.65747607052642));
#264157=CARTESIAN_POINT('Ctrl Pts',(-0.184899658410045,-1.54492824617979,
5.65435476902267));
#264158=CARTESIAN_POINT('Ctrl Pts',(-0.222155199826792,-1.54001260163709,
5.65176609003573));
#264159=CARTESIAN_POINT('Ctrl Pts',(-0.391195909823523,-1.51144519651127,
5.64014255456864));
#264160=CARTESIAN_POINT('Ctrl Pts',(-0.519765890991624,-1.47219211228039,
5.63159716724919));
#264161=CARTESIAN_POINT('Ctrl Pts',(-0.674428952727528,-1.40214638010192,
5.62017948898414));
#264162=CARTESIAN_POINT('Ctrl Pts',(-0.7066046586172,-1.38621010063511,
5.6177396996839));
#264163=CARTESIAN_POINT('Ctrl Pts',(-0.759285193505354,-1.3578071077113,
5.61361176207627));
#264164=CARTESIAN_POINT('Ctrl Pts',(-0.780105265922131,-1.34595312433692,
5.61194415670442));
#264165=CARTESIAN_POINT('Ctrl Pts',(-0.808149145782261,-1.32911695124852,
5.60964355769668));
#264166=CARTESIAN_POINT('Ctrl Pts',(-0.815617590338711,-1.32454703677803,
5.60902549188111));
#264167=CARTESIAN_POINT('Ctrl Pts',(-0.82809905274682,-1.31676408567938,
5.60798325730435));
#264168=CARTESIAN_POINT('Ctrl Pts',(-0.833132990323881,-1.31358483438699,
5.60756033558916));
#264169=CARTESIAN_POINT('Ctrl Pts',(-0.843029163522539,-1.30725500421949,
5.6067237496953));
#264170=CARTESIAN_POINT('Ctrl Pts',(-0.847892297447702,-1.30410600292387,
5.60631014902021));
#264171=CARTESIAN_POINT('Ctrl Pts',(-0.858557168427101,-1.29711535964268,
5.60539755846031));
#264172=CARTESIAN_POINT('Ctrl Pts',(-0.864350920414028,-1.2932618262127,
5.60489812922958));
#264173=CARTESIAN_POINT('Ctrl Pts',(-0.88458334349444,-1.27960817232303,
5.60314101875784));
#264174=CARTESIAN_POINT('Ctrl Pts',(-0.898882291490211,-1.26960440539808,
5.60187568824488));
#264175=CARTESIAN_POINT('Ctrl Pts',(-1.02117629704056,-1.18094401615705,
5.59084334430135));
#264176=CARTESIAN_POINT('Ctrl Pts',(-1.11876750765334,-1.08893218909319,
5.58052442856601));
#264177=CARTESIAN_POINT('Ctrl Pts',(-1.25053687268821,-0.92804920404406,
5.56440632368165));
#264178=CARTESIAN_POINT('Ctrl Pts',(-1.29350224133291,-0.86716335104238,
5.5586654505749));
#264179=CARTESIAN_POINT('Ctrl Pts',(-1.338640577178,-0.792331752790214,
5.55218852672417));
#264180=CARTESIAN_POINT('Ctrl Pts',(-1.34519567651387,-0.78115096032571,
5.55123521126765));
#264181=CARTESIAN_POINT('Ctrl Pts',(-1.35400462724587,-0.765686042958562,
5.54993760172661));
#264182=CARTESIAN_POINT('Ctrl Pts',(-1.35637912969309,-0.761471801979394,
5.5495861124621));
#264183=CARTESIAN_POINT('Ctrl Pts',(-1.36034220414077,-0.754360822834889,
5.54899665487783));
#264184=CARTESIAN_POINT('Ctrl Pts',(-1.36194125923689,-0.751470006381479,
5.5487580282248));
#264185=CARTESIAN_POINT('Ctrl Pts',(-1.36496280836634,-0.745966240713117,
5.54830564895086));
#264186=CARTESIAN_POINT('Ctrl Pts',(-1.36638702998467,-0.743354279737981,
5.54809178376104));
#264187=CARTESIAN_POINT('Ctrl Pts',(-1.3701076083442,-0.736484077874733,
5.54753137357699));
#264188=CARTESIAN_POINT('Ctrl Pts',(-1.3723916330671,-0.732219135625162,
5.54718560497088));
#264189=CARTESIAN_POINT('Ctrl Pts',(-1.38028903064516,-0.717305611915265,
5.54598368591826));
#264190=CARTESIAN_POINT('Ctrl Pts',(-1.38579885374374,-0.70660222864203,
5.54513373818601));
#264191=CARTESIAN_POINT('Ctrl Pts',(-1.43514813428337,-0.607938203977148,
5.53740421887553));
#264192=CARTESIAN_POINT('Ctrl Pts',(-1.47069023433529,-0.516057534786653,
5.53095906933564));
#264193=CARTESIAN_POINT('Ctrl Pts',(-1.52907535595516,-0.308614489205268,
5.51677667812562));
#264194=CARTESIAN_POINT('Ctrl Pts',(-1.54797135539625,-0.192596692072913,
5.50905452405191));
#264195=CARTESIAN_POINT('Ctrl Pts',(-1.5543052043772,-0.0623707568372182,
5.49994839313294));
#264196=CARTESIAN_POINT('Ctrl Pts',(-1.55477884503724,-0.049168117372399,
5.4990207193885));
#264197=CARTESIAN_POINT('Ctrl Pts',(-1.55524412947786,-0.0290477502464651,
5.49759945213287));
#264198=CARTESIAN_POINT('Ctrl Pts',(-1.55535789835207,-0.0221332172942355,
5.49710967003003));
#264199=CARTESIAN_POINT('Ctrl Pts',(-1.55547562514631,-0.0101006118354341,
5.49625490273249));
#264200=CARTESIAN_POINT('Ctrl Pts',(-1.55550043820327,-0.00498280903079771,
5.49589057438442));
#264201=CARTESIAN_POINT('Ctrl Pts',(-1.55549944070673,0.00651333868513192,
5.49507039971071));
#264202=CARTESIAN_POINT('Ctrl Pts',(-1.55545965525977,0.0128915569025155,
5.49461412335422));
#264203=CARTESIAN_POINT('Ctrl Pts',(-1.55524796979287,0.029978431198106,
5.49338838448767));
#264204=CARTESIAN_POINT('Ctrl Pts',(-1.5550047003345,0.0406856873065747,
5.49261671029927));
#264205=CARTESIAN_POINT('Ctrl Pts',(-1.5532456061059,0.0939025174494717,
5.48876282624848));
#264206=CARTESIAN_POINT('Ctrl Pts',(-1.55009723945784,0.13633596400759,
5.48563029389698));
#264207=CARTESIAN_POINT('Ctrl Pts',(-1.52691884218012,0.336889722907466,
5.47052607851178));
#264208=CARTESIAN_POINT('Ctrl Pts',(-1.48441224788886,0.491407369625553,
5.45787219155486));
#264209=CARTESIAN_POINT('Ctrl Pts',(-1.40823479323957,0.661189805556878,
5.44383764123695));
#264210=CARTESIAN_POINT('Ctrl Pts',(-1.39664399424696,0.685334206331063,
5.44184206252578));
#264211=CARTESIAN_POINT('Ctrl Pts',(-1.38147966816369,0.714937890392895,
5.43940584921647));
#264212=CARTESIAN_POINT('Ctrl Pts',(-1.37848855595424,0.720688258359481,
5.43893313586419));
#264213=CARTESIAN_POINT('Ctrl Pts',(-1.37373225928131,0.729694210803432,
5.43819379019823));
#264214=CARTESIAN_POINT('Ctrl Pts',(-1.3719912905888,0.732962387027253,
5.43792569601348));
#264215=CARTESIAN_POINT('Ctrl Pts',(-1.36873267570472,0.739027223064927,
5.43742861652167));
#264216=CARTESIAN_POINT('Ctrl Pts',(-1.36721813286294,0.741825418456715,
5.43719944991717));
#264217=CARTESIAN_POINT('Ctrl Pts',(-1.36374449084891,0.748196374914809,
5.43667806259875));
#264218=CARTESIAN_POINT('Ctrl Pts',(-1.36177993410677,0.751766096497224,
5.43638619272176));
#264219=CARTESIAN_POINT('Ctrl Pts',(-1.35569526299095,0.762720202165408,
5.4354912558632));
#264220=CARTESIAN_POINT('Ctrl Pts',(-1.35152885188499,0.770078907600953,
5.43489104086439));
#264221=CARTESIAN_POINT('Ctrl Pts',(-1.34170198202646,0.787109660189673,
5.43350333120464));
#264222=CARTESIAN_POINT('Ctrl Pts',(-1.33599652822017,0.79675537022244,
5.43271844246537));
#264223=CARTESIAN_POINT('Ctrl Pts',(-1.31588020877409,0.829940509631854,
5.43001877061165));
#264224=CARTESIAN_POINT('Ctrl Pts',(-1.30094669851466,0.853158756935452,
5.42813106263847));
#264225=CARTESIAN_POINT('Ctrl Pts',(-1.20865960042166,0.988581441625445,
5.41705054041824));
#264226=CARTESIAN_POINT('Ctrl Pts',(-1.11744993954983,1.09062446694038,
5.40835566747347));
#264227=CARTESIAN_POINT('Ctrl Pts',(-0.977262860678338,1.21115569376459,
5.39587975576391));
#264228=CARTESIAN_POINT('Ctrl Pts',(-0.938961870076119,1.24108445488677,
5.39255089490556));
#264229=CARTESIAN_POINT('Ctrl Pts',(-0.889937014517213,1.27582317964514,
5.38834499465083));
#264230=CARTESIAN_POINT('Ctrl Pts',(-0.880474350500349,1.282371857557,5.38753565908545));
#264231=CARTESIAN_POINT('Ctrl Pts',(-0.865453774515862,1.29252228595158,
5.38625435279685));
#264232=CARTESIAN_POINT('Ctrl Pts',(-0.859943891123002,1.29619466021367,
5.38578504985767));
#264233=CARTESIAN_POINT('Ctrl Pts',(-0.849724527981963,1.30291209473848,
5.38491582838685));
#264234=CARTESIAN_POINT('Ctrl Pts',(-0.845021684222362,1.30596709443694,
5.38451628993596));
#264235=CARTESIAN_POINT('Ctrl Pts',(-0.834553409773153,1.31268714034153,
5.38362791242899));
#264236=CARTESIAN_POINT('Ctrl Pts',(-0.828780175938554,1.31633975074721,
5.38313862267693));
#264237=CARTESIAN_POINT('Ctrl Pts',(-0.812113376640613,1.32673139574289,
5.38172781738645));
#264238=CARTESIAN_POINT('Ctrl Pts',(-0.801160612843261,1.33337391122609,
5.38080279354729));
#264239=CARTESIAN_POINT('Ctrl Pts',(-0.71317080460275,1.38526150080613,
5.37338631186429));
#264240=CARTESIAN_POINT('Ctrl Pts',(-0.632462609298558,1.42391980058423,
5.3666581715158));
#264241=CARTESIAN_POINT('Ctrl Pts',(-0.459368629489077,1.48919986369108,
5.35242585160925));
#264242=CARTESIAN_POINT('Ctrl Pts',(-0.36691683939528,1.51463122860939,
5.34492977670614));
#264243=CARTESIAN_POINT('Ctrl Pts',(-0.234905577203705,1.53813994148863,
5.33471467655072));
#264244=CARTESIAN_POINT('Ctrl Pts',(-0.196856071665377,1.54347121938797,
5.33182783774703));
#264245=CARTESIAN_POINT('Ctrl Pts',(-0.152090523920295,1.5480607640834,
5.32852625739485));
#264246=CARTESIAN_POINT('Ctrl Pts',(-0.145532139610621,1.54869107868809,
5.32804493713997));
#264247=CARTESIAN_POINT('Ctrl Pts',(-0.134903172230235,1.54964449297277,
5.32726893519353));
#264248=CARTESIAN_POINT('Ctrl Pts',(-0.130835066101718,1.54999326030462,
5.32697289176202));
#264249=CARTESIAN_POINT('Ctrl Pts',(-0.123593649868051,1.55058536948606,
5.3264476868671));
#264250=CARTESIAN_POINT('Ctrl Pts',(-0.120420926686394,1.55083499427229,
5.32621818161246));
#264251=CARTESIAN_POINT('Ctrl Pts',(-0.113560861469582,1.55135355374082,
5.32572326280352));
#264252=CARTESIAN_POINT('Ctrl Pts',(-0.109873324350047,1.55161908061548,
5.32545804116904));
#264253=CARTESIAN_POINT('Ctrl Pts',(-0.0995688161021603,1.5523241534375,
5.3247190905951));
#264254=CARTESIAN_POINT('Ctrl Pts',(-0.0929498230270874,1.55273454302193,
5.32424695333003));
#264255=CARTESIAN_POINT('Ctrl Pts',(-0.053861911191322,1.55490722049207,
5.32147257228365));
#264256=CARTESIAN_POINT('Ctrl Pts',(-0.02134391341106,1.55569354281076,
5.31922059879102));
#264257=CARTESIAN_POINT('Ctrl Pts',(0.165266267824599,1.5543525388127,5.30649548754598));
#264258=CARTESIAN_POINT('Ctrl Pts',(0.318342429843081,1.53035681546692,
5.29674899074108));
#264259=CARTESIAN_POINT('Ctrl Pts',(0.504687949867082,1.47192569638736,
5.2834961145528));
#264260=CARTESIAN_POINT('Ctrl Pts',(0.543463772375996,1.45805411647056,
5.2806632859163));
#264261=CARTESIAN_POINT('Ctrl Pts',(0.591797969527179,1.43856711438559,
5.27701219482872));
#264262=CARTESIAN_POINT('Ctrl Pts',(0.601911013982638,1.4343651207774,5.27624150181153));
#264263=CARTESIAN_POINT('Ctrl Pts',(0.61794896698783,1.42750183782438,5.27500804314016));
#264264=CARTESIAN_POINT('Ctrl Pts',(0.623903170190132,1.42490956018206,
5.27454762081009));
#264265=CARTESIAN_POINT('Ctrl Pts',(0.635026300503056,1.4199838059676,5.27368272997243));
#264266=CARTESIAN_POINT('Ctrl Pts',(0.640199055061689,1.41765919031144,
5.27327856989081));
#264267=CARTESIAN_POINT('Ctrl Pts',(0.651743242714566,1.41239521027049,
5.27237216394042));
#264268=CARTESIAN_POINT('Ctrl Pts',(0.658107696066416,1.40944093235926,
5.27186941199308));
#264269=CARTESIAN_POINT('Ctrl Pts',(0.676841997207182,1.40059021144632,
5.27038037702634));
#264270=CARTESIAN_POINT('Ctrl Pts',(0.689153872910023,1.39457339236177,
5.26938995481999));
#264271=CARTESIAN_POINT('Ctrl Pts',(0.798461747688608,1.33935363625879,
5.26048765781328));
#264272=CARTESIAN_POINT('Ctrl Pts',(0.890107321274177,1.2802768811826,5.25221726769949));
#264273=CARTESIAN_POINT('Ctrl Pts',(1.05773847899523,1.1454648875892,5.23556725138612));
#264274=CARTESIAN_POINT('Ctrl Pts',(1.1335961695884,1.07045045700489,5.22724289133022));
#264275=CARTESIAN_POINT('Ctrl Pts',(1.20862984886372,0.979250053559702,
5.21850438455071));
#264276=CARTESIAN_POINT('Ctrl Pts',(1.21595192674479,0.970143140305076,
5.21764575323557));
#264277=CARTESIAN_POINT('Ctrl Pts',(1.22612325787585,0.957196345648021,
5.21644558075253));
#264278=CARTESIAN_POINT('Ctrl Pts',(1.22905826174672,0.953424815332332,
5.21609837002398));
#264279=CARTESIAN_POINT('Ctrl Pts',(1.2339655426084,0.947058557291241,5.21551641121575));
#264280=CARTESIAN_POINT('Ctrl Pts',(1.23594711074264,0.944471074958277,
5.21528101827747));
#264281=CARTESIAN_POINT('Ctrl Pts',(1.23996884025106,0.939185268137,5.21480249108676));
#264282=CARTESIAN_POINT('Ctrl Pts',(1.24200835466986,0.936486486932858,
5.21455940195158));
#264283=CARTESIAN_POINT('Ctrl Pts',(1.24716584365623,0.929615370937746,
5.21394355765565));
#264284=CARTESIAN_POINT('Ctrl Pts',(1.25027172890505,0.925433944402657,
5.21357163640402));
#264285=CARTESIAN_POINT('Ctrl Pts',(1.26266356395552,0.908574667351218,
5.21208312612106));
#264286=CARTESIAN_POINT('Ctrl Pts',(1.27177857845415,0.895771455267055,
5.21097768334453));
#264287=CARTESIAN_POINT('Ctrl Pts',(1.29510390025228,0.861934082654363,
5.20811430674465));
#264288=CARTESIAN_POINT('Ctrl Pts',(1.30899663067788,0.840685708132529,
5.20637362846489));
#264289=CARTESIAN_POINT('Ctrl Pts',(1.36545653188261,0.749536845693514,
5.19910236539426));
#264290=CARTESIAN_POINT('Ctrl Pts',(1.40297178841824,0.676708759370786,
5.19376122252171));
#264291=CARTESIAN_POINT('Ctrl Pts',(1.43457674133486,0.601306762992946,
5.18837549714138));
#264292=CARTESIAN_POINT('',(-1.55596208451267,0.00138090387652695,5.3559437743963));
#264293=CARTESIAN_POINT('Ctrl Pts',(1.43231908414271,0.600352779935808,
5.05019128547067));
#264294=CARTESIAN_POINT('Ctrl Pts',(1.32160532361985,0.862577042890051,
5.07050276174236));
#264295=CARTESIAN_POINT('Ctrl Pts',(0.815607745123861,1.52283096854995,
5.12785138087118));
#264296=CARTESIAN_POINT('Ctrl Pts',(-0.66589513819016,1.71353370282299,
5.22223714285715));
#264297=CARTESIAN_POINT('Ctrl Pts',(-1.4993495737318,0.726990709360215,
5.30384316289402));
#264298=CARTESIAN_POINT('Ctrl Pts',(-1.55692912760588,0.106428400307349,
5.34841204007373));
#264299=CARTESIAN_POINT('Ctrl Pts',(-1.55596208451267,0.00138090387652695,
5.3559437743963));
#264300=CARTESIAN_POINT('Ctrl Pts',(-1.5554993720197,0.00139772898855563,
5.35620969761336));
#264301=CARTESIAN_POINT('Ctrl Pts',(-1.55560008096552,-0.110678863304792,
5.36359495551528));
#264302=CARTESIAN_POINT('Ctrl Pts',(-1.54358838605568,-0.222430311866365,
5.37091855286445));
#264303=CARTESIAN_POINT('Ctrl Pts',(-1.51593216532635,-0.349052143694656,
5.37983742834118));
#264304=CARTESIAN_POINT('Ctrl Pts',(-1.51190115728801,-0.366118257267673,
5.38105217793184));
#264305=CARTESIAN_POINT('Ctrl Pts',(-1.50518211486557,-0.392558335020044,
5.38295601981498));
#264306=CARTESIAN_POINT('Ctrl Pts',(-1.50269290442263,-0.401981682143839,
5.38363891226452));
#264307=CARTESIAN_POINT('Ctrl Pts',(-1.49837405339774,-0.417730531464308,
5.38478784617263));
#264308=CARTESIAN_POINT('Ctrl Pts',(-1.49659248347777,-0.424069023660975,
5.38525234836641));
#264309=CARTESIAN_POINT('Ctrl Pts',(-1.4930045361474,-0.436530012191539,
5.38616974755778));
#264310=CARTESIAN_POINT('Ctrl Pts',(-1.49120060468622,-0.442653081857937,
5.38662255778795));
#264311=CARTESIAN_POINT('Ctrl Pts',(-1.4876929703892,-0.454294206575662,
5.38748737435947));
#264312=CARTESIAN_POINT('Ctrl Pts',(-1.48599612138359,-0.459814229721807,
5.38789915097486));
#264313=CARTESIAN_POINT('Ctrl Pts',(-1.48204883040551,-0.47240509624171,
5.38884233841758));
#264314=CARTESIAN_POINT('Ctrl Pts',(-1.47977846693024,-0.479469494273115,
5.38937439355564));
#264315=CARTESIAN_POINT('Ctrl Pts',(-1.47371965499815,-0.497868919860951,
5.39076776819668));
#264316=CARTESIAN_POINT('Ctrl Pts',(-1.46985102681954,-0.509176813133323,
5.39163170128635));
#264317=CARTESIAN_POINT('Ctrl Pts',(-1.43071575014064,-0.619404096999735,
5.40012957990073));
#264318=CARTESIAN_POINT('Ctrl Pts',(-1.3856547099048,-0.714535842966949,
5.40809739847534));
#264319=CARTESIAN_POINT('Ctrl Pts',(-1.29946391861826,-0.857193203136812,
5.4209844183645));
#264320=CARTESIAN_POINT('Ctrl Pts',(-1.26444586653384,-0.908054745038845,
5.42578839805882));
#264321=CARTESIAN_POINT('Ctrl Pts',(-1.20330473306388,-0.986438128405728,
5.43343549883851));
#264322=CARTESIAN_POINT('Ctrl Pts',(-1.1790344887421,-1.01532288560463,
5.43631180977595));
#264323=CARTESIAN_POINT('Ctrl Pts',(-1.13985601310225,-1.05864857444442,
5.44068672169018));
#264324=CARTESIAN_POINT('Ctrl Pts',(-1.12566964056317,-1.07372087017383,
5.44222077248859));
#264325=CARTESIAN_POINT('Ctrl Pts',(-1.10716166983749,-1.09261445886645,
5.44415454710481));
#264326=CARTESIAN_POINT('Ctrl Pts',(-1.10311471663873,-1.09670016121536,
5.44457338548001));
#264327=CARTESIAN_POINT('Ctrl Pts',(-1.09688818726383,-1.10291697094071,
5.44521157948093));
#264328=CARTESIAN_POINT('Ctrl Pts',(-1.09472491065436,-1.10506421106432,
5.44543217107678));
#264329=CARTESIAN_POINT('Ctrl Pts',(-1.09026344195423,-1.10946664861493,
5.44588475691598));
#264330=CARTESIAN_POINT('Ctrl Pts',(-1.08796458636857,-1.11172104253873,
5.4461166809356));
#264331=CARTESIAN_POINT('Ctrl Pts',(-1.08272857119958,-1.11682399298928,
5.44664204814988));
#264332=CARTESIAN_POINT('Ctrl Pts',(-1.07978716487821,-1.11966810698839,
5.44693514648195));
#264333=CARTESIAN_POINT('Ctrl Pts',(-1.07212295850001,-1.1270205145044,
5.44769370277198));
#264334=CARTESIAN_POINT('Ctrl Pts',(-1.06738287120381,-1.1315107991009,
5.44815781635469));
#264335=CARTESIAN_POINT('Ctrl Pts',(-1.0362445132388,-1.16063836124619,
5.45117513167626));
#264336=CARTESIAN_POINT('Ctrl Pts',(-1.00902089527395,-1.18438230583711,
5.45366643288268));
#264337=CARTESIAN_POINT('Ctrl Pts',(-0.903616925325389,-1.27003839080889,
5.4628879131404));
#264338=CARTESIAN_POINT('Ctrl Pts',(-0.820369091235699,-1.32533724535424,
5.46934827738685));
#264339=CARTESIAN_POINT('Ctrl Pts',(-0.680639846534117,-1.39991112836339,
5.4798238499985));
#264340=CARTESIAN_POINT('Ctrl Pts',(-0.627368189042677,-1.42458063477618,
5.48373908755192));
#264341=CARTESIAN_POINT('Ctrl Pts',(-0.541301285447167,-1.45867182259952,
5.49006298510955));
#264342=CARTESIAN_POINT('Ctrl Pts',(-0.509370679774071,-1.47012645220616,
5.49240826590177));
#264343=CARTESIAN_POINT('Ctrl Pts',(-0.467890339048307,-1.48349329864626,
5.49546655712975));
#264344=CARTESIAN_POINT('Ctrl Pts',(-0.458660256851397,-1.48637293361412,
5.49614778182696));
#264345=CARTESIAN_POINT('Ctrl Pts',(-0.44329539777211,-1.49100977702656,
5.49728323622555));
#264346=CARTESIAN_POINT('Ctrl Pts',(-0.437175483210059,-1.49281564821363,
5.49773587425982));
#264347=CARTESIAN_POINT('Ctrl Pts',(-0.425495351505285,-1.49618425093073,
5.49860056120874));
#264348=CARTESIAN_POINT('Ctrl Pts',(-0.419937189310278,-1.49775377224279,
5.49901238154789));
#264349=CARTESIAN_POINT('Ctrl Pts',(-0.407213825088192,-1.50127022239679,
5.49995595064675));
#264350=CARTESIAN_POINT('Ctrl Pts',(-0.400043213580722,-1.50319686126834,
5.50048834559686));
#264351=CARTESIAN_POINT('Ctrl Pts',(-0.381280279539176,-1.50809442823809,
5.50188319398329));
#264352=CARTESIAN_POINT('Ctrl Pts',(-0.369667179995152,-1.5109829969951,
5.50274827004915));
#264353=CARTESIAN_POINT('Ctrl Pts',(-0.257367010087211,-1.53754371967827,
5.51113228396625));
#264354=CARTESIAN_POINT('Ctrl Pts',(-0.15460955814862,-1.5512466469733,
5.51897438915023));
#264355=CARTESIAN_POINT('Ctrl Pts',(0.0337023303501034,-1.55745725200963,
5.53353688051234));
#264356=CARTESIAN_POINT('Ctrl Pts',(0.118766336248085,-1.55328824256979,
5.54017788768958));
#264357=CARTESIAN_POINT('Ctrl Pts',(0.237667903967209,-1.53763204424795,
5.54928528431979));
#264358=CARTESIAN_POINT('Ctrl Pts',(0.272110665054296,-1.53191207206746,
5.55190087127096));
#264359=CARTESIAN_POINT('Ctrl Pts',(0.313022189079387,-1.52369415666191,
5.55495900003768));
#264360=CARTESIAN_POINT('Ctrl Pts',(0.319700713136032,-1.52230687856444,
5.5554566467108));
#264361=CARTESIAN_POINT('Ctrl Pts',(0.330052900554546,-1.52008536627153,
5.55622536916249));
#264362=CARTESIAN_POINT('Ctrl Pts',(0.333732912440647,-1.51928166640972,
5.55649811147286));
#264363=CARTESIAN_POINT('Ctrl Pts',(0.34055438795616,-1.51776590225812,
5.55700266307007));
#264364=CARTESIAN_POINT('Ctrl Pts',(0.343696534133728,-1.51705745375395,
5.55723466527917));
#264365=CARTESIAN_POINT('Ctrl Pts',(0.350841000766122,-1.51542327972931,
5.55776127428947));
#264366=CARTESIAN_POINT('Ctrl Pts',(0.354841866555703,-1.51449145766812,
5.55805552944753));
#264367=CARTESIAN_POINT('Ctrl Pts',(0.365244785517725,-1.51202507799577,
5.55881907974442));
#264368=CARTESIAN_POINT('Ctrl Pts',(0.371640959276129,-1.51046568689452,
5.55928700114717));
#264369=CARTESIAN_POINT('Ctrl Pts',(0.414111780358202,-1.49982516061323,
5.56238493240159));
#264370=CARTESIAN_POINT('Ctrl Pts',(0.449864175281268,-1.48949214936153,
5.5649491993143));
#264371=CARTESIAN_POINT('Ctrl Pts',(0.626308820930151,-1.43156237469475,
5.57754451570754));
#264372=CARTESIAN_POINT('Ctrl Pts',(0.760046158775416,-1.36527287940747,
5.58697157107993));
#264373=CARTESIAN_POINT('Ctrl Pts',(0.904919711866183,-1.26548438444147,
5.59891337837999));
#264374=CARTESIAN_POINT('Ctrl Pts',(0.92706035373409,-1.24935558150297,
5.60078995742166));
#264375=CARTESIAN_POINT('Ctrl Pts',(0.964273401359281,-1.22071297504079,
5.60404411337837));
#264376=CARTESIAN_POINT('Ctrl Pts',(0.979556766843766,-1.20848328107542,
5.60541097795788));
#264377=CARTESIAN_POINT('Ctrl Pts',(1.00087363731089,-1.19075551272447,
5.60736348297189));
#264378=CARTESIAN_POINT('Ctrl Pts',(1.0071013489349,-1.1854929765185,5.60793962953443));
#264379=CARTESIAN_POINT('Ctrl Pts',(1.01775605099478,-1.17634500107702,
5.60893542568157));
#264380=CARTESIAN_POINT('Ctrl Pts',(1.02220292202003,-1.17248288915765,
5.60935411215551));
#264381=CARTESIAN_POINT('Ctrl Pts',(1.03066809774478,-1.16504611343838,
5.61015711698945));
#264382=CARTESIAN_POINT('Ctrl Pts',(1.03469001598894,-1.16147567500198,
5.61054125578786));
#264383=CARTESIAN_POINT('Ctrl Pts',(1.04407511456429,-1.15305666689221,
5.61144386434116));
#264384=CARTESIAN_POINT('Ctrl Pts',(1.04942312719099,-1.14819145562112,
5.61196302930434));
#264385=CARTESIAN_POINT('Ctrl Pts',(1.06769778090363,-1.13133224605936,
5.61375391933813));
#264386=CARTESIAN_POINT('Ctrl Pts',(1.08045383737794,-1.1191562268552,5.61503335872999));
#264387=CARTESIAN_POINT('Ctrl Pts',(1.1844558585827,-1.01644785851733,5.62571641954513));
#264388=CARTESIAN_POINT('Ctrl Pts',(1.26434595302489,-0.915159639529413,
5.63562496555821));
#264389=CARTESIAN_POINT('Ctrl Pts',(1.37123089292751,-0.73850445279877,
5.65163257242835));
#264390=CARTESIAN_POINT('Ctrl Pts',(1.40653370284033,-0.668826317083173,
5.65766084437124));
#264391=CARTESIAN_POINT('Ctrl Pts',(1.44156922136692,-0.584495995090591,
5.66443251661433));
#264392=CARTESIAN_POINT('Ctrl Pts',(1.4465177870522,-0.572139591269316,
5.66541195377123));
#264393=CARTESIAN_POINT('Ctrl Pts',(1.45307946601034,-0.55512572373256,
5.66674172138828));
#264394=CARTESIAN_POINT('Ctrl Pts',(1.45482977518503,-0.550522325348872,
5.66709963914956));
#264395=CARTESIAN_POINT('Ctrl Pts',(1.45773423973904,-0.542772848290416,
5.66769893223863));
#264396=CARTESIAN_POINT('Ctrl Pts',(1.45890013233382,-0.539631247376007,
5.66794099318638));
#264397=CARTESIAN_POINT('Ctrl Pts',(1.46109388075835,-0.533660921638923,
5.66839928900607));
#264398=CARTESIAN_POINT('Ctrl Pts',(1.46212369030483,-0.530832951450371,
5.6686156421557));
#264399=CARTESIAN_POINT('Ctrl Pts',(1.46480244351849,-0.523409863400469,
5.66918168088108));
#264400=CARTESIAN_POINT('Ctrl Pts',(1.46643799155516,-0.51880989031911,
5.6695305790947));
#264401=CARTESIAN_POINT('Ctrl Pts',(1.47204851976286,-0.502791782365244,
5.67073929244131));
#264402=CARTESIAN_POINT('Ctrl Pts',(1.47591215050701,-0.49133468100059,
5.6715928711729));
#264403=CARTESIAN_POINT('Ctrl Pts',(1.50981852203538,-0.386779001030871,
5.67929331027264));
#264404=CARTESIAN_POINT('Ctrl Pts',(1.53115450803153,-0.291070212453557,
5.68571083158051));
#264405=CARTESIAN_POINT('Ctrl Pts',(1.55755952524534,-0.080982927464409,
5.69964733234562));
#264406=CARTESIAN_POINT('Ctrl Pts',(1.55930812127068,0.0332129866934599,
5.70714925867247));
#264407=CARTESIAN_POINT('Ctrl Pts',(1.54712797524903,0.161902788200686,
5.71615158635484));
#264408=CARTESIAN_POINT('Ctrl Pts',(1.54544903856824,0.177213780866496,
5.71723092341854));
#264409=CARTESIAN_POINT('Ctrl Pts',(1.54262628416476,0.199848140760663,
5.71883993188617));
#264410=CARTESIAN_POINT('Ctrl Pts',(1.54165700654947,0.207192670463991,
5.71936412982183));
#264411=CARTESIAN_POINT('Ctrl Pts',(1.53983905227946,0.220248215519711,
5.72029980260937));
#264412=CARTESIAN_POINT('Ctrl Pts',(1.53901096706326,0.22596199897237,5.72071062205208));
#264413=CARTESIAN_POINT('Ctrl Pts',(1.53719943496688,0.237989444999662,
5.72157824138033));
#264414=CARTESIAN_POINT('Ctrl Pts',(1.53620885773022,0.244301907434522,
5.72203525921971));
#264415=CARTESIAN_POINT('Ctrl Pts',(1.53348304950316,0.260999717136409,
5.72324866261563));
#264416=CARTESIAN_POINT('Ctrl Pts',(1.5316812403549,0.271373696731041,5.72400713829426));
#264417=CARTESIAN_POINT('Ctrl Pts',(1.52344421706974,0.31610042155577,5.72729782624887));
#264418=CARTESIAN_POINT('Ctrl Pts',(1.51595801684094,0.350246609163335,
5.729862966271));
#264419=CARTESIAN_POINT('Ctrl Pts',(1.4884278583792,0.458280961304234,5.73815604510771));
#264420=CARTESIAN_POINT('Ctrl Pts',(1.46409864409644,0.530874509686054,
5.74400369568442));
#264421=CARTESIAN_POINT('Ctrl Pts',(1.43457651448711,0.601307304198132,
5.74991065382822));
#264422=CARTESIAN_POINT('Origin',(0.,0.,-1.29405622560371));
#264423=CARTESIAN_POINT('',(1.43315705713265,0.600696421508096,6.58835745434585));
#264424=CARTESIAN_POINT('',(1.43457668334549,0.60130690134194,6.45155991302018));
#264425=CARTESIAN_POINT('',(1.43457668357355,0.601306900797845,-1.29405622560371));
#264426=CARTESIAN_POINT('',(-1.55592048424612,-0.00138931664391115,6.1940562256037));
#264427=CARTESIAN_POINT('Ctrl Pts',(-1.55592048424612,-0.00138931664391115,
6.1940562256037));
#264428=CARTESIAN_POINT('Ctrl Pts',(-1.55690316545381,-0.107885618591398,
6.20169131463905));
#264429=CARTESIAN_POINT('Ctrl Pts',(-1.49836903718625,-0.730118810983662,
6.24637833226625));
#264430=CARTESIAN_POINT('Ctrl Pts',(-0.660529380526586,-1.71587418409115,
6.32811727848531));
#264431=CARTESIAN_POINT('Ctrl Pts',(1.08360676610026,-1.48536852485539,
6.43927306426084));
#264432=CARTESIAN_POINT('Ctrl Pts',(1.67047740112632,-0.244146230934245,
6.5260197895477));
#264433=CARTESIAN_POINT('Ctrl Pts',(1.50279954967853,0.438061975745323,
6.57571458624271));
#264434=CARTESIAN_POINT('Ctrl Pts',(1.43315705713258,0.600696421508238,
6.58835745434586));
#264435=CARTESIAN_POINT('Ctrl Pts',(-1.55549936581116,-0.0014046213329422,
6.19381419951655));
#264436=CARTESIAN_POINT('Ctrl Pts',(-1.55559995768813,0.109992377391697,
6.18647623964182));
#264437=CARTESIAN_POINT('Ctrl Pts',(-1.5437345883581,0.221069845459952,
6.1791922833572));
#264438=CARTESIAN_POINT('Ctrl Pts',(-1.51645035231152,0.346779410486837,
6.17033606758573));
#264439=CARTESIAN_POINT('Ctrl Pts',(-1.51251281990397,0.36356919682226,
6.16914097311621));
#264440=CARTESIAN_POINT('Ctrl Pts',(-1.50595038895181,0.389596986829181,
6.16726719245273));
#264441=CARTESIAN_POINT('Ctrl Pts',(-1.50351762436012,0.398882353793074,
6.1665945059703));
#264442=CARTESIAN_POINT('Ctrl Pts',(-1.49929592233644,0.414408159240896,
6.16546232485091));
#264443=CARTESIAN_POINT('Ctrl Pts',(-1.49755355186387,0.420661077583915,
6.1650043224194));
#264444=CARTESIAN_POINT('Ctrl Pts',(-1.49404420316901,0.432957051387873,
6.16409959416163));
#264445=CARTESIAN_POINT('Ctrl Pts',(-1.49227957028254,0.439000650760043,
6.16365295158166));
#264446=CARTESIAN_POINT('Ctrl Pts',(-1.48884660487773,0.45049812884336,
6.16279942718374));
#264447=CARTESIAN_POINT('Ctrl Pts',(-1.48718486789767,0.455953883688627,
6.16239276649154));
#264448=CARTESIAN_POINT('Ctrl Pts',(-1.48331670470011,0.46840755989857,
6.16146065461254));
#264449=CARTESIAN_POINT('Ctrl Pts',(-1.48109070555724,0.475399208145836,
6.16093457016266));
#264450=CARTESIAN_POINT('Ctrl Pts',(-1.47514528317225,0.493626078830945,
6.1595556612995));
#264451=CARTESIAN_POINT('Ctrl Pts',(-1.47134701874494,0.504834872206382,
6.15870026636689));
#264452=CARTESIAN_POINT('Ctrl Pts',(-1.43223606788575,0.616060375724229,
6.15013613425963));
#264453=CARTESIAN_POINT('Ctrl Pts',(-1.38691635996763,0.712239245048984,
6.14208580235825));
#264454=CARTESIAN_POINT('Ctrl Pts',(-1.29902174483058,0.858048841244031,
6.12891833708842));
#264455=CARTESIAN_POINT('Ctrl Pts',(-1.26248897714576,0.910948445461001,
6.12391547192843));
#264456=CARTESIAN_POINT('Ctrl Pts',(-1.20080679163367,0.989397948564389,
6.11624966212053));
#264457=CARTESIAN_POINT('Ctrl Pts',(-1.17786910808064,1.01659726025983,
6.11354162528091));
#264458=CARTESIAN_POINT('Ctrl Pts',(-1.14072582611868,1.05769456292195,
6.10939709115395));
#264459=CARTESIAN_POINT('Ctrl Pts',(-1.12715345633909,1.07214662429912,
6.10792885481236));
#264460=CARTESIAN_POINT('Ctrl Pts',(-1.10934199121306,1.09040031210602,
6.10606465355531));
#264461=CARTESIAN_POINT('Ctrl Pts',(-1.10535398718619,1.09444280792487,
6.10565117240773));
#264462=CARTESIAN_POINT('Ctrl Pts',(-1.09922437005198,1.10058849816159,
6.105021724754));
#264463=CARTESIAN_POINT('Ctrl Pts',(-1.09709871711301,1.10270742417311,
6.10480454717122));
#264464=CARTESIAN_POINT('Ctrl Pts',(-1.09270613010868,1.10706083609024,
6.10435805271474));
#264465=CARTESIAN_POINT('Ctrl Pts',(-1.09043850050444,1.10929448683168,
6.10412880875691));
#264466=CARTESIAN_POINT('Ctrl Pts',(-1.08524260572583,1.1143811962086,6.10360636966391));
#264467=CARTESIAN_POINT('Ctrl Pts',(-1.08230993985161,1.11722968044911,
6.10331353096193));
#264468=CARTESIAN_POINT('Ctrl Pts',(-1.07460924746732,1.12465054782277,
6.10254977915666));
#264469=CARTESIAN_POINT('Ctrl Pts',(-1.06982319776137,1.1292042415359,6.10208026472591));
#264470=CARTESIAN_POINT('Ctrl Pts',(-1.03678564814397,1.16023926800848,
6.09887323626815));
#264471=CARTESIAN_POINT('Ctrl Pts',(-1.00757999456037,1.18569086175973,
6.09620718836363));
#264472=CARTESIAN_POINT('Ctrl Pts',(-0.968707744519267,1.21709157635007,
6.09282295284952));
#264473=CARTESIAN_POINT('Ctrl Pts',(-0.959887216061676,1.22406010563807,
6.0920654352186));
#264474=CARTESIAN_POINT('Ctrl Pts',(-0.857030882951737,1.30352467453182,
6.08334134968763));
#264475=CARTESIAN_POINT('Ctrl Pts',(-0.755066623329114,1.36512092762015,
6.07570822534614));
#264476=CARTESIAN_POINT('Ctrl Pts',(-0.597442886922968,1.43722723014515,
6.06406984218799));
#264477=CARTESIAN_POINT('Ctrl Pts',(-0.546646606590043,1.45730454093235,
6.06034658884857));
#264478=CARTESIAN_POINT('Ctrl Pts',(-0.482900812913554,1.47869786334938,
6.05564817972521));
#264479=CARTESIAN_POINT('Ctrl Pts',(-0.470848745896762,1.48257951152687,
6.05475886305659));
#264480=CARTESIAN_POINT('Ctrl Pts',(-0.452145866058088,1.48835215892423,
6.05337658536766));
#264481=CARTESIAN_POINT('Ctrl Pts',(-0.445527371360085,1.49034673540911,
6.05288700943861));
#264482=CARTESIAN_POINT('Ctrl Pts',(-0.433986256752834,1.49374106475996,
6.05203246962971));
#264483=CARTESIAN_POINT('Ctrl Pts',(-0.429069574434188,1.4951607735452,
6.05166816146186));
#264484=CARTESIAN_POINT('Ctrl Pts',(-0.418007402686111,1.49829595569729,
6.05084785963008));
#264485=CARTESIAN_POINT('Ctrl Pts',(-0.411858215829622,1.49999792245561,
6.05039143505964));
#264486=CARTESIAN_POINT('Ctrl Pts',(-0.395350600192748,1.50445772777548,
6.04916487957339));
#264487=CARTESIAN_POINT('Ctrl Pts',(-0.384974009857124,1.50714636076748,
6.0483925318378));
#264488=CARTESIAN_POINT('Ctrl Pts',(-0.33811869748617,1.51877139069401,
6.04489832091019));
#264489=CARTESIAN_POINT('Ctrl Pts',(-0.301354286149111,1.52649138082734,
6.04213801313193));
#264490=CARTESIAN_POINT('Ctrl Pts',(-0.108483908898618,1.55975255500343,
6.02754708258555));
#264491=CARTESIAN_POINT('Ctrl Pts',(0.0505287076312072,1.56269865734192,
6.01501648797829));
#264492=CARTESIAN_POINT('Ctrl Pts',(0.239710993218713,1.53726795454164,
6.00054666131007));
#264493=CARTESIAN_POINT('Ctrl Pts',(0.272045959317536,1.53187647077777,
5.99809467836447));
#264494=CARTESIAN_POINT('Ctrl Pts',(0.310706905389217,1.52416719476881,
5.99520665769792));
#264495=CARTESIAN_POINT('Ctrl Pts',(0.317216300699603,1.52282574233159,
5.99472190467843));
#264496=CARTESIAN_POINT('Ctrl Pts',(0.327336207596194,1.52067253162558,
5.99397083314885));
#264497=CARTESIAN_POINT('Ctrl Pts',(0.33095265342718,1.5198895628334,5.99370294002241));
#264498=CARTESIAN_POINT('Ctrl Pts',(0.337673996924638,1.51840924914802,
5.99320603882047));
#264499=CARTESIAN_POINT('Ctrl Pts',(0.340779520636499,1.51771528777115,
5.99297685066957));
#264500=CARTESIAN_POINT('Ctrl Pts',(0.347860498016751,1.51611014028559,
5.99245516477276));
#264501=CARTESIAN_POINT('Ctrl Pts',(0.351834509882506,1.51519284655054,
5.99216301945526));
#264502=CARTESIAN_POINT('Ctrl Pts',(0.362203979803586,1.51275633716185,
5.99140227279873));
#264503=CARTESIAN_POINT('Ctrl Pts',(0.368593585181396,1.51121217293298,
5.99093505228011));
#264504=CARTESIAN_POINT('Ctrl Pts',(0.411948749266478,1.50044327043869,
5.98777415159275));
#264505=CARTESIAN_POINT('Ctrl Pts',(0.448578125712332,1.48990269616049,
5.98514964017806));
#264506=CARTESIAN_POINT('Ctrl Pts',(0.625805278134611,1.43177286890446,
5.97251027938462));
#264507=CARTESIAN_POINT('Ctrl Pts',(0.759482126864277,1.36557645836434,
5.96308836602181));
#264508=CARTESIAN_POINT('Ctrl Pts',(0.915561793950484,1.25817735681684,
5.95022170537104));
#264509=CARTESIAN_POINT('Ctrl Pts',(0.948425911564556,1.23359290205442,
5.94739625490069));
#264510=CARTESIAN_POINT('Ctrl Pts',(0.988499181471111,1.20106691792519,
5.94377758968457));
#264511=CARTESIAN_POINT('Ctrl Pts',(0.99665214115052,1.19431020794068,5.94303193172343));
#264512=CARTESIAN_POINT('Ctrl Pts',(1.00958418624195,1.18336822870272,5.94183359383481));
#264513=CARTESIAN_POINT('Ctrl Pts',(1.01440782510956,1.17923592041396,5.94138307855857));
#264514=CARTESIAN_POINT('Ctrl Pts',(1.02350543414919,1.17134506807683,5.94052656219198));
#264515=CARTESIAN_POINT('Ctrl Pts',(1.02778436002013,1.16759237320069,5.94012080749884));
#264516=CARTESIAN_POINT('Ctrl Pts',(1.03745688906656,1.15901502189924,5.9391969029256));
#264517=CARTESIAN_POINT('Ctrl Pts',(1.04283757767704,1.15417607017538,5.93867815987015));
#264518=CARTESIAN_POINT('Ctrl Pts',(1.056680474666,1.14155107371608,5.93733098230401));
#264519=CARTESIAN_POINT('Ctrl Pts',(1.06509032282664,1.13370854740197,5.9365001668849));
#264520=CARTESIAN_POINT('Ctrl Pts',(1.12386011639745,1.07767222660874,5.93060478248615));
#264521=CARTESIAN_POINT('Ctrl Pts',(1.17100979067523,1.02624186046265,5.92539909596041));
#264522=CARTESIAN_POINT('Ctrl Pts',(1.30267052076028,0.861698690562025,
5.90933031214765));
#264523=CARTESIAN_POINT('Ctrl Pts',(1.37539926577459,0.740101219154342,
5.89814771015041));
#264524=CARTESIAN_POINT('Ctrl Pts',(1.43203068847703,0.607354196561737,
5.88739643025262));
#264525=CARTESIAN_POINT('Ctrl Pts',(1.43330846763704,0.604332565412531,
5.88715246788332));
#264526=CARTESIAN_POINT('Ctrl Pts',(1.4345766835797,0.601306900783166,5.88690895590303));
#264527=CARTESIAN_POINT('Ctrl Pts',(1.43457651448711,0.601307304198132,
5.74991065382822));
#264528=CARTESIAN_POINT('Ctrl Pts',(1.41180695153713,0.655630077304515,
5.7544665194476));
#264529=CARTESIAN_POINT('Ctrl Pts',(1.38594843674904,0.708667726693511,
5.75905554294631));
#264530=CARTESIAN_POINT('Ctrl Pts',(1.33828009928411,0.793770154190295,
5.76656295528035));
#264531=CARTESIAN_POINT('Ctrl Pts',(1.31820785094815,0.826675988765404,
5.7695033392196));
#264532=CARTESIAN_POINT('Ctrl Pts',(1.28915655018164,0.870548113609486,
5.77344569337955));
#264533=CARTESIAN_POINT('Ctrl Pts',(1.28122078522012,0.882185900063432,
5.77449363627982));
#264534=CARTESIAN_POINT('Ctrl Pts',(1.26730896618942,0.902003769100277,
5.77627985810507));
#264535=CARTESIAN_POINT('Ctrl Pts',(1.26140920459256,0.910236039896046,
5.77702236001538));
#264536=CARTESIAN_POINT('Ctrl Pts',(1.25282153391853,0.921975032771996,
5.77808122089535));
#264537=CARTESIAN_POINT('Ctrl Pts',(1.25019860012604,0.925528615681598,
5.77840176484539));
#264538=CARTESIAN_POINT('Ctrl Pts',(1.24561469228472,0.931683906540591,
5.778956939514));
#264539=CARTESIAN_POINT('Ctrl Pts',(1.24366063115574,0.934290692831366,
5.77919204018651));
#264540=CARTESIAN_POINT('Ctrl Pts',(1.23953760697897,0.93975509601168,5.77968480380213));
#264541=CARTESIAN_POINT('Ctrl Pts',(1.23736694113728,0.942611358558621,
5.7799423448059));
#264542=CARTESIAN_POINT('Ctrl Pts',(1.23153622841073,0.950228831547422,
5.78062919244219));
#264543=CARTESIAN_POINT('Ctrl Pts',(1.22785840833142,0.954976463811629,
5.7810572760752));
#264544=CARTESIAN_POINT('Ctrl Pts',(1.21155863938543,0.975767705815738,
5.78293258594268));
#264545=CARTESIAN_POINT('Ctrl Pts',(1.19864835055544,0.991584182083082,
5.78436079627033));
#264546=CARTESIAN_POINT('Ctrl Pts',(1.08772916974027,1.12213852820329,5.79620824773255));
#264547=CARTESIAN_POINT('Ctrl Pts',(0.973805412762164,1.22231978636575,
5.80575577791448));
#264548=CARTESIAN_POINT('Ctrl Pts',(0.816008943042499,1.32479985295201,
5.81839198853135));
#264549=CARTESIAN_POINT('Ctrl Pts',(0.784082562296911,1.34394176064681,
5.82091823074569));
#264550=CARTESIAN_POINT('Ctrl Pts',(0.729908212316746,1.37383497412449,
5.8251826310554));
#264551=CARTESIAN_POINT('Ctrl Pts',(0.708034904521157,1.38523463398125,
5.82689855265673));
#264552=CARTESIAN_POINT('Ctrl Pts',(0.677893886280831,1.4000427547761,5.82925996470202));
#264553=CARTESIAN_POINT('Ctrl Pts',(0.669853373008423,1.40390750727926,
5.82988959876278));
#264554=CARTESIAN_POINT('Ctrl Pts',(0.656313131284455,1.41027295878831,
5.83094962045063));
#264555=CARTESIAN_POINT('Ctrl Pts',(0.650831199682456,1.41281120190569,
5.83137870557954));
#264556=CARTESIAN_POINT('Ctrl Pts',(0.640002896059365,1.41774852543471,
5.83222618540237));
#264557=CARTESIAN_POINT('Ctrl Pts',(0.634657473828427,1.42014945605064,
5.83264450813044));
#264558=CARTESIAN_POINT('Ctrl Pts',(0.622882337572623,1.42535857592253,
5.83356599127214));
#264559=CARTESIAN_POINT('Ctrl Pts',(0.616446963624959,1.42815356823556,
5.83406959144869));
#264560=CARTESIAN_POINT('Ctrl Pts',(0.593908526390495,1.43776167638116,
5.83583345824784));
#264561=CARTESIAN_POINT('Ctrl Pts',(0.577710222744153,1.44434650551658,
5.83710137774138));
#264562=CARTESIAN_POINT('Ctrl Pts',(0.43681501265674,1.49887303322602,5.84813642402534));
#264563=CARTESIAN_POINT('Ctrl Pts',(0.306557510246776,1.53082804601885,
5.85845467701028));
#264564=CARTESIAN_POINT('Ctrl Pts',(0.100195224064705,1.55403864404595,
5.87454796021508));
#264565=CARTESIAN_POINT('Ctrl Pts',(0.026025065254874,1.55704861479061,
5.8802657231426));
#264566=CARTESIAN_POINT('Ctrl Pts',(-0.0610735337307294,1.55435490044076,
5.88672445621464));
#264567=CARTESIAN_POINT('Ctrl Pts',(-0.0740578598872797,1.5537903964849,
5.88768047043065));
#264568=CARTESIAN_POINT('Ctrl Pts',(-0.0919055364529692,1.55279020712327,
5.88898382568743));
#264569=CARTESIAN_POINT('Ctrl Pts',(-0.0967757044030916,1.55249428976086,
5.88933837610575));
#264570=CARTESIAN_POINT('Ctrl Pts',(-0.104978896586389,1.55195710225332,
5.88993362701216));
#264571=CARTESIAN_POINT('Ctrl Pts',(-0.108312648043226,1.55172800032342,
5.89017499331925));
#264572=CARTESIAN_POINT('Ctrl Pts',(-0.114655805699035,1.55127154422388,
5.89063317994442));
#264573=CARTESIAN_POINT('Ctrl Pts',(-0.117665317002589,1.55104617316807,
5.8908501125612));
#264574=CARTESIAN_POINT('Ctrl Pts',(-0.125586291950338,1.55042981399786,
5.89141992489533));
#264575=CARTESIAN_POINT('Ctrl Pts',(-0.130496641383189,1.55002424278468,
5.89177199683449));
#264576=CARTESIAN_POINT('Ctrl Pts',(-0.147716255580492,1.54851957701059,
5.89300281948117));
#264577=CARTESIAN_POINT('Ctrl Pts',(-0.160014695861664,1.5472970933286,
5.89387502824556));
#264578=CARTESIAN_POINT('Ctrl Pts',(-0.259622846841005,1.53619550216969,
5.90089320826332));
#264579=CARTESIAN_POINT('Ctrl Pts',(-0.34598004547932,1.51907968591768,
5.90669544162653));
#264580=CARTESIAN_POINT('Ctrl Pts',(-0.513515191808521,1.4708351981456,
5.91817767831307));
#264581=CARTESIAN_POINT('Ctrl Pts',(-0.594445555122932,1.44003025540019,
5.92384110794829));
#264582=CARTESIAN_POINT('Ctrl Pts',(-0.712488709514929,1.38344388420044,
5.93270686741078));
#264583=CARTESIAN_POINT('Ctrl Pts',(-0.751736218238954,1.36251575173322,
5.93576237472295));
#264584=CARTESIAN_POINT('Ctrl Pts',(-0.79946059501787,1.33437732309553,
5.93964473527473));
#264585=CARTESIAN_POINT('Ctrl Pts',(-0.808831239408744,1.32871821643117,
5.94041530704239));
#264586=CARTESIAN_POINT('Ctrl Pts',(-0.823653889917207,1.31955164057771,
5.94164787498295));
#264587=CARTESIAN_POINT('Ctrl Pts',(-0.829145175752436,1.31610810260629,
5.94210752728332));
#264588=CARTESIAN_POINT('Ctrl Pts',(-0.839472076276543,1.3095419107176,
5.94297777585417));
#264589=CARTESIAN_POINT('Ctrl Pts',(-0.844312206399271,1.30642653037365,
5.94338809776495));
#264590=CARTESIAN_POINT('Ctrl Pts',(-0.855209122891349,1.29932681226943,
5.94431749154319));
#264591=CARTESIAN_POINT('Ctrl Pts',(-0.861255532406906,1.29532687518016,
5.94483713926254));
#264592=CARTESIAN_POINT('Ctrl Pts',(-0.876725669093412,1.28493657140105,
5.94617703026707));
#264593=CARTESIAN_POINT('Ctrl Pts',(-0.886107443914718,1.27848483620163,
5.9469995688791));
#264594=CARTESIAN_POINT('Ctrl Pts',(-0.947728311148291,1.23510481133937,
5.95246967027297));
#264595=CARTESIAN_POINT('Ctrl Pts',(-0.997710069147358,1.19509219453146,
5.95723511038795));
#264596=CARTESIAN_POINT('Ctrl Pts',(-1.11598861430016,1.08780259006151,
5.96937179304928));
#264597=CARTESIAN_POINT('Ctrl Pts',(-1.18080297379458,1.01707756660921,
5.97684597219249));
#264598=CARTESIAN_POINT('Ctrl Pts',(-1.27351028392199,0.895021840161294,
5.98867373891221));
#264599=CARTESIAN_POINT('Ctrl Pts',(-1.30575501748159,0.847288556945824,
5.99307022136888));
#264600=CARTESIAN_POINT('Ctrl Pts',(-1.34117731913795,0.788007435196004,
5.99817649747513));
#264601=CARTESIAN_POINT('Ctrl Pts',(-1.3469627845853,0.778076858113244,
5.99902046879497));
#264602=CARTESIAN_POINT('Ctrl Pts',(-1.35493256617952,0.764041613367275,
6.00019640535912));
#264603=CARTESIAN_POINT('Ctrl Pts',(-1.35720917065368,0.759990206811264,
6.00053389786424));
#264604=CARTESIAN_POINT('Ctrl Pts',(-1.3610697066289,0.753047390055815,
6.00110884453054));
#264605=CARTESIAN_POINT('Ctrl Pts',(-1.36266265370051,0.750161056731348,
6.00134686549667));
#264606=CARTESIAN_POINT('Ctrl Pts',(-1.36572057929681,0.744578380764795,
6.00180528211072));
#264607=CARTESIAN_POINT('Ctrl Pts',(-1.36718676185103,0.741882756560779,
6.00202575753861));
#264608=CARTESIAN_POINT('Ctrl Pts',(-1.37069988566621,0.73537797940553,
6.00255572686452));
#264609=CARTESIAN_POINT('Ctrl Pts',(-1.37273895409416,0.731564566030282,
6.00286472744016));
#264610=CARTESIAN_POINT('Ctrl Pts',(-1.38019015543334,0.717488670432404,
6.00399926211218));
#264611=CARTESIAN_POINT('Ctrl Pts',(-1.38550350642506,0.707173891056844,
6.00481887936912));
#264612=CARTESIAN_POINT('Ctrl Pts',(-1.43919734741206,0.600009622085865,
6.0132234902045));
#264613=CARTESIAN_POINT('Ctrl Pts',(-1.47746462869008,0.498404016884063,
6.02027769473693));
#264614=CARTESIAN_POINT('Ctrl Pts',(-1.5313287821953,0.292479790475092,
6.03429394692431));
#264615=CARTESIAN_POINT('Ctrl Pts',(-1.54751808866646,0.188932480653449,
6.04122168592858));
#264616=CARTESIAN_POINT('Ctrl Pts',(-1.55402229161874,0.0694525188932073,
6.04955785862182));
#264617=CARTESIAN_POINT('Ctrl Pts',(-1.55462402921913,0.0543418335736241,
6.0506178362248));
#264618=CARTESIAN_POINT('Ctrl Pts',(-1.55519079218697,0.0318736557810259,
6.05220346647178));
#264619=CARTESIAN_POINT('Ctrl Pts',(-1.55532409756881,0.0245209748386396,
6.05272387752729));
#264620=CARTESIAN_POINT('Ctrl Pts',(-1.55546890945959,0.0114009480816709,
6.05365532295415));
#264621=CARTESIAN_POINT('Ctrl Pts',(-1.55550048769016,0.00563392131872312,
6.05406572381775));
#264622=CARTESIAN_POINT('Ctrl Pts',(-1.55549944508379,-0.00655278324734221,
6.0549350968532));
#264623=CARTESIAN_POINT('Ctrl Pts',(-1.55545915372167,-0.0129723339010835,
6.05539430070872));
#264624=CARTESIAN_POINT('Ctrl Pts',(-1.55524616967184,-0.0300557611713273,
6.0566197336781));
#264625=CARTESIAN_POINT('Ctrl Pts',(-1.55500354024369,-0.0407182559079988,
6.05738812754367));
#264626=CARTESIAN_POINT('Ctrl Pts',(-1.55329993415077,-0.0922686507356349,
6.06112097744222));
#264627=CARTESIAN_POINT('Ctrl Pts',(-1.5503359179664,-0.133087012044085,
6.06413170916431));
#264628=CARTESIAN_POINT('Ctrl Pts',(-1.52914025500215,-0.321667487676258,
6.0783112911403));
#264629=CARTESIAN_POINT('Ctrl Pts',(-1.49136253134308,-0.46643782989504,
6.09007018255088));
#264630=CARTESIAN_POINT('Ctrl Pts',(-1.41905879998039,-0.638169093086119,
6.1042558048259));
#264631=CARTESIAN_POINT('Ctrl Pts',(-1.40325369535684,-0.672210759999545,
6.10707424891338));
#264632=CARTESIAN_POINT('Ctrl Pts',(-1.38323788402782,-0.711531270015986,
6.1103113770089));
#264633=CARTESIAN_POINT('Ctrl Pts',(-1.3802069597247,-0.717392880136795,
6.11079344491076));
#264634=CARTESIAN_POINT('Ctrl Pts',(-1.37522663822729,-0.726876094037405,
6.11157233636648));
#264635=CARTESIAN_POINT('Ctrl Pts',(-1.37330006023757,-0.730509485345017,
6.1118705146768));
#264636=CARTESIAN_POINT('Ctrl Pts',(-1.36983869633044,-0.736975286810254,
6.1124006425734));
#264637=CARTESIAN_POINT('Ctrl Pts',(-1.3683095041684,-0.739810603353431,
6.11263293470359));
#264638=CARTESIAN_POINT('Ctrl Pts',(-1.3649747403771,-0.745947967920077,
6.11313537206751));
#264639=CARTESIAN_POINT('Ctrl Pts',(-1.36316599255241,-0.749248216729731,
6.11340531230543));
#264640=CARTESIAN_POINT('Ctrl Pts',(-1.35805285445855,-0.758497862705271,
6.11416130786497));
#264641=CARTESIAN_POINT('Ctrl Pts',(-1.35472131826895,-0.764432284504369,
6.11464567830022));
#264642=CARTESIAN_POINT('Ctrl Pts',(-1.334210215944,-0.800413180279256,
6.11757960881499));
#264643=CARTESIAN_POINT('Ctrl Pts',(-1.31606909580525,-0.82990406590892,
6.11997223452674));
#264644=CARTESIAN_POINT('Ctrl Pts',(-1.2507873815931,-0.928496024990666,
6.12801729146392));
#264645=CARTESIAN_POINT('Ctrl Pts',(-1.19906559260512,-0.994393284479451,
6.13348066747959));
#264646=CARTESIAN_POINT('Ctrl Pts',(-1.07091092811761,-1.13304431993926,
6.14591691450504));
#264647=CARTESIAN_POINT('Ctrl Pts',(-0.991893969471411,-1.20282216477062,
6.15289694048487));
#264648=CARTESIAN_POINT('Ctrl Pts',(-0.896738851148734,-1.27105566128855,
6.16107437810008));
#264649=CARTESIAN_POINT('Ctrl Pts',(-0.886947588750496,-1.27790728227964,
6.16191304189168));
#264650=CARTESIAN_POINT('Ctrl Pts',(-0.870950596091194,-1.28882906773578,
6.16327935965435));
#264651=CARTESIAN_POINT('Ctrl Pts',(-0.86479284395614,-1.29296892471322,
6.16380437894695));
#264652=CARTESIAN_POINT('Ctrl Pts',(-0.853790332077212,-1.3002521558323,
6.16474097235305));
#264653=CARTESIAN_POINT('Ctrl Pts',(-0.8489572067864,-1.30341292739308,
6.16515188630179));
#264654=CARTESIAN_POINT('Ctrl Pts',(-0.838744861992011,-1.31001070789687,
6.16601914337189));
#264655=CARTESIAN_POINT('Ctrl Pts',(-0.833361874563006,-1.31344165538679,
6.16647570153448));
#264656=CARTESIAN_POINT('Ctrl Pts',(-0.819068431820425,-1.32242860615638,
6.16768657598666));
#264657=CARTESIAN_POINT('Ctrl Pts',(-0.810122707848137,-1.32792759688571,
6.16844296684248));
#264658=CARTESIAN_POINT('Ctrl Pts',(-0.767698548077798,-1.35341775800188,
6.17202393764307));
#264659=CARTESIAN_POINT('Ctrl Pts',(-0.733534626916184,-1.37223435959762,
6.17489034764616));
#264660=CARTESIAN_POINT('Ctrl Pts',(-0.564657761904698,-1.45713813560855,
6.18899145817112));
#264661=CARTESIAN_POINT('Ctrl Pts',(-0.42157343428595,-1.50477619778259,
6.2008391547421));
#264662=CARTESIAN_POINT('Ctrl Pts',(-0.236034660355262,-1.53796949024919,
6.21519928309077));
#264663=CARTESIAN_POINT('Ctrl Pts',(-0.197893471849304,-1.54334095333417,
6.21809367851642));
#264664=CARTESIAN_POINT('Ctrl Pts',(-0.152977552361988,-1.54797360731217,
6.22140692768028));
#264665=CARTESIAN_POINT('Ctrl Pts',(-0.14636207657615,-1.5486131108868,
6.221892504896));
#264666=CARTESIAN_POINT('Ctrl Pts',(-0.135632464236921,-1.54958094815667,
6.22267593050289));
#264667=CARTESIAN_POINT('Ctrl Pts',(-0.131520855827859,-1.54993533600361,
6.22297515898371));
#264668=CARTESIAN_POINT('Ctrl Pts',(-0.124196093301675,-1.55053731502337,
6.22350642476018));
#264669=CARTESIAN_POINT('Ctrl Pts',(-0.120983540116742,-1.55079128789203,
6.22373881061804));
#264670=CARTESIAN_POINT('Ctrl Pts',(-0.114027742097437,-1.55131944169977,
6.2242406188666));
#264671=CARTESIAN_POINT('Ctrl Pts',(-0.110284291180253,-1.55159005929032,
6.22450984083079));
#264672=CARTESIAN_POINT('Ctrl Pts',(-0.0997973042108043,-1.55231002837404,
6.22526178711578));
#264673=CARTESIAN_POINT('Ctrl Pts',(-0.0930516552347153,-1.55272899116993,
6.22574285538301));
#264674=CARTESIAN_POINT('Ctrl Pts',(-0.0526068693072738,-1.55497643860261,
6.22861269498564));
#264675=CARTESIAN_POINT('Ctrl Pts',(-0.0188551430630736,-1.55575194808541,
6.23094738317539));
#264676=CARTESIAN_POINT('Ctrl Pts',(0.191501298438252,-1.55373711752684,
6.24527279663668));
#264677=CARTESIAN_POINT('Ctrl Pts',(0.366529471419132,-1.52198541230324,
6.25635598380528));
#264678=CARTESIAN_POINT('Ctrl Pts',(0.553100067501514,-1.45400867752475,
6.27007414253767));
#264679=CARTESIAN_POINT('Ctrl Pts',(0.573537611795688,-1.44606896228839,
6.27160172034684));
#264680=CARTESIAN_POINT('Ctrl Pts',(0.601917957479531,-1.43434729809278,
6.27376142898982));
#264681=CARTESIAN_POINT('Ctrl Pts',(0.610007533615243,-1.4309256452903,
6.27438147415663));
#264682=CARTESIAN_POINT('Ctrl Pts',(0.623033575706379,-1.42528547965077,
6.27538728972449));
#264683=CARTESIAN_POINT('Ctrl Pts',(0.627988287562152,-1.42310935781394,
6.27577161646394));
#264684=CARTESIAN_POINT('Ctrl Pts',(0.638286731446648,-1.41852200105435,
6.2765741441187));
#264685=CARTESIAN_POINT('Ctrl Pts',(0.643628379213044,-1.41610632607762,
6.27699249168142));
#264686=CARTESIAN_POINT('Ctrl Pts',(0.656226386956023,-1.41032307423207,
6.27798416631339));
#264687=CARTESIAN_POINT('Ctrl Pts',(0.66347061416635,-1.40692963020744,
6.27855837480454));
#264688=CARTESIAN_POINT('Ctrl Pts',(0.687522377090093,-1.39543589454731,
6.28047830867178));
#264689=CARTESIAN_POINT('Ctrl Pts',(0.704209720761646,-1.38708938707098,
6.28183250063242));
#264690=CARTESIAN_POINT('Ctrl Pts',(0.743550666022141,-1.36651933913611,
6.28507959997411));
#264691=CARTESIAN_POINT('Ctrl Pts',(0.766058271678354,-1.35403001421563,
6.28698140805058));
#264692=CARTESIAN_POINT('Ctrl Pts',(0.917605537363094,-1.26494924863414,
6.30009522657793));
#264693=CARTESIAN_POINT('Ctrl Pts',(1.03527503212876,-1.17059290372971,
6.3119445922639));
#264694=CARTESIAN_POINT('Ctrl Pts',(1.16385246951167,-1.0327203076879,6.32630784546666));
#264695=CARTESIAN_POINT('Ctrl Pts',(1.18906945241916,-1.00358270876691,
6.32920353471376));
#264696=CARTESIAN_POINT('Ctrl Pts',(1.21734097895795,-0.968351884577592,
6.33251808115515));
#264697=CARTESIAN_POINT('Ctrl Pts',(1.22146788821302,-0.963141024819116,
6.3330037193182));
#264698=CARTESIAN_POINT('Ctrl Pts',(1.2281028550902,-0.954652114442307,
6.3337872236471));
#264699=CARTESIAN_POINT('Ctrl Pts',(1.23063143399829,-0.951390328419722,
6.33408647034435));
#264700=CARTESIAN_POINT('Ctrl Pts',(1.23511128678741,-0.945563717713477,
6.33461775589966));
#264701=CARTESIAN_POINT('Ctrl Pts',(1.23706759690874,-0.943002861286291,
6.33485014342425));
#264702=CARTESIAN_POINT('Ctrl Pts',(1.24128499793184,-0.93744647247841,
6.33535194094589));
#264703=CARTESIAN_POINT('Ctrl Pts',(1.24354320844632,-0.934448834546821,
6.33562115059495));
#264704=CARTESIAN_POINT('Ctrl Pts',(1.24983707636303,-0.926030883822506,
6.33637302751293));
#264705=CARTESIAN_POINT('Ctrl Pts',(1.25384836018243,-0.920592314411871,
6.33685403922019));
#264706=CARTESIAN_POINT('Ctrl Pts',(1.27767042080742,-0.887849380866199,
6.33972279858213));
#264707=CARTESIAN_POINT('Ctrl Pts',(1.29662596430493,-0.859930095167336,
6.34205651048334));
#264708=CARTESIAN_POINT('Ctrl Pts',(1.40886595318109,-0.682452361077834,
6.35635658870539));
#264709=CARTESIAN_POINT('Ctrl Pts',(1.47707432958275,-0.518562963539632,
6.36741842354178));
#264710=CARTESIAN_POINT('Ctrl Pts',(1.5213142930603,-0.325077958816658,
6.38112630161971));
#264711=CARTESIAN_POINT('Ctrl Pts',(1.52579753660768,-0.303339164458439,
6.38267241735419));
#264712=CARTESIAN_POINT('Ctrl Pts',(1.53141188168072,-0.272829350451758,
6.38485418796489));
#264713=CARTESIAN_POINT('Ctrl Pts',(1.53293579996874,-0.264132605411793,
6.38547742388281));
#264714=CARTESIAN_POINT('Ctrl Pts',(1.53527557458462,-0.250077061660111,
6.3864870355796));
#264715=CARTESIAN_POINT('Ctrl Pts',(1.53613761871812,-0.244726054374228,
6.38687194625963));
#264716=CARTESIAN_POINT('Ctrl Pts',(1.53787287635663,-0.233584165689512,
6.38767460144337));
#264717=CARTESIAN_POINT('Ctrl Pts',(1.53874138608654,-0.227792649823775,
6.38809248764551));
#264718=CARTESIAN_POINT('Ctrl Pts',(1.54071371698038,-0.214114252100162,
6.38908109957948));
#264719=CARTESIAN_POINT('Ctrl Pts',(1.5417897057404,-0.206223591147435,
6.3896526917213));
#264720=CARTESIAN_POINT('Ctrl Pts',(1.5451571337787,-0.180027796294164,
6.39155478977296));
#264721=CARTESIAN_POINT('Ctrl Pts',(1.54718344155232,-0.161690813930811,
6.39289354811955));
#264722=CARTESIAN_POINT('Ctrl Pts',(1.55122017601129,-0.118066018562273,
6.39609723055154));
#264723=CARTESIAN_POINT('Ctrl Pts',(1.5529390133741,-0.0927572297755599,
6.39797074142814));
#264724=CARTESIAN_POINT('Ctrl Pts',(1.56055818214423,0.0828679691374859,
6.41107826785458));
#264725=CARTESIAN_POINT('Ctrl Pts',(1.54523986935127,0.233298120599414,
6.42295609127557));
#264726=CARTESIAN_POINT('Ctrl Pts',(1.49913029790243,0.416765548773638,
6.43737179825731));
#264727=CARTESIAN_POINT('Ctrl Pts',(1.48826951949714,0.454026026771004,
6.44028882961641));
#264728=CARTESIAN_POINT('Ctrl Pts',(1.47392367033915,0.497165599076847,
6.44362480996212));
#264729=CARTESIAN_POINT('Ctrl Pts',(1.47178113440391,0.503472854818314,
6.44411149011784));
#264730=CARTESIAN_POINT('Ctrl Pts',(1.46824420866228,0.513669408261775,
6.44489634019957));
#264731=CARTESIAN_POINT('Ctrl Pts',(1.46687475475194,0.517567166843468,
6.44519589821853));
#264732=CARTESIAN_POINT('Ctrl Pts',(1.46440932251141,0.524495923211836,
6.44572752200996));
#264733=CARTESIAN_POINT('Ctrl Pts',(1.46331943955215,0.527529009501955,
6.44595993823178));
#264734=CARTESIAN_POINT('Ctrl Pts',(1.46094103086649,0.534083904337845,
6.44646155339418));
#264735=CARTESIAN_POINT('Ctrl Pts',(1.45964919597237,0.537604443846408,
6.44673055332526));
#264736=CARTESIAN_POINT('Ctrl Pts',(1.45599858235928,0.547443018496049,
6.44748124927357));
#264737=CARTESIAN_POINT('Ctrl Pts',(1.45361139066549,0.55375053920999,6.44796129809443));
#264738=CARTESIAN_POINT('Ctrl Pts',(1.44584453024801,0.573876043197192,
6.44948969276664));
#264739=CARTESIAN_POINT('Ctrl Pts',(1.44030845088325,0.587632253594381,
6.45052937770318));
#264740=CARTESIAN_POINT('Ctrl Pts',(1.43457668334549,0.60130690134194,6.45155991302018));
#264741=CARTESIAN_POINT('Origin',(0.,0.,-1.29405622560371));
#264742=CARTESIAN_POINT('',(1.4345768221925,0.601306570085576,7.28923406038337));
#264743=CARTESIAN_POINT('',(1.43457650415244,0.601307328854198,7.14927790964297));
#264744=CARTESIAN_POINT('',(1.43457668357355,0.601306900797845,-1.29405622560371));
#264745=CARTESIAN_POINT('',(-1.55751602490984,0.000817960485851865,6.89405622560371));
#264746=CARTESIAN_POINT('Ctrl Pts',(1.43457682219249,0.601306570085596,
7.28923406038337));
#264747=CARTESIAN_POINT('Ctrl Pts',(1.44980351843734,0.564979234582981,
7.28657956429081));
#264748=CARTESIAN_POINT('Ctrl Pts',(1.46365495195722,0.52806263480983,7.28389089081866));
#264749=CARTESIAN_POINT('Ctrl Pts',(1.48191627802783,0.473122508224971,
7.27987552565566));
#264750=CARTESIAN_POINT('Ctrl Pts',(1.48742440572936,0.455509988635428,
7.27858631906853));
#264751=CARTESIAN_POINT('Ctrl Pts',(1.49467709042677,0.430783218925999,
7.27677168274819));
#264752=CARTESIAN_POINT('Ctrl Pts',(1.49668686348088,0.423747820942215,
7.27625485183045));
#264753=CARTESIAN_POINT('Ctrl Pts',(1.50008137180983,0.411539550455861,
7.27535698876009));
#264754=CARTESIAN_POINT('Ctrl Pts',(1.50148918227773,0.406373175586266,
7.27497670898746));
#264755=CARTESIAN_POINT('Ctrl Pts',(1.50436096109021,0.395615662351214,
7.27418417387299));
#264756=CARTESIAN_POINT('Ctrl Pts',(1.50582049732888,0.390023437391185,
7.2737717821648));
#264757=CARTESIAN_POINT('Ctrl Pts',(1.50918820865661,0.376819297021503,
7.27279705461033));
#264758=CARTESIAN_POINT('Ctrl Pts',(1.51106999725939,0.369200881570351,
7.27223387958147));
#264759=CARTESIAN_POINT('Ctrl Pts',(1.51710528139918,0.34394773934382,7.27036429166985));
#264760=CARTESIAN_POINT('Ctrl Pts',(1.52100818995956,0.326255293828729,
7.26904992232478));
#264761=CARTESIAN_POINT('Ctrl Pts',(1.54049053092949,0.229973750910464,
7.26186964160514));
#264762=CARTESIAN_POINT('Ctrl Pts',(1.55028696858727,0.150351130317674,
7.25582347061479));
#264763=CARTESIAN_POINT('Ctrl Pts',(1.55827222221061,-0.0260542502123737,
7.24224319494439));
#264764=CARTESIAN_POINT('Ctrl Pts',(1.55365686578769,-0.122643212766432,
7.23468248039912));
#264765=CARTESIAN_POINT('Ctrl Pts',(1.53471228532792,-0.256371141204358,
7.22439181526886));
#264766=CARTESIAN_POINT('Ctrl Pts',(1.5278829947406,-0.294350353101164,
7.2214920862619));
#264767=CARTESIAN_POINT('Ctrl Pts',(1.51823964181167,-0.338485099496349,
7.21817753884491));
#264768=CARTESIAN_POINT('Ctrl Pts',(1.51679037739624,-0.344921335538409,
7.21769556919996));
#264769=CARTESIAN_POINT('Ctrl Pts',(1.51437734263109,-0.355328307549209,
7.21691872867417));
#264770=CARTESIAN_POINT('Ctrl Pts',(1.51343882013,-0.359304718558758,7.21662249137146));
#264771=CARTESIAN_POINT('Ctrl Pts',(1.51174131779941,-0.366372171276095,
7.2160970752956));
#264772=CARTESIAN_POINT('Ctrl Pts',(1.51098850913695,-0.369464620467438,
7.21586755163463));
#264773=CARTESIAN_POINT('Ctrl Pts',(1.50934116187564,-0.376142475060763,
7.21537274391553));
#264774=CARTESIAN_POINT('Ctrl Pts',(1.50844333872061,-0.379727006041249,
7.21510765096319));
#264775=CARTESIAN_POINT('Ctrl Pts',(1.5059006669027,-0.389727208140776,
7.21436942384523));
#264776=CARTESIAN_POINT('Ctrl Pts',(1.50422757777804,-0.396135726473404,
7.21389787631992));
#264777=CARTESIAN_POINT('Ctrl Pts',(1.49413664832617,-0.433801555090046,
7.21113436112351));
#264778=CARTESIAN_POINT('Ctrl Pts',(1.48478492887269,-0.464803415669506,
7.20889220545473));
#264779=CARTESIAN_POINT('Ctrl Pts',(1.4260832831902,-0.639485621365874,
7.19632423251459));
#264780=CARTESIAN_POINT('Ctrl Pts',(1.35686271881169,-0.775620951241863,
7.18670765682073));
#264781=CARTESIAN_POINT('Ctrl Pts',(1.24400408316791,-0.934827104907211,
7.17348550232125));
#264782=CARTESIAN_POINT('Ctrl Pts',(1.21755533854447,-0.969023372149023,
7.17051536321887));
#264783=CARTESIAN_POINT('Ctrl Pts',(1.18256389585577,-1.01056729328593,
7.16671092483038));
#264784=CARTESIAN_POINT('Ctrl Pts',(1.17531782166127,-1.01898558811702,
7.16592938978439));
#264785=CARTESIAN_POINT('Ctrl Pts',(1.16366968831985,-1.0322285341878,7.16468250086537));
#264786=CARTESIAN_POINT('Ctrl Pts',(1.15932622761147,-1.03710442382538,
7.16421957951519));
#264787=CARTESIAN_POINT('Ctrl Pts',(1.1511556392524,-1.04616111033051,7.16335244141609));
#264788=CARTESIAN_POINT('Ctrl Pts',(1.14733609830745,-1.05034863284039,
7.16294854828634));
#264789=CARTESIAN_POINT('Ctrl Pts',(1.13876972896462,-1.05963782169625,
7.16204590495589));
#264790=CARTESIAN_POINT('Ctrl Pts',(1.13401135776446,-1.06472862566507,
7.16154666784467));
#264791=CARTESIAN_POINT('Ctrl Pts',(1.11995694726716,-1.07956382596798,
7.16007824939796));
#264792=CARTESIAN_POINT('Ctrl Pts',(1.11056858721707,-1.08921944985359,
7.15910510005958));
#264793=CARTESIAN_POINT('Ctrl Pts',(1.08901498001704,-1.11081826568846,
7.15688769233486));
#264794=CARTESIAN_POINT('Ctrl Pts',(1.07677656674325,-1.12268563225708,
7.15564028887177));
#264795=CARTESIAN_POINT('Ctrl Pts',(1.03595626132954,-1.16098683240311,
7.15151629245127));
#264796=CARTESIAN_POINT('Ctrl Pts',(1.00657885799072,-1.1865472344246,7.14860518128167));
#264797=CARTESIAN_POINT('Ctrl Pts',(0.913670224496102,-1.26144911397863,
7.13956943016963));
#264798=CARTESIAN_POINT('Ctrl Pts',(0.847249784712435,-1.30698614250228,
7.13333326578048));
#264799=CARTESIAN_POINT('Ctrl Pts',(0.704178867092309,-1.38956895390409,
7.12052553051608));
#264800=CARTESIAN_POINT('Ctrl Pts',(0.627390403625713,-1.4258873899547,
7.11397574231193));
#264801=CARTESIAN_POINT('Ctrl Pts',(0.540634244719874,-1.45854621330736,
7.10716491698234));
#264802=CARTESIAN_POINT('Ctrl Pts',(0.533232397201672,-1.46126851074942,
7.1065884075079));
#264803=CARTESIAN_POINT('Ctrl Pts',(0.522032304066222,-1.4652913141117,
7.1057232813387));
#264804=CARTESIAN_POINT('Ctrl Pts',(0.518249353345248,-1.46663355015495,
7.10543231148562));
#264805=CARTESIAN_POINT('Ctrl Pts',(0.511462736045827,-1.46901198587162,
7.10491257500398));
#264806=CARTESIAN_POINT('Ctrl Pts',(0.50846106464916,-1.47005363554193,
7.10468349336731));
#264807=CARTESIAN_POINT('Ctrl Pts',(0.501911855616568,-1.47230390344355,
7.10418540366442));
#264808=CARTESIAN_POINT('Ctrl Pts',(0.498363140151507,-1.47350889927565,
7.10391660983425));
#264809=CARTESIAN_POINT('Ctrl Pts',(0.488301147792028,-1.47688502414884,
7.10315748672371));
#264810=CARTESIAN_POINT('Ctrl Pts',(0.481777693494745,-1.47902591058986,
7.10266889240957));
#264811=CARTESIAN_POINT('Ctrl Pts',(0.440048746574028,-1.49241525217801,
7.09956488126824));
#264812=CARTESIAN_POINT('Ctrl Pts',(0.404462467550888,-1.50245028302582,
7.09701469974492));
#264813=CARTESIAN_POINT('Ctrl Pts',(0.316362647524366,-1.523935797338,7.09085932684453));
#264814=CARTESIAN_POINT('Ctrl Pts',(0.263548412745544,-1.53395197480168,
7.087303362482));
#264815=CARTESIAN_POINT('Ctrl Pts',(0.0863369584395551,-1.55813474255322,
7.07551464856515));
#264816=CARTESIAN_POINT('Ctrl Pts',(-0.0392162564204408,-1.56003060934021,
7.06735179576436));
#264817=CARTESIAN_POINT('Ctrl Pts',(-0.173350459862813,-1.54584129878287,
7.05799061092119));
#264818=CARTESIAN_POINT('Ctrl Pts',(-0.183056160874355,-1.5447220259772,
7.05730989789165));
#264819=CARTESIAN_POINT('Ctrl Pts',(-0.203488662192368,-1.5421704577941,
7.0558693254736));
#264820=CARTESIAN_POINT('Ctrl Pts',(-0.214212303050778,-1.54071750665779,
7.055108876351));
#264821=CARTESIAN_POINT('Ctrl Pts',(-0.231875947900591,-1.53813628064714,
7.05384861515069));
#264822=CARTESIAN_POINT('Ctrl Pts',(-0.238825142958862,-1.53707261416418,
7.05335084032911));
#264823=CARTESIAN_POINT('Ctrl Pts',(-0.251367648035335,-1.53506570814196,
7.05244874767385));
#264824=CARTESIAN_POINT('Ctrl Pts',(-0.256963496349401,-1.53413890595804,
7.05204495623546));
#264825=CARTESIAN_POINT('Ctrl Pts',(-0.268945449604897,-1.53208702189175,
7.05117745086141));
#264826=CARTESIAN_POINT('Ctrl Pts',(-0.275329818535755,-1.53095257476621,
7.05071344698351));
#264827=CARTESIAN_POINT('Ctrl Pts',(-0.292714567407997,-1.52775119425046,
7.04944502247785));
#264828=CARTESIAN_POINT('Ctrl Pts',(-0.303699840449521,-1.52560542875238,
7.04863811472978));
#264829=CARTESIAN_POINT('Ctrl Pts',(-0.3628927446723,-1.51337856776211,
7.04426007127144));
#264830=CARTESIAN_POINT('Ctrl Pts',(-0.410618861651596,-1.50113190230789,
7.04062059963461));
#264831=CARTESIAN_POINT('Ctrl Pts',(-0.564861692088216,-1.45364658881012,
7.02848372873606));
#264832=CARTESIAN_POINT('Ctrl Pts',(-0.668151969939364,-1.4091572707714,
7.01972644472135));
#264833=CARTESIAN_POINT('Ctrl Pts',(-0.821178600096131,-1.322611668823,
7.00615400190544));
#264834=CARTESIAN_POINT('Ctrl Pts',(-0.874641579021902,-1.28788204446359,
7.00129040258078));
#264835=CARTESIAN_POINT('Ctrl Pts',(-0.932214900820325,-1.24523843313029,
6.9960257821059));
#264836=CARTESIAN_POINT('Ctrl Pts',(-0.938563377745482,-1.24046046683518,
6.99544490834053));
#264837=CARTESIAN_POINT('Ctrl Pts',(-0.948073631203309,-1.23318808472561,
6.99457453775762));
#264838=CARTESIAN_POINT('Ctrl Pts',(-0.951262659299366,-1.2307297902086,
6.99428264628133));
#264839=CARTESIAN_POINT('Ctrl Pts',(-0.95681758258171,-1.22641323116009,
6.99377419655252));
#264840=CARTESIAN_POINT('Ctrl Pts',(-0.959187660756776,-1.22456046479528,
6.99355726002511));
#264841=CARTESIAN_POINT('Ctrl Pts',(-0.96437944529423,-1.2204775582992,
6.99308205609744));
#264842=CARTESIAN_POINT('Ctrl Pts',(-0.967198794575505,-1.21824450637017,
6.99282399965478));
#264843=CARTESIAN_POINT('Ctrl Pts',(-0.974789562867427,-1.2121893137751,
6.99212912982872));
#264844=CARTESIAN_POINT('Ctrl Pts',(-0.979546302858022,-1.20834873615893,
6.99169360192371));
#264845=CARTESIAN_POINT('Ctrl Pts',(-0.990201661037585,-1.19964136128516,
6.9907174700733));
#264846=CARTESIAN_POINT('Ctrl Pts',(-0.996087330823707,-1.1947588713179,
6.99017791987711));
#264847=CARTESIAN_POINT('Ctrl Pts',(-1.01418301167748,-1.17952082557038,
6.98851704219005));
#264848=CARTESIAN_POINT('Ctrl Pts',(-1.02626975563306,-1.16901967276755,
6.98740481155359));
#264849=CARTESIAN_POINT('Ctrl Pts',(-1.07330159088528,-1.12686590671051,
6.98305529545409));
#264850=CARTESIAN_POINT('Ctrl Pts',(-1.10696471594757,-1.09381577668366,
6.97989357237831));
#264851=CARTESIAN_POINT('Ctrl Pts',(-1.1840559434951,-1.01091753964176,
6.97238029030133));
#264852=CARTESIAN_POINT('Ctrl Pts',(-1.22590920149169,-0.959734154720861,
6.9680656534008));
#264853=CARTESIAN_POINT('Ctrl Pts',(-1.3154604921601,-0.834765592845174,
6.95790059055422));
#264854=CARTESIAN_POINT('Ctrl Pts',(-1.36041206472146,-0.759305903550564,
6.95202242856061));
#264855=CARTESIAN_POINT('Ctrl Pts',(-1.403971165674,-0.669766280299547,
6.94506804150315));
#264856=CARTESIAN_POINT('Ctrl Pts',(-1.40905461392838,-0.659004541281474,
6.94423274570462));
#264857=CARTESIAN_POINT('Ctrl Pts',(-1.41707987438916,-0.641497476987945,
6.94287421868809));
#264858=CARTESIAN_POINT('Ctrl Pts',(-1.42009826241936,-0.634787606287648,
6.94235361754942));
#264859=CARTESIAN_POINT('Ctrl Pts',(-1.42537267035586,-0.622836701043467,
6.94142638720285));
#264860=CARTESIAN_POINT('Ctrl Pts',(-1.42764768549906,-0.617604153212343,
6.94102041464069));
#264861=CARTESIAN_POINT('Ctrl Pts',(-1.43236828068934,-0.606581294118535,
6.94016513852163));
#264862=CARTESIAN_POINT('Ctrl Pts',(-1.43480764956757,-0.600788452368654,
6.93971563284157));
#264863=CARTESIAN_POINT('Ctrl Pts',(-1.44114729873036,-0.585474656329408,
6.93852715202588));
#264864=CARTESIAN_POINT('Ctrl Pts',(-1.44498828118243,-0.575929655106208,
6.9377861945832));
#264865=CARTESIAN_POINT('Ctrl Pts',(-1.46240779871984,-0.531369994085493,
6.93432566127589));
#264866=CARTESIAN_POINT('Ctrl Pts',(-1.4748090098645,-0.49591186200197,
6.93156733891674));
#264867=CARTESIAN_POINT('Ctrl Pts',(-1.53046738830976,-0.316138069170886,
6.91754578495121));
#264868=CARTESIAN_POINT('Ctrl Pts',(-1.55387437704227,-0.166532381881811,
6.90565390303645));
#264869=CARTESIAN_POINT('Ctrl Pts',(-1.55547524062006,-0.0103886318065344,
6.89374573174244));
#264870=CARTESIAN_POINT('Ctrl Pts',(-1.55550243327175,-0.00483002150656961,
6.89332261268853));
#264871=CARTESIAN_POINT('Ctrl Pts',(-1.55549982932971,0.000728666766646221,
6.89290035850054));
#264872=CARTESIAN_POINT('Ctrl Pts',(1.43315705713258,0.600696421508238,
6.58835745434586));
#264873=CARTESIAN_POINT('Ctrl Pts',(1.29870118847464,0.914687993023714,
6.61276651483456));
#264874=CARTESIAN_POINT('Ctrl Pts',(0.70689197534916,1.60275587211439,6.6742275039151));
#264875=CARTESIAN_POINT('Ctrl Pts',(-0.852081690047566,1.62925752158921,
6.7727404215875));
#264876=CARTESIAN_POINT('Ctrl Pts',(-1.53450515466516,0.61017599513106,
6.85023095151808));
#264877=CARTESIAN_POINT('Ctrl Pts',(-1.55781672113823,0.0479304507923726,
6.89066955285682));
#264878=CARTESIAN_POINT('Ctrl Pts',(-1.55751602490984,0.000817960485851865,
6.89405622560371));
#264879=CARTESIAN_POINT('',(-1.55549951640608,-0.00134079452263982,6.75626891037593));
#264880=CARTESIAN_POINT('Ctrl Pts',(1.43457668334549,0.60130690134194,6.45155991302018));
#264881=CARTESIAN_POINT('Ctrl Pts',(1.42736364796658,0.618515505380319,
6.45285677086583));
#264882=CARTESIAN_POINT('Ctrl Pts',(1.41984071126925,0.635594942557183,
6.45413914262176));
#264883=CARTESIAN_POINT('Ctrl Pts',(1.34044988766294,0.807387152896391,
6.46703010256774));
#264884=CARTESIAN_POINT('Ctrl Pts',(1.24390481061379,0.949416472487348,
6.47775656379845));
#264885=CARTESIAN_POINT('Ctrl Pts',(1.12478115298201,1.07445425078909,6.48962931242059));
#264886=CARTESIAN_POINT('Ctrl Pts',(1.12334294696658,1.07595780706174,6.48977246789771));
#264887=CARTESIAN_POINT('Ctrl Pts',(1.10455265666818,1.09552316378153,6.49164040861345));
#264888=CARTESIAN_POINT('Ctrl Pts',(1.08677070458871,1.11316525595325,6.49338159815424));
#264889=CARTESIAN_POINT('Ctrl Pts',(1.06183692715151,1.13673588571189,6.49579275338506));
#264890=CARTESIAN_POINT('Ctrl Pts',(1.05504579303966,1.14304177599866,6.49644649928914));
#264891=CARTESIAN_POINT('Ctrl Pts',(1.04413300796446,1.1529947066736,6.49749255663191));
#264892=CARTESIAN_POINT('Ctrl Pts',(1.040047568465,1.15668128101585,6.49788319246831));
#264893=CARTESIAN_POINT('Ctrl Pts',(1.03161038509193,1.16421389465039,6.49868798350287));
#264894=CARTESIAN_POINT('Ctrl Pts',(1.02725649685429,1.16805739033491,6.49910223607983));
#264895=CARTESIAN_POINT('Ctrl Pts',(1.01710971179226,1.17691408920699,6.50006530675118));
#264896=CARTESIAN_POINT('Ctrl Pts',(1.01130114299623,1.18190902081393,6.50061486652449));
#264897=CARTESIAN_POINT('Ctrl Pts',(0.992679622734716,1.19768435022372,
6.50237132424888));
#264898=CARTESIAN_POINT('Ctrl Pts',(0.979729781961769,1.20830052130919,
6.50358483294207));
#264899=CARTESIAN_POINT('Ctrl Pts',(0.913324580904114,1.26096956222477,
6.50977010574473));
#264900=CARTESIAN_POINT('Ctrl Pts',(0.857331032259533,1.29968730097642,
6.51486986700256));
#264901=CARTESIAN_POINT('Ctrl Pts',(0.713250637645021,1.3859437523413,6.52770373386735));
#264902=CARTESIAN_POINT('Ctrl Pts',(0.622769007797595,1.42888895221082,
6.53553148005357));
#264903=CARTESIAN_POINT('Ctrl Pts',(0.51911339925616,1.46635860418252,6.54398248008834));
#264904=CARTESIAN_POINT('Ctrl Pts',(0.509395006342337,1.4697629103079,6.54476981505109));
#264905=CARTESIAN_POINT('Ctrl Pts',(0.463009340447153,1.48549623018356,
6.54850207613884));
#264906=CARTESIAN_POINT('Ctrl Pts',(0.425920608118182,1.49655235562314,
6.55141066086021));
#264907=CARTESIAN_POINT('Ctrl Pts',(0.382010178631786,1.50787690680752,
6.5547381475351));
#264908=CARTESIAN_POINT('Ctrl Pts',(0.375555019197983,1.5094975900748,6.55522440426853));
#264909=CARTESIAN_POINT('Ctrl Pts',(0.365077905219191,1.5120566874842,6.55600870752146));
#264910=CARTESIAN_POINT('Ctrl Pts',(0.361062357294251,1.51302058091003,
6.5563081390591));
#264911=CARTESIAN_POINT('Ctrl Pts',(0.35390621333556,1.51470823214912,6.55683962538624));
#264912=CARTESIAN_POINT('Ctrl Pts',(0.3507671671067,1.51543823086579,6.55707202990087));
#264913=CARTESIAN_POINT('Ctrl Pts',(0.343969443372104,1.51699681727166,
6.55757371893119));
#264914=CARTESIAN_POINT('Ctrl Pts',(0.340310034417461,1.5178219272582,6.55784280389447));
#264915=CARTESIAN_POINT('Ctrl Pts',(0.330058127270287,1.52009454899066,
6.55859397860941));
#264916=CARTESIAN_POINT('Ctrl Pts',(0.323459032658118,1.52151242645805,
6.55907441777574));
#264917=CARTESIAN_POINT('Ctrl Pts',(0.283967576647959,1.5297289881583,6.56193227462683));
#264918=CARTESIAN_POINT('Ctrl Pts',(0.250868261128905,1.53550444636292,
6.56425613363933));
#264919=CARTESIAN_POINT('Ctrl Pts',(0.046521088956556,1.56437525767921,
6.57831224024227));
#264920=CARTESIAN_POINT('Ctrl Pts',(-0.127397564425102,1.55987665963063,
6.5891687766805));
#264921=CARTESIAN_POINT('Ctrl Pts',(-0.321462024222304,1.52212410634915,
6.60278457595101));
#264922=CARTESIAN_POINT('Ctrl Pts',(-0.345772531017217,1.51678636097919,
6.60451489800401));
#264923=CARTESIAN_POINT('Ctrl Pts',(-0.378921775291969,1.50866960674231,
6.60691330690904));
#264924=CARTESIAN_POINT('Ctrl Pts',(-0.387880194449341,1.50639126466654,
6.60756539915968));
#264925=CARTESIAN_POINT('Ctrl Pts',(-0.402134019548054,1.5026305973321,
6.60860947540982));
#264926=CARTESIAN_POINT('Ctrl Pts',(-0.407442896471344,1.50119977565252,
6.60899979547739));
#264927=CARTESIAN_POINT('Ctrl Pts',(-0.418345622164745,1.49819923408625,
6.60980443324914));
#264928=CARTESIAN_POINT('Ctrl Pts',(-0.423938478027348,1.49662626255378,
6.61021885061083));
#264929=CARTESIAN_POINT('Ctrl Pts',(-0.4368995041676,1.49290253809984,6.6111831512814));
#264930=CARTESIAN_POINT('Ctrl Pts',(-0.444260773028511,1.49072852211365,
6.61173378227081));
#264931=CARTESIAN_POINT('Ctrl Pts',(-0.467124464799687,1.48379176121603,
6.61345340950718));
#264932=CARTESIAN_POINT('Ctrl Pts',(-0.482568248420444,1.47884113578744,
6.61462849091278));
#264933=CARTESIAN_POINT('Ctrl Pts',(-0.518624909398208,1.4666579594764,
6.61740484021058));
#264934=CARTESIAN_POINT('Ctrl Pts',(-0.539167956053008,1.45923102824412,
6.6190122249473));
#264935=CARTESIAN_POINT('Ctrl Pts',(-0.61172113015982,1.43125967582583,
6.62478252197996));
#264936=CARTESIAN_POINT('Ctrl Pts',(-0.662767142101544,1.40834849525905,
6.62901760050886));
#264937=CARTESIAN_POINT('Ctrl Pts',(-0.805636238460955,1.33473450397939,
6.64135282472932));
#264938=CARTESIAN_POINT('Ctrl Pts',(-0.893714272359956,1.27743504748951,
6.64957962180708));
#264939=CARTESIAN_POINT('Ctrl Pts',(-1.00275147222613,1.18966639630935,
6.66021633085421));
#264940=CARTESIAN_POINT('Ctrl Pts',(-1.02938985958108,1.16669346722089,
6.66285361299601));
#264941=CARTESIAN_POINT('Ctrl Pts',(-1.05999000382307,1.138439034368,6.66590847478991));
#264942=CARTESIAN_POINT('Ctrl Pts',(-1.06472364982352,1.13401313775313,
6.66638178559031));
#264943=CARTESIAN_POINT('Ctrl Pts',(-1.07238998807715,1.12675489037632,
6.66714935083362));
#264944=CARTESIAN_POINT('Ctrl Pts',(-1.07533938486133,1.12394042453737,
6.66744489768758));
#264945=CARTESIAN_POINT('Ctrl Pts',(-1.08059762100106,1.11888310018409,
6.66797219560122));
#264946=CARTESIAN_POINT('Ctrl Pts',(-1.08291058636913,1.11664464937999,
6.668204274092));
#264947=CARTESIAN_POINT('Ctrl Pts',(-1.08740207938593,1.11227077324681,
6.66865519817617));
#264948=CARTESIAN_POINT('Ctrl Pts',(-1.08958126134632,1.1101361315753,6.66887410067713));
#264949=CARTESIAN_POINT('Ctrl Pts',(-1.09585025457557,1.10395902869163,
6.66950423968003));
#264950=CARTESIAN_POINT('Ctrl Pts',(-1.09992400754824,1.09990022178073,
6.66991422425773));
#264951=CARTESIAN_POINT('Ctrl Pts',(-1.11869757792601,1.08098691574727,
6.67180650976796));
#264952=CARTESIAN_POINT('Ctrl Pts',(-1.13312048253265,1.06585884091123,
6.67326859409705));
#264953=CARTESIAN_POINT('Ctrl Pts',(-1.17305867459872,1.02224061320622,
6.67735749206441));
#264954=CARTESIAN_POINT('Ctrl Pts',(-1.19783561822219,0.993092552341752,
6.67994298350009));
#264955=CARTESIAN_POINT('Ctrl Pts',(-1.25855679429963,0.916075632111055,
6.68649708116946));
#264956=CARTESIAN_POINT('Ctrl Pts',(-1.29285867530171,0.866992930502283,
6.69041836967635));
#264957=CARTESIAN_POINT('Ctrl Pts',(-1.37997084549852,0.72563207510828,
6.70135419759506));
#264958=CARTESIAN_POINT('Ctrl Pts',(-1.42627666917936,0.629755019693429,
6.70839998321902));
#264959=CARTESIAN_POINT('Ctrl Pts',(-1.46650654768444,0.518729596602149,
6.71664778198961));
#264960=CARTESIAN_POINT('Ctrl Pts',(-1.4704317857451,0.507496008336282,
6.71748292678769));
#264961=CARTESIAN_POINT('Ctrl Pts',(-1.4765898541024,0.489200862225769,
6.71884463418445));
#264962=CARTESIAN_POINT('Ctrl Pts',(-1.47890186885667,0.482166298815238,
6.71936859154224));
#264963=CARTESIAN_POINT('Ctrl Pts',(-1.48292687951533,0.469618407404525,
6.72030399492354));
#264964=CARTESIAN_POINT('Ctrl Pts',(-1.48465958643075,0.464111505284981,
6.72071478693031));
#264965=CARTESIAN_POINT('Ctrl Pts',(-1.48824595880427,0.452487644748402,
6.72158251356072));
#264966=CARTESIAN_POINT('Ctrl Pts',(-1.49009265289354,0.446368666114793,
6.72203966699562));
#264967=CARTESIAN_POINT('Ctrl Pts',(-1.49376838642326,0.433912164038169,
6.72297112580997));
#264968=CARTESIAN_POINT('Ctrl Pts',(-1.49559492870028,0.427574046377751,
6.72344550199953));
#264969=CARTESIAN_POINT('Ctrl Pts',(-1.50002826236283,0.411814306676032,
6.7246261969643));
#264970=CARTESIAN_POINT('Ctrl Pts',(-1.50258662212174,0.40237948007269,
6.72533406332898));
#264971=CARTESIAN_POINT('Ctrl Pts',(-1.5095040387726,0.375882834090415,
6.7273251544176));
#264972=CARTESIAN_POINT('Ctrl Pts',(-1.51366241564198,0.358770668745993,
6.72861467932014));
#264973=CARTESIAN_POINT('Ctrl Pts',(-1.54286918620225,0.229019096079115,
6.73842229826593));
#264974=CARTESIAN_POINT('Ctrl Pts',(-1.55559877422798,0.113999451242998,
6.74732589837675));
#264975=CARTESIAN_POINT('Ctrl Pts',(-1.55549942292528,-0.00133988026452862,
6.75626900298645));
#264976=CARTESIAN_POINT('Ctrl Pts',(-1.55549942214842,-0.00134078183929962,
6.75626907289215));
#264977=CARTESIAN_POINT('Ctrl Pts',(-1.55542406061211,-0.0887709831925335,
6.76304817777256));
#264978=CARTESIAN_POINT('Ctrl Pts',(-1.54797750370825,-0.176053511463977,
6.76981111638233));
#264979=CARTESIAN_POINT('Ctrl Pts',(-1.53227353243141,-0.267862619476418,
6.77665509403429));
#264980=CARTESIAN_POINT('Ctrl Pts',(-1.53128442875315,-0.273460348044416,
6.77707126039852));
#264981=CARTESIAN_POINT('Ctrl Pts',(-1.52958837228819,-0.282761156806125,
6.77776073212102));
#264982=CARTESIAN_POINT('Ctrl Pts',(-1.52889861437371,-0.286467255018727,
6.77803493630822));
#264983=CARTESIAN_POINT('Ctrl Pts',(-1.52762537391392,-0.293172822163733,
6.77853005890441));
#264984=CARTESIAN_POINT('Ctrl Pts',(-1.52704651614358,-0.296173132900708,
6.77875122983635));
#264985=CARTESIAN_POINT('Ctrl Pts',(-1.52584008499915,-0.302328685466161,
6.77920421689561));
#264986=CARTESIAN_POINT('Ctrl Pts',(-1.52521157115125,-0.305483653691516,
6.77943596681603));
#264987=CARTESIAN_POINT('Ctrl Pts',(-1.52377009509107,-0.312604114455763,
6.77995806155847));
#264988=CARTESIAN_POINT('Ctrl Pts',(-1.52295144016092,-0.316568392267801,
6.78024807961978));
#264989=CARTESIAN_POINT('Ctrl Pts',(-1.52043416371531,-0.328522331506228,
6.78112075071142));
#264990=CARTESIAN_POINT('Ctrl Pts',(-1.51868804075455,-0.33650202237091,
6.78170078783826));
#264991=CARTESIAN_POINT('Ctrl Pts',(-1.50010832170874,-0.418318627315836,
6.7876257421574));
#264992=CARTESIAN_POINT('Ctrl Pts',(-1.4779638882258,-0.490858206746161,
6.79269476745083));
#264993=CARTESIAN_POINT('Ctrl Pts',(-1.42975813781908,-0.615395146280879,
6.80152888825742));
#264994=CARTESIAN_POINT('Ctrl Pts',(-1.40591156335138,-0.668081036752133,
6.80531088671053));
#264995=CARTESIAN_POINT('Ctrl Pts',(-1.34488506924146,-0.785090540428699,
6.81403720897344));
#264996=CARTESIAN_POINT('Ctrl Pts',(-1.30592450511069,-0.848317269759493,
6.81899829000765));
#264997=CARTESIAN_POINT('Ctrl Pts',(-1.24967850604569,-0.926484625750097,
6.8256513668287));
#264998=CARTESIAN_POINT('Ctrl Pts',(-1.23636979593911,-0.944171474002994,
6.82719367026841));
#264999=CARTESIAN_POINT('Ctrl Pts',(-1.21860185400942,-0.966764439633387,
6.82921570760253));
#265000=CARTESIAN_POINT('Ctrl Pts',(-1.21448184658903,-0.971935081283433,
6.82968209512258));
#265001=CARTESIAN_POINT('Ctrl Pts',(-1.2063075296743,-0.982060783460762,
6.83060269910703));
#265002=CARTESIAN_POINT('Ctrl Pts',(-1.20225534038524,-0.987017392374869,
6.83105682521746));
#265003=CARTESIAN_POINT('Ctrl Pts',(-1.19449268146211,-0.996393890818971,
6.8319226446484));
#265004=CARTESIAN_POINT('Ctrl Pts',(-1.19078797909769,-1.00081843454054,
6.8323340994998));
#265005=CARTESIAN_POINT('Ctrl Pts',(-1.18228615972498,-1.01085816439156,
6.83327443050409));
#265006=CARTESIAN_POINT('Ctrl Pts',(-1.17747353227078,-1.0164599693611,
6.83380393687924));
#265007=CARTESIAN_POINT('Ctrl Pts',(-1.16484554529409,-1.03094866997374,
6.83518627327986));
#265008=CARTESIAN_POINT('Ctrl Pts',(-1.1569684640822,-1.0397808727059,6.83604164962985));
#265009=CARTESIAN_POINT('Ctrl Pts',(-1.09613056009097,-1.10644826859371,
6.84259752373628));
#265010=CARTESIAN_POINT('Ctrl Pts',(-1.03897406707593,-1.16028405762339,
6.84847809352742));
#265011=CARTESIAN_POINT('Ctrl Pts',(-0.906068315858519,-1.26774612903609,
6.86156960601368));
#265012=CARTESIAN_POINT('Ctrl Pts',(-0.829082082361456,-1.3193793267871,
6.86880720546502));
#265013=CARTESIAN_POINT('Ctrl Pts',(-0.717326181869039,-1.38066816991362,
6.8785934699848));
#265014=CARTESIAN_POINT('Ctrl Pts',(-0.686125915325519,-1.39643583182716,
6.88125293451276));
#265015=CARTESIAN_POINT('Ctrl Pts',(-0.636560140915106,-1.41942205170845,
6.88533985310382));
#265016=CARTESIAN_POINT('Ctrl Pts',(-0.618544707175861,-1.42736481544873,
6.88679769713944));
#265017=CARTESIAN_POINT('Ctrl Pts',(-0.595253848761335,-1.43710960264431,
6.88864304755565));
#265018=CARTESIAN_POINT('Ctrl Pts',(-0.590113880236908,-1.43922783649988,
6.88904786030592));
#265019=CARTESIAN_POINT('Ctrl Pts',(-0.582142460661991,-1.44246305618098,
6.88967179880626));
#265020=CARTESIAN_POINT('Ctrl Pts',(-0.579318973528266,-1.44359933509804,
6.88989205012515));
#265021=CARTESIAN_POINT('Ctrl Pts',(-0.573499579563226,-1.44592145830078,
6.8903444370472));
#265022=CARTESIAN_POINT('Ctrl Pts',(-0.570503361138275,-1.44710626652208,
6.89057649990763));
#265023=CARTESIAN_POINT('Ctrl Pts',(-0.563667641530295,-1.44978481574006,
6.89110401104251));
#265024=CARTESIAN_POINT('Ctrl Pts',(-0.559825875760635,-1.45127261806413,
6.89139910277527));
#265025=CARTESIAN_POINT('Ctrl Pts',(-0.549793038126816,-1.45511227211957,
6.89216627057087));
#265026=CARTESIAN_POINT('Ctrl Pts',(-0.543592691746166,-1.45743991260658,
6.89263695144555));
#265027=CARTESIAN_POINT('Ctrl Pts',(-0.501703795651539,-1.47286069798531,
6.89579497216544));
#265028=CARTESIAN_POINT('Ctrl Pts',(-0.46555689445601,-1.48468269548983,
6.8984136264371));
#265029=CARTESIAN_POINT('Ctrl Pts',(-0.420054569411901,-1.49773869614989,
6.90162168801619));
#265030=CARTESIAN_POINT('Ctrl Pts',(-0.411076558086052,-1.50022768692937,
6.90225044801685));
#265031=CARTESIAN_POINT('Ctrl Pts',(-0.259385083996849,-1.54081741856284,
6.91281121068327));
#265032=CARTESIAN_POINT('Ctrl Pts',(-0.111985542306284,-1.55848057479781,
6.92221832751334));
#265033=CARTESIAN_POINT('Ctrl Pts',(0.0690446190827033,-1.55432480770115,
6.93459354645539));
#265034=CARTESIAN_POINT('Ctrl Pts',(0.102354712595635,-1.55248703731043,
6.93690059672432));
#265035=CARTESIAN_POINT('Ctrl Pts',(0.145152533173765,-1.54874251088973,
6.93991546402861));
#265036=CARTESIAN_POINT('Ctrl Pts',(0.154718873959221,-1.54781610199424,
6.94059261513072));
#265037=CARTESIAN_POINT('Ctrl Pts',(0.170629645649542,-1.54612632096563,
6.94172456580286));
#265038=CARTESIAN_POINT('Ctrl Pts',(0.176979158084729,-1.54541238889452,
6.9421778105535));
#265039=CARTESIAN_POINT('Ctrl Pts',(0.189057317595645,-1.54397892295273,
6.94304295589299));
#265040=CARTESIAN_POINT('Ctrl Pts',(0.194786723712315,-1.54326657271953,
6.94345462385947));
#265041=CARTESIAN_POINT('Ctrl Pts',(0.207858741765374,-1.54156734549442,
6.94439685641547));
#265042=CARTESIAN_POINT('Ctrl Pts',(0.215198485994634,-1.5405598804762,
6.94492806061016));
#265043=CARTESIAN_POINT('Ctrl Pts',(0.234320339342767,-1.53779586741691,
6.94631774691426));
#265044=CARTESIAN_POINT('Ctrl Pts',(0.246089762117461,-1.53595636838536,
6.94717882004342));
#265045=CARTESIAN_POINT('Ctrl Pts',(0.362470814006211,-1.51639466813727,
6.95575211592624));
#265046=CARTESIAN_POINT('Ctrl Pts',(0.465008717111574,-1.48815186590056,
6.96380569461293));
#265047=CARTESIAN_POINT('Ctrl Pts',(0.641150984790634,-1.41964222218781,
6.97842215571859));
#265048=CARTESIAN_POINT('Ctrl Pts',(0.715920133943383,-1.38344422793985,
6.98489615127094));
#265049=CARTESIAN_POINT('Ctrl Pts',(0.817169494143555,-1.32400980897541,
6.99380873929622));
#265050=CARTESIAN_POINT('Ctrl Pts',(0.846305289703434,-1.30557871142229,
6.99639069397384));
#265051=CARTESIAN_POINT('Ctrl Pts',(0.880427828268098,-1.28237018621743,
6.99941483807776));
#265052=CARTESIAN_POINT('Ctrl Pts',(0.886023439824617,-1.2785104316846,
6.99991075757306));
#265053=CARTESIAN_POINT('Ctrl Pts',(0.894676066689899,-1.27245791107993,
7.00067739409668));
#265054=CARTESIAN_POINT('Ctrl Pts',(0.897750640820932,-1.27029059175353,
7.00094976353715));
#265055=CARTESIAN_POINT('Ctrl Pts',(0.903443768448993,-1.26624641600661,
7.00145398002501));
#265056=CARTESIAN_POINT('Ctrl Pts',(0.906064331919369,-1.26437259364856,
7.00168601771242));
#265057=CARTESIAN_POINT('Ctrl Pts',(0.912018893128433,-1.26008679097672,
7.00221316009567));
#265058=CARTESIAN_POINT('Ctrl Pts',(0.915349151790441,-1.25766971561904,
7.00250791024947));
#265059=CARTESIAN_POINT('Ctrl Pts',(0.924001119187815,-1.25133761568002,
7.00327360038148));
#265060=CARTESIAN_POINT('Ctrl Pts',(0.929307620550339,-1.24740179860647,
7.00374315395292));
#265061=CARTESIAN_POINT('Ctrl Pts',(0.964709381324021,-1.22079311296761,
7.00687650154718));
#265062=CARTESIAN_POINT('Ctrl Pts',(0.994000345917764,-1.19706470475705,
7.00947282622629));
#265063=CARTESIAN_POINT('Ctrl Pts',(1.1347085111601,-1.0743475660386,7.02212957897043));
#265064=CARTESIAN_POINT('Ctrl Pts',(1.23236022889502,-0.960770979524193,
7.03158855237073));
#265065=CARTESIAN_POINT('Ctrl Pts',(1.32675847905031,-0.812410522510614,
7.04353423970992));
#265066=CARTESIAN_POINT('Ctrl Pts',(1.34056179585364,-0.789425648698518,
7.04537209575693));
#265067=CARTESIAN_POINT('Ctrl Pts',(1.36324602177683,-0.749340520580184,
7.04856496693988));
#265068=CARTESIAN_POINT('Ctrl Pts',(1.37241603328718,-0.732410476557945,
7.0499098137681));
#265069=CARTESIAN_POINT('Ctrl Pts',(1.38499413251151,-0.708122247654651,
7.05183624861529));
#265070=CARTESIAN_POINT('Ctrl Pts',(1.38866284015097,-0.700900404222524,
7.05240868918543));
#265071=CARTESIAN_POINT('Ctrl Pts',(1.39489713048349,-0.688387117170729,
7.05340009949497));
#265072=CARTESIAN_POINT('Ctrl Pts',(1.39748944876384,-0.683109117621849,
7.05381812868427));
#265073=CARTESIAN_POINT('Ctrl Pts',(1.40240011178259,-0.672965987145075,
7.054621284566));
#265074=CARTESIAN_POINT('Ctrl Pts',(1.40472322609171,-0.668103248094057,
7.0550062386791));
#265075=CARTESIAN_POINT('Ctrl Pts',(1.41012281025365,-0.656648180570069,
7.05591291528658));
#265076=CARTESIAN_POINT('Ctrl Pts',(1.41317837217083,-0.650046196926284,
7.05643534891474));
#265077=CARTESIAN_POINT('Ctrl Pts',(1.42358928812409,-0.627131557897748,
7.05824841579472));
#265078=CARTESIAN_POINT('Ctrl Pts',(1.43070913907085,-0.610714140918362,
7.05954701895264));
#265079=CARTESIAN_POINT('Ctrl Pts',(1.48548617045424,-0.478187581895869,
7.07003102146907));
#265080=CARTESIAN_POINT('Ctrl Pts',(1.51920425457528,-0.356844221990392,
7.0796947388204));
#265081=CARTESIAN_POINT('Ctrl Pts',(1.54593906630705,-0.180223371577389,
7.0935459493728));
#265082=CARTESIAN_POINT('Ctrl Pts',(1.55119672392109,-0.127268864418318,
7.09766363105027));
#265083=CARTESIAN_POINT('Ctrl Pts',(1.55548881281783,-0.0373288627441701,
7.10451216913307));
#265084=CARTESIAN_POINT('Ctrl Pts',(1.55593676981206,-0.00045633274773518,
7.10727837327658));
#265085=CARTESIAN_POINT('Ctrl Pts',(1.55491207236157,0.0433196824626526,
7.11048814905978));
#265086=CARTESIAN_POINT('Ctrl Pts',(1.55470393780829,0.0502376176737323,
7.1109931767934));
#265087=CARTESIAN_POINT('Ctrl Pts',(1.55431043866859,0.0609398164856241,
7.11177080789822));
#265088=CARTESIAN_POINT('Ctrl Pts',(1.55415741421752,0.0647250620030301,
7.11204513871522));
#265089=CARTESIAN_POINT('Ctrl Pts',(1.5538487872311,0.07172557385834,7.11255113535687));
#265090=CARTESIAN_POINT('Ctrl Pts',(1.5536970342818,0.0749408938002778,
7.11278300378511));
#265091=CARTESIAN_POINT('Ctrl Pts',(1.55333035531211,0.0822295222501443,
7.11330741894152));
#265092=CARTESIAN_POINT('Ctrl Pts',(1.55310938838683,0.0863024669016945,
7.11359962603701));
#265093=CARTESIAN_POINT('Ctrl Pts',(1.55249548642105,0.0968509159461085,
7.11435434134753));
#265094=CARTESIAN_POINT('Ctrl Pts',(1.55207805314158,0.103325002420016,
7.11481552756932));
#265095=CARTESIAN_POINT('Ctrl Pts',(1.54912856434855,0.145006556759354,
7.11777284290209));
#265096=CARTESIAN_POINT('Ctrl Pts',(1.54543897428523,0.180125158876393,
7.12020985217078));
#265097=CARTESIAN_POINT('Ctrl Pts',(1.53803873330106,0.233128265713526,
7.12384636490497));
#265098=CARTESIAN_POINT('Ctrl Pts',(1.53520372741407,0.251120474114648,
7.12507346123859));
#265099=CARTESIAN_POINT('Ctrl Pts',(1.52292842849498,0.321017374935997,
7.12982605222567));
#265100=CARTESIAN_POINT('Ctrl Pts',(1.51116591693839,0.372479776320444,
7.13329485088506));
#265101=CARTESIAN_POINT('Ctrl Pts',(1.4796724576334,0.483856277205171,7.14091293977094));
#265102=CARTESIAN_POINT('Ctrl Pts',(1.45888357768414,0.543316423205788,
7.14505442302371));
#265103=CARTESIAN_POINT('Ctrl Pts',(1.43457650415244,0.601307328854198,
7.14927790964297));
#265104=CARTESIAN_POINT('Origin',(0.,0.,-1.29405622560371));
#265105=CARTESIAN_POINT('',(1.43457668592364,0.601306895191089,7.98692484967426));
#265106=CARTESIAN_POINT('',(1.43457666579773,0.601306943206762,7.84913521677167));
#265107=CARTESIAN_POINT('',(1.43457668357355,0.601306900797845,-1.29405622560371));
#265108=CARTESIAN_POINT('Ctrl Pts',(1.43457668592364,0.601306895191089,
7.98692484967426));
#265109=CARTESIAN_POINT('Ctrl Pts',(1.4484903359964,0.568112201815517,7.98444320077674));
#265110=CARTESIAN_POINT('Ctrl Pts',(1.46125114251322,0.534436261602293,
7.98201129489878));
#265111=CARTESIAN_POINT('Ctrl Pts',(1.51632301583225,0.372322798635339,
7.97057171645316));
#265112=CARTESIAN_POINT('Ctrl Pts',(1.54293548610503,0.239187956891495,
7.96190572417245));
#265113=CARTESIAN_POINT('Ctrl Pts',(1.55443513335324,0.0680494455109081,
7.95021155000991));
#265114=CARTESIAN_POINT('Ctrl Pts',(1.55560003676253,0.0317408277435369,
7.94770345237973));
#265115=CARTESIAN_POINT('Ctrl Pts',(1.55546336579658,-0.0147475571720663,
7.94444182936921));
#265116=CARTESIAN_POINT('Ctrl Pts',(1.55533362640663,-0.0249213681375513,
7.94372497744379));
#265117=CARTESIAN_POINT('Ctrl Pts',(1.55496285388788,-0.0413517238984559,
7.94256201781539));
#265118=CARTESIAN_POINT('Ctrl Pts',(1.55478383588616,-0.0476094909004445,
7.94211785127168));
#265119=CARTESIAN_POINT('Ctrl Pts',(1.55436924002932,-0.0595747001656667,
7.94126613811837));
#265120=CARTESIAN_POINT('Ctrl Pts',(1.55413998810361,-0.0652822719111739,
7.94085879608236));
#265121=CARTESIAN_POINT('Ctrl Pts',(1.55354685010361,-0.078265591668855,
7.93992970910407));
#265122=CARTESIAN_POINT('Ctrl Pts',(1.55316328151474,-0.0855402590273948,
7.93940735707378));
#265123=CARTESIAN_POINT('Ctrl Pts',(1.55201724681829,-0.104713251272965,
7.93802583144157));
#265124=CARTESIAN_POINT('Ctrl Pts',(1.55116906911848,-0.11660576185849,
7.93716400149181));
#265125=CARTESIAN_POINT('Ctrl Pts',(1.54263816321354,-0.219530350653884,
7.92966112478029));
#265126=CARTESIAN_POINT('Ctrl Pts',(1.52708790129757,-0.309714086254081,
7.92277153388331));
#265127=CARTESIAN_POINT('Ctrl Pts',(1.48792472941349,-0.457680949966964,
7.91098407923764));
#265128=CARTESIAN_POINT('Ctrl Pts',(1.46858901422948,-0.516369892297193,
7.90617844004671));
#265129=CARTESIAN_POINT('Ctrl Pts',(1.42269008746057,-0.632032078818221,
7.89655816682876));
#265130=CARTESIAN_POINT('Ctrl Pts',(1.39605716109568,-0.688867094774696,
7.89175328311457));
#265131=CARTESIAN_POINT('Ctrl Pts',(1.36035606595042,-0.754422945728574,
7.88622983645625));
#265132=CARTESIAN_POINT('Ctrl Pts',(1.35452908330613,-0.76483566405017,
7.88535317364935));
#265133=CARTESIAN_POINT('Ctrl Pts',(1.34624942920058,-0.779239786077756,
7.88414245658443));
#265134=CARTESIAN_POINT('Ctrl Pts',(1.3438978763913,-0.783288369120164,
7.88380238047899));
#265135=CARTESIAN_POINT('Ctrl Pts',(1.33987152789863,-0.790148878032278,
7.88322656256454));
#265136=CARTESIAN_POINT('Ctrl Pts',(1.33820608510347,-0.792966225833744,
7.88299022825843));
#265137=CARTESIAN_POINT('Ctrl Pts',(1.33499378199385,-0.798361377661278,
7.88253793627869));
#265138=CARTESIAN_POINT('Ctrl Pts',(1.33344833169778,-0.800939969296144,
7.88232188687473));
#265139=CARTESIAN_POINT('Ctrl Pts',(1.32973590387375,-0.807093645464354,
7.88180654684937));
#265140=CARTESIAN_POINT('Ctrl Pts',(1.32756195490934,-0.810664532074981,
7.88150770589522));
#265141=CARTESIAN_POINT('Ctrl Pts',(1.31971501779874,-0.823437539563362,
7.88043932172574));
#265142=CARTESIAN_POINT('Ctrl Pts',(1.31396035915565,-0.832589515672145,
7.87967487155107));
#265143=CARTESIAN_POINT('Ctrl Pts',(1.24525467391682,-0.939369426124861,
7.87075886489449));
#265144=CARTESIAN_POINT('Ctrl Pts',(1.17164260428635,-1.02972668702184,
7.86322724283071));
#265145=CARTESIAN_POINT('Ctrl Pts',(1.01627665008431,-1.18195865824474,
7.84889218010191));
#265146=CARTESIAN_POINT('Ctrl Pts',(0.93716956593279,-1.24561354629004,
7.84215103890584));
#265147=CARTESIAN_POINT('Ctrl Pts',(0.841555827145406,-1.30825589206276,
7.83416536255652));
#265148=CARTESIAN_POINT('Ctrl Pts',(0.830578836038413,-1.31525224513411,
7.83325114060816));
#265149=CARTESIAN_POINT('Ctrl Pts',(0.813672050998817,-1.32573199055336,
7.83184627477718));
#265150=CARTESIAN_POINT('Ctrl Pts',(0.807804618642334,-1.3293153172613,
7.83135930643416));
#265151=CARTESIAN_POINT('Ctrl Pts',(0.79753186809214,-1.33549590794552,
7.83050763376491));
#265152=CARTESIAN_POINT('Ctrl Pts',(0.793137102364446,-1.33811058454446,
7.83014357080237));
#265153=CARTESIAN_POINT('Ctrl Pts',(0.783207544126694,-1.343952096949,7.82932160713624));
#265154=CARTESIAN_POINT('Ctrl Pts',(0.77766557730404,-1.34716648699303,
7.82886326424046));
#265155=CARTESIAN_POINT('Ctrl Pts',(0.762694701399174,-1.35572656615261,
7.82762613312845));
#265156=CARTESIAN_POINT('Ctrl Pts',(0.753229667836946,-1.36100800370388,
7.82684506106099));
#265157=CARTESIAN_POINT('Ctrl Pts',(0.709646099979314,-1.38473351386116,
7.82325268350788));
#265158=CARTESIAN_POINT('Ctrl Pts',(0.674903213385856,-1.401994882431,7.82040023457189));
#265159=CARTESIAN_POINT('Ctrl Pts',(0.496623167178186,-1.48240722903888,
7.80580461695882));
#265160=CARTESIAN_POINT('Ctrl Pts',(0.344802928880277,-1.52488064767716,
7.79338364404336));
#265161=CARTESIAN_POINT('Ctrl Pts',(0.156776018803869,-1.54792438909802,
7.77902478567505));
#265162=CARTESIAN_POINT('Ctrl Pts',(0.12421220902423,-1.55087728726743,
7.77657922809565));
#265163=CARTESIAN_POINT('Ctrl Pts',(0.0849470063881252,-1.55319295690233,
7.7736977351942));
#265164=CARTESIAN_POINT('Ctrl Pts',(0.0783147489128923,-1.55354148951048,
7.77321333429218));
#265165=CARTESIAN_POINT('Ctrl Pts',(0.0679851028948251,-1.55401800483553,
7.77246268840421));
#265166=CARTESIAN_POINT('Ctrl Pts',(0.064289252963008,-1.55417528815055,
7.77219487161495));
#265167=CARTESIAN_POINT('Ctrl Pts',(0.0574129588258846,-1.55444335023006,
7.77169803797595));
#265168=CARTESIAN_POINT('Ctrl Pts',(0.0542327646099745,-1.55455755264304,
7.7714688415151));
#265169=CARTESIAN_POINT('Ctrl Pts',(0.0469744318787375,-1.55479590250337,
7.77094704166991));
#265170=CARTESIAN_POINT('Ctrl Pts',(0.0428961428320419,-1.55491376534127,
7.77065479132075));
#265171=CARTESIAN_POINT('Ctrl Pts',(0.0322411489464894,-1.55517974266837,
7.76989358968594));
#265172=CARTESIAN_POINT('Ctrl Pts',(0.0256637941083301,-1.55530218845769,
7.76942602191656));
#265173=CARTESIAN_POINT('Ctrl Pts',(-0.0191120575347989,-1.5558516215098,
7.76625761562317));
#265174=CARTESIAN_POINT('Ctrl Pts',(-0.0573181555389714,-1.55491310732951,
7.76362631915188));
#265175=CARTESIAN_POINT('Ctrl Pts',(-0.243697359489083,-1.543454180537,
7.75097367563435));
#265176=CARTESIAN_POINT('Ctrl Pts',(-0.389874003196824,-1.51315690462803,
7.74154475309823));
#265177=CARTESIAN_POINT('Ctrl Pts',(-0.554886744404079,-1.45341230531076,
7.72962467096044));
#265178=CARTESIAN_POINT('Ctrl Pts',(-0.579984266073731,-1.4435805283024,
7.72777716468133));
#265179=CARTESIAN_POINT('Ctrl Pts',(-0.622581294392751,-1.4256032907814,
7.72457213111181));
#265180=CARTESIAN_POINT('Ctrl Pts',(-0.640208273143459,-1.41777484826615,
7.72322496936125));
#265181=CARTESIAN_POINT('Ctrl Pts',(-0.664975222466122,-1.40621937454652,
7.72130003448778));
#265182=CARTESIAN_POINT('Ctrl Pts',(-0.672239329712773,-1.40276129653536,
7.72073148345927));
#265183=CARTESIAN_POINT('Ctrl Pts',(-0.684706589668946,-1.39670717923464,
7.71974865975055));
#265184=CARTESIAN_POINT('Ctrl Pts',(-0.689922667784157,-1.39413800223002,
7.71933532465271));
#265185=CARTESIAN_POINT('Ctrl Pts',(-0.699875088446938,-1.38916640987235,
7.71854250394612));
#265186=CARTESIAN_POINT('Ctrl Pts',(-0.704613781951205,-1.3867688598829,
7.71816319296184));
#265187=CARTESIAN_POINT('Ctrl Pts',(-0.715695166034011,-1.3810907539711,
7.71727184466424));
#265188=CARTESIAN_POINT('Ctrl Pts',(-0.722027681939302,-1.37779071877645,
7.71675912804184));
#265189=CARTESIAN_POINT('Ctrl Pts',(-0.743728774016894,-1.36629103287496,
7.71499035452341));
#265190=CARTESIAN_POINT('Ctrl Pts',(-0.758981695200941,-1.357877172766,
7.71372676072522));
#265191=CARTESIAN_POINT('Ctrl Pts',(-0.903270818546592,-1.27509334835873,
7.7015721810353));
#265192=CARTESIAN_POINT('Ctrl Pts',(-1.0211140946012,-1.18282131655117,
7.68997794583094));
#265193=CARTESIAN_POINT('Ctrl Pts',(-1.16573200959568,-1.03164476795007,
7.67381614680732));
#265194=CARTESIAN_POINT('Ctrl Pts',(-1.20487961982564,-0.985641336427132,
7.66919820917181));
#265195=CARTESIAN_POINT('Ctrl Pts',(-1.24831497998684,-0.928130945372148,
7.66386735198637));
#265196=CARTESIAN_POINT('Ctrl Pts',(-1.25526612206363,-0.918707965513631,
7.66300727902685));
#265197=CARTESIAN_POINT('Ctrl Pts',(-1.26482664167549,-0.90543658544346,
7.66181548120623));
#265198=CARTESIAN_POINT('Ctrl Pts',(-1.26752594902065,-0.901653932402147,
7.66147797555259));
#265199=CARTESIAN_POINT('Ctrl Pts',(-1.27209353211102,-0.895192137311736,
7.66090521043141));
#265200=CARTESIAN_POINT('Ctrl Pts',(-1.27397038085016,-0.892519123977094,
7.66066937316643));
#265201=CARTESIAN_POINT('Ctrl Pts',(-1.27756312786667,-0.887367899797427,
7.66021701520931));
#265202=CARTESIAN_POINT('Ctrl Pts',(-1.27928025122308,-0.884890600317002,
7.66000040771928));
#265203=CARTESIAN_POINT('Ctrl Pts',(-1.28337878888532,-0.878940762208461,
7.65948237489491));
#265204=CARTESIAN_POINT('Ctrl Pts',(-1.28575334300132,-0.875463489417652,
7.65918140991428));
#265205=CARTESIAN_POINT('Ctrl Pts',(-1.29428883190386,-0.862854571490478,
7.6580963667929));
#265206=CARTESIAN_POINT('Ctrl Pts',(-1.30036703847048,-0.853666899575775,
7.65731759472373));
#265207=CARTESIAN_POINT('Ctrl Pts',(-1.36838130548613,-0.748445831285959,
7.64852315279615));
#265208=CARTESIAN_POINT('Ctrl Pts',(-1.41966190567854,-0.645916061713906,
7.64110544999641));
#265209=CARTESIAN_POINT('Ctrl Pts',(-1.49487787601367,-0.442159977318249,
7.6267953288364));
#265210=CARTESIAN_POINT('Ctrl Pts',(-1.52083831292748,-0.342361535955896,
7.61995605885141));
#265211=CARTESIAN_POINT('Ctrl Pts',(-1.53877546691929,-0.22786020952655,
7.61185946083534));
#265212=CARTESIAN_POINT('Ctrl Pts',(-1.54063110139788,-0.214955818453811,
7.61094384646689));
#265213=CARTESIAN_POINT('Ctrl Pts',(-1.54321775922033,-0.195208920423094,
7.60953728221444));
#265214=CARTESIAN_POINT('Ctrl Pts',(-1.5440659790193,-0.188382124067505,
7.60905002182774));
#265215=CARTESIAN_POINT('Ctrl Pts',(-1.54546577691489,-0.176470783312541,
7.60819802898854));
#265216=CARTESIAN_POINT('Ctrl Pts',(-1.54603761988124,-0.171388686163955,
7.60783393950662));
#265217=CARTESIAN_POINT('Ctrl Pts',(-1.5472690277887,-0.159936903911657,
7.60701216700153));
#265218=CARTESIAN_POINT('Ctrl Pts',(-1.54791433749113,-0.153565813610403,
7.60655404306999));
#265219=CARTESIAN_POINT('Ctrl Pts',(-1.54954462222545,-0.136414433117057,
7.60531811971433));
#265220=CARTESIAN_POINT('Ctrl Pts',(-1.55045641628011,-0.125627719988751,
7.60453804413628));
#265221=CARTESIAN_POINT('Ctrl Pts',(-1.55410823177456,-0.0762959265605068,
7.60095704199649));
#265222=CARTESIAN_POINT('Ctrl Pts',(-1.55552369452298,-0.0376697688026779,
7.59811528973775));
#265223=CARTESIAN_POINT('Ctrl Pts',(-1.55540688544925,0.150416635516563,
7.58408028982375));
#265224=CARTESIAN_POINT('Ctrl Pts',(-1.53377345062266,0.299066134190454,
7.57227920445095));
#265225=CARTESIAN_POINT('Ctrl Pts',(-1.48021912918154,0.479632940477266,
7.55792515932282));
#265226=CARTESIAN_POINT('Ctrl Pts',(-1.46774814891127,0.51653889492002,
7.55499703045648));
#265227=CARTESIAN_POINT('Ctrl Pts',(-1.45154947782828,0.55913167113645,
7.55165343608403));
#265228=CARTESIAN_POINT('Ctrl Pts',(-1.44915565021815,0.565307012043805,
7.55116956610826));
#265229=CARTESIAN_POINT('Ctrl Pts',(-1.44521858207372,0.575274069562436,
7.55039027216243));
#265230=CARTESIAN_POINT('Ctrl Pts',(-1.44369972204418,0.579075227144306,
7.55009346803085));
#265231=CARTESIAN_POINT('Ctrl Pts',(-1.44097297017293,0.585821887140048,
7.549567433638));
#265232=CARTESIAN_POINT('Ctrl Pts',(-1.4397710258027,0.588769715745958,
7.5493378552839));
#265233=CARTESIAN_POINT('Ctrl Pts',(-1.43715635942363,0.595126426887807,
7.54884336836737));
#265234=CARTESIAN_POINT('Ctrl Pts',(-1.4357405569223,0.598533975132536,
7.54857864854596));
#265235=CARTESIAN_POINT('Ctrl Pts',(-1.43175906701959,0.608021190500929,
7.54784251799717));
#265236=CARTESIAN_POINT('Ctrl Pts',(-1.42916675767156,0.614089714134972,
7.54737267936209));
#265237=CARTESIAN_POINT('Ctrl Pts',(-1.4137968856831,0.649445622806684,
7.54464031872284));
#265238=CARTESIAN_POINT('Ctrl Pts',(-1.40015682304061,0.678352780941315,
7.54242630705351));
#265239=CARTESIAN_POINT('Ctrl Pts',(-1.31926184017515,0.836937168853864,
7.53027955017825));
#265240=CARTESIAN_POINT('Ctrl Pts',(-1.23489001193914,0.957063538313597,
7.52101017719817));
#265241=CARTESIAN_POINT('Ctrl Pts',(-1.10166319482847,1.09922410818106,
7.50786412318238));
#265242=CARTESIAN_POINT('Ctrl Pts',(-1.06668764609383,1.13319552506213,
7.50452525525777));
#265243=CARTESIAN_POINT('Ctrl Pts',(-1.02154822820113,1.17309510832862,
7.50030817755837));
#265244=CARTESIAN_POINT('Ctrl Pts',(-1.01283400866784,1.18062702577618,
7.49949811776615));
#265245=CARTESIAN_POINT('Ctrl Pts',(-0.998977887428836,1.19233691020467,
7.4982159153385));
#265246=CARTESIAN_POINT('Ctrl Pts',(-0.993891436302199,1.1965801007002,
7.49774644674226));
#265247=CARTESIAN_POINT('Ctrl Pts',(-0.984448981794201,1.20435538824518,
7.4968770678271));
#265248=CARTESIAN_POINT('Ctrl Pts',(-0.980100661277052,1.20789668068229,
7.49647753857119));
#265249=CARTESIAN_POINT('Ctrl Pts',(-0.97041495948219,1.21569802645794,
7.49558936661091));
#265250=CARTESIAN_POINT('Ctrl Pts',(-0.965068509004436,1.21994657886965,
7.4951002742896));
#265251=CARTESIAN_POINT('Ctrl Pts',(-0.94962358502861,1.23205480764965,
7.49369060207251));
#265252=CARTESIAN_POINT('Ctrl Pts',(-0.939456083731016,1.23982508880584,
7.49276652264346));
#265253=CARTESIAN_POINT('Ctrl Pts',(-0.858021967181582,1.30048239965521,
7.48539426721553));
#265254=CARTESIAN_POINT('Ctrl Pts',(-0.782457311706423,1.34729779674673,
7.47871271480738));
#265255=CARTESIAN_POINT('Ctrl Pts',(-0.617249944267438,1.43104726627118,
7.46446618506832));
#265256=CARTESIAN_POINT('Ctrl Pts',(-0.527299781985503,1.4665771805919,
7.45690437412503));
#265257=CARTESIAN_POINT('Ctrl Pts',(-0.397943811212079,1.50422120406867,
7.44664242473013));
#265258=CARTESIAN_POINT('Ctrl Pts',(-0.360865070993057,1.51354474945307,
7.44377009301013));
#265259=CARTESIAN_POINT('Ctrl Pts',(-0.317041739816991,1.52286180224509,
7.44048306877063));
#265260=CARTESIAN_POINT('Ctrl Pts',(-0.310597780899483,1.52418914709239,
7.44000244062227));
#265261=CARTESIAN_POINT('Ctrl Pts',(-0.300144060798938,1.52627338320887,
7.4392273325203));
#265262=CARTESIAN_POINT('Ctrl Pts',(-0.296139492547621,1.52705543432753,
7.43893149580905));
#265263=CARTESIAN_POINT('Ctrl Pts',(-0.289006193982606,1.52841937851943,
7.43840651592074));
#265264=CARTESIAN_POINT('Ctrl Pts',(-0.285878716748918,1.52900743516621,
7.43817703012195));
#265265=CARTESIAN_POINT('Ctrl Pts',(-0.279112012511478,1.53025828436994,
7.43768199208547));
#265266=CARTESIAN_POINT('Ctrl Pts',(-0.275472223684608,1.53091769444417,
7.43741663263853));
#265267=CARTESIAN_POINT('Ctrl Pts',(-0.265291788270658,1.53272457173178,
7.43667690704203));
#265268=CARTESIAN_POINT('Ctrl Pts',(-0.258745990050451,1.53384316752804,
7.43620413796779));
#265269=CARTESIAN_POINT('Ctrl Pts',(-0.219951830195686,1.54021719316147,
7.43341804977357));
#265270=CARTESIAN_POINT('Ctrl Pts',(-0.187548638084819,1.54449788451224,
7.43115549720283));
#265271=CARTESIAN_POINT('Ctrl Pts',(0.000741595742554217,1.56335808149029,
7.41825407281852));
#265272=CARTESIAN_POINT('Ctrl Pts',(0.157984611973251,1.55535825196448,
7.408361542596));
#265273=CARTESIAN_POINT('Ctrl Pts',(0.349576205186626,1.51621079659059,
7.39506688557467));
#265274=CARTESIAN_POINT('Ctrl Pts',(0.387445070355439,1.50697862893708,
7.39238197219455));
#265275=CARTESIAN_POINT('Ctrl Pts',(0.435368255556078,1.49336954259144,
7.38889056135292));
#265276=CARTESIAN_POINT('Ctrl Pts',(0.445780026480189,1.49029469101661,
7.38812631095396));
#265277=CARTESIAN_POINT('Ctrl Pts',(0.462287246255746,1.48523124370274,
7.38690513489867));
#265278=CARTESIAN_POINT('Ctrl Pts',(0.468404199163538,1.48331346966603,
7.3864505234079));
#265279=CARTESIAN_POINT('Ctrl Pts',(0.479378581668486,1.47979815207504,
7.38563106308403));
#265280=CARTESIAN_POINT('Ctrl Pts',(0.484240347923218,1.47821435514059,
7.38526667009684));
#265281=CARTESIAN_POINT('Ctrl Pts',(0.495615530637807,1.4744465707116,7.38441084253332));
#265282=CARTESIAN_POINT('Ctrl Pts',(0.502122417439701,1.4722433627612,7.38391878089058));
#265283=CARTESIAN_POINT('Ctrl Pts',(0.520891652498736,1.46574926636116,
7.38249202597401));
#265284=CARTESIAN_POINT('Ctrl Pts',(0.533114847244496,1.46134785936857,
7.38155369987066));
#265285=CARTESIAN_POINT('Ctrl Pts',(0.638448881193241,1.42192110264971,
7.37338576809402));
#265286=CARTESIAN_POINT('Ctrl Pts',(0.728037177866663,1.37819849138836,
7.36585900048933));
#265287=CARTESIAN_POINT('Ctrl Pts',(0.906587736774849,1.26876831388936,
7.34969140542793));
#265288=CARTESIAN_POINT('Ctrl Pts',(0.993997183648702,1.20151844453834,
7.34106041651668));
#265289=CARTESIAN_POINT('Ctrl Pts',(1.08523484875561,1.11449751864845,7.33165915261177));
#265290=CARTESIAN_POINT('Ctrl Pts',(1.09671131097907,1.10320612333384,7.33046909443327));
#265291=CARTESIAN_POINT('Ctrl Pts',(1.11219993606577,1.08748663153601,7.32885505999204));
#265292=CARTESIAN_POINT('Ctrl Pts',(1.11636447197925,1.0832110784049,7.32842027621277));
#265293=CARTESIAN_POINT('Ctrl Pts',(1.12296740869996,1.07635359371893,7.32772977833455));
#265294=CARTESIAN_POINT('Ctrl Pts',(1.12542169884342,1.07378715776256,7.32747286772583));
#265295=CARTESIAN_POINT('Ctrl Pts',(1.1300800178901,1.068882466794,7.32698479525348));
#265296=CARTESIAN_POINT('Ctrl Pts',(1.13228556417248,1.06654581525542,7.32675352223954));
#265297=CARTESIAN_POINT('Ctrl Pts',(1.13745098943792,1.06103925700916,7.32621139669419));
#265298=CARTESIAN_POINT('Ctrl Pts',(1.14040487350684,1.05786378328897,7.32590100187879));
#265299=CARTESIAN_POINT('Ctrl Pts',(1.15003152216796,1.04742779549515,7.32488802482539));
#265300=CARTESIAN_POINT('Ctrl Pts',(1.15664871235854,1.0401159830777,7.32418949077711));
#265301=CARTESIAN_POINT('Ctrl Pts',(1.22661614222199,0.961310351995921,
7.31677292968199));
#265302=CARTESIAN_POINT('Ctrl Pts',(1.28333255929694,0.884176656949972,
7.31048285538611));
#265303=CARTESIAN_POINT('Ctrl Pts',(1.3714501797936,0.737816074514749,7.29923695429479));
#265304=CARTESIAN_POINT('Ctrl Pts',(1.40551794632882,0.670634250618102,
7.29429994409142));
#265305=CARTESIAN_POINT('Ctrl Pts',(1.43457682219249,0.601306570085596,
7.28923406038337));
#265306=CARTESIAN_POINT('Ctrl Pts',(1.43457650415244,0.601307328854198,
7.14927790964297));
#265307=CARTESIAN_POINT('Ctrl Pts',(1.41398943702625,0.650423182547385,
7.15285502485694));
#265308=CARTESIAN_POINT('Ctrl Pts',(1.39087866118477,0.69848514105456,7.15649046759798));
#265309=CARTESIAN_POINT('Ctrl Pts',(1.35892565540541,0.75702021784198,7.16114736762822));
#265310=CARTESIAN_POINT('Ctrl Pts',(1.35237734923916,0.76865729223107,7.16208487945091));
#265311=CARTESIAN_POINT('Ctrl Pts',(1.34217024319219,0.786262206804669,
7.1635218694139));
#265312=CARTESIAN_POINT('Ctrl Pts',(1.33861951138496,0.792292256939287,
7.16401746119829));
#265313=CARTESIAN_POINT('Ctrl Pts',(1.33208386438546,0.8032221012684,7.16492206085695));
#265314=CARTESIAN_POINT('Ctrl Pts',(1.32911228162822,0.808129758721763,
7.16533057855338));
#265315=CARTESIAN_POINT('Ctrl Pts',(1.32263175798516,0.818700104313822,
7.16621560053504));
#265316=CARTESIAN_POINT('Ctrl Pts',(1.31911346601522,0.824356894348964,
7.166692441843));
#265317=CARTESIAN_POINT('Ctrl Pts',(1.30944361895239,0.839683876093768,
7.16799333233084));
#265318=CARTESIAN_POINT('Ctrl Pts',(1.30322145758343,0.849308790968366,
7.16881997710542));
#265319=CARTESIAN_POINT('Ctrl Pts',(1.27115064649358,0.897736061732842,
7.17302969502846));
#265320=CARTESIAN_POINT('Ctrl Pts',(1.24367576003486,0.935427047437751,
7.17647328433812));
#265321=CARTESIAN_POINT('Ctrl Pts',(1.1299708632001,1.07753154109983,7.19014209277467));
#265322=CARTESIAN_POINT('Ctrl Pts',(1.03195347200524,1.17173855075625,7.2008022149012));
#265323=CARTESIAN_POINT('Ctrl Pts',(0.887859264275082,1.27796447570786,
7.21448426746454));
#265324=CARTESIAN_POINT('Ctrl Pts',(0.851629092608341,1.30238858240716,
7.21777675723082));
#265325=CARTESIAN_POINT('Ctrl Pts',(0.808266580492868,1.32903629235091,
7.22151003593733));
#265326=CARTESIAN_POINT('Ctrl Pts',(0.80209165533007,1.33277204104875,7.22203692171207));
#265327=CARTESIAN_POINT('Ctrl Pts',(0.792581609299095,1.33843545862533,
7.22284087991231));
#265328=CARTESIAN_POINT('Ctrl Pts',(0.789265067188458,1.34039387453564,
7.22311986563767));
#265329=CARTESIAN_POINT('Ctrl Pts',(0.783166996480675,1.34396430028767,
7.22363024431901));
#265330=CARTESIAN_POINT('Ctrl Pts',(0.780387754915278,1.34558000031406,
7.22386186790278));
#265331=CARTESIAN_POINT('Ctrl Pts',(0.774138150741288,1.34918730445588,
7.2243805180618));
#265332=CARTESIAN_POINT('Ctrl Pts',(0.770665107094253,1.35117413852363,
7.22466723736186));
#265333=CARTESIAN_POINT('Ctrl Pts',(0.761762942798098,1.35622133480047,
7.22539842056664));
#265334=CARTESIAN_POINT('Ctrl Pts',(0.756322957720293,1.35926254898649,
7.22584169583896));
#265335=CARTESIAN_POINT('Ctrl Pts',(0.723864564103367,1.37715316083802,
7.22846647902005));
#265336=CARTESIAN_POINT('Ctrl Pts',(0.696425516106974,1.39123059601253,
7.23060305489848));
#265337=CARTESIAN_POINT('Ctrl Pts',(0.655607738352279,1.41066129077763,
7.23368941997518));
#265338=CARTESIAN_POINT('Ctrl Pts',(0.642546320808682,1.41665840404741,
7.23466360318313));
#265339=CARTESIAN_POINT('Ctrl Pts',(0.535898850775492,1.46384680800252,
7.24252425889092));
#265340=CARTESIAN_POINT('Ctrl Pts',(0.438538686898448,1.49590150191927,
7.24913551212262));
#265341=CARTESIAN_POINT('Ctrl Pts',(0.270498627689884,1.53339438374838,
7.26056963867525));
#265342=CARTESIAN_POINT('Ctrl Pts',(0.201324681096081,1.54399944986193,
7.26527976158312));
#265343=CARTESIAN_POINT('Ctrl Pts',(0.114754839431906,1.55135425860986,
7.27131859697339));
#265344=CARTESIAN_POINT('Ctrl Pts',(0.0978099212591027,1.55251469836456,
7.2725071375248));
#265345=CARTESIAN_POINT('Ctrl Pts',(0.0731557546212608,1.55379787836017,
7.27424741052073));
#265346=CARTESIAN_POINT('Ctrl Pts',(0.0654588031021716,1.55414116234069,
7.27479227033663));
#265347=CARTESIAN_POINT('Ctrl Pts',(0.0519495029807814,1.55464314382103,
7.27575144859764));
#265348=CARTESIAN_POINT('Ctrl Pts',(0.046138172307158,1.55482646069212,
7.27616499118432));
#265349=CARTESIAN_POINT('Ctrl Pts',(0.0348383495075163,1.55511950479854,
7.27697097312598));
#265350=CARTESIAN_POINT('Ctrl Pts',(0.0293500280368556,1.55523276689732,
7.27736329587723));
#265351=CARTESIAN_POINT('Ctrl Pts',(0.0146647588522598,1.55545806464564,
7.2784154044956));
#265352=CARTESIAN_POINT('Ctrl Pts',(0.00546734866940089,1.55551758182868,
7.27907681780282));
#265353=CARTESIAN_POINT('Ctrl Pts',(-0.028301481047181,1.55543660874141,
7.28151468293943));
#265354=CARTESIAN_POINT('Ctrl Pts',(-0.0528668654284095,1.55479547992107,
7.28330656675624));
#265355=CARTESIAN_POINT('Ctrl Pts',(-0.0823972219991191,1.55332415382531,
7.28548418914188));
#265356=CARTESIAN_POINT('Ctrl Pts',(-0.0873876539609487,1.55305139191809,
7.28585300083938));
#265357=CARTESIAN_POINT('Ctrl Pts',(-0.0978636054624743,1.55242815555241,
7.28662891961178));
#265358=CARTESIAN_POINT('Ctrl Pts',(-0.103348746186629,1.55207264608256,
7.2870361690614));
#265359=CARTESIAN_POINT('Ctrl Pts',(-0.261417359777088,1.54098607779415,
7.29880057662247));
#265360=CARTESIAN_POINT('Ctrl Pts',(-0.411578121216026,1.50783404403569,
7.31086310221171));
#265361=CARTESIAN_POINT('Ctrl Pts',(-0.594161124822741,1.43817948313455,
7.32578728750056));
#265362=CARTESIAN_POINT('Ctrl Pts',(-0.633249149293904,1.42140211836148,
7.328990172764));
#265363=CARTESIAN_POINT('Ctrl Pts',(-0.678073181700608,1.39994587100844,
7.33263496929858));
#265364=CARTESIAN_POINT('Ctrl Pts',(-0.684520533918495,1.39680468407892,
7.333158517463));
#265365=CARTESIAN_POINT('Ctrl Pts',(-0.6943882030226,1.39191236577429,7.33395846109885));
#265366=CARTESIAN_POINT('Ctrl Pts',(-0.697824026860519,1.39019302217144,
7.334236740962));
#265367=CARTESIAN_POINT('Ctrl Pts',(-0.704123452002819,1.38701144624944,
7.33474644209801));
#265368=CARTESIAN_POINT('Ctrl Pts',(-0.706988878182494,1.38555307160924,
7.33497808977931));
#265369=CARTESIAN_POINT('Ctrl Pts',(-0.71341996703927,1.38225478797445,
7.33549755542729));
#265370=CARTESIAN_POINT('Ctrl Pts',(-0.716983039370784,1.38040996464118,
7.3357850614605));
#265371=CARTESIAN_POINT('Ctrl Pts',(-0.726094470739885,1.37564761643639,
7.33651960615635));
#265372=CARTESIAN_POINT('Ctrl Pts',(-0.731632474806084,1.37271026454167,
7.33696543753028));
#265373=CARTESIAN_POINT('Ctrl Pts',(-0.764812012845302,1.35485403219029,
7.33963364953554));
#265374=CARTESIAN_POINT('Ctrl Pts',(-0.792016620364079,1.33913288715165,
7.34180936497323));
#265375=CARTESIAN_POINT('Ctrl Pts',(-0.901735160130949,1.27121370357814,
7.35061355678636));
#265376=CARTESIAN_POINT('Ctrl Pts',(-0.979727552594015,1.21212543894205,
7.35695310320468));
#265377=CARTESIAN_POINT('Ctrl Pts',(-1.12131590887796,1.08220389796188,
7.36963683760438));
#265378=CARTESIAN_POINT('Ctrl Pts',(-1.18498025485092,1.01209307693474,
7.37595089388379));
#265379=CARTESIAN_POINT('Ctrl Pts',(-1.24972659564271,0.926246903548408,
7.38346285296436));
#265380=CARTESIAN_POINT('Ctrl Pts',(-1.25743823670015,0.91575048618445,
7.38437762187835));
#265381=CARTESIAN_POINT('Ctrl Pts',(-1.26904923122958,0.89952338225409,
7.38578686996342));
#265382=CARTESIAN_POINT('Ctrl Pts',(-1.27304374357368,0.893861225606914,
7.38627769340818));
#265383=CARTESIAN_POINT('Ctrl Pts',(-1.27995575823998,0.883923243014669,
7.3871376894154));
#265384=CARTESIAN_POINT('Ctrl Pts',(-1.28289002168109,0.87965915767313,
7.38750621778068));
#265385=CARTESIAN_POINT('Ctrl Pts',(-1.28946897310009,0.869995663453272,
7.38834038882606));
#265386=CARTESIAN_POINT('Ctrl Pts',(-1.29310111469933,0.864587873957569,
7.38880649552927));
#265387=CARTESIAN_POINT('Ctrl Pts',(-1.30282756740133,0.849908047852611,
7.39006998705747));
#265388=CARTESIAN_POINT('Ctrl Pts',(-1.30885671215645,0.840593513760586,
7.39086977975392));
#265389=CARTESIAN_POINT('Ctrl Pts',(-1.33649926011445,0.796869566371059,
7.39461605198089));
#265390=CARTESIAN_POINT('Ctrl Pts',(-1.35685678220359,0.761689231409419,
7.39760780518503));
#265391=CARTESIAN_POINT('Ctrl Pts',(-1.38448052263844,0.709322980046774,
7.40203334317762));
#265392=CARTESIAN_POINT('Ctrl Pts',(-1.39285332149625,0.692737312959795,
7.40343101771053));
#265393=CARTESIAN_POINT('Ctrl Pts',(-1.45625877456422,0.561338527483712,
7.41447081481527));
#265394=CARTESIAN_POINT('Ctrl Pts',(-1.49729632470014,0.44032785169477,
7.42449674037175));
#265395=CARTESIAN_POINT('Ctrl Pts',(-1.53130192038005,0.276253267129787,
7.43727361028639));
#265396=CARTESIAN_POINT('Ctrl Pts',(-1.53794026375515,0.236520353452068,
7.44030240415309));
#265397=CARTESIAN_POINT('Ctrl Pts',(-1.54392402291332,0.189549359214922,
7.44377455408231));
#265398=CARTESIAN_POINT('Ctrl Pts',(-1.54477056875129,0.18252189773683,
7.44429119016678));
#265399=CARTESIAN_POINT('Ctrl Pts',(-1.54600032748235,0.171691132720457,
7.44508281345796));
#265400=CARTESIAN_POINT('Ctrl Pts',(-1.54641752623545,0.167891908783323,
7.44535962579538));
#265401=CARTESIAN_POINT('Ctrl Pts',(-1.54716001997004,0.160892720638553,
7.44586793269665));
#265402=CARTESIAN_POINT('Ctrl Pts',(-1.54748939183999,0.157693302018606,
7.44609964486358));
#265403=CARTESIAN_POINT('Ctrl Pts',(-1.54820971888121,0.150476598889468,
7.44662087074211));
#265404=CARTESIAN_POINT('Ctrl Pts',(-1.54859496304228,0.146458806106144,
7.44691006256263));
#265405=CARTESIAN_POINT('Ctrl Pts',(-1.54954575356094,0.136119392907673,
7.44765182348297));
#265406=CARTESIAN_POINT('Ctrl Pts',(-1.55008826370437,0.129795646622869,
7.44810314480199));
#265407=CARTESIAN_POINT('Ctrl Pts',(-1.55318941425712,0.0908495592073391,
7.45086922410159));
#265408=CARTESIAN_POINT('Ctrl Pts',(-1.55475707142191,0.0581536124806726,
7.4531332783272));
#265409=CARTESIAN_POINT('Ctrl Pts',(-1.55542535573004,0.0172809625157889,
7.4559183916929));
#265410=CARTESIAN_POINT('Ctrl Pts',(-1.55549454975572,0.00913120996006105,
7.45647148409281));
#265411=CARTESIAN_POINT('Ctrl Pts',(-1.55558306867206,-0.13120281373001,
7.46596250448332));
#265412=CARTESIAN_POINT('Ctrl Pts',(-1.53881797602093,-0.26286247137312,
7.47441018750964));
#265413=CARTESIAN_POINT('Ctrl Pts',(-1.4925081184459,-0.441266040778045,
7.4868162065679));
#265414=CARTESIAN_POINT('Ctrl Pts',(-1.47688878599857,-0.491014008997499,
7.49037918562025));
#265415=CARTESIAN_POINT('Ctrl Pts',(-1.45504567123091,-0.550036002399161,
7.49478217292608));
#265416=CARTESIAN_POINT('Ctrl Pts',(-1.45118142837119,-0.560151730168049,
7.49554312891732));
#265417=CARTESIAN_POINT('Ctrl Pts',(-1.44461681341238,-0.576812472106778,
7.49680736949767));
#265418=CARTESIAN_POINT('Ctrl Pts',(-1.44197676452556,-0.583380984559844,
7.4973086347027));
#265419=CARTESIAN_POINT('Ctrl Pts',(-1.43711434861855,-0.595244125472339,
7.49821921669866));
#265420=CARTESIAN_POINT('Ctrl Pts',(-1.43490731337792,-0.600544936129068,
7.49862801047416));
#265421=CARTESIAN_POINT('Ctrl Pts',(-1.43010113693995,-0.611910552986962,
7.49950871304516));
#265422=CARTESIAN_POINT('Ctrl Pts',(-1.42749266247622,-0.617971263759118,
7.49998093199145));
#265423=CARTESIAN_POINT('Ctrl Pts',(-1.42024089598966,-0.634529594556464,
7.50127828213408));
#265424=CARTESIAN_POINT('Ctrl Pts',(-1.41551992219933,-0.644992516036362,
7.50210604663793));
#265425=CARTESIAN_POINT('Ctrl Pts',(-1.3886593592306,-0.7028070478571,7.50672556396649));
#265426=CARTESIAN_POINT('Ctrl Pts',(-1.36426220500353,-0.749066096014676,
7.51059451184402));
#265427=CARTESIAN_POINT('Ctrl Pts',(-1.27167108507637,-0.9050456889936,
7.52426660179247));
#265428=CARTESIAN_POINT('Ctrl Pts',(-1.19218687269172,-1.00744147854868,
7.53442651934219));
#265429=CARTESIAN_POINT('Ctrl Pts',(-1.08977095396671,-1.11005928583765,
7.54551256557175));
#265430=CARTESIAN_POINT('Ctrl Pts',(-1.07838302587464,-1.1211255203613,
7.54672085795936));
#265431=CARTESIAN_POINT('Ctrl Pts',(-1.04550822943724,-1.15210718197175,
7.55013613159798));
#265432=CARTESIAN_POINT('Ctrl Pts',(-1.02362396859282,-1.1715940765663,
7.55232380795466));
#265433=CARTESIAN_POINT('Ctrl Pts',(-0.996054008029764,-1.19478110321958,
7.55496377647592));
#265434=CARTESIAN_POINT('Ctrl Pts',(-0.990879334823756,-1.19907615260726,
7.55545442047196));
#265435=CARTESIAN_POINT('Ctrl Pts',(-0.982747568153337,-1.20573703816376,
7.55621767786679));
#265436=CARTESIAN_POINT('Ctrl Pts',(-0.97980949717901,-1.20812579559375,
7.55649188164494));
#265437=CARTESIAN_POINT('Ctrl Pts',(-0.974357567619555,-1.21252544012498,
7.55699776171194));
#265438=CARTESIAN_POINT('Ctrl Pts',(-0.971846207608002,-1.21453923841869,
7.55722963983249));
#265439=CARTESIAN_POINT('Ctrl Pts',(-0.966136717817111,-1.21908849066606,
7.55775422589511));
#265440=CARTESIAN_POINT('Ctrl Pts',(-0.962934853161479,-1.22161916127019,
7.55804659326358));
#265441=CARTESIAN_POINT('Ctrl Pts',(-0.953163544083775,-1.22927986295967,
7.55893344045983));
#265442=CARTESIAN_POINT('Ctrl Pts',(-0.946562650311138,-1.23436983131031,
7.55952517771302));
#265443=CARTESIAN_POINT('Ctrl Pts',(-0.93118061511606,-1.24603500794568,
7.5608879987941));
#265444=CARTESIAN_POINT('Ctrl Pts',(-0.92237008940139,-1.25257096157342,
7.56165662960579));
#265445=CARTESIAN_POINT('Ctrl Pts',(-0.891928383832259,-1.27465827217729,
7.56427450201624));
#265446=CARTESIAN_POINT('Ctrl Pts',(-0.869966124707353,-1.2897476806665,
7.56609857267938));
#265447=CARTESIAN_POINT('Ctrl Pts',(-0.744964293400565,-1.37098473805262,
7.57619099081975));
#265448=CARTESIAN_POINT('Ctrl Pts',(-0.634780217955134,-1.42535231875577,
7.5840448544213));
#265449=CARTESIAN_POINT('Ctrl Pts',(-0.460876068021626,-1.48695062201216,
7.59638505187517));
#265450=CARTESIAN_POINT('Ctrl Pts',(-0.401218774456614,-1.50414456753985,
7.60060300657389));
#265451=CARTESIAN_POINT('Ctrl Pts',(-0.329660130594825,-1.52020803139373,
7.60572997214039));
#265452=CARTESIAN_POINT('Ctrl Pts',(-0.31859424337832,-1.52256558368447,
7.60652457906888));
#265453=CARTESIAN_POINT('Ctrl Pts',(-0.300418613494051,-1.52623102748755,
7.60783309026897));
#265454=CARTESIAN_POINT('Ctrl Pts',(-0.293323589054237,-1.52761047440765,
7.60834471761083));
#265455=CARTESIAN_POINT('Ctrl Pts',(-0.28056355729229,-1.52999916630627,
7.60926647645861));
#265456=CARTESIAN_POINT('Ctrl Pts',(-0.274902038801047,-1.53102652688094,
7.6096760251542));
#265457=CARTESIAN_POINT('Ctrl Pts',(-0.262837521846903,-1.53314672458383,
7.61055004194072));
#265458=CARTESIAN_POINT('Ctrl Pts',(-0.256433135898578,-1.53423091040514,
7.61101477565972));
#265459=CARTESIAN_POINT('Ctrl Pts',(-0.239155631092851,-1.53704458258821,
7.61227068502825));
#265460=CARTESIAN_POINT('Ctrl Pts',(-0.228270811383216,-1.53869876513861,
7.61306421925459));
#265461=CARTESIAN_POINT('Ctrl Pts',(-0.172508789370332,-1.54656831177633,
7.61714203885514));
#265462=CARTESIAN_POINT('Ctrl Pts',(-0.127397517273259,-1.55093582030455,
7.6204836108021));
#265463=CARTESIAN_POINT('Ctrl Pts',(0.00710775874016667,-1.55805053643489,
7.63058333437894));
#265464=CARTESIAN_POINT('Ctrl Pts',(0.0966102331198495,-1.5550674457057,
7.63749282959576));
#265465=CARTESIAN_POINT('Ctrl Pts',(0.219958641650496,-1.54026410120411,
7.64712659900582));
#265466=CARTESIAN_POINT('Ctrl Pts',(0.254419274053056,-1.53494828579841,
7.64982844410327));
#265467=CARTESIAN_POINT('Ctrl Pts',(0.343449220867888,-1.51813384095952,
7.65680151142424));
#265468=CARTESIAN_POINT('Ctrl Pts',(0.397637107601824,-1.50485016320981,
7.66103921955609));
#265469=CARTESIAN_POINT('Ctrl Pts',(0.458579561074521,-1.48638748216307,
7.66571797101357));
#265470=CARTESIAN_POINT('Ctrl Pts',(0.466140996847573,-1.48403353705964,
7.66629689758326));
#265471=CARTESIAN_POINT('Ctrl Pts',(0.477542316735609,-1.48038845951527,
7.66716707162346));
#265472=CARTESIAN_POINT('Ctrl Pts',(0.481395524026743,-1.47913995476937,
7.66746068056055));
#265473=CARTESIAN_POINT('Ctrl Pts',(0.488300437989079,-1.4768728049707,
7.66798591503389));
#265474=CARTESIAN_POINT('Ctrl Pts',(0.491353886214399,-1.47585973552692,
7.66821785683763));
#265475=CARTESIAN_POINT('Ctrl Pts',(0.49801717093406,-1.4736260269877,7.66872329208184));
#265476=CARTESIAN_POINT('Ctrl Pts',(0.501625667673291,-1.47240159614631,
7.66899655962782));
#265477=CARTESIAN_POINT('Ctrl Pts',(0.511873158073115,-1.46888238506152,
7.6697714073045));
#265478=CARTESIAN_POINT('Ctrl Pts',(0.518501272205361,-1.46655583827937,
7.67027116530838));
#265479=CARTESIAN_POINT('Ctrl Pts',(0.561873409342252,-1.45100090043244,
7.67353353147966));
#265480=CARTESIAN_POINT('Ctrl Pts',(0.598127702132498,-1.4364362977732,
7.6762233711843));
#265481=CARTESIAN_POINT('Ctrl Pts',(0.740704026296866,-1.37282250640302,
7.68679917912225));
#265482=CARTESIAN_POINT('Ctrl Pts',(0.841888953050843,-1.31320640691412,
7.69432490466026));
#265483=CARTESIAN_POINT('Ctrl Pts',(0.946141601383891,-1.23473720740609,
7.70302539410244));
#265484=CARTESIAN_POINT('Ctrl Pts',(0.956745708425602,-1.22653884528527,
7.70392201923503));
#265485=CARTESIAN_POINT('Ctrl Pts',(1.0070467310327,-1.18660033216036,7.70823597009322));
#265486=CARTESIAN_POINT('Ctrl Pts',(1.04527436196011,-1.15306726263229,
7.71170006718917));
#265487=CARTESIAN_POINT('Ctrl Pts',(1.09251232593085,-1.10734807081034,
7.71628113087147));
#265488=CARTESIAN_POINT('Ctrl Pts',(1.10308489011261,-1.09681658922292,
7.71732729402976));
#265489=CARTESIAN_POINT('Ctrl Pts',(1.11861159496126,-1.08089863363399,
7.71889622211266));
#265490=CARTESIAN_POINT('Ctrl Pts',(1.12368212060252,-1.07562644310819,
7.7194139079532));
#265491=CARTESIAN_POINT('Ctrl Pts',(1.1326805079814,-1.06613710508224,7.72034232949656));
#265492=CARTESIAN_POINT('Ctrl Pts',(1.13662250295984,-1.06193349326789,
7.72075244743263));
#265493=CARTESIAN_POINT('Ctrl Pts',(1.14492159629079,-1.05298446849821,
7.72162317146589));
#265494=CARTESIAN_POINT('Ctrl Pts',(1.14927274318288,-1.04823371059283,
7.72208401944987));
#265495=CARTESIAN_POINT('Ctrl Pts',(1.16081725136802,-1.03547066548159,
7.72331850520579));
#265496=CARTESIAN_POINT('Ctrl Pts',(1.16795702523926,-1.0274106124187,7.72409436458778));
#265497=CARTESIAN_POINT('Ctrl Pts',(1.20264076782716,-0.987427549722852,
7.72792566049681));
#265498=CARTESIAN_POINT('Ctrl Pts',(1.22896007070618,-0.954470793493423,
7.73103038492061));
#265499=CARTESIAN_POINT('Ctrl Pts',(1.34534226448227,-0.79593286110363,
7.74574064312489));
#265500=CARTESIAN_POINT('Ctrl Pts',(1.41769039691832,-0.658479161179764,
7.7579806652478));
#265501=CARTESIAN_POINT('Ctrl Pts',(1.47885315116279,-0.483261694965158,
7.77203516592401));
#265502=CARTESIAN_POINT('Ctrl Pts',(1.48822529707258,-0.453579451468234,
7.77436214251193));
#265503=CARTESIAN_POINT('Ctrl Pts',(1.49840357577635,-0.417619491806089,
7.77710175178937));
#265504=CARTESIAN_POINT('Ctrl Pts',(1.50006958328761,-0.411595146538542,
7.77755806504056));
#265505=CARTESIAN_POINT('Ctrl Pts',(1.50274391385478,-0.401692709279255,
7.77830359925158));
#265506=CARTESIAN_POINT('Ctrl Pts',(1.50377362481527,-0.39782054949852,
7.77859399515349));
#265507=CARTESIAN_POINT('Ctrl Pts',(1.5056026007616,-0.390834229148045,
7.77911585070944));
#265508=CARTESIAN_POINT('Ctrl Pts',(1.50640717759243,-0.387721552142953,
7.77934760804672));
#265509=CARTESIAN_POINT('Ctrl Pts',(1.50815325127212,-0.380879007136704,
7.77985543096226));
#265510=CARTESIAN_POINT('Ctrl Pts',(1.5090905638084,-0.377148138653765,
7.78013125484866));
#265511=CARTESIAN_POINT('Ctrl Pts',(1.51174107369642,-0.366429982573151,
7.78092070089002));
#265512=CARTESIAN_POINT('Ctrl Pts',(1.51341968106794,-0.35943411122582,
7.78143239121367));
#265513=CARTESIAN_POINT('Ctrl Pts',(1.52481154014552,-0.310461559730384,
7.78499091343881));
#265514=CARTESIAN_POINT('Ctrl Pts',(1.53282668064198,-0.268104121047499,
7.78794893120415));
#265515=CARTESIAN_POINT('Ctrl Pts',(1.56259413327522,-0.0649040653522604,
7.80180981163363));
#265516=CARTESIAN_POINT('Ctrl Pts',(1.56084819286634,0.098344275979195,
7.81208305174017));
#265517=CARTESIAN_POINT('Ctrl Pts',(1.5297333463465,0.283059065311713,7.82498177226162));
#265518=CARTESIAN_POINT('Ctrl Pts',(1.52498161346089,0.307632088629587,
7.82672155928336));
#265519=CARTESIAN_POINT('Ctrl Pts',(1.51766163396118,0.341129362340106,
7.82913106988495));
#265520=CARTESIAN_POINT('Ctrl Pts',(1.51560305295116,0.350162042918745,
7.82978460283131));
#265521=CARTESIAN_POINT('Ctrl Pts',(1.51219342557476,0.364529243151413,
7.8308304050178));
#265522=CARTESIAN_POINT('Ctrl Pts',(1.51089452116865,0.369876019702916,
7.83122100016026));
#265523=CARTESIAN_POINT('Ctrl Pts',(1.50816630265589,0.380852183806567,
7.83202577124372));
#265524=CARTESIAN_POINT('Ctrl Pts',(1.50673377486618,0.386480675290505,
7.83244004485625));
#265525=CARTESIAN_POINT('Ctrl Pts',(1.50333819150548,0.399516270086498,
7.83340327303896));
#265526=CARTESIAN_POINT('Ctrl Pts',(1.50135187074254,0.40691709773435,7.8339529700567));
#265527=CARTESIAN_POINT('Ctrl Pts',(1.49484833245561,0.430452603071676,
7.83571031090906));
#265528=CARTESIAN_POINT('Ctrl Pts',(1.49012520958054,0.446528609978834,
7.83692457487138));
#265529=CARTESIAN_POINT('Ctrl Pts',(1.47049041665882,0.509574951384381,
7.84174352386162));
#265530=CARTESIAN_POINT('Ctrl Pts',(1.45361447403242,0.555887219104188,
7.84541014903729));
#265531=CARTESIAN_POINT('Ctrl Pts',(1.43457666579773,0.601306943206762,
7.84913521677167));
#265532=CARTESIAN_POINT('Origin',(0.,0.,-1.29405622560371));
#265533=CARTESIAN_POINT('',(1.43456415251412,0.601298694836466,8.68837676241652));
#265534=CARTESIAN_POINT('',(1.43457668241997,0.601306903550017,8.55150209358323));
#265535=CARTESIAN_POINT('',(1.43457668357355,0.601306900797845,-1.29405622560371));
#265536=CARTESIAN_POINT('',(-1.55430433363989,-0.00129356757865576,8.29405691353744));
#265537=CARTESIAN_POINT('Ctrl Pts',(-1.55430433363989,-0.00129356757865576,
8.29405691353744));
#265538=CARTESIAN_POINT('Ctrl Pts',(-1.55556915289093,-0.163823035851805,
8.30567841650669));
#265539=CARTESIAN_POINT('Ctrl Pts',(-1.45729141273118,-0.84303952995183,
8.35435184806778));
#265540=CARTESIAN_POINT('Ctrl Pts',(-0.472877852103197,-1.77676948847047,
8.44007720822072));
#265541=CARTESIAN_POINT('Ctrl Pts',(1.23652006183316,-1.36071356826243,
8.55123299399628));
#265542=CARTESIAN_POINT('Ctrl Pts',(1.66634991413392,-0.123264202437792,
8.63399951206154));
#265543=CARTESIAN_POINT('Ctrl Pts',(1.482431870734,0.490255529475159,8.67971410153496));
#265544=CARTESIAN_POINT('Ctrl Pts',(1.43456415251406,0.601298694836608,
8.68837676241653));
#265545=CARTESIAN_POINT('Ctrl Pts',(-1.55549950636669,-0.00123923080959585,
8.29474377359494));
#265546=CARTESIAN_POINT('Ctrl Pts',(-1.55555800331462,0.0721869404360917,
8.28986293506811));
#265547=CARTESIAN_POINT('Ctrl Pts',(-1.55041757773132,0.145517316076241,
8.28490362734154));
#265548=CARTESIAN_POINT('Ctrl Pts',(-1.53880297273442,0.227494320910168,
8.27912116304748));
#265549=CARTESIAN_POINT('Ctrl Pts',(-1.53740301704474,0.236770376927224,
8.2784634717434));
#265550=CARTESIAN_POINT('Ctrl Pts',(-1.53490673599696,0.25235400078937,
8.27735257567762));
#265551=CARTESIAN_POINT('Ctrl Pts',(-1.53385520664464,0.258668577097848,
8.27690077535223));
#265552=CARTESIAN_POINT('Ctrl Pts',(-1.53185454943286,0.270241444900713,
8.27606961412405));
#265553=CARTESIAN_POINT('Ctrl Pts',(-1.53091724405785,0.27550170546079,
8.27569063094717));
#265554=CARTESIAN_POINT('Ctrl Pts',(-1.52892979495897,0.286332080958602,
8.27490782764597));
#265555=CARTESIAN_POINT('Ctrl Pts',(-1.52787627095401,0.291901486109944,
8.27450390570557));
#265556=CARTESIAN_POINT('Ctrl Pts',(-1.52545868616356,0.304310175100152,
8.27360083350147));
#265557=CARTESIAN_POINT('Ctrl Pts',(-1.52407902999164,0.311146257036973,
8.27310119413207));
#265558=CARTESIAN_POINT('Ctrl Pts',(-1.52047867761881,0.328387009307086,
8.27183559523233));
#265559=CARTESIAN_POINT('Ctrl Pts',(-1.51819714916477,0.338778456780612,
8.2710677113846));
#265560=CARTESIAN_POINT('Ctrl Pts',(-1.50435830457567,0.398859574621789,
8.26659771098052));
#265561=CARTESIAN_POINT('Ctrl Pts',(-1.49046996029146,0.447974403057745,
8.26282169437105));
#265562=CARTESIAN_POINT('Ctrl Pts',(-1.46171716586699,0.533378582557028,
8.25603193112348));
#265563=CARTESIAN_POINT('Ctrl Pts',(-1.44784595434876,0.569957461870795,
8.25304859337332));
#265564=CARTESIAN_POINT('Ctrl Pts',(-1.3917206393871,0.70264629207826,8.24196843163985));
#265565=CARTESIAN_POINT('Ctrl Pts',(-1.34114979006821,0.794931228218884,
8.23372851004576));
#265566=CARTESIAN_POINT('Ctrl Pts',(-1.26394783602608,0.907190332163691,
8.22341385383531));
#265567=CARTESIAN_POINT('Ctrl Pts',(-1.2454505818406,0.932422453899455,
8.22107613301032));
#265568=CARTESIAN_POINT('Ctrl Pts',(-1.22215290023892,0.962271206866444,
8.21830261698896));
#265569=CARTESIAN_POINT('Ctrl Pts',(-1.21806939548715,0.967435030923994,
8.21782250223291));
#265570=CARTESIAN_POINT('Ctrl Pts',(-1.21164816643309,0.97544992744695,
8.21707703902307));
#265571=CARTESIAN_POINT('Ctrl Pts',(-1.2093329463875,0.978318795550197,
8.216810152838));
#265572=CARTESIAN_POINT('Ctrl Pts',(-1.20499915399602,0.983650052755884,
8.21631413699351));
#265573=CARTESIAN_POINT('Ctrl Pts',(-1.20298324009485,0.986114451662576,
8.21608483339675));
#265574=CARTESIAN_POINT('Ctrl Pts',(-1.19835508364815,0.991736930764364,
8.21556161803745));
#265575=CARTESIAN_POINT('Ctrl Pts',(-1.19573791829188,0.994890887557919,
8.21526806682134));
#265576=CARTESIAN_POINT('Ctrl Pts',(-1.1888481588737,1.00312730512772,8.21450122317806));
#265577=CARTESIAN_POINT('Ctrl Pts',(-1.18455537518924,1.00819288949375,
8.21402934790199));
#265578=CARTESIAN_POINT('Ctrl Pts',(-1.15459670129965,1.04308930798161,
8.21077562438545));
#265579=CARTESIAN_POINT('Ctrl Pts',(-1.1278366120487,1.07196738629967,8.20806760178269));
#265580=CARTESIAN_POINT('Ctrl Pts',(-1.06915709114227,1.13065784706923,
8.20245030725981));
#265581=CARTESIAN_POINT('Ctrl Pts',(-1.03702062841388,1.1602037328346,8.19955350748688));
#265582=CARTESIAN_POINT('Ctrl Pts',(-0.938469635021524,1.24343933836468,
8.19103707450139));
#265583=CARTESIAN_POINT('Ctrl Pts',(-0.868836231641056,1.29305437859497,
8.18546985188624));
#265584=CARTESIAN_POINT('Ctrl Pts',(-0.763174934736102,1.35593435694536,
8.17721510886089));
#265585=CARTESIAN_POINT('Ctrl Pts',(-0.730179824001388,1.37398364306361,
8.17466352251371));
#265586=CARTESIAN_POINT('Ctrl Pts',(-0.681686880066569,1.39827040782312,
8.17092603907807));
#265587=CARTESIAN_POINT('Ctrl Pts',(-0.666690549737799,1.40548241228625,
8.16977197673378));
#265588=CARTESIAN_POINT('Ctrl Pts',(-0.639697457887556,1.41793466311354,
8.16769576166707));
#265589=CARTESIAN_POINT('Ctrl Pts',(-0.627744647926366,1.42326673012896,
8.16677676610204));
#265590=CARTESIAN_POINT('Ctrl Pts',(-0.609427304986174,1.43116234551455,
8.16536829773446));
#265591=CARTESIAN_POINT('Ctrl Pts',(-0.603110521025703,1.43383576325269,
8.16488256109587));
#265592=CARTESIAN_POINT('Ctrl Pts',(-0.59154038896699,1.43864254257833,
8.16399271655461));
#265593=CARTESIAN_POINT('Ctrl Pts',(-0.58629263596578,1.44078913812796,
8.16358906422052));
#265594=CARTESIAN_POINT('Ctrl Pts',(-0.574997115473913,1.44533764610249,
8.16272004480705));
#265595=CARTESIAN_POINT('Ctrl Pts',(-0.568945796546169,1.44773038659055,
8.16225437810499));
#265596=CARTESIAN_POINT('Ctrl Pts',(-0.552617302692956,1.45406862042579,
8.1609974539653));
#265597=CARTESIAN_POINT('Ctrl Pts',(-0.542313132386138,1.45794303420796,
8.1602038410533));
#265598=CARTESIAN_POINT('Ctrl Pts',(-0.492638271464822,1.47602153529082,
8.15637516730867));
#265599=CARTESIAN_POINT('Ctrl Pts',(-0.452749721826082,1.48874078033503,
8.153291737583));
#265600=CARTESIAN_POINT('Ctrl Pts',(-0.396595415101199,1.5041811741996,
8.14893429421699));
#265601=CARTESIAN_POINT('Ctrl Pts',(-0.380723384715419,1.50827669866467,
8.14770094190195));
#265602=CARTESIAN_POINT('Ctrl Pts',(-0.265723312576222,1.53601978136456,
8.13875370447867));
#265603=CARTESIAN_POINT('Ctrl Pts',(-0.164554415138191,1.55012375297761,
8.13080024651919));
#265604=CARTESIAN_POINT('Ctrl Pts',(-0.00266892152673535,1.55665938383207,
8.11828696858117));
#265605=CARTESIAN_POINT('Ctrl Pts',(0.0575071180737391,1.55559962465264,
8.11368801022367));
#265606=CARTESIAN_POINT('Ctrl Pts',(0.128473761944692,1.55022461798343,
8.10842694656259));
#265607=CARTESIAN_POINT('Ctrl Pts',(0.139461833169841,1.54927476236112,
8.10761705045185));
#265608=CARTESIAN_POINT('Ctrl Pts',(0.155134359159196,1.5477518639912,8.10646944470276));
#265609=CARTESIAN_POINT('Ctrl Pts',(0.159827419346596,1.54727428062307,
8.10612677052034));
#265610=CARTESIAN_POINT('Ctrl Pts',(0.1677794949402,1.54642848094481,8.1055478592966));
#265611=CARTESIAN_POINT('Ctrl Pts',(0.171039623380809,1.54607129641874,
8.10531101485583));
#265612=CARTESIAN_POINT('Ctrl Pts',(0.177278292394793,1.54536780351663,
8.10485875628473));
#265613=CARTESIAN_POINT('Ctrl Pts',(0.180256981511212,1.54502319145505,
8.10464324552976));
#265614=CARTESIAN_POINT('Ctrl Pts',(0.188163432242469,1.54408529787098,
8.10407228480597));
#265615=CARTESIAN_POINT('Ctrl Pts',(0.193089438524406,1.54347703412698,
8.10371766807415));
#265616=CARTESIAN_POINT('Ctrl Pts',(0.210704272527838,1.54121630308869,
8.10245330711154));
#265617=CARTESIAN_POINT('Ctrl Pts',(0.223375968460891,1.53943080005486,
8.10155064672995));
#265618=CARTESIAN_POINT('Ctrl Pts',(0.240675904031166,1.53677503314644,
8.10032593511558));
#265619=CARTESIAN_POINT('Ctrl Pts',(0.245323884734482,1.5360399038166,8.09999764791956));
#265620=CARTESIAN_POINT('Ctrl Pts',(0.275934691326711,1.53105597921151,
8.09784016383745));
#265621=CARTESIAN_POINT('Ctrl Pts',(0.301791122452567,1.52616993207907,
8.09603938571672));
#265622=CARTESIAN_POINT('Ctrl Pts',(0.474057723194178,1.48906721226896,
8.08411180186584));
#265623=CARTESIAN_POINT('Ctrl Pts',(0.615273187488639,1.43648768689398,
8.07459684579213));
#265624=CARTESIAN_POINT('Ctrl Pts',(0.780661816275275,1.34597113673286,
8.06176754120594));
#265625=CARTESIAN_POINT('Ctrl Pts',(0.813828608596464,1.32618013281126,
8.05910472413832));
#265626=CARTESIAN_POINT('Ctrl Pts',(0.854935022211891,1.29952844186988,
8.05566874818335));
#265627=CARTESIAN_POINT('Ctrl Pts',(0.863590412455415,1.29379273983518,
8.0549373796178));
#265628=CARTESIAN_POINT('Ctrl Pts',(0.877409291745758,1.28443487770958,
8.05375659357633));
#265629=CARTESIAN_POINT('Ctrl Pts',(0.882609412425551,1.28086714505725,
8.05330922865636));
#265630=CARTESIAN_POINT('Ctrl Pts',(0.892468757460877,1.27401423325673,
8.0524551602779));
#265631=CARTESIAN_POINT('Ctrl Pts',(0.897131909043185,1.27073486053164,
8.05204868271276));
#265632=CARTESIAN_POINT('Ctrl Pts',(0.907739537359039,1.26318752922213,
8.05111817032449));
#265633=CARTESIAN_POINT('Ctrl Pts',(0.91367209445602,1.25890313451357,8.05059351002539));
#265634=CARTESIAN_POINT('Ctrl Pts',(0.92906665220717,1.24761930298959,8.04922077452249));
#265635=CARTESIAN_POINT('Ctrl Pts',(0.938479674543701,1.24055417283532,
8.04837016622288));
#265636=CARTESIAN_POINT('Ctrl Pts',(1.01078806641354,1.18498772500172,8.04174676509041));
#265637=CARTESIAN_POINT('Ctrl Pts',(1.06995465723761,1.131848726626,8.03578874999882));
#265638=CARTESIAN_POINT('Ctrl Pts',(1.19852823919503,0.997248252399454,
8.02152436166095));
#265639=CARTESIAN_POINT('Ctrl Pts',(1.26411410745924,0.912682093294212,
8.01314245103618));
#265640=CARTESIAN_POINT('Ctrl Pts',(1.34036313858407,0.790200050946843,
8.00216318935175));
#265641=CARTESIAN_POINT('Ctrl Pts',(1.35904440555938,0.75762018550548,7.99934476888847));
#265642=CARTESIAN_POINT('Ctrl Pts',(1.37974025109851,0.718292842199205,
7.99608726125419));
#265643=CARTESIAN_POINT('Ctrl Pts',(1.38290994378434,0.712171229262564,
7.99558425044966));
#265644=CARTESIAN_POINT('Ctrl Pts',(1.38774265323152,0.702683903396858,
7.99481113663631));
#265645=CARTESIAN_POINT('Ctrl Pts',(1.38943430421857,0.699333007058198,
7.99453931024038));
#265646=CARTESIAN_POINT('Ctrl Pts',(1.39253523132513,0.693134887057267,
7.99403883668529));
#265647=CARTESIAN_POINT('Ctrl Pts',(1.39394790605636,0.690289488341606,
7.99380998574304));
#265648=CARTESIAN_POINT('Ctrl Pts',(1.3971224453454,0.683845869428415,7.99329375981481));
#265649=CARTESIAN_POINT('Ctrl Pts',(1.39887912982315,0.680245162820598,
7.99300670775675));
#265650=CARTESIAN_POINT('Ctrl Pts',(1.40403681074975,0.669568900780746,
7.99215964817462));
#265651=CARTESIAN_POINT('Ctrl Pts',(1.40739824525674,0.662474199451847,
7.99160201259709));
#265652=CARTESIAN_POINT('Ctrl Pts',(1.41900527544585,0.637489073498865,
7.98965553833988));
#265653=CARTESIAN_POINT('Ctrl Pts',(1.42696355777115,0.619470026600121,
7.98828273283126));
#265654=CARTESIAN_POINT('Ctrl Pts',(1.43457668592364,0.601306895191089,
7.98692484967426));
#265655=CARTESIAN_POINT('',(-1.55549984464226,0.000695210683922209,8.15469955740614));
#265656=CARTESIAN_POINT('Ctrl Pts',(1.43457666579773,0.601306943206762,
7.84913521677167));
#265657=CARTESIAN_POINT('Ctrl Pts',(1.42730805505206,0.618648135565035,
7.85055744285088));
#265658=CARTESIAN_POINT('Ctrl Pts',(1.41972430193386,0.635859233078565,
7.85198801424808));
#265659=CARTESIAN_POINT('Ctrl Pts',(1.37048245083437,0.742334480696986,
7.86095394217987));
#265660=CARTESIAN_POINT('Ctrl Pts',(1.3207408205474,0.827601753122177,7.86866671493112));
#265661=CARTESIAN_POINT('Ctrl Pts',(1.2564382022965,0.917104424693805,7.87712260980895));
#265662=CARTESIAN_POINT('Ctrl Pts',(1.24949566175549,0.926540924272781,
7.87801871951594));
#265663=CARTESIAN_POINT('Ctrl Pts',(1.219219555577,0.966733816464096,7.88185276884756));
#265664=CARTESIAN_POINT('Ctrl Pts',(1.19484968360784,0.996697268569604,
7.88475525689621));
#265665=CARTESIAN_POINT('Ctrl Pts',(1.16500159638469,1.03072584615701,7.88807662292849));
#265666=CARTESIAN_POINT('Ctrl Pts',(1.16058348785602,1.03569805515343,7.8885625842427));
#265667=CARTESIAN_POINT('Ctrl Pts',(1.15337162942885,1.04371029388466,7.88934650595298));
#265668=CARTESIAN_POINT('Ctrl Pts',(1.15059749402807,1.04676773972782,7.8896458492236));
#265669=CARTESIAN_POINT('Ctrl Pts',(1.14563616852879,1.05219219018185,7.89017723965831));
#265670=CARTESIAN_POINT('Ctrl Pts',(1.14345376789805,1.05456347230107,7.890409636042));
#265671=CARTESIAN_POINT('Ctrl Pts',(1.13871450846461,1.05968089353644,7.89091137680006));
#265672=CARTESIAN_POINT('Ctrl Pts',(1.1361550814151,1.06242456659007,7.8911805212424));
#265673=CARTESIAN_POINT('Ctrl Pts',(1.12896122891252,1.07008055832774,7.89193203090513));
#265674=CARTESIAN_POINT('Ctrl Pts',(1.1243046280568,1.07497207659651,7.89241274316735));
#265675=CARTESIAN_POINT('Ctrl Pts',(1.09625128525972,1.10405895436659,7.89527579304267));
#265676=CARTESIAN_POINT('Ctrl Pts',(1.07210398950781,1.12752229277917,7.89760434502244));
#265677=CARTESIAN_POINT('Ctrl Pts',(0.91825730188085,1.26759542740874,7.91177412484334));
#265678=CARTESIAN_POINT('Ctrl Pts',(0.770475841595645,1.36248779742735,
7.92272624386276));
#265679=CARTESIAN_POINT('Ctrl Pts',(0.605598892397629,1.43277818241746,
7.93508636522951));
#265680=CARTESIAN_POINT('Ctrl Pts',(0.601170094425466,1.43464206519247,
7.93541834226346));
#265681=CARTESIAN_POINT('Ctrl Pts',(0.578159704862451,1.44420084922901,
7.93714316009448));
#265682=CARTESIAN_POINT('Ctrl Pts',(0.559439533646009,1.45155505605429,
7.93854638720514));
#265683=CARTESIAN_POINT('Ctrl Pts',(0.532628873587588,1.46149193906925,
7.94055866077775));
#265684=CARTESIAN_POINT('Ctrl Pts',(0.524651142286897,1.46437473985649,
7.94115774668733));
#265685=CARTESIAN_POINT('Ctrl Pts',(0.511597302619728,1.46897145976029,
7.94213872303459));
#265686=CARTESIAN_POINT('Ctrl Pts',(0.506535134111979,1.47072468743797,
7.94251930801296));
#265687=CARTESIAN_POINT('Ctrl Pts',(0.495869849559574,1.47435689957113,
7.94332155963113));
#265688=CARTESIAN_POINT('Ctrl Pts',(0.490264892187487,1.47623016793789,
7.9437434072615));
#265689=CARTESIAN_POINT('Ctrl Pts',(0.476799849649903,1.48064526287979,
7.94475747505836));
#265690=CARTESIAN_POINT('Ctrl Pts',(0.468929997378719,1.48315647987392,
7.94535068714778));
#265691=CARTESIAN_POINT('Ctrl Pts',(0.441718424162171,1.49160128371891,
7.94740389332921));
#265692=CARTESIAN_POINT('Ctrl Pts',(0.422281935910763,1.49721990729342,
7.94887404595857));
#265693=CARTESIAN_POINT('Ctrl Pts',(0.375120281843121,1.50986185401646,
7.95245173759724));
#265694=CARTESIAN_POINT('Ctrl Pts',(0.347301152079581,1.51650247644447,
7.95457078053504));
#265695=CARTESIAN_POINT('Ctrl Pts',(0.152721044668739,1.55731550160999,
7.96945553271814));
#265696=CARTESIAN_POINT('Ctrl Pts',(-0.0184402589523456,1.56467212140176,
7.98304228174234));
#265697=CARTESIAN_POINT('Ctrl Pts',(-0.202249216803116,1.54236832477644,
7.99684462788507));
#265698=CARTESIAN_POINT('Ctrl Pts',(-0.217098798676894,1.54034832101533,
7.99795273923506));
#265699=CARTESIAN_POINT('Ctrl Pts',(-0.238234470083694,1.53716147417307,
7.99951788751245));
#265700=CARTESIAN_POINT('Ctrl Pts',(-0.244545590625157,1.53617008118294,
7.99998370275324));
#265701=CARTESIAN_POINT('Ctrl Pts',(-0.254511481761831,1.53454159793358,
8.0007166509895));
#265702=CARTESIAN_POINT('Ctrl Pts',(-0.258170294445346,1.53393028198326,
8.00098518130552));
#265703=CARTESIAN_POINT('Ctrl Pts',(-0.264690632544561,1.53281687064055,
8.00146268690545));
#265704=CARTESIAN_POINT('Ctrl Pts',(-0.267552916491008,1.53231985140351,
8.00167193948902));
#265705=CARTESIAN_POINT('Ctrl Pts',(-0.274371886361038,1.53111608706629,
8.00216960642937));
#265706=CARTESIAN_POINT('Ctrl Pts',(-0.278327240138321,1.5304020231553,
8.00245760334093));
#265707=CARTESIAN_POINT('Ctrl Pts',(-0.290172500371273,1.52821614486414,
8.00331817593359));
#265708=CARTESIAN_POINT('Ctrl Pts',(-0.298053992456243,1.52669855907883,
8.00388824145394));
#265709=CARTESIAN_POINT('Ctrl Pts',(-0.391399048218723,1.5079744873099,
8.01061360755716));
#265710=CARTESIAN_POINT('Ctrl Pts',(-0.475296904680038,1.48367051915359,
8.01640117515553));
#265711=CARTESIAN_POINT('Ctrl Pts',(-0.675038640745276,1.40710951123746,
8.03050681749235));
#265712=CARTESIAN_POINT('Ctrl Pts',(-0.787350601947044,1.34748242581591,
8.03876534231254));
#265713=CARTESIAN_POINT('Ctrl Pts',(-0.905761800256386,1.26471030273796,
8.04879311890734));
#265714=CARTESIAN_POINT('Ctrl Pts',(-0.920162887013234,1.25427142391436,
8.05003638002903));
#265715=CARTESIAN_POINT('Ctrl Pts',(-0.94018249975763,1.23922950647102,
8.05180018777003));
#265716=CARTESIAN_POINT('Ctrl Pts',(-0.9459530192095,1.2348302655848,8.05231284062802));
#265717=CARTESIAN_POINT('Ctrl Pts',(-0.955951634973251,1.2270964572363,
8.05320867774298));
#265718=CARTESIAN_POINT('Ctrl Pts',(-0.960193625093525,1.22377998217461,
8.05359114624131));
#265719=CARTESIAN_POINT('Ctrl Pts',(-0.968867534849446,1.21692567872993,
8.05437821398781));
#265720=CARTESIAN_POINT('Ctrl Pts',(-0.973297493021202,1.21338551011197,
8.05478290256705));
#265721=CARTESIAN_POINT('Ctrl Pts',(-0.983346662927458,1.2052643489925,
8.055707198145));
#265722=CARTESIAN_POINT('Ctrl Pts',(-0.988953368012524,1.20066816524898,
8.05622741087243));
#265723=CARTESIAN_POINT('Ctrl Pts',(-1.00101201611682,1.19064113529947,
8.05735621021343));
#265724=CARTESIAN_POINT('Ctrl Pts',(-1.00745230361953,1.18519670105929,
8.05796533989271));
#265725=CARTESIAN_POINT('Ctrl Pts',(-1.02464008268982,1.17042532736829,
8.05960809504129));
#265726=CARTESIAN_POINT('Ctrl Pts',(-1.03530415450326,1.16100302704433,
8.06064560209993));
#265727=CARTESIAN_POINT('Ctrl Pts',(-1.06800974981506,1.13129688163075,
8.06388562423304));
#265728=CARTESIAN_POINT('Ctrl Pts',(-1.08959456654628,1.11052281400064,
8.06610804271856));
#265729=CARTESIAN_POINT('Ctrl Pts',(-1.17685988271648,1.02154084800991,
8.07545410371289));
#265730=CARTESIAN_POINT('Ctrl Pts',(-1.23683677135708,0.948037675725988,
8.08278659224037));
#265731=CARTESIAN_POINT('Ctrl Pts',(-1.31342154224361,0.834443983160994,
8.09340763237767));
#265732=CARTESIAN_POINT('Ctrl Pts',(-1.33564789414527,0.798384548309486,
8.09668419310973));
#265733=CARTESIAN_POINT('Ctrl Pts',(-1.36516207445875,0.745811564344188,
8.10129358583867));
#265734=CARTESIAN_POINT('Ctrl Pts',(-1.37367692318553,0.730009683604519,
8.102658280228));
#265735=CARTESIAN_POINT('Ctrl Pts',(-1.39441034049294,0.68988459796727,
8.10606612882671));
#265736=CARTESIAN_POINT('Ctrl Pts',(-1.40626831732991,0.665380053068993,
8.10809531623437));
#265737=CARTESIAN_POINT('Ctrl Pts',(-1.42018317087241,0.634588971080162,
8.11057059727069));
#265738=CARTESIAN_POINT('Ctrl Pts',(-1.4228504663441,0.62858567879715,8.11104974353517));
#265739=CARTESIAN_POINT('Ctrl Pts',(-1.42698098787906,0.619128080526867,
8.11179897662974));
#265740=CARTESIAN_POINT('Ctrl Pts',(-1.42846984503033,0.615685165089961,
8.11207056314471));
#265741=CARTESIAN_POINT('Ctrl Pts',(-1.43121475475749,0.609274127607548,
8.11257408126341));
#265742=CARTESIAN_POINT('Ctrl Pts',(-1.43247402632282,0.606307513605492,
8.11280619870262));
#265743=CARTESIAN_POINT('Ctrl Pts',(-1.43532596925313,0.599530372652278,
8.11333448478689));
#265744=CARTESIAN_POINT('Ctrl Pts',(-1.43691269073794,0.595717404482938,
8.1136302926996));
#265745=CARTESIAN_POINT('Ctrl Pts',(-1.44175014153162,0.583960994625517,
8.11453812868929));
#265746=CARTESIAN_POINT('Ctrl Pts',(-1.44495040187356,0.575996752476573,
8.11514722111935));
#265747=CARTESIAN_POINT('Ctrl Pts',(-1.45224261295408,0.557405865129144,
8.11655624172759));
#265748=CARTESIAN_POINT('Ctrl Pts',(-1.45628418123386,0.546759825960961,
8.11735347964851));
#265749=CARTESIAN_POINT('Ctrl Pts',(-1.50866120053581,0.404089323234228,
8.12792178803465));
#265750=CARTESIAN_POINT('Ctrl Pts',(-1.5390041328113,0.266130468189784,
8.13687311818724));
#265751=CARTESIAN_POINT('Ctrl Pts',(-1.55377744778944,0.0842840725283926,
8.14902846580751));
#265752=CARTESIAN_POINT('Ctrl Pts',(-1.55548116180681,0.0424971396828533,
8.15184108608667));
#265753=CARTESIAN_POINT('Ctrl Pts',(-1.55549984464226,0.000695210683922209,
8.15469955740614));
#265754=CARTESIAN_POINT('Ctrl Pts',(-1.55549984541589,0.000693477583077501,
8.1546996759179));
#265755=CARTESIAN_POINT('Ctrl Pts',(-1.55551244193536,-0.0275610537365116,
8.15663175905029));
#265756=CARTESIAN_POINT('Ctrl Pts',(-1.55475520526371,-0.0558094470224839,
8.15858374748494));
#265757=CARTESIAN_POINT('Ctrl Pts',(-1.55275005271705,-0.0928773194767488,
8.16117949874512));
#265758=CARTESIAN_POINT('Ctrl Pts',(-1.55219521431651,-0.101729708683359,
8.16180197062797));
#265759=CARTESIAN_POINT('Ctrl Pts',(-1.55112211179105,-0.116787020498887,
8.16286536690637));
#265760=CARTESIAN_POINT('Ctrl Pts',(-1.55064223989501,-0.122994535146789,
8.16330509806123));
#265761=CARTESIAN_POINT('Ctrl Pts',(-1.54967842768822,-0.134558327597623,
8.16412683505985));
#265762=CARTESIAN_POINT('Ctrl Pts',(-1.54920394879388,-0.139915318991582,
8.16450854067227));
#265763=CARTESIAN_POINT('Ctrl Pts',(-1.54818471353681,-0.150781257181499,
8.16528492657029));
#265764=CARTESIAN_POINT('Ctrl Pts',(-1.54763831026069,-0.156289967383135,
8.16567965304291));
#265765=CARTESIAN_POINT('Ctrl Pts',(-1.54629651323254,-0.169120008274647,
8.16660166535254));
#265766=CARTESIAN_POINT('Ctrl Pts',(-1.54547851332105,-0.176438786676814,
8.16712965264073));
#265767=CARTESIAN_POINT('Ctrl Pts',(-1.5432187838445,-0.195434006353405,
8.16850542309485));
#265768=CARTESIAN_POINT('Ctrl Pts',(-1.54169652016432,-0.207100196109016,
8.16935571296635));
#265769=CARTESIAN_POINT('Ctrl Pts',(-1.53458140822736,-0.257192479572518,
8.17303044559702));
#265770=CARTESIAN_POINT('Ctrl Pts',(-1.52768355327927,-0.295415877311185,
8.17589525876432));
#265771=CARTESIAN_POINT('Ctrl Pts',(-1.4880610929816,-0.476015974110608,
8.18973221108268));
#265772=CARTESIAN_POINT('Ctrl Pts',(-1.43681605042174,-0.613566951592995,
8.20126562593808));
#265773=CARTESIAN_POINT('Ctrl Pts',(-1.34874398360052,-0.775861864746508,
8.21532888814008));
#265774=CARTESIAN_POINT('Ctrl Pts',(-1.32906243806224,-0.809114098102147,
8.21823095575528));
#265775=CARTESIAN_POINT('Ctrl Pts',(-1.30437138717968,-0.847493126873946,
8.22157678999231));
#265776=CARTESIAN_POINT('Ctrl Pts',(-1.3005416550474,-0.85335849691161,
8.22208801214488));
#265777=CARTESIAN_POINT('Ctrl Pts',(-1.29456988272814,-0.862370892743268,
8.22287311261104));
#265778=CARTESIAN_POINT('Ctrl Pts',(-1.29245576033801,-0.865536161191009,
8.22314877020993));
#265779=CARTESIAN_POINT('Ctrl Pts',(-1.288533175707,-0.871362643832293,
8.223655994387));
#265780=CARTESIAN_POINT('Ctrl Pts',(-1.28672808660578,-0.874025991316987,
8.22388777160646));
#265781=CARTESIAN_POINT('Ctrl Pts',(-1.28262892148569,-0.880033947065127,
8.22441044702358));
#265782=CARTESIAN_POINT('Ctrl Pts',(-1.2803300236797,-0.883375191915229,
8.22470101522176));
#265783=CARTESIAN_POINT('Ctrl Pts',(-1.27348971330408,-0.893234182090516,
8.22555818849869));
#265784=CARTESIAN_POINT('Ctrl Pts',(-1.26891131982115,-0.899726304753611,
8.22612236931559));
#265785=CARTESIAN_POINT('Ctrl Pts',(-1.23122461094052,-0.952305819261857,
8.2306920474689));
#265786=CARTESIAN_POINT('Ctrl Pts',(-1.1956622249532,-0.996591178561573,
8.23454392134266));
#265787=CARTESIAN_POINT('Ctrl Pts',(-1.08738312172775,-1.1172649361665,
8.24536949961092));
#265788=CARTESIAN_POINT('Ctrl Pts',(-1.00922571578585,-1.18833810846182,
8.2521792645424));
#265789=CARTESIAN_POINT('Ctrl Pts',(-0.891813400720532,-1.27510750763813,
8.26195329623408));
#265790=CARTESIAN_POINT('Ctrl Pts',(-0.858214452678401,-1.29795910761857,
8.26470255861118));
#265791=CARTESIAN_POINT('Ctrl Pts',(-0.808824990976642,-1.32879360651692,
8.26870880145344));
#265792=CARTESIAN_POINT('Ctrl Pts',(-0.793731531196933,-1.3378641670446,
8.26992853616171));
#265793=CARTESIAN_POINT('Ctrl Pts',(-0.770024961148751,-1.35156848268343,
8.27183939208041));
#265794=CARTESIAN_POINT('Ctrl Pts',(-0.761516328677205,-1.35638072743053,
8.27252425541972));
#265795=CARTESIAN_POINT('Ctrl Pts',(-0.745483964851621,-1.36524978059206,
8.27381326905052));
#265796=CARTESIAN_POINT('Ctrl Pts',(-0.737971020715449,-1.36932540786271,
8.27441673131353));
#265797=CARTESIAN_POINT('Ctrl Pts',(-0.725213945074318,-1.37611039546432,
8.27544063255058));
#265798=CARTESIAN_POINT('Ctrl Pts',(-0.719987222419312,-1.37885223444655,
8.27585991592883));
#265799=CARTESIAN_POINT('Ctrl Pts',(-0.709527589709048,-1.3842634711791,
8.27669860793923));
#265800=CARTESIAN_POINT('Ctrl Pts',(-0.704294910821525,-1.38693310402755,
8.27711799977296));
#265801=CARTESIAN_POINT('Ctrl Pts',(-0.692728956386209,-1.39275154554504,
8.27804465802654));
#265802=CARTESIAN_POINT('Ctrl Pts',(-0.686389104643297,-1.39588691110642,
8.27855238301017));
#265803=CARTESIAN_POINT('Ctrl Pts',(-0.663983446606174,-1.40677805405715,
8.28034612251041));
#265804=CARTESIAN_POINT('Ctrl Pts',(-0.647806371713254,-1.41430030980481,
8.28164013901022));
#265805=CARTESIAN_POINT('Ctrl Pts',(-0.512491814695007,-1.47441226928871,
8.29245971060249));
#265806=CARTESIAN_POINT('Ctrl Pts',(-0.387335072559399,-1.51211650823842,
8.3025050722933));
#265807=CARTESIAN_POINT('Ctrl Pts',(-0.183365180826234,-1.54655688073541,
8.31854055383755));
#265808=CARTESIAN_POINT('Ctrl Pts',(-0.106900169584929,-1.55371682464372,
8.32446377851203));
#265809=CARTESIAN_POINT('Ctrl Pts',(-0.0170093461110924,-1.55546304857193,
8.33112977073088));
#265810=CARTESIAN_POINT('Ctrl Pts',(-0.00380383773568808,-1.55555140555301,
8.33210139524807));
#265811=CARTESIAN_POINT('Ctrl Pts',(0.0143113180819958,-1.55544191170809,
8.33342236134905));
#265812=CARTESIAN_POINT('Ctrl Pts',(0.0192207864782227,-1.55538899239275,
8.33377916317426));
#265813=CARTESIAN_POINT('Ctrl Pts',(0.0274773969647955,-1.55526089462312,
8.33437711564759));
#265814=CARTESIAN_POINT('Ctrl Pts',(0.030824659769978,-1.55519815418104,
8.33461894534316));
#265815=CARTESIAN_POINT('Ctrl Pts',(0.0371833147952799,-1.55505843138009,
8.33507720001624));
#265816=CARTESIAN_POINT('Ctrl Pts',(0.0401947167397025,-1.55498350765366,
8.3352937413044));
#265817=CARTESIAN_POINT('Ctrl Pts',(0.048100675981779,-1.55476382519448,
8.33586101039787));
#265818=CARTESIAN_POINT('Ctrl Pts',(0.0529948541975249,-1.55460470034463,
8.33621094419673));
#265819=CARTESIAN_POINT('Ctrl Pts',(0.0700577243134016,-1.55396926154776,
8.3374268945739));
#265820=CARTESIAN_POINT('Ctrl Pts',(0.0822219186751048,-1.55337314608538,
8.33828657539033));
#265821=CARTESIAN_POINT('Ctrl Pts',(0.189904609910514,-1.54682755096889,
8.34584330448779));
#265822=CARTESIAN_POINT('Ctrl Pts',(0.284706751868626,-1.53221637266549,
8.35213025716064));
#265823=CARTESIAN_POINT('Ctrl Pts',(0.489974097122149,-1.48085445827633,
8.36605780251259));
#265824=CARTESIAN_POINT('Ctrl Pts',(0.598861091612789,-1.44026555854898,
8.37368077995249));
#265825=CARTESIAN_POINT('Ctrl Pts',(0.715983769892291,-1.38100876611635,
8.38282184065024));
#265826=CARTESIAN_POINT('Ctrl Pts',(0.729636696281835,-1.37384432615348,
8.38390226794513));
#265827=CARTESIAN_POINT('Ctrl Pts',(0.749691127121491,-1.36293741271369,
8.38551259198718));
#265828=CARTESIAN_POINT('Ctrl Pts',(0.756176307316571,-1.35935005273988,
8.38603700206355));
#265829=CARTESIAN_POINT('Ctrl Pts',(0.767667799366387,-1.35288570745279,
8.38697291250531));
#265830=CARTESIAN_POINT('Ctrl Pts',(0.77268423118742,-1.35002691263698,
8.38738375623345));
#265831=CARTESIAN_POINT('Ctrl Pts',(0.78321698762521,-1.3439465049668,8.38825128139421));
#265832=CARTESIAN_POINT('Ctrl Pts',(0.788729601884819,-1.34071871426513,
8.38870818002621));
#265833=CARTESIAN_POINT('Ctrl Pts',(0.803269051301569,-1.3320847535513,
8.38992092757991));
#265834=CARTESIAN_POINT('Ctrl Pts',(0.812261045021169,-1.32662087427383,
8.39067886258509));
#265835=CARTESIAN_POINT('Ctrl Pts',(0.850821362833999,-1.3026511416881,
8.39396403196277));
#265836=CARTESIAN_POINT('Ctrl Pts',(0.879815810956882,-1.28324618304458,
8.39652405763323));
#265837=CARTESIAN_POINT('Ctrl Pts',(1.0182149848856,-1.18372429314097,8.40920365416642));
#265838=CARTESIAN_POINT('Ctrl Pts',(1.11746302435258,-1.09051780445893,
8.41982343343961));
#265839=CARTESIAN_POINT('Ctrl Pts',(1.23605321658796,-0.945735629460135,
8.43422792636109));
#265840=CARTESIAN_POINT('Ctrl Pts',(1.26675074408639,-0.904205276125732,
8.43815510800583));
#265841=CARTESIAN_POINT('Ctrl Pts',(1.30135394670512,-0.852159935255421,
8.44277167605445));
#265842=CARTESIAN_POINT('Ctrl Pts',(1.30728342132691,-0.843035422761084,
8.44357019096705));
#265843=CARTESIAN_POINT('Ctrl Pts',(1.31555406803297,-0.830011092872329,
8.44469388930826));
#265844=CARTESIAN_POINT('Ctrl Pts',(1.3179744641749,-0.826162352933088,
8.44502397726409));
#265845=CARTESIAN_POINT('Ctrl Pts',(1.32211131616985,-0.81951977910019,
8.44559022517637));
#265846=CARTESIAN_POINT('Ctrl Pts',(1.32383586434436,-0.816731048646797,
8.44582690949355));
#265847=CARTESIAN_POINT('Ctrl Pts',(1.32739993131185,-0.810926722507489,
8.44631734578963));
#265848=CARTESIAN_POINT('Ctrl Pts',(1.3292380063044,-0.807910298360363,
8.44657100449176));
#265849=CARTESIAN_POINT('Ctrl Pts',(1.33404494526406,-0.799960924884837,
8.44723637418835));
#265850=CARTESIAN_POINT('Ctrl Pts',(1.33699676246489,-0.795017645888552,
8.44764699291721));
#265851=CARTESIAN_POINT('Ctrl Pts',(1.3491905121833,-0.774337312145648,
8.44935228504416));
#265852=CARTESIAN_POINT('Ctrl Pts',(1.35818305471665,-0.758453807609469,
8.45063191425919));
#265853=CARTESIAN_POINT('Ctrl Pts',(1.44007360680162,-0.607681298488383,
8.46253424349309));
#265854=CARTESIAN_POINT('Ctrl Pts',(1.49294033200526,-0.462852173570799,
8.47222293855819));
#265855=CARTESIAN_POINT('Ctrl Pts',(1.53127017564436,-0.276020082219223,
8.48503002308784));
#265856=CARTESIAN_POINT('Ctrl Pts',(1.53745600752223,-0.239173856146586,
8.48756523609307));
#265857=CARTESIAN_POINT('Ctrl Pts',(1.5455232677581,-0.177622247026707,
8.49184336619711));
#265858=CARTESIAN_POINT('Ctrl Pts',(1.54815166592574,-0.153029849557383,
8.49356385512024));
#265859=CARTESIAN_POINT('Ctrl Pts',(1.55092970867647,-0.119486563925837,
8.49593056843196));
#265860=CARTESIAN_POINT('Ctrl Pts',(1.5515901191088,-0.11058072412401,8.49656084221378));
#265861=CARTESIAN_POINT('Ctrl Pts',(1.55256877394082,-0.0956397921955695,
8.4976216397552));
#265862=CARTESIAN_POINT('Ctrl Pts',(1.55292860474211,-0.0896075575141326,
8.49805085678861));
#265863=CARTESIAN_POINT('Ctrl Pts',(1.55356803438445,-0.0777234470354274,
8.49889836466892));
#265864=CARTESIAN_POINT('Ctrl Pts',(1.55384974080651,-0.0718717813026383,
8.49931658235498));
#265865=CARTESIAN_POINT('Ctrl Pts',(1.55439592261739,-0.0590145182079294,
8.50023755327579));
#265866=CARTESIAN_POINT('Ctrl Pts',(1.554646105391,-0.0520084764169287,
8.50074074441379));
#265867=CARTESIAN_POINT('Ctrl Pts',(1.55535375237179,-0.027558308799545,
8.50250166755727));
#265868=CARTESIAN_POINT('Ctrl Pts',(1.55556501577039,-0.0101089593831158,
8.50376701847313));
#265869=CARTESIAN_POINT('Ctrl Pts',(1.55485085571641,0.141242898917533,
8.51482172073673));
#265870=CARTESIAN_POINT('Ctrl Pts',(1.53693109243143,0.274477213372955,
8.52516514656097));
#265871=CARTESIAN_POINT('Ctrl Pts',(1.484104561208,0.471030322134393,8.54093747456058));
#265872=CARTESIAN_POINT('Ctrl Pts',(1.46151586399023,0.537036359679634,
8.54631269398345));
#265873=CARTESIAN_POINT('Ctrl Pts',(1.43457668241997,0.601306903550017,
8.55150209358323));
#265874=CARTESIAN_POINT('Origin',(0.,0.,-1.29405622560371));
#265875=CARTESIAN_POINT('',(1.43457668359376,0.601306900749626,9.38971141570882));
#265876=CARTESIAN_POINT('',(1.43457655129078,0.601307216393289,9.25009119722734));
#265877=CARTESIAN_POINT('',(1.43457668357355,0.601306900797845,-1.29405622560371));
#265878=CARTESIAN_POINT('',(-1.55786019784847,-0.000159437891840058,8.99395693065775));
#265879=CARTESIAN_POINT('Ctrl Pts',(1.43457668359376,0.601306900749626,
9.38971141570882));
#265880=CARTESIAN_POINT('Ctrl Pts',(1.43708782974321,0.59531589730263,9.38925480768558));
#265881=CARTESIAN_POINT('Ctrl Pts',(1.43956140763381,0.589309257252912,
9.3887969624209));
#265882=CARTESIAN_POINT('Ctrl Pts',(1.44448384727649,0.577140049795941,
9.38786918830465));
#265883=CARTESIAN_POINT('Ctrl Pts',(1.44693105037016,0.570977018036914,
9.38739921991267));
#265884=CARTESIAN_POINT('Ctrl Pts',(1.45137486284903,0.559573679883019,
9.38652936498683));
#265885=CARTESIAN_POINT('Ctrl Pts',(1.45338269392861,0.554337838511073,
9.38612986247685));
#265886=CARTESIAN_POINT('Ctrl Pts',(1.45776990785797,0.542709563069248,
9.38524230590606));
#265887=CARTESIAN_POINT('Ctrl Pts',(1.46013563181875,0.536312136776179,
9.38475380546448));
#265888=CARTESIAN_POINT('Ctrl Pts',(1.46680529529987,0.517904662512241,
9.38334752778272));
#265889=CARTESIAN_POINT('Ctrl Pts',(1.47100356448313,0.50585720219307,9.38242627721276));
#265890=CARTESIAN_POINT('Ctrl Pts',(1.502679910392,0.411227603627131,9.3751815920839));
#265891=CARTESIAN_POINT('Ctrl Pts',(1.52332624045224,0.32653810716284,9.36863416421773));
#265892=CARTESIAN_POINT('Ctrl Pts',(1.55089160657538,0.150456047651188,
9.35493523266033));
#265893=CARTESIAN_POINT('Ctrl Pts',(1.55704487368799,0.0592675873812509,
9.34779588125369));
#265894=CARTESIAN_POINT('Ctrl Pts',(1.554950757354,-0.0427167520753653,
9.33999099470973));
#265895=CARTESIAN_POINT('Ctrl Pts',(1.55461718296239,-0.0534976892118548,
9.33916836363109));
#265896=CARTESIAN_POINT('Ctrl Pts',(1.55273367216501,-0.0990413922451764,
9.33570553358018));
#265897=CARTESIAN_POINT('Ctrl Pts',(1.55012949824933,-0.133753731040844,
9.33309649786047));
#265898=CARTESIAN_POINT('Ctrl Pts',(1.54566909894136,-0.174723661316817,
9.33007416584904));
#265899=CARTESIAN_POINT('Ctrl Pts',(1.54493610074346,-0.181090501291612,
9.32960613141598));
#265900=CARTESIAN_POINT('Ctrl Pts',(1.54367825470275,-0.191452152488843,
9.32884730646945));
#265901=CARTESIAN_POINT('Ctrl Pts',(1.54317720960378,-0.195449690426616,
9.32855524849525));
#265902=CARTESIAN_POINT('Ctrl Pts',(1.54225311823264,-0.202597311335451,
9.32803434909998));
#265903=CARTESIAN_POINT('Ctrl Pts',(1.54183594517856,-0.205748074262633,
9.32780518648238));
#265904=CARTESIAN_POINT('Ctrl Pts',(1.54090733402752,-0.212600089139369,
9.32730782159261));
#265905=CARTESIAN_POINT('Ctrl Pts',(1.54039221751622,-0.216300778946665,
9.3270398285977));
#265906=CARTESIAN_POINT('Ctrl Pts',(1.53890020230165,-0.226743979105504,
9.32628524355941));
#265907=CARTESIAN_POINT('Ctrl Pts',(1.53789231821848,-0.233482091007748,
9.32580035375259));
#265908=CARTESIAN_POINT('Ctrl Pts',(1.53129768603991,-0.275673285368937,
9.32277535445665));
#265909=CARTESIAN_POINT('Ctrl Pts',(1.52452904303368,-0.310934195779292,
9.32029670515759));
#265910=CARTESIAN_POINT('Ctrl Pts',(1.49645596996693,-0.434004670457138,
9.31171915445632));
#265911=CARTESIAN_POINT('Ctrl Pts',(1.46873082809848,-0.520166288232315,
9.30583967550527));
#265912=CARTESIAN_POINT('Ctrl Pts',(1.39593911572236,-0.693108312589602,
9.29346503308832));
#265913=CARTESIAN_POINT('Ctrl Pts',(1.34987471105787,-0.779024492887918,
9.28697864986752));
#265914=CARTESIAN_POINT('Ctrl Pts',(1.28949204232985,-0.870019024575766,
9.27935186945889));
#265915=CARTESIAN_POINT('Ctrl Pts',(1.28277559157784,-0.879891810432988,
9.27851388472833));
#265916=CARTESIAN_POINT('Ctrl Pts',(1.27177663628408,-0.895665999834283,
9.27715741122022));
#265917=CARTESIAN_POINT('Ctrl Pts',(1.26756504606718,-0.901616463126115,
9.27664160918329));
#265918=CARTESIAN_POINT('Ctrl Pts',(1.25997870785372,-0.912176815841824,
9.27571873238146));
#265919=CARTESIAN_POINT('Ctrl Pts',(1.25662007403171,-0.916798165110904,
9.27531228195168));
#265920=CARTESIAN_POINT('Ctrl Pts',(1.2495293832226,-0.926442512273304,
9.27445854994562));
#265921=CARTESIAN_POINT('Ctrl Pts',(1.24579232860497,-0.93146169001161,
9.27401107922755));
#265922=CARTESIAN_POINT('Ctrl Pts',(1.23590712222881,-0.944572447064959,
9.27283379027277));
#265923=CARTESIAN_POINT('Ctrl Pts',(1.22970987159247,-0.952626445741894,
9.27210205667022));
#265924=CARTESIAN_POINT('Ctrl Pts',(1.20108555357693,-0.989082078169204,
9.26875021014017));
#265925=CARTESIAN_POINT('Ctrl Pts',(1.17775222723403,-1.01675422411608,
9.2660942621835));
#265926=CARTESIAN_POINT('Ctrl Pts',(1.06269048508816,-1.14393216648936,
9.2533311911762));
#265927=CARTESIAN_POINT('Ctrl Pts',(0.959206442916029,-1.2319913831661,
9.24272983267382));
#265928=CARTESIAN_POINT('Ctrl Pts',(0.798833805246429,-1.33587377223353,
9.22802347072433));
#265929=CARTESIAN_POINT('Ctrl Pts',(0.750393671296776,-1.36367338065486,
9.22378151251973));
#265930=CARTESIAN_POINT('Ctrl Pts',(0.693574904321774,-1.39233447116312,
9.21910651229777));
#265931=CARTESIAN_POINT('Ctrl Pts',(0.686564799796904,-1.39580450279551,
9.21853478569913));
#265932=CARTESIAN_POINT('Ctrl Pts',(0.67593036465239,-1.40096909078124,
9.21767541117008));
#265933=CARTESIAN_POINT('Ctrl Pts',(0.672325322353087,-1.4027027172853,
9.21738545518905));
#265934=CARTESIAN_POINT('Ctrl Pts',(0.665845668532286,-1.4057879944465,
9.2168667970653));
#265935=CARTESIAN_POINT('Ctrl Pts',(0.66297358222074,-1.40714475784646,
9.21663778568924));
#265936=CARTESIAN_POINT('Ctrl Pts',(0.656693993042301,-1.41008771915786,
9.21613899712574));
#265937=CARTESIAN_POINT('Ctrl Pts',(0.653284895777016,-1.41167036590579,
9.21586943888595));
#265938=CARTESIAN_POINT('Ctrl Pts',(0.643586594910419,-1.41613007004704,
9.21510597516643));
#265939=CARTESIAN_POINT('Ctrl Pts',(0.637283786663551,-1.41897761097587,
9.21461383622869));
#265940=CARTESIAN_POINT('Ctrl Pts',(0.596207884186789,-1.43720636569848,
9.21143126205587));
#265941=CARTESIAN_POINT('Ctrl Pts',(0.560896216417073,-1.45135178853981,
9.2088099338956));
#265942=CARTESIAN_POINT('Ctrl Pts',(0.421501637436629,-1.50134244486121,
9.19876834908841));
#265943=CARTESIAN_POINT('Ctrl Pts',(0.314248318636299,-1.52739794544497,
9.19167233571938));
#265944=CARTESIAN_POINT('Ctrl Pts',(0.130036948838862,-1.55190538356977,
9.17932935659739));
#265945=CARTESIAN_POINT('Ctrl Pts',(0.0543187616693528,-1.55639548479748,
9.17421689624834));
#265946=CARTESIAN_POINT('Ctrl Pts',(-0.03308692001655,-1.55519184969553,
9.16810953719753));
#265947=CARTESIAN_POINT('Ctrl Pts',(-0.0447531224733314,-1.55489986128824,
9.16729031136669));
#265948=CARTESIAN_POINT('Ctrl Pts',(-0.0636978486098668,-1.55421232422148,
9.16595283738004));
#265949=CARTESIAN_POINT('Ctrl Pts',(-0.0709789740614843,-1.55389682625837,
9.1654370863183));
#265950=CARTESIAN_POINT('Ctrl Pts',(-0.083947558787496,-1.55324354698987,
9.16451529420166));
#265951=CARTESIAN_POINT('Ctrl Pts',(-0.089635926527065,-1.55292566080488,
9.16410988204529));
#265952=CARTESIAN_POINT('Ctrl Pts',(-0.101633093109031,-1.55218907996871,
9.16325247746616));
#265953=CARTESIAN_POINT('Ctrl Pts',(-0.107941326798252,-1.55176315634095,
9.16280026595736));
#265954=CARTESIAN_POINT('Ctrl Pts',(-0.124675497895407,-1.55053075424559,
9.1615969031419));
#265955=CARTESIAN_POINT('Ctrl Pts',(-0.135096039160965,-1.54965759118301,
9.16084367912342));
#265956=CARTESIAN_POINT('Ctrl Pts',(-0.184794427023072,-1.54498816071306,
9.15723217088881));
#265957=CARTESIAN_POINT('Ctrl Pts',(-0.2239238094753,-1.53980356022411,
9.1543308907466));
#265958=CARTESIAN_POINT('Ctrl Pts',(-0.410048982104664,-1.50789795051632,
9.14023845424061));
#265959=CARTESIAN_POINT('Ctrl Pts',(-0.552875578340974,-1.46157820652359,
9.12844228588015));
#265960=CARTESIAN_POINT('Ctrl Pts',(-0.721762028534701,-1.37846019630435,
9.11409711253588));
#265961=CARTESIAN_POINT('Ctrl Pts',(-0.756005457253897,-1.35998136604669,
9.11117246334961));
#265962=CARTESIAN_POINT('Ctrl Pts',(-0.795720985351208,-1.33658524018408,
9.10779036250197));
#265963=CARTESIAN_POINT('Ctrl Pts',(-0.801893410212408,-1.33289120142185,
9.10726503162118));
#265964=CARTESIAN_POINT('Ctrl Pts',(-0.811369857228142,-1.32713013278613,
9.10645922271762));
#265965=CARTESIAN_POINT('Ctrl Pts',(-0.814692000188145,-1.32509334776792,
9.10617687020374));
#265966=CARTESIAN_POINT('Ctrl Pts',(-0.820654653568288,-1.32140678180109,
9.10567039636167));
#265967=CARTESIAN_POINT('Ctrl Pts',(-0.823297871655288,-1.31976155363469,
9.10544598877598));
#265968=CARTESIAN_POINT('Ctrl Pts',(-0.829104539703971,-1.31612305349541,
9.10495324606138));
#265969=CARTESIAN_POINT('Ctrl Pts',(-0.832265743548619,-1.31412631151305,
9.10468514359611));
#265970=CARTESIAN_POINT('Ctrl Pts',(-0.838844900947324,-1.30993739144024,
9.10412741121316));
#265971=CARTESIAN_POINT('Ctrl Pts',(-0.842261538605066,-1.30774318537765,
9.10383791417431));
#265972=CARTESIAN_POINT('Ctrl Pts',(-0.8510686045647,-1.30203834826217,
9.1030919321819));
#265973=CARTESIAN_POINT('Ctrl Pts',(-0.856445986912409,-1.29850756839574,
9.1026367012634));
#265974=CARTESIAN_POINT('Ctrl Pts',(-0.872244722920112,-1.28799330753161,
9.10129947321614));
#265975=CARTESIAN_POINT('Ctrl Pts',(-0.882603961824333,-1.28091681528722,
9.10042296128793));
#265976=CARTESIAN_POINT('Ctrl Pts',(-0.919532160059527,-1.25503008217532,
9.09729507261248));
#265977=CARTESIAN_POINT('Ctrl Pts',(-0.945596347514915,-1.23551113238845,
9.09508102422457));
#265978=CARTESIAN_POINT('Ctrl Pts',(-1.02755900790384,-1.17001649347504,
9.08802938135205));
#265979=CARTESIAN_POINT('Ctrl Pts',(-1.0808695580341,-1.12095414855578,
9.08329936039649));
#265980=CARTESIAN_POINT('Ctrl Pts',(-1.20085631060762,-0.993979871023113,
9.07178861950553));
#265981=CARTESIAN_POINT('Ctrl Pts',(-1.26361801551808,-0.912861827809228,
9.06498491870761));
#265982=CARTESIAN_POINT('Ctrl Pts',(-1.32425082194038,-0.816137499257763,
9.0570112643999));
#265983=CARTESIAN_POINT('Ctrl Pts',(-1.33042931883999,-0.806026346372209,
9.05617960397344));
#265984=CARTESIAN_POINT('Ctrl Pts',(-1.34024787976547,-0.78953769599985,
9.05482583732866));
#265985=CARTESIAN_POINT('Ctrl Pts',(-1.34395944369447,-0.783203142861648,
9.0543063308309));
#265986=CARTESIAN_POINT('Ctrl Pts',(-1.35047453122471,-0.771901110008587,
9.05338033180251));
#265987=CARTESIAN_POINT('Ctrl Pts',(-1.35329585806625,-0.766944001914903,
9.05297448964885));
#265988=CARTESIAN_POINT('Ctrl Pts',(-1.35917282831588,-0.756484688098322,
9.05211875231449));
#265989=CARTESIAN_POINT('Ctrl Pts',(-1.3622224618819,-0.750979242558053,
9.05166865125024));
#265990=CARTESIAN_POINT('Ctrl Pts',(-1.37018709592266,-0.736392690734526,
9.05047689615475));
#265991=CARTESIAN_POINT('Ctrl Pts',(-1.37504515341261,-0.727281024994862,
9.04973324006295));
#265992=CARTESIAN_POINT('Ctrl Pts',(-1.39733941673783,-0.684444434102731,
9.04624014078062));
#265993=CARTESIAN_POINT('Ctrl Pts',(-1.41362643656675,-0.650139571347242,
9.04345105471816));
#265994=CARTESIAN_POINT('Ctrl Pts',(-1.48811712682496,-0.477175770179261,
9.02941492504455));
#265995=CARTESIAN_POINT('Ctrl Pts',(-1.52724876445989,-0.331188207408493,
9.01754441939057));
#265996=CARTESIAN_POINT('Ctrl Pts',(-1.54810063201712,-0.154104849470554,
9.0039485522831));
#265997=CARTESIAN_POINT('Ctrl Pts',(-1.55062342261023,-0.126218411708337,
9.00183410260287));
#265998=CARTESIAN_POINT('Ctrl Pts',(-1.55336170101859,-0.0829644403757517,
8.99860940119671));
#265999=CARTESIAN_POINT('Ctrl Pts',(-1.55410453770933,-0.0676373139414937,
8.99747738523281));
#266000=CARTESIAN_POINT('Ctrl Pts',(-1.55480004012722,-0.0469638390379281,
8.99596701961603));
#266001=CARTESIAN_POINT('Ctrl Pts',(-1.55495211093905,-0.0416257360374791,
8.99557851124372));
#266002=CARTESIAN_POINT('Ctrl Pts',(-1.55514835847844,-0.0332155277550246,
8.99496885980852));
#266003=CARTESIAN_POINT('Ctrl Pts',(-1.55521092786053,-0.0301439624707253,
8.99474671740288));
#266004=CARTESIAN_POINT('Ctrl Pts',(-1.55531754705947,-0.0240188204175105,
8.99430478429321));
#266005=CARTESIAN_POINT('Ctrl Pts',(-1.55536170413299,-0.0209653386465418,
8.99408499822506));
#266006=CARTESIAN_POINT('Ctrl Pts',(-1.55543652242247,-0.0144683391402729,
8.99361843759601));
#266007=CARTESIAN_POINT('Ctrl Pts',(-1.55546474138346,-0.0110248379756254,
8.99337180139868));
#266008=CARTESIAN_POINT('Ctrl Pts',(-1.55549342183002,-0.00514031481975871,
8.99295139280277));
#266009=CARTESIAN_POINT('Ctrl Pts',(-1.55549957307726,-0.00269935885603639,
8.99277731573819));
#266010=CARTESIAN_POINT('Ctrl Pts',(-1.55549997854072,-0.000258379212321887,
8.99260354023743));
#266011=CARTESIAN_POINT('Ctrl Pts',(1.43456415251406,0.601298694836608,
8.68837676241653));
#266012=CARTESIAN_POINT('Ctrl Pts',(1.27769209139973,0.965209298280632,
8.71676603012681));
#266013=CARTESIAN_POINT('Ctrl Pts',(0.593832905914069,1.67495416287262,
8.78220722642894));
#266014=CARTESIAN_POINT('Ctrl Pts',(-1.01228645751357,1.52943817244966,
8.8841003002866));
#266015=CARTESIAN_POINT('Ctrl Pts',(-1.55731054943609,0.506487777198142,
8.95760410643398));
#266016=CARTESIAN_POINT('Ctrl Pts',(-1.55803294000962,-0.000152196472590984,
8.9940559839895));
#266017=CARTESIAN_POINT('Ctrl Pts',(1.43457668241997,0.601306903550017,
8.55150209358323));
#266018=CARTESIAN_POINT('Ctrl Pts',(1.43294790499825,0.605192782950805,
8.55181585132967));
#266019=CARTESIAN_POINT('Ctrl Pts',(1.43130322378101,0.609072319093551,
8.55212891636632));
#266020=CARTESIAN_POINT('Ctrl Pts',(1.42452938068502,0.624871727868597,
8.55340300328474));
#266021=CARTESIAN_POINT('Ctrl Pts',(1.41926682430825,0.636734123311139,
8.55435758008135));
#266022=CARTESIAN_POINT('Ctrl Pts',(1.4118231888063,0.652961952056135,8.5556593120359));
#266023=CARTESIAN_POINT('Ctrl Pts',(1.40976930475961,0.657384618296571,
8.55601365367349));
#266024=CARTESIAN_POINT('Ctrl Pts',(1.40627318000372,0.664821145362487,
8.55660865427335));
#266025=CARTESIAN_POINT('Ctrl Pts',(1.4048419793831,0.667840119964732,8.55684997783004));
#266026=CARTESIAN_POINT('Ctrl Pts',(1.40209925353854,0.673577793675263,
8.5573081591844));
#266027=CARTESIAN_POINT('Ctrl Pts',(1.40078952982971,0.676297312171823,
8.5575251289057));
#266028=CARTESIAN_POINT('Ctrl Pts',(1.39731990249647,0.683448347075764,
8.55809518131543));
#266029=CARTESIAN_POINT('Ctrl Pts',(1.39514680971701,0.687873487020718,
8.55844745492299));
#266030=CARTESIAN_POINT('Ctrl Pts',(1.38744511501492,0.703370060084105,
8.55967966761848));
#266031=CARTESIAN_POINT('Ctrl Pts',(1.38180527781063,0.714386161877841,
8.56055304538535));
#266032=CARTESIAN_POINT('Ctrl Pts',(1.3377637669938,0.797937479593499,8.56716652542998));
#266033=CARTESIAN_POINT('Ctrl Pts',(1.29380119009789,0.867409091330136,
8.57260762206276));
#266034=CARTESIAN_POINT('Ctrl Pts',(1.2205720385713,0.965081595183283,8.58065486027094));
#266035=CARTESIAN_POINT('Ctrl Pts',(1.19536561268969,0.996132333608182,
8.58327948272111));
#266036=CARTESIAN_POINT('Ctrl Pts',(1.10759113573785,1.09612243001964,8.5920647709369));
#266037=CARTESIAN_POINT('Ctrl Pts',(1.04004740167493,1.16040509418459,8.59828717763937));
#266038=CARTESIAN_POINT('Ctrl Pts',(0.956991100698802,1.22634302913323,
8.60569621180159));
#266039=CARTESIAN_POINT('Ctrl Pts',(0.946710687737284,1.2342965800921,8.60660912083667));
#266040=CARTESIAN_POINT('Ctrl Pts',(0.930803212418372,1.24628791549676,
8.60801609844018));
#266041=CARTESIAN_POINT('Ctrl Pts',(0.92524666303307,1.25041864921468,8.60850652985363));
#266042=CARTESIAN_POINT('Ctrl Pts',(0.91508175162889,1.25787038362365,8.60940194129295));
#266043=CARTESIAN_POINT('Ctrl Pts',(0.910482397524518,1.26120351902126,
8.6098064427075));
#266044=CARTESIAN_POINT('Ctrl Pts',(0.900415563992273,1.2684151518989,8.61069044981573));
#266045=CARTESIAN_POINT('Ctrl Pts',(0.894941084224529,1.27228363135493,
8.61117032897003));
#266046=CARTESIAN_POINT('Ctrl Pts',(0.879889594374731,1.28277438548819,
8.61248748947261));
#266047=CARTESIAN_POINT('Ctrl Pts',(0.870263134664788,1.28932458484947,
8.61332747572133));
#266048=CARTESIAN_POINT('Ctrl Pts',(0.819552601233491,1.32300325537439,
8.61774073083784));
#266049=CARTESIAN_POINT('Ctrl Pts',(0.777275618046955,1.34827508421444,
8.62138181587654));
#266050=CARTESIAN_POINT('Ctrl Pts',(0.604355723756177,1.4408029212872,8.63614013232065));
#266051=CARTESIAN_POINT('Ctrl Pts',(0.465696561192639,1.49140060577076,
8.64776999108561));
#266052=CARTESIAN_POINT('Ctrl Pts',(0.302173282617808,1.5260022509477,8.66041392425533));
#266053=CARTESIAN_POINT('Ctrl Pts',(0.282250441036827,1.52981251854891,
8.66193530806882));
#266054=CARTESIAN_POINT('Ctrl Pts',(0.249089931401012,1.53548458794357,
8.66443020459504));
#266055=CARTESIAN_POINT('Ctrl Pts',(0.235893068706918,1.53756730132498,
8.66541335235504));
#266056=CARTESIAN_POINT('Ctrl Pts',(0.217789249468635,1.54018583851988,
8.66674729738313));
#266057=CARTESIAN_POINT('Ctrl Pts',(0.21290465038176,1.5408686465746,8.667105742651));
#266058=CARTESIAN_POINT('Ctrl Pts',(0.204694528961621,1.54197653622339,
8.66770566979936));
#266059=CARTESIAN_POINT('Ctrl Pts',(0.201370768142125,1.54241411524346,
8.66794784041032));
#266060=CARTESIAN_POINT('Ctrl Pts',(0.195061706470477,1.54322397298209,
8.66840615734571));
#266061=CARTESIAN_POINT('Ctrl Pts',(0.192076708130791,1.54359834112799,
8.66862242287279));
#266062=CARTESIAN_POINT('Ctrl Pts',(0.184251652195814,1.54455668247093,
8.66918788678919));
#266063=CARTESIAN_POINT('Ctrl Pts',(0.179409849818223,1.54512657222969,
8.66953630091653));
#266064=CARTESIAN_POINT('Ctrl Pts',(0.162592392152359,1.54702590296565,
8.67074163023774));
#266065=CARTESIAN_POINT('Ctrl Pts',(0.15060362899934,1.54823899994514,8.67159235524857));
#266066=CARTESIAN_POINT('Ctrl Pts',(0.133465560367894,1.54977217136858,
8.67279788754486));
#266067=CARTESIAN_POINT('Ctrl Pts',(0.12832728995872,1.55020609832039,8.67315796928092));
#266068=CARTESIAN_POINT('Ctrl Pts',(-0.0473456028925387,1.56416223982192,
8.68542544609605));
#266069=CARTESIAN_POINT('Ctrl Pts',(-0.21896689607696,1.54948982019231,
8.69612922595204));
#266070=CARTESIAN_POINT('Ctrl Pts',(-0.412518540428051,1.50007614896009,
8.70966938683897));
#266071=CARTESIAN_POINT('Ctrl Pts',(-0.440057686731791,1.49222956312449,
8.71162862253972));
#266072=CARTESIAN_POINT('Ctrl Pts',(-0.486677539757825,1.47754366397614,
8.71501316555678));
#266073=CARTESIAN_POINT('Ctrl Pts',(-0.505870275489752,1.47108310604703,
8.7164265467917));
#266074=CARTESIAN_POINT('Ctrl Pts',(-0.532709714808772,1.46146122095425,
8.71843401251776));
#266075=CARTESIAN_POINT('Ctrl Pts',(-0.540466264432843,1.45861055559183,
8.71901785001398));
#266076=CARTESIAN_POINT('Ctrl Pts',(-0.553730691119689,1.45361532165968,
8.72002278118651));
#266077=CARTESIAN_POINT('Ctrl Pts',(-0.559249796227693,1.45150089400996,
8.72044286456909));
#266078=CARTESIAN_POINT('Ctrl Pts',(-0.569747765982819,1.44741024827953,
8.72124569819816));
#266079=CARTESIAN_POINT('Ctrl Pts',(-0.57472874595762,1.44543966007406,
8.72162825472493));
#266080=CARTESIAN_POINT('Ctrl Pts',(-0.587568008358263,1.44028330093527,
8.72261864630698));
#266081=CARTESIAN_POINT('Ctrl Pts',(-0.595410506342982,1.43705896714615,
8.72322777187408));
#266082=CARTESIAN_POINT('Ctrl Pts',(-0.621745983254385,1.42597892004827,
8.72528761661021));
#266083=CARTESIAN_POINT('Ctrl Pts',(-0.640112304522696,1.41782936757454,
8.72674821329347));
#266084=CARTESIAN_POINT('Ctrl Pts',(-0.820588347441405,1.33352665846721,
8.74134837108429));
#266085=CARTESIAN_POINT('Ctrl Pts',(-0.96853620943392,1.23026973780936,
8.75554746866012));
#266086=CARTESIAN_POINT('Ctrl Pts',(-1.11963404372768,1.08034496154894,
8.77169781227758));
#266087=CARTESIAN_POINT('Ctrl Pts',(-1.14287605070558,1.05572742568699,
8.77423221042278));
#266088=CARTESIAN_POINT('Ctrl Pts',(-1.16977861139558,1.0253019055079,8.77720822069005));
#266089=CARTESIAN_POINT('Ctrl Pts',(-1.17422589995149,1.02020563490455,
8.77770164613725));
#266090=CARTESIAN_POINT('Ctrl Pts',(-1.18108987088981,1.01223567492973,
8.77846526972874));
#266091=CARTESIAN_POINT('Ctrl Pts',(-1.18352955728001,1.0093820548104,8.77873709998626));
#266092=CARTESIAN_POINT('Ctrl Pts',(-1.18804408426532,1.00406269131246,
8.77924083474713));
#266093=CARTESIAN_POINT('Ctrl Pts',(-1.19012157667092,1.00159935469506,
8.77947292658358));
#266094=CARTESIAN_POINT('Ctrl Pts',(-1.1948411351344,0.995967835180395,
8.78000085310709));
#266095=CARTESIAN_POINT('Ctrl Pts',(-1.19747826187294,0.992795588388715,
8.78029632900425));
#266096=CARTESIAN_POINT('Ctrl Pts',(-1.20432761903731,0.984489377877451,
8.78106515970762));
#266097=CARTESIAN_POINT('Ctrl Pts',(-1.20851970640838,0.979338793532901,
8.78153710941247));
#266098=CARTESIAN_POINT('Ctrl Pts',(-1.23672130387915,0.944232209751514,
8.78472285229903));
#266099=CARTESIAN_POINT('Ctrl Pts',(-1.25965013735718,0.9134200517235,8.78736658101541));
#266100=CARTESIAN_POINT('Ctrl Pts',(-1.36637287071368,0.758330177962056,
8.8001202779947));
#266101=CARTESIAN_POINT('Ctrl Pts',(-1.43304413195573,0.623241797617836,
8.80963197987196));
#266102=CARTESIAN_POINT('Ctrl Pts',(-1.49148170260505,0.44339652385938,
8.82249267980329));
#266103=CARTESIAN_POINT('Ctrl Pts',(-1.50218482803531,0.405658042549305,
8.8251959633974));
#266104=CARTESIAN_POINT('Ctrl Pts',(-1.51393597937493,0.357335664355005,
8.82868325567042));
#266105=CARTESIAN_POINT('Ctrl Pts',(-1.51631805605968,0.34708856200853,
8.82942417908086));
#266106=CARTESIAN_POINT('Ctrl Pts',(-1.51997912360252,0.330582088682228,
8.83062032884774));
#266107=CARTESIAN_POINT('Ctrl Pts',(-1.52132384427807,0.324337497316657,
8.83107344951197));
#266108=CARTESIAN_POINT('Ctrl Pts',(-1.52381076358988,0.312432945245481,
8.83193850072135));
#266109=CARTESIAN_POINT('Ctrl Pts',(-1.52495998770773,0.306774547097003,
8.83235019947034));
#266110=CARTESIAN_POINT('Ctrl Pts',(-1.52751244883558,0.293838229614379,
8.83329270352586));
#266111=CARTESIAN_POINT('Ctrl Pts',(-1.52889521403715,0.28655646477498,
8.83382414977589));
#266112=CARTESIAN_POINT('Ctrl Pts',(-1.53236650727532,0.267535611177085,
8.83521488493412));
#266113=CARTESIAN_POINT('Ctrl Pts',(-1.53437215786387,0.255782099308269,
8.83607677127004));
#266114=CARTESIAN_POINT('Ctrl Pts',(-1.54913520174073,0.162835522053381,
8.84291379045758));
#266115=CARTESIAN_POINT('Ctrl Pts',(-1.55557218656414,0.0807845889713736,
8.84908756436364));
#266116=CARTESIAN_POINT('Ctrl Pts',(-1.5554125167081,-0.0994275799248632,
8.86291519286666));
#266117=CARTESIAN_POINT('Ctrl Pts',(-1.54605549837665,-0.197245125438095,
8.87059845036504));
#266118=CARTESIAN_POINT('Ctrl Pts',(-1.51963977204217,-0.334714930633707,
8.88128956086565));
#266119=CARTESIAN_POINT('Ctrl Pts',(-1.51006240959696,-0.3755681086635,
8.88444990933905));
#266120=CARTESIAN_POINT('Ctrl Pts',(-1.49702438071354,-0.422545335812145,
8.8880285740104));
#266121=CARTESIAN_POINT('Ctrl Pts',(-1.4951614769981,-0.429090572582635,
8.88852590314068));
#266122=CARTESIAN_POINT('Ctrl Pts',(-1.49208659238871,-0.439630840598437,
8.88932449275765));
#266123=CARTESIAN_POINT('Ctrl Pts',(-1.49090140557738,-0.443633491905357,
8.88962721962317));
#266124=CARTESIAN_POINT('Ctrl Pts',(-1.48877148275661,-0.450721793436307,
8.89016230824777));
#266125=CARTESIAN_POINT('Ctrl Pts',(-1.4878332444938,-0.453809321490379,
8.89039503857323));
#266126=CARTESIAN_POINT('Ctrl Pts',(-1.48579246223208,-0.460450707248406,
8.8908948976787));
#266127=CARTESIAN_POINT('Ctrl Pts',(-1.48468677412678,-0.464003532476387,
8.89116184068603));
#266128=CARTESIAN_POINT('Ctrl Pts',(-1.48158149721771,-0.473856739139912,
8.89190098289509));
#266129=CARTESIAN_POINT('Ctrl Pts',(-1.47955444991638,-0.480148493722978,
8.89237161572774));
#266130=CARTESIAN_POINT('Ctrl Pts',(-1.46773046541493,-0.516062982034744,
8.89505140105996));
#266131=CARTESIAN_POINT('Ctrl Pts',(-1.45708328553198,-0.545401107985013,
8.89721447049713));
#266132=CARTESIAN_POINT('Ctrl Pts',(-1.41869925217996,-0.641999750913337,
8.9043122384248));
#266133=CARTESIAN_POINT('Ctrl Pts',(-1.38712772717246,-0.70763677550596,
8.90909774444182));
#266134=CARTESIAN_POINT('Ctrl Pts',(-1.29606025304211,-0.867256095542365,
8.92119401540413));
#266135=CARTESIAN_POINT('Ctrl Pts',(-1.23088839732899,-0.957504446385221,
8.92849406760265));
#266136=CARTESIAN_POINT('Ctrl Pts',(-1.14421176049384,-1.0539008406205,
8.93748288452177));
#266137=CARTESIAN_POINT('Ctrl Pts',(-1.13150404915165,-1.06753270193161,
8.93878462573347));
#266138=CARTESIAN_POINT('Ctrl Pts',(-1.11341233445029,-1.08625410923874,
8.94061782036083));
#266139=CARTESIAN_POINT('Ctrl Pts',(-1.10823187230834,-1.09153888164788,
8.94114051852411));
#266140=CARTESIAN_POINT('Ctrl Pts',(-1.0991918139056,-1.10063026964419,
8.94204894269147));
#266141=CARTESIAN_POINT('Ctrl Pts',(-1.09534962970172,-1.1044540830527,
8.94243390127562));
#266142=CARTESIAN_POINT('Ctrl Pts',(-1.08731545425743,-1.11236668567763,
8.94323656779136));
#266143=CARTESIAN_POINT('Ctrl Pts',(-1.08312021128489,-1.11645203508887,
8.94365441701959));
#266144=CARTESIAN_POINT('Ctrl Pts',(-1.07316743844822,-1.12603520082923,
8.94464278213152));
#266145=CARTESIAN_POINT('Ctrl Pts',(-1.06739062119892,-1.13151265209997,
8.94521416321622));
#266146=CARTESIAN_POINT('Ctrl Pts',(-1.04810047996199,-1.1495239616127,
8.94711482768254));
#266147=CARTESIAN_POINT('Ctrl Pts',(-1.03440691260082,-1.16186154052354,
8.94845234641342));
#266148=CARTESIAN_POINT('Ctrl Pts',(-1.00137744485528,-1.19057352380103,
8.95165254750529));
#266149=CARTESIAN_POINT('Ctrl Pts',(-0.981854856164721,-1.20672408124809,
8.95352379176451));
#266150=CARTESIAN_POINT('Ctrl Pts',(-0.843709525186548,-1.31543617809473,
8.96663084708343));
#266151=CARTESIAN_POINT('Ctrl Pts',(-0.712601543449115,-1.39082797112042,
8.97851098818748));
#266152=CARTESIAN_POINT('Ctrl Pts',(-0.536671406595769,-1.46050356352762,
8.99293089748741));
#266153=CARTESIAN_POINT('Ctrl Pts',(-0.500057279028089,-1.47344161718641,
8.99584960600123));
#266154=CARTESIAN_POINT('Ctrl Pts',(-0.456633636296178,-1.48698028122117,
8.99918727561483));
#266155=CARTESIAN_POINT('Ctrl Pts',(-0.450260599096057,-1.48892243977853,
8.9996740426337));
#266156=CARTESIAN_POINT('Ctrl Pts',(-0.439915312128538,-1.49200262678201,
9.00045900488997));
#266157=CARTESIAN_POINT('Ctrl Pts',(-0.435950750804253,-1.49316585284811,
9.00075858885146));
#266158=CARTESIAN_POINT('Ctrl Pts',(-0.428885350400509,-1.49520834458975,
9.00129024084628));
#266159=CARTESIAN_POINT('Ctrl Pts',(-0.425786374017088,-1.49609378112933,
9.00152265947749));
#266160=CARTESIAN_POINT('Ctrl Pts',(-0.419075911288086,-1.49798854844369,
9.00202425952587));
#266161=CARTESIAN_POINT('Ctrl Pts',(-0.41546352436777,-1.49899445343014,
9.00229324204476));
#266162=CARTESIAN_POINT('Ctrl Pts',(-0.405345345873723,-1.50177257451984,
9.00304383996673));
#266163=CARTESIAN_POINT('Ctrl Pts',(-0.39883151078298,-1.50351559533693,
9.00352380886692));
#266164=CARTESIAN_POINT('Ctrl Pts',(-0.359920645324104,-1.51365698279392,
9.00637275468749));
#266165=CARTESIAN_POINT('Ctrl Pts',(-0.327267814101156,-1.52105112787937,
9.00868856120706));
#266166=CARTESIAN_POINT('Ctrl Pts',(-0.12732290473174,-1.5595898679393,
9.02255901386915));
#266167=CARTESIAN_POINT('Ctrl Pts',(0.0439083767719911,-1.56416577747891,
9.03325970940069));
#266168=CARTESIAN_POINT('Ctrl Pts',(0.215299283205228,-1.54053058283668,
9.04514989790096));
#266169=CARTESIAN_POINT('Ctrl Pts',(0.2181015203611,-1.54013635261787,9.04534458652009));
#266170=CARTESIAN_POINT('Ctrl Pts',(0.245474402131607,-1.53620921956422,
9.04724918874785));
#266171=CARTESIAN_POINT('Ctrl Pts',(0.269956974732322,-1.53209645942151,
9.04897514164185));
#266172=CARTESIAN_POINT('Ctrl Pts',(0.303396730470763,-1.5256526278948,
9.05136842418234));
#266173=CARTESIAN_POINT('Ctrl Pts',(0.312448017306929,-1.52382471005529,
9.05201984930471));
#266174=CARTESIAN_POINT('Ctrl Pts',(0.326860148154003,-1.52078036055114,
9.05306312648649));
#266175=CARTESIAN_POINT('Ctrl Pts',(0.332231852587348,-1.51961589100823,
9.05345331931353));
#266176=CARTESIAN_POINT('Ctrl Pts',(0.343269472975116,-1.51716185160155,
9.05425789634303));
#266177=CARTESIAN_POINT('Ctrl Pts',(0.348934552610121,-1.51586895586077,
9.05467238112592));
#266178=CARTESIAN_POINT('Ctrl Pts',(0.362071532443969,-1.51279326491763,
9.05563718252595));
#266179=CARTESIAN_POINT('Ctrl Pts',(0.369537679069446,-1.51098681556572,
9.05618824926663));
#266180=CARTESIAN_POINT('Ctrl Pts',(0.393345254603278,-1.50503951676996,
9.05795441980577));
#266181=CARTESIAN_POINT('Ctrl Pts',(0.409632369885046,-1.5006884141512,
9.05917623794978));
#266182=CARTESIAN_POINT('Ctrl Pts',(0.492119489609785,-1.47720913826289,
9.06543586224443));
#266183=CARTESIAN_POINT('Ctrl Pts',(0.557057287389644,-1.45396460422588,
9.07060518040054));
#266184=CARTESIAN_POINT('Ctrl Pts',(0.677789300441647,-1.40147099197126,
9.08067182051833));
#266185=CARTESIAN_POINT('Ctrl Pts',(0.733775945339606,-1.37298630199348,
9.08554254086479));
#266186=CARTESIAN_POINT('Ctrl Pts',(0.829035159674219,-1.31702641011422,
9.09410680469196));
#266187=CARTESIAN_POINT('Ctrl Pts',(0.869052328162863,-1.29097109248076,
9.09779766728948));
#266188=CARTESIAN_POINT('Ctrl Pts',(0.938199312171517,-1.24127468990473,
9.10428000736169));
#266189=CARTESIAN_POINT('Ctrl Pts',(0.967793867134395,-1.21834166079712,
9.10709139056436));
#266190=CARTESIAN_POINT('Ctrl Pts',(1.00159821008633,-1.19013644556336,
9.11032143640038));
#266191=CARTESIAN_POINT('Ctrl Pts',(1.00663464826271,-1.18587959866864,
9.11080317628418));
#266192=CARTESIAN_POINT('Ctrl Pts',(1.01476690024465,-1.17891699866809,
9.11158164379128));
#266193=CARTESIAN_POINT('Ctrl Pts',(1.0178792558709,-1.17623083325594,9.1118797238133));
#266194=CARTESIAN_POINT('Ctrl Pts',(1.02341123827559,-1.171417971529,9.11240974545337));
#266195=CARTESIAN_POINT('Ctrl Pts',(1.02583493705782,-1.16929607425101,
9.1126420290517));
#266196=CARTESIAN_POINT('Ctrl Pts',(1.03107663833455,-1.16467823275677,
9.1131445263873));
#266197=CARTESIAN_POINT('Ctrl Pts',(1.03389217465392,-1.16217958680195,
9.11341453469688));
#266198=CARTESIAN_POINT('Ctrl Pts',(1.04177558718018,-1.15513213524064,
9.11417091436946));
#266199=CARTESIAN_POINT('Ctrl Pts',(1.04682278671226,-1.15056015995352,
9.11465559809923));
#266200=CARTESIAN_POINT('Ctrl Pts',(1.07739951787051,-1.12249463870121,
9.11759571596163));
#266201=CARTESIAN_POINT('Ctrl Pts',(1.10216958258371,-1.09818332411337,
9.11999393635995));
#266202=CARTESIAN_POINT('Ctrl Pts',(1.18407214874722,-1.01223192990374,
9.12807091655622));
#266203=CARTESIAN_POINT('Ctrl Pts',(1.23701709666197,-0.946800618795461,
9.13355893523025));
#266204=CARTESIAN_POINT('Ctrl Pts',(1.34346167849062,-0.790978414027506,
9.14598957386394));
#266205=CARTESIAN_POINT('Ctrl Pts',(1.39361947133258,-0.698824797248738,
9.15293884176142));
#266206=CARTESIAN_POINT('Ctrl Pts',(1.43877118918238,-0.591321061156696,
9.16108200174805));
#266207=CARTESIAN_POINT('Ctrl Pts',(1.4432726163604,-0.580247596361419,
9.16192087094849));
#266208=CARTESIAN_POINT('Ctrl Pts',(1.45036101584806,-0.562217256554662,
9.16328745778708));
#266209=CARTESIAN_POINT('Ctrl Pts',(1.45302666345906,-0.555291663628217,
9.16381253902381));
#266210=CARTESIAN_POINT('Ctrl Pts',(1.45767844013214,-0.542943059928113,
9.16474920191221));
#266211=CARTESIAN_POINT('Ctrl Pts',(1.45968413064646,-0.537527523243102,
9.16516012304043));
#266212=CARTESIAN_POINT('Ctrl Pts',(1.46384306085866,-0.526103112962152,
9.16602735304448));
#266213=CARTESIAN_POINT('Ctrl Pts',(1.46598955907289,-0.520091917587838,
9.16648387674281));
#266214=CARTESIAN_POINT('Ctrl Pts',(1.47156856927894,-0.504159117042972,
9.16769456159315));
#266215=CARTESIAN_POINT('Ctrl Pts',(1.47493768409899,-0.494215830760699,
9.16845079614699));
#266216=CARTESIAN_POINT('Ctrl Pts',(1.49033700413312,-0.447207340245067,
9.17202983869718));
#266217=CARTESIAN_POINT('Ctrl Pts',(1.50107123344732,-0.409735820065769,
9.17489442187347));
#266218=CARTESIAN_POINT('Ctrl Pts',(1.54626152262505,-0.226207679508899,
9.18899459191443));
#266219=CARTESIAN_POINT('Ctrl Pts',(1.5608619184384,-0.0760940320435691,
9.2008434729993));
#266220=CARTESIAN_POINT('Ctrl Pts',(1.55192565273712,0.11220605471138,9.21520581950105));
#266221=CARTESIAN_POINT('Ctrl Pts',(1.54867179088438,0.150597893631395,
9.21810113358521));
#266222=CARTESIAN_POINT('Ctrl Pts',(1.54318869143675,0.195430526934642,
9.22141530384782));
#266223=CARTESIAN_POINT('Ctrl Pts',(1.54233950766328,0.20202295796946,9.22190092432289));
#266224=CARTESIAN_POINT('Ctrl Pts',(1.54089460277449,0.212699564731272,
9.22268440580536));
#266225=CARTESIAN_POINT('Ctrl Pts',(1.54032485093962,0.216787076043851,
9.22298364721597));
#266226=CARTESIAN_POINT('Ctrl Pts',(1.53928124184963,0.224062253529249,
9.22351492703107));
#266227=CARTESIAN_POINT('Ctrl Pts',(1.53881374123598,0.227250754586009,
9.22374731407181));
#266228=CARTESIAN_POINT('Ctrl Pts',(1.53778033195706,0.234149494723338,
9.22424911470589));
#266229=CARTESIAN_POINT('Ctrl Pts',(1.5372109044494,0.237859141680731,9.22451832792846));
#266230=CARTESIAN_POINT('Ctrl Pts',(1.53557856595667,0.248242595406701,
9.22527022497462));
#266231=CARTESIAN_POINT('Ctrl Pts',(1.53448556483765,0.254911698724805,
9.22575125309384));
#266232=CARTESIAN_POINT('Ctrl Pts',(1.52767568739513,0.294831317394578,
9.22862032584849));
#266233=CARTESIAN_POINT('Ctrl Pts',(1.52092120064672,0.327898834581176,
9.23095432098361));
#266234=CARTESIAN_POINT('Ctrl Pts',(1.49346582700328,0.443063532072579,
9.23901662325647));
#266235=CARTESIAN_POINT('Ctrl Pts',(1.46718301667972,0.523515915387443,
9.24453541249253));
#266236=CARTESIAN_POINT('Ctrl Pts',(1.43457655129078,0.601307216393289,
9.25009119722734));
#266237=CARTESIAN_POINT('Origin',(0.,0.,-1.29405622560371));
#266238=CARTESIAN_POINT('',(1.43457678342463,0.601306662576624,10.0876445460468));
#266239=CARTESIAN_POINT('',(1.4345766815454,0.601306905636538,9.94872080685755));
#266240=CARTESIAN_POINT('',(1.43457668357355,0.601306900797845,-1.29405622560371));
#266241=CARTESIAN_POINT('Ctrl Pts',(1.43457678342482,0.601306662576175,
10.0876445460468));
#266242=CARTESIAN_POINT('Ctrl Pts',(1.47844253086014,0.496653268933943,
10.0801366808513));
#266243=CARTESIAN_POINT('Ctrl Pts',(1.51076896683316,0.387410400172105,
10.0727718155593));
#266244=CARTESIAN_POINT('Ctrl Pts',(1.53762167463432,0.238194528969206,
10.0624490528545));
#266245=CARTESIAN_POINT('Ctrl Pts',(1.54296881157422,0.200658646562479,
10.0598339115176));
#266246=CARTESIAN_POINT('Ctrl Pts',(1.54802077539321,0.152703766849103,
10.0564515996699));
#266247=CARTESIAN_POINT('Ctrl Pts',(1.54899983593301,0.142429844505044,
10.0557246046814));
#266248=CARTESIAN_POINT('Ctrl Pts',(1.55041114718988,0.125877401753474,
10.0545491900554));
#266249=CARTESIAN_POINT('Ctrl Pts',(1.55090766847366,0.11960454572007,10.0541027891499));
#266250=CARTESIAN_POINT('Ctrl Pts',(1.5517816891392,0.107640027855507,10.0532494452295));
#266251=CARTESIAN_POINT('Ctrl Pts',(1.55216596926851,0.101948950930017,
10.0528427217393));
#266252=CARTESIAN_POINT('Ctrl Pts',(1.55297339534685,0.0889259204743075,
10.0519100672809));
#266253=CARTESIAN_POINT('Ctrl Pts',(1.55337593174265,0.0815928749452438,
10.0513835004106));
#266254=CARTESIAN_POINT('Ctrl Pts',(1.55429255227922,0.0624139347931474,
10.050002498383));
#266255=CARTESIAN_POINT('Ctrl Pts',(1.55472313640854,0.0505647303947134,
10.0491454799586));
#266256=CARTESIAN_POINT('Ctrl Pts',(1.55762805556826,-0.0661224749199538,
10.040666643287));
#266257=CARTESIAN_POINT('Ctrl Pts',(1.54962956088441,-0.170929903483639,
10.0327114813115));
#266258=CARTESIAN_POINT('Ctrl Pts',(1.51630818856622,-0.35705656482159,
10.0180914144968));
#266259=CARTESIAN_POINT('Ctrl Pts',(1.49474476658779,-0.438655801965744,
10.0115109153316));
#266260=CARTESIAN_POINT('Ctrl Pts',(1.45512961956112,-0.550799475247924,
10.0024806842266));
#266261=CARTESIAN_POINT('Ctrl Pts',(1.44249072004974,-0.583097986228494,
9.99988295825648));
#266262=CARTESIAN_POINT('Ctrl Pts',(1.42611305243361,-0.62115004119941,
9.99684734036577));
#266263=CARTESIAN_POINT('Ctrl Pts',(1.42340413339682,-0.627332837894983,
9.99635491101084));
#266264=CARTESIAN_POINT('Ctrl Pts',(1.41913885838132,-0.636897958311962,
9.99559456524021));
#266265=CARTESIAN_POINT('Ctrl Pts',(1.41761050755092,-0.640292556837241,
9.99532501235459));
#266266=CARTESIAN_POINT('Ctrl Pts',(1.41475421204201,-0.646576274980252,
9.99482662492826));
#266267=CARTESIAN_POINT('Ctrl Pts',(1.41342960668861,-0.649466786786311,
9.9945976002582));
#266268=CARTESIAN_POINT('Ctrl Pts',(1.41039888165141,-0.656027150627278,
9.99407831408346));
#266269=CARTESIAN_POINT('Ctrl Pts',(1.40868729902373,-0.65969441584352,
9.99378839214965));
#266270=CARTESIAN_POINT('Ctrl Pts',(1.40420270791728,-0.669206134942573,
9.99303725764256));
#266271=CARTESIAN_POINT('Ctrl Pts',(1.40140748219221,-0.675040123760145,
9.99257736950926));
#266272=CARTESIAN_POINT('Ctrl Pts',(1.38283468593363,-0.71319127534365,
9.98957421366076));
#266273=CARTESIAN_POINT('Ctrl Pts',(1.36597528757749,-0.744973549731163,
9.98709249666989));
#266274=CARTESIAN_POINT('Ctrl Pts',(1.34313440185583,-0.78464411938279,
9.98398395977101));
#266275=CARTESIAN_POINT('Ctrl Pts',(1.33816096509159,-0.793096245307337,
9.98332101981667));
#266276=CARTESIAN_POINT('Ctrl Pts',(1.28624675827276,-0.879443289256175,
9.97653590590134));
#266277=CARTESIAN_POINT('Ctrl Pts',(1.23263816642673,-0.953129719043354,
9.97063088270741));
#266278=CARTESIAN_POINT('Ctrl Pts',(1.11574952135114,-1.08731432660721,
9.95885933593548));
#266279=CARTESIAN_POINT('Ctrl Pts',(1.05320970919655,-1.14799621593321,
9.95302188042457));
#266280=CARTESIAN_POINT('Ctrl Pts',(0.976065209279602,-1.2112141445352,
9.94605144783859));
#266281=CARTESIAN_POINT('Ctrl Pts',(0.966099084841004,-1.21917822236438,
9.94515522833313));
#266282=CARTESIAN_POINT('Ctrl Pts',(0.950656027440404,-1.23121074138343,
9.94377233504581));
#266283=CARTESIAN_POINT('Ctrl Pts',(0.94524823212154,-1.23536737418218,
9.94328915855291));
#266284=CARTESIAN_POINT('Ctrl Pts',(0.935344942960903,-1.24287631458332,
9.94240617457333));
#266285=CARTESIAN_POINT('Ctrl Pts',(0.930858300528754,-1.24624015282011,
9.94200682789183));
#266286=CARTESIAN_POINT('Ctrl Pts',(0.921026522439148,-1.25352876660994,
9.94113315067698));
#266287=CARTESIAN_POINT('Ctrl Pts',(0.915674302963068,-1.25744375306774,
9.94065845034418));
#266288=CARTESIAN_POINT('Ctrl Pts',(0.900931545649483,-1.26808359532461,
9.93935325727198));
#266289=CARTESIAN_POINT('Ctrl Pts',(0.891491049673795,-1.27473814944232,
9.93852009259508));
#266290=CARTESIAN_POINT('Ctrl Pts',(0.841448092651728,-1.30918536701686,
9.9341162857535));
#266291=CARTESIAN_POINT('Ctrl Pts',(0.799622372412186,-1.33514204815298,
9.93047776386972));
#266292=CARTESIAN_POINT('Ctrl Pts',(0.629242157930082,-1.42999852539775,
9.91580440818312));
#266293=CARTESIAN_POINT('Ctrl Pts',(0.492527918992509,-1.48264895356484,
9.90426496893743));
#266294=CARTESIAN_POINT('Ctrl Pts',(0.319577904150437,-1.52264816033673,
9.89082068520897));
#266295=CARTESIAN_POINT('Ctrl Pts',(0.288443018036543,-1.52885200404884,
9.88844783324883));
#266296=CARTESIAN_POINT('Ctrl Pts',(0.250641988381717,-1.53518800786845,
9.88564033074139));
#266297=CARTESIAN_POINT('Ctrl Pts',(0.244139559977051,-1.53623549798116,
9.8851599990577));
#266298=CARTESIAN_POINT('Ctrl Pts',(0.233986672846962,-1.53780495571834,
9.88441427347687));
#266299=CARTESIAN_POINT('Ctrl Pts',(0.230340782598476,-1.53835528066253,
9.88414734013157));
#266300=CARTESIAN_POINT('Ctrl Pts',(0.223543067305137,-1.53935664610953,
9.88365128310761));
#266301=CARTESIAN_POINT('Ctrl Pts',(0.220391844459914,-1.53981096958914,
9.88342198520346));
#266302=CARTESIAN_POINT('Ctrl Pts',(0.213181922643759,-1.54082786398965,
9.88289884277056));
#266303=CARTESIAN_POINT('Ctrl Pts',(0.209122382309097,-1.54138407570767,
9.88260535840243));
#266304=CARTESIAN_POINT('Ctrl Pts',(0.198482043803342,-1.54279913517462,
9.8818388049991));
#266305=CARTESIAN_POINT('Ctrl Pts',(0.191897771730655,-1.54363193235054,
9.88136715137549));
#266306=CARTESIAN_POINT('Ctrl Pts',(0.146307234202684,-1.54910213285693,
9.87811868363861));
#266307=CARTESIAN_POINT('Ctrl Pts',(0.10713878918169,-1.5523031775849,9.87541542431602));
#266308=CARTESIAN_POINT('Ctrl Pts',(-0.0818442132904599,-1.56055889476217,
9.86261126892046));
#266309=CARTESIAN_POINT('Ctrl Pts',(-0.231737247206432,-1.54542760266506,
9.85309825107761));
#266310=CARTESIAN_POINT('Ctrl Pts',(-0.414665255115307,-1.49970916326379,
9.84026833650741));
#266311=CARTESIAN_POINT('Ctrl Pts',(-0.451806187156601,-1.48894109772049,
9.83760231444335));
#266312=CARTESIAN_POINT('Ctrl Pts',(-0.498367017896825,-1.47353943476071,
9.83416273279154));
#266313=CARTESIAN_POINT('Ctrl Pts',(-0.508195841200293,-1.4701786041158,
9.8334310733035));
#266314=CARTESIAN_POINT('Ctrl Pts',(-0.523937362672284,-1.46461929249572,
9.83224992994934));
#266315=CARTESIAN_POINT('Ctrl Pts',(-0.529871756009032,-1.4624828040043,
9.83180250089712));
#266316=CARTESIAN_POINT('Ctrl Pts',(-0.541144691661499,-1.45834672485435,
9.83094838389672));
#266317=CARTESIAN_POINT('Ctrl Pts',(-0.546485569241593,-1.45635375792664,
9.83054192226394));
#266318=CARTESIAN_POINT('Ctrl Pts',(-0.558655647288737,-1.4517360794013,
9.82961155029829));
#266319=CARTESIAN_POINT('Ctrl Pts',(-0.565477481690202,-1.4490924714439,
9.82908701517361));
#266320=CARTESIAN_POINT('Ctrl Pts',(-0.583218917641197,-1.44207292758878,
9.82771482185608));
#266321=CARTESIAN_POINT('Ctrl Pts',(-0.594107792879591,-1.43762114295616,
9.82686463384183));
#266322=CARTESIAN_POINT('Ctrl Pts',(-0.678079545492833,-1.40217338642281,
9.82024461101965));
#266323=CARTESIAN_POINT('Ctrl Pts',(-0.748730734262422,-1.36575270583019,
9.81428974285974));
#266324=CARTESIAN_POINT('Ctrl Pts',(-0.90718489793107,-1.26806896540939,
9.80002539570256));
#266325=CARTESIAN_POINT('Ctrl Pts',(-0.992068713572339,-1.20282254056915,
9.79163998644903));
#266326=CARTESIAN_POINT('Ctrl Pts',(-1.09685968115574,-1.10357998845685,
9.7806568559953));
#266327=CARTESIAN_POINT('Ctrl Pts',(-1.12317979586336,-1.07678116415248,
9.77783793554676));
#266328=CARTESIAN_POINT('Ctrl Pts',(-1.15315574278301,-1.0439634116067,
9.77457992730635));
#266329=CARTESIAN_POINT('Ctrl Pts',(-1.15777113129653,-1.03884252135484,
9.77407689384493));
#266330=CARTESIAN_POINT('Ctrl Pts',(-1.16484691146803,-1.03088603299751,
9.77330375271329));
#266331=CARTESIAN_POINT('Ctrl Pts',(-1.16733126051641,-1.02807201557891,
9.77303192146778));
#266332=CARTESIAN_POINT('Ctrl Pts',(-1.17189930655405,-1.02285989138455,
9.77253144340425));
#266333=CARTESIAN_POINT('Ctrl Pts',(-1.17398583034206,-1.02046441027476,
9.77230259277415));
#266334=CARTESIAN_POINT('Ctrl Pts',(-1.17868709994172,-1.01503350692562,
9.77178637310993));
#266335=CARTESIAN_POINT('Ctrl Pts',(-1.18129746361163,-1.01199436914875,
9.77149932696935));
#266336=CARTESIAN_POINT('Ctrl Pts',(-1.18898785429494,-1.00297046566973,
9.77065230112957));
#266337=CARTESIAN_POINT('Ctrl Pts',(-1.19403445353265,-0.996957172249979,
9.7700946930963));
#266338=CARTESIAN_POINT('Ctrl Pts',(-1.23450839700174,-0.94798208819109,
9.7656057184469));
#266339=CARTESIAN_POINT('Ctrl Pts',(-1.26765569712896,-0.903178661932668,
9.76182260192153));
#266340=CARTESIAN_POINT('Ctrl Pts',(-1.37277829468245,-0.743862757981147,
9.74906930194352));
#266341=CARTESIAN_POINT('Ctrl Pts',(-1.43219874660425,-0.621819782193494,
9.74040512651302));
#266342=CARTESIAN_POINT('Ctrl Pts',(-1.48663399272524,-0.4591529194858,
9.72871071651736));
#266343=CARTESIAN_POINT('Ctrl Pts',(-1.49695835129795,-0.424284537689517,
9.72620009026614));
#266344=CARTESIAN_POINT('Ctrl Pts',(-1.50859712903308,-0.379234158149677,
9.72293561295762));
#266345=CARTESIAN_POINT('Ctrl Pts',(-1.51104622228774,-0.369355045692685,
9.72221851612086));
#266346=CARTESIAN_POINT('Ctrl Pts',(-1.51484499153238,-0.353361151494857,
9.72105525580279));
#266347=CARTESIAN_POINT('Ctrl Pts',(-1.51625503271118,-0.347260889605912,
9.72061103533954));
#266348=CARTESIAN_POINT('Ctrl Pts',(-1.51888094265229,-0.335579437573681,
9.71975928366385));
#266349=CARTESIAN_POINT('Ctrl Pts',(-1.52010297571201,-0.329999725008494,
9.7193519573891));
#266350=CARTESIAN_POINT('Ctrl Pts',(-1.52281322792954,-0.317290354479505,
9.71842299595069));
#266351=CARTESIAN_POINT('Ctrl Pts',(-1.5242821500401,-0.310156766697294,
9.71790075429078));
#266352=CARTESIAN_POINT('Ctrl Pts',(-1.52802243903776,-0.291324050560442,
9.71651971325704));
#266353=CARTESIAN_POINT('Ctrl Pts',(-1.53020950684352,-0.279608882365264,
9.71565826053547));
#266354=CARTESIAN_POINT('Ctrl Pts',(-1.54780879990943,-0.17893796457108,
9.70823388929048));
#266355=CARTESIAN_POINT('Ctrl Pts',(-1.555581235732,-0.0888385080196809,
9.70142856197073));
#266356=CARTESIAN_POINT('Ctrl Pts',(-1.55541935066541,0.0896033524905979,
9.68769192438867));
#266357=CARTESIAN_POINT('Ctrl Pts',(-1.54783931923097,0.177627251609025,
9.68079338785291));
#266358=CARTESIAN_POINT('Ctrl Pts',(-1.52999796541242,0.281008854757881,
9.67277117261743));
#266359=CARTESIAN_POINT('Ctrl Pts',(-1.52688927605936,0.297437267115137,
9.67149922133837));
#266360=CARTESIAN_POINT('Ctrl Pts',(-1.51775431724925,0.341786168768107,
9.66807830749043));
#266361=CARTESIAN_POINT('Ctrl Pts',(-1.51122257092077,0.369597845716856,
9.66594675006831));
#266362=CARTESIAN_POINT('Ctrl Pts',(-1.50223829838421,0.403613839664403,
9.66336902220448));
#266363=CARTESIAN_POINT('Ctrl Pts',(-1.50050767899166,0.410000909998151,
9.66288630213274));
#266364=CARTESIAN_POINT('Ctrl Pts',(-1.49773682393734,0.419974520795588,
9.66213474774306));
#266365=CARTESIAN_POINT('Ctrl Pts',(-1.49672437117302,0.423568588813101,
9.66186437361502));
#266366=CARTESIAN_POINT('Ctrl Pts',(-1.49482611716555,0.430215332498108,
9.66136523909301));
#266367=CARTESIAN_POINT('Ctrl Pts',(-1.49394390779455,0.433268916027962,
9.66113628362256));
#266368=CARTESIAN_POINT('Ctrl Pts',(-1.49192135315733,0.440189939157331,
9.66061813197997));
#266369=CARTESIAN_POINT('Ctrl Pts',(-1.49077532831515,0.444055658696583,
9.66032926924321));
#266370=CARTESIAN_POINT('Ctrl Pts',(-1.48724160960258,0.455807564853408,
9.65945266655478));
#266371=CARTESIAN_POINT('Ctrl Pts',(-1.48480622351122,0.463679445348387,
9.65886761190597));
#266372=CARTESIAN_POINT('Ctrl Pts',(-1.47902163853053,0.481863877358021,
9.65752023059936));
#266373=CARTESIAN_POINT('Ctrl Pts',(-1.47562689931451,0.492161633671748,
9.65676030541721));
#266374=CARTESIAN_POINT('Ctrl Pts',(-1.46362596516928,0.527324945947235,
9.65417330326446));
#266375=CARTESIAN_POINT('Ctrl Pts',(-1.45449626084364,0.55200848865195,
9.6523708787466));
#266376=CARTESIAN_POINT('Ctrl Pts',(-1.40057364947584,0.687153546254603,
9.64251576904411));
#266377=CARTESIAN_POINT('Ctrl Pts',(-1.34382377608123,0.792419283826056,
9.63486114319564));
#266378=CARTESIAN_POINT('Ctrl Pts',(-1.23788923570902,0.944221226886848,
9.62250620004183));
#266379=CARTESIAN_POINT('Ctrl Pts',(-1.19678263446667,0.995807730607634,
9.61803459043951));
#266380=CARTESIAN_POINT('Ctrl Pts',(-1.14489923276042,1.05305042924463,
9.6126343443291));
#266381=CARTESIAN_POINT('Ctrl Pts',(-1.1371735514339,1.06138860063923,9.61183608812386));
#266382=CARTESIAN_POINT('Ctrl Pts',(-1.12440860889715,1.07486618760146,
9.6105261244484));
#266383=CARTESIAN_POINT('Ctrl Pts',(-1.11942373693226,1.08005672770383,
9.61001674524638));
#266384=CARTESIAN_POINT('Ctrl Pts',(-1.11043540563666,1.0892868324814,9.60910202445981));
#266385=CARTESIAN_POINT('Ctrl Pts',(-1.10644544424069,1.0933394124673,9.60869727540878));
#266386=CARTESIAN_POINT('Ctrl Pts',(-1.09793578888721,1.10188833260888,
9.60783671878387));
#266387=CARTESIAN_POINT('Ctrl Pts',(-1.09341050841158,1.10637893685565,
9.60738066856671));
#266388=CARTESIAN_POINT('Ctrl Pts',(-1.08121946132528,1.11832872127012,
9.60615617554746));
#266389=CARTESIAN_POINT('Ctrl Pts',(-1.07350427129386,1.125736745982,9.60538552890128));
#266390=CARTESIAN_POINT('Ctrl Pts',(-1.03485889349432,1.16208498716031,
9.60154566508982));
#266391=CARTESIAN_POINT('Ctrl Pts',(-1.00283485146302,1.18983026800243,
9.59842656632351));
#266392=CARTESIAN_POINT('Ctrl Pts',(-0.846779639675462,1.3142555991856,
9.58349671095936));
#266393=CARTESIAN_POINT('Ctrl Pts',(-0.709716708672483,1.39305102056663,
9.57102424986713));
#266394=CARTESIAN_POINT('Ctrl Pts',(-0.536331559427122,1.46039686847863,
9.55696809261493));
#266395=CARTESIAN_POINT('Ctrl Pts',(-0.509184505099739,1.47008230223421,
9.55481711825901));
#266396=CARTESIAN_POINT('Ctrl Pts',(-0.475472072141567,1.48106400817749,
9.55221923524248));
#266397=CARTESIAN_POINT('Ctrl Pts',(-0.469149067865993,1.48307904174806,
9.55173511721245));
#266398=CARTESIAN_POINT('Ctrl Pts',(-0.459244309671248,1.48616583467769,
9.55098185849182));
#266399=CARTESIAN_POINT('Ctrl Pts',(-0.45567135978787,1.48726522073147,
9.55071116696772));
#266400=CARTESIAN_POINT('Ctrl Pts',(-0.449053517919327,1.4892754239568,
9.55021174171513));
#266401=CARTESIAN_POINT('Ctrl Pts',(-0.446009820069313,1.49018978359114,
9.54998281100287));
#266402=CARTESIAN_POINT('Ctrl Pts',(-0.439103712939263,1.49224139799925,
9.54946508886609));
#266403=CARTESIAN_POINT('Ctrl Pts',(-0.435239681428837,1.49337298800968,
9.5491766285439));
#266404=CARTESIAN_POINT('Ctrl Pts',(-0.423482380285726,1.49676662932743,
9.54830246331214));
#266405=CARTESIAN_POINT('Ctrl Pts',(-0.415575384644471,1.49898124624159,
9.54771942192633));
#266406=CARTESIAN_POINT('Ctrl Pts',(-0.319936120803106,1.52495325243211,
9.54072143669122));
#266407=CARTESIAN_POINT('Ctrl Pts',(-0.230286500239397,1.5410435690689,
9.53470551968568));
#266408=CARTESIAN_POINT('Ctrl Pts',(-0.0177832922187705,1.56021036104209,
9.52064810628876));
#266409=CARTESIAN_POINT('Ctrl Pts',(0.105020370939977,1.55677191647627,
9.51264851258683));
#266410=CARTESIAN_POINT('Ctrl Pts',(0.244019536252181,1.536346684342,9.50290022371281));
#266411=CARTESIAN_POINT('Ctrl Pts',(0.261846837541059,1.53340890009237,
9.50163758066318));
#266412=CARTESIAN_POINT('Ctrl Pts',(0.286751970780154,1.52885779125364,
9.49985443320377));
#266413=CARTESIAN_POINT('Ctrl Pts',(0.293876328611617,1.52750434988096,
9.49934213432499));
#266414=CARTESIAN_POINT('Ctrl Pts',(0.306228277737918,1.52506819176618,
9.49844996192172));
#266415=CARTESIAN_POINT('Ctrl Pts',(0.311460287824334,1.52400827932011,
9.49807081762084));
#266416=CARTESIAN_POINT('Ctrl Pts',(0.322357059308416,1.52174233032004,
9.49727852833045));
#266417=CARTESIAN_POINT('Ctrl Pts',(0.328020737820953,1.52053154767105,
9.49686523745411));
#266418=CARTESIAN_POINT('Ctrl Pts',(0.341410582989951,1.51759077149081,
9.49588454481544));
#266419=CARTESIAN_POINT('Ctrl Pts',(0.34913049802757,1.51583337703686,9.4953162749674));
#266420=CARTESIAN_POINT('Ctrl Pts',(0.374867717183696,1.5097674087971,9.49341197712675));
#266421=CARTESIAN_POINT('Ctrl Pts',(0.392820788270152,1.50519606936468,
9.49206758059581));
#266422=CARTESIAN_POINT('Ctrl Pts',(0.435360243601908,1.49355149905255,
9.48884226064361));
#266423=CARTESIAN_POINT('Ctrl Pts',(0.459861486105481,1.48619039687422,
9.48695250844848));
#266424=CARTESIAN_POINT('Ctrl Pts',(0.626579731903588,1.43158466077983,
9.47386860437107));
#266425=CARTESIAN_POINT('Ctrl Pts',(0.761494314389863,1.3646056987717,9.46203677239422));
#266426=CARTESIAN_POINT('Ctrl Pts',(0.916990895997634,1.25707924778209,
9.44762524639557));
#266427=CARTESIAN_POINT('Ctrl Pts',(0.948418356069569,1.23354116440051,
9.44467330728708));
#266428=CARTESIAN_POINT('Ctrl Pts',(0.984081462484981,1.20466093030836,
9.44130603679204));
#266429=CARTESIAN_POINT('Ctrl Pts',(0.989211620154896,1.20045185516356,
9.44082122096884));
#266430=CARTESIAN_POINT('Ctrl Pts',(0.997465580391936,1.19359099042189,
9.44004070619022));
#266431=CARTESIAN_POINT('Ctrl Pts',(1.00060604381264,1.19095952181927,9.43974362021254));
#266432=CARTESIAN_POINT('Ctrl Pts',(1.00616835225893,1.18626119946765,9.43921727788989));
#266433=CARTESIAN_POINT('Ctrl Pts',(1.00859428143507,1.18419929176145,9.4389876718591));
#266434=CARTESIAN_POINT('Ctrl Pts',(1.01381616451833,1.17973328797119,9.43849334226401));
#266435=CARTESIAN_POINT('Ctrl Pts',(1.01660990311454,1.17732669715817,9.43822880627326));
#266436=CARTESIAN_POINT('Ctrl Pts',(1.02437030589653,1.17059348741227,9.43749370800106));
#266437=CARTESIAN_POINT('Ctrl Pts',(1.02931816425105,1.16624515314938,9.4370247106712));
#266438=CARTESIAN_POINT('Ctrl Pts',(1.05795374878651,1.14075509224693,9.43430750979954));
#266439=CARTESIAN_POINT('Ctrl Pts',(1.0810194200989,1.11892166638026,9.43210718981094));
#266440=CARTESIAN_POINT('Ctrl Pts',(1.20615091865032,0.992990455380167,
9.41999162257703));
#266441=CARTESIAN_POINT('Ctrl Pts',(1.29386065716655,0.875650069229085,
9.41073992067343));
#266442=CARTESIAN_POINT('Ctrl Pts',(1.38760487917842,0.704665237915422,
9.39758699089129));
#266443=CARTESIAN_POINT('Ctrl Pts',(1.40919323568639,0.660434704966541,
9.39421755039785));
#266444=CARTESIAN_POINT('Ctrl Pts',(1.43064719267416,0.610618044335124,
9.39042104283477));
#266445=CARTESIAN_POINT('Ctrl Pts',(1.43262330446223,0.605967203421737,
9.39006660355166));
#266446=CARTESIAN_POINT('Ctrl Pts',(1.43457668359376,0.601306900749626,
9.38971141570882));
#266447=CARTESIAN_POINT('',(-1.55550041510621,0.000136228757878965,9.55740355867135));
#266448=CARTESIAN_POINT('Ctrl Pts',(1.43457655129078,0.601307216393289,
9.25009119722734));
#266449=CARTESIAN_POINT('Ctrl Pts',(1.39925071630394,0.685586288962663,
9.25611033277065));
#266450=CARTESIAN_POINT('Ctrl Pts',(1.35650306920638,0.766741828868003,
9.2621775061668));
#266451=CARTESIAN_POINT('Ctrl Pts',(1.29474908886411,0.862377045314231,
9.27004055526603));
#266452=CARTESIAN_POINT('Ctrl Pts',(1.28235765822098,0.880697520446168,
9.27158128126093));
#266453=CARTESIAN_POINT('Ctrl Pts',(1.26448653094339,0.905942486002453,
9.27375665296959));
#266454=CARTESIAN_POINT('Ctrl Pts',(1.25933167991373,0.91309456745673,9.27437897720188));
#266455=CARTESIAN_POINT('Ctrl Pts',(1.2509114597129,0.924570235499429,9.27538750389055));
#266456=CARTESIAN_POINT('Ctrl Pts',(1.24768375595191,0.928921333695101,
9.27577224738425));
#266457=CARTESIAN_POINT('Ctrl Pts',(1.24091876103452,0.937941999962577,
9.27657486403914));
#266458=CARTESIAN_POINT('Ctrl Pts',(1.23737769561372,0.94260861626253,9.27699288030599));
#266459=CARTESIAN_POINT('Ctrl Pts',(1.22895452807975,0.953579886961219,
9.27798235884503));
#266460=CARTESIAN_POINT('Ctrl Pts',(1.22405018088686,0.959867169553989,
9.27855469177296));
#266461=CARTESIAN_POINT('Ctrl Pts',(1.20760308448201,0.980621003952878,
9.28046182767233));
#266462=CARTESIAN_POINT('Ctrl Pts',(1.19585091354144,0.994918740762502,
9.28180494327615));
#266463=CARTESIAN_POINT('Ctrl Pts',(1.16732537036019,1.02838730456784,9.28502086956314));
#266464=CARTESIAN_POINT('Ctrl Pts',(1.15033115388183,1.04736195604734,9.28690235491231));
#266465=CARTESIAN_POINT('Ctrl Pts',(1.02987131190614,1.17539013727228,9.30001157764069));
#266466=CARTESIAN_POINT('Ctrl Pts',(0.911540348493249,1.26935278601737,
9.31188129206641));
#266467=CARTESIAN_POINT('Ctrl Pts',(0.74814260735315,1.36431735631842,9.32628221208198));
#266468=CARTESIAN_POINT('Ctrl Pts',(0.71395069661022,1.38251735329988,9.32919330152686));
#266469=CARTESIAN_POINT('Ctrl Pts',(0.673122833155897,1.40233028077393,
9.33252330485184));
#266470=CARTESIAN_POINT('Ctrl Pts',(0.667115096777648,1.40519821262707,
9.33300968509803));
#266471=CARTESIAN_POINT('Ctrl Pts',(0.657350513322305,1.40978282363793,
9.33379414786567));
#266472=CARTESIAN_POINT('Ctrl Pts',(0.653605000356183,1.41152322395584,
9.33409361630183));
#266473=CARTESIAN_POINT('Ctrl Pts',(0.646924438379127,1.41459513914092,
9.33462514272473));
#266474=CARTESIAN_POINT('Ctrl Pts',(0.643992146163158,1.41593246768541,
9.3348575506479));
#266475=CARTESIAN_POINT('Ctrl Pts',(0.637638114176911,1.41880652461627,
9.3353592180977));
#266476=CARTESIAN_POINT('Ctrl Pts',(0.634214969746228,1.42033999165668,
9.3356282782304));
#266477=CARTESIAN_POINT('Ctrl Pts',(0.624618154356527,1.42459746757173,
9.3363793131292));
#266478=CARTESIAN_POINT('Ctrl Pts',(0.618432155295258,1.42729375290562,
9.33685963829998));
#266479=CARTESIAN_POINT('Ctrl Pts',(0.581378974405374,1.44315795998708,
9.33971533143563));
#266480=CARTESIAN_POINT('Ctrl Pts',(0.550106972934137,1.45536564275558,
9.34203723514331));
#266481=CARTESIAN_POINT('Ctrl Pts',(0.356175812631202,1.52392495300936,
9.35604722185994));
#266482=CARTESIAN_POINT('Ctrl Pts',(0.185490220824298,1.55396684056293,
9.36686501370038));
#266483=CARTESIAN_POINT('Ctrl Pts',(-0.0120678110005505,1.55566063466285,
9.38046416801924));
#266484=CARTESIAN_POINT('Ctrl Pts',(-0.0374716295706017,1.55525605346374,
9.38222981017678));
#266485=CARTESIAN_POINT('Ctrl Pts',(-0.0721656983561482,1.55385302752024,
9.3846696218158));
#266486=CARTESIAN_POINT('Ctrl Pts',(-0.0814746903087904,1.55339273438509,
9.38532705890838));
#266487=CARTESIAN_POINT('Ctrl Pts',(-0.0962825259984223,1.55252707533458,
9.38637754027212));
#266488=CARTESIAN_POINT('Ctrl Pts',(-0.101784431729667,1.55217607651114,
9.38676888278129));
#266489=CARTESIAN_POINT('Ctrl Pts',(-0.113073418369649,1.55139560597441,
9.38757402947499));
#266490=CARTESIAN_POINT('Ctrl Pts',(-0.118860187128812,1.55096298421891,
9.38798792599675));
#266491=CARTESIAN_POINT('Ctrl Pts',(-0.132248435259629,1.54988670472818,
9.38894830748156));
#266492=CARTESIAN_POINT('Ctrl Pts',(-0.139847814388744,1.54921949093484,
9.38949552099795));
#266493=CARTESIAN_POINT('Ctrl Pts',(-0.163936856610407,1.54692582527297,
9.39123692584105));
#266494=CARTESIAN_POINT('Ctrl Pts',(-0.180405092044375,1.54509183066003,
9.39243756899137));
#266495=CARTESIAN_POINT('Ctrl Pts',(-0.262947097655967,1.5345619246884,
9.39850874866032));
#266496=CARTESIAN_POINT('Ctrl Pts',(-0.328433903797956,1.52189038212225,
9.4035019907975));
#266497=CARTESIAN_POINT('Ctrl Pts',(-0.476647727485408,1.48319893279626,
9.41519942571041));
#266498=CARTESIAN_POINT('Ctrl Pts',(-0.558422937732378,1.45438454627873,
9.42195336348554));
#266499=CARTESIAN_POINT('Ctrl Pts',(-0.694598924932757,1.39321516591301,
9.43347428204779));
#266500=CARTESIAN_POINT('Ctrl Pts',(-0.750227506234502,1.3640663126175,
9.43826323764434));
#266501=CARTESIAN_POINT('Ctrl Pts',(-0.810773125802581,1.32751298511043,
9.44346104725598));
#266502=CARTESIAN_POINT('Ctrl Pts',(-0.817565385733237,1.32334070988243,
9.44404391076425));
#266503=CARTESIAN_POINT('Ctrl Pts',(-0.8277340879076,1.31698621316253,9.44491579890265));
#266504=CARTESIAN_POINT('Ctrl Pts',(-0.831134496108052,1.31484290175978,
9.44520723584989));
#266505=CARTESIAN_POINT('Ctrl Pts',(-0.837195233256664,1.31098985169396,
9.44572640893649));
#266506=CARTESIAN_POINT('Ctrl Pts',(-0.839858691861754,1.30928515925039,
9.4459544683676));
#266507=CARTESIAN_POINT('Ctrl Pts',(-0.845068258151721,1.30592844375465,
9.44640033957755));
#266508=CARTESIAN_POINT('Ctrl Pts',(-0.847614717978009,1.30427709917736,
9.44661819421686));
#266509=CARTESIAN_POINT('Ctrl Pts',(-0.855013277450244,1.29944841497385,
9.44725094642093));
#266510=CARTESIAN_POINT('Ctrl Pts',(-0.859852533126146,1.29625133053721,
9.44766455468977));
#266511=CARTESIAN_POINT('Ctrl Pts',(-0.88188397542213,1.28151845156964,
9.44954692479818));
#266512=CARTESIAN_POINT('Ctrl Pts',(-0.89886369078421,1.26966651692676,
9.45099587553947));
#266513=CARTESIAN_POINT('Ctrl Pts',(-0.945886659920381,1.23542786647326,
9.45501907256936));
#266514=CARTESIAN_POINT('Ctrl Pts',(-0.975366516869028,1.21228881970871,
9.45755387958667));
#266515=CARTESIAN_POINT('Ctrl Pts',(-1.10670458390996,1.10130433638461,
9.46905320362962));
#266516=CARTESIAN_POINT('Ctrl Pts',(-1.19773202792704,1.00155159020856,
9.47767223554719));
#266517=CARTESIAN_POINT('Ctrl Pts',(-1.29606726630938,0.860911004548675,
9.48935687944838));
#266518=CARTESIAN_POINT('Ctrl Pts',(-1.316240197144,0.82974061218526,9.49191717714124));
#266519=CARTESIAN_POINT('Ctrl Pts',(-1.34079541171658,0.788646703524483,
9.49527281946354));
#266520=CARTESIAN_POINT('Ctrl Pts',(-1.34621697080266,0.779356026647765,
9.49603018461435));
#266521=CARTESIAN_POINT('Ctrl Pts',(-1.35472951465828,0.764414589223952,
9.49724653003967));
#266522=CARTESIAN_POINT('Ctrl Pts',(-1.35788258919811,0.758799442404477,
9.49770327383646));
#266523=CARTESIAN_POINT('Ctrl Pts',(-1.36351211466083,0.74862665376947,
9.49853015719919));
#266524=CARTESIAN_POINT('Ctrl Pts',(-1.36600082351253,0.744075871486197,
9.49889985258664));
#266525=CARTESIAN_POINT('Ctrl Pts',(-1.37181133849836,0.733323526834958,
9.49977290745003));
#266526=CARTESIAN_POINT('Ctrl Pts',(-1.37511390039701,0.727111753012827,
9.50027693937888));
#266527=CARTESIAN_POINT('Ctrl Pts',(-1.38464602345614,0.70888559788463,
9.5017549747366));
#266528=CARTESIAN_POINT('Ctrl Pts',(-1.39076092336078,0.696812337508565,
9.50273296704253));
#266529=CARTESIAN_POINT('Ctrl Pts',(-1.44694706164432,0.582191914322762,
9.51201021512522));
#266530=CARTESIAN_POINT('Ctrl Pts',(-1.48573717247729,0.474528771854461,
9.52070710677491));
#266531=CARTESIAN_POINT('Ctrl Pts',(-1.52957679191973,0.292185873805893,
9.53523409757297));
#266532=CARTESIAN_POINT('Ctrl Pts',(-1.54166922380741,0.219623954117895,
9.5409547588679));
#266533=CARTESIAN_POINT('Ctrl Pts',(-1.5500708800315,0.130799409081583,
9.54773268412755));
#266534=CARTESIAN_POINT('Ctrl Pts',(-1.55131563965779,0.115100141296424,
9.5489219718076));
#266535=CARTESIAN_POINT('Ctrl Pts',(-1.55366363609054,0.0784258028527149,
9.55167626828863));
#266536=CARTESIAN_POINT('Ctrl Pts',(-1.55458095330774,0.0574410695691954,
9.55323403154435));
#266537=CARTESIAN_POINT('Ctrl Pts',(-1.55521238816227,0.0304967721539908,
9.55520564980473));
#266538=CARTESIAN_POINT('Ctrl Pts',(-1.55531763178217,0.0245498015049972,
9.55563902857444));
#266539=CARTESIAN_POINT('Ctrl Pts',(-1.55543133538284,0.0150427069836612,
9.55632884370575));
#266540=CARTESIAN_POINT('Ctrl Pts',(-1.55546168833773,0.011482984387568,
9.55658645680835));
#266541=CARTESIAN_POINT('Ctrl Pts',(-1.55549033932317,0.00585819086112859,
9.55699242080158));
#266542=CARTESIAN_POINT('Ctrl Pts',(-1.55549674561761,0.00379323407447863,
9.5571412223948));
#266543=CARTESIAN_POINT('Ctrl Pts',(-1.55549962955002,0.00119753963184114,
9.5573279757493));
#266544=CARTESIAN_POINT('Ctrl Pts',(-1.55549994758783,0.000666849136197624,
9.55736614218525));
#266545=CARTESIAN_POINT('Ctrl Pts',(-1.55549999404086,0.000136157597505023,
9.55740429344755));
#266546=CARTESIAN_POINT('Ctrl Pts',(-1.55549999403006,0.000136280906002111,
9.55740428458294));
#266547=CARTESIAN_POINT('Ctrl Pts',(-1.55550006570921,-0.000681859550039542,
9.557463100469));
#266548=CARTESIAN_POINT('Ctrl Pts',(-1.55549949191725,-0.00150000170682517,
9.55752188023614));
#266549=CARTESIAN_POINT('Ctrl Pts',(-1.55549308453614,-0.00579941781312716,
9.55783058495101));
#266550=CARTESIAN_POINT('Ctrl Pts',(-1.55547620951391,-0.00928070896563226,
9.55807989708535));
#266551=CARTESIAN_POINT('Ctrl Pts',(-1.5553836847996,-0.0205577661163616,
9.55888548227781));
#266552=CARTESIAN_POINT('Ctrl Pts',(-1.55526111365173,-0.0283531966144095,
9.5594392283958));
#266553=CARTESIAN_POINT('Ctrl Pts',(-1.55394268147482,-0.0850725358237559,
9.56344768583682));
#266554=CARTESIAN_POINT('Ctrl Pts',(-1.55049704041156,-0.133922680817761,
9.56678882158552));
#266555=CARTESIAN_POINT('Ctrl Pts',(-1.53339288906358,-0.27867166500983,
9.57657273091826));
#266556=CARTESIAN_POINT('Ctrl Pts',(-1.51308294930104,-0.373541611719926,
9.58284323455126));
#266557=CARTESIAN_POINT('Ctrl Pts',(-1.4631520794489,-0.532588207295485,
9.59391411071522));
#266558=CARTESIAN_POINT('Ctrl Pts',(-1.43775269713861,-0.597770419429405,
9.59862255813638));
#266559=CARTESIAN_POINT('Ctrl Pts',(-1.40084422436254,-0.676390462343084,
9.60465938316445));
#266560=CARTESIAN_POINT('Ctrl Pts',(-1.39337715789063,-0.691641999031352,
9.60584769950275));
#266561=CARTESIAN_POINT('Ctrl Pts',(-1.38216170330981,-0.713630596333607,
9.60758770403325));
#266562=CARTESIAN_POINT('Ctrl Pts',(-1.37861036667116,-0.720467247820372,
9.60813252262895));
#266563=CARTESIAN_POINT('Ctrl Pts',(-1.37229002590633,-0.732416643203587,
9.60909165336074));
#266564=CARTESIAN_POINT('Ctrl Pts',(-1.36954284416077,-0.73754081295495,
9.60950518988078));
#266565=CARTESIAN_POINT('Ctrl Pts',(-1.36414606302589,-0.747473013212312,
9.61031117867769));
#266566=CARTESIAN_POINT('Ctrl Pts',(-1.3614996076125,-0.752282662166422,
9.61070351444077));
#266567=CARTESIAN_POINT('Ctrl Pts',(-1.35435075472932,-0.765113649228796,
9.61175570311962));
#266568=CARTESIAN_POINT('Ctrl Pts',(-1.34980263262482,-0.773109118614836,
9.61241718392743));
#266569=CARTESIAN_POINT('Ctrl Pts',(-1.33284229411428,-0.802318999292765,
9.61485561940009));
#266570=CARTESIAN_POINT('Ctrl Pts',(-1.31999927844321,-0.823277677706043,
9.61664801562009));
#266571=CARTESIAN_POINT('Ctrl Pts',(-1.30451222442658,-0.847256668671183,
9.61875041354431));
#266572=CARTESIAN_POINT('Ctrl Pts',(-1.30234591519674,-0.850582813682114,
9.61904321555013));
#266573=CARTESIAN_POINT('Ctrl Pts',(-1.22168218710971,-0.973403093064545,
9.62989889045855));
#266574=CARTESIAN_POINT('Ctrl Pts',(-1.12710574260796,-1.08149784058133,
9.64108519363977));
#266575=CARTESIAN_POINT('Ctrl Pts',(-0.989105531915848,-1.20117892341108,
9.65515452313245));
#266576=CARTESIAN_POINT('Ctrl Pts',(-0.958083469561142,-1.22606570119661,
9.65819115278687));
#266577=CARTESIAN_POINT('Ctrl Pts',(-0.908828346513758,-1.26256704799,9.66278675240287));
#266578=CARTESIAN_POINT('Ctrl Pts',(-0.891251083219132,-1.27503574316913,
9.66438489333406));
#266579=CARTESIAN_POINT('Ctrl Pts',(-0.868553741871806,-1.29043760852088,
9.66639051646606));
#266580=CARTESIAN_POINT('Ctrl Pts',(-0.863669434580082,-1.29371168919657,
9.66681876443209));
#266581=CARTESIAN_POINT('Ctrl Pts',(-0.856231437671663,-1.29863667736652,
9.66746571604367));
#266582=CARTESIAN_POINT('Ctrl Pts',(-0.853691355145765,-1.30030787325152,
9.66768573767221));
#266583=CARTESIAN_POINT('Ctrl Pts',(-0.848615468916188,-1.30362616528251,
9.66812356735667));
#266584=CARTESIAN_POINT('Ctrl Pts',(-0.846079791288125,-1.30527329704007,
9.6683413704027));
#266585=CARTESIAN_POINT('Ctrl Pts',(-0.840249403161727,-1.30903648631074,
9.66884009100542));
#266586=CARTESIAN_POINT('Ctrl Pts',(-0.836951497723282,-1.31114750252352,
9.66912067337497));
#266587=CARTESIAN_POINT('Ctrl Pts',(-0.827315327278335,-1.31726452150416,
9.66993621517443));
#266588=CARTESIAN_POINT('Ctrl Pts',(-0.820955906036507,-1.32123725223603,
9.67046904664975));
#266589=CARTESIAN_POINT('Ctrl Pts',(-0.776875434624696,-1.3483331707083,
9.6741271973021));
#266590=CARTESIAN_POINT('Ctrl Pts',(-0.738207254345492,-1.3698863903696,
9.67715964479529));
#266591=CARTESIAN_POINT('Ctrl Pts',(-0.621197293782455,-1.42871018188696,
9.68598506849212));
#266592=CARTESIAN_POINT('Ctrl Pts',(-0.54060113359116,-1.46111294880882,
9.69162587110098));
#266593=CARTESIAN_POINT('Ctrl Pts',(-0.37027140464894,-1.51355595170738,
9.70339885958134));
#266594=CARTESIAN_POINT('Ctrl Pts',(-0.280630773527694,-1.5327084213721,
9.7095218113252));
#266595=CARTESIAN_POINT('Ctrl Pts',(-0.176965063265548,-1.54545519503463,
9.71681927175854));
#266596=CARTESIAN_POINT('Ctrl Pts',(-0.164076045708595,-1.54687666826049,
9.71773004930059));
#266597=CARTESIAN_POINT('Ctrl Pts',(-0.144286528843685,-1.54880905757599,
9.71913442451726));
#266598=CARTESIAN_POINT('Ctrl Pts',(-0.137397653596425,-1.5494353749754,
9.71962440626672));
#266599=CARTESIAN_POINT('Ctrl Pts',(-0.124845041246703,-1.55049225315724,
9.7205193532912));
#266600=CARTESIAN_POINT('Ctrl Pts',(-0.119182655145225,-1.55093778230113,
9.72092384255929));
#266601=CARTESIAN_POINT('Ctrl Pts',(-0.106826879336625,-1.55184189883895,
9.7218082462049));
#266602=CARTESIAN_POINT('Ctrl Pts',(-0.100132735566828,-1.55228821222174,
9.72228853639637));
#266603=CARTESIAN_POINT('Ctrl Pts',(-0.081788762242601,-1.55339209409597,
9.72360790227887));
#266604=CARTESIAN_POINT('Ctrl Pts',(-0.0701343008674653,-1.55396189325335,
9.72444969784083));
#266605=CARTESIAN_POINT('Ctrl Pts',(-0.00891603221280406,-1.55626485655855,
9.72889111642858));
#266606=CARTESIAN_POINT('Ctrl Pts',(0.0406978766529117,-1.55575784430602,
9.73255959986612));
#266607=CARTESIAN_POINT('Ctrl Pts',(0.237230812759556,-1.5443423685084,
9.74737792992191));
#266608=CARTESIAN_POINT('Ctrl Pts',(0.382278354418441,-1.51496709974836,
9.75904126554015));
#266609=CARTESIAN_POINT('Ctrl Pts',(0.549010781067511,-1.45569567812998,
9.77241859469092));
#266610=CARTESIAN_POINT('Ctrl Pts',(0.576713291064678,-1.44494457729338,
9.77463643653261));
#266611=CARTESIAN_POINT('Ctrl Pts',(0.610097398241374,-1.43087521091526,
9.77728952885686));
#266612=CARTESIAN_POINT('Ctrl Pts',(0.616085866998809,-1.42830700938748,
9.77776465592653));
#266613=CARTESIAN_POINT('Ctrl Pts',(0.625449601076448,-1.42422144978071,
9.77850614488328));
#266614=CARTESIAN_POINT('Ctrl Pts',(0.628835797811732,-1.42272958838604,
9.77877399319462));
#266615=CARTESIAN_POINT('Ctrl Pts',(0.635168128936506,-1.41991272011558,
9.77927428318958));
#266616=CARTESIAN_POINT('Ctrl Pts',(0.638115428237316,-1.41859063344479,
9.7795068875135));
#266617=CARTESIAN_POINT('Ctrl Pts',(0.644828018557296,-1.41555437596949,
9.78003611097663));
#266618=CARTESIAN_POINT('Ctrl Pts',(0.648590604447967,-1.41383435866132,
9.78033236893495));
#266619=CARTESIAN_POINT('Ctrl Pts',(0.658545719602895,-1.4092354024515,
9.78111530670266));
#266620=CARTESIAN_POINT('Ctrl Pts',(0.66472632047392,-1.40633061820943,
9.78160045738315));
#266621=CARTESIAN_POINT('Ctrl Pts',(0.70927592023042,-1.38503369897656,
9.78509208769269));
#266622=CARTESIAN_POINT('Ctrl Pts',(0.746899326153401,-1.36511277164091,
9.78801234269924));
#266623=CARTESIAN_POINT('Ctrl Pts',(0.867674552347196,-1.29467370050598,
9.79744803569534));
#266624=CARTESIAN_POINT('Ctrl Pts',(0.946910897578922,-1.23790195036941,
9.80374979812193));
#266625=CARTESIAN_POINT('Ctrl Pts',(1.07727269227693,-1.12461329298098,
9.81519049687603));
#266626=CARTESIAN_POINT('Ctrl Pts',(1.13053296868357,-1.07105763208144,
9.82025538835076));
#266627=CARTESIAN_POINT('Ctrl Pts',(1.19120373928502,-1.00046275146492,
9.82672009022015));
#266628=CARTESIAN_POINT('Ctrl Pts',(1.20248388478312,-0.986876146266399,
9.82795511937148));
#266629=CARTESIAN_POINT('Ctrl Pts',(1.21842558041628,-0.966995655092733,
9.82975096597959));
#266630=CARTESIAN_POINT('Ctrl Pts',(1.22327502903952,-0.960853626356437,
9.83030426788144));
#266631=CARTESIAN_POINT('Ctrl Pts',(1.23165797599887,-0.950069948665049,
9.83127322520721));
#266632=CARTESIAN_POINT('Ctrl Pts',(1.23521212625693,-0.945444487345753,
9.83168805491645));
#266633=CARTESIAN_POINT('Ctrl Pts',(1.24203947258411,-0.93645499428858,
9.8324928149631));
#266634=CARTESIAN_POINT('Ctrl Pts',(1.24531589921918,-0.932093513301942,
9.83288261071643));
#266635=CARTESIAN_POINT('Ctrl Pts',(1.25394680562262,-0.920477569518755,
9.83391909000782));
#266636=CARTESIAN_POINT('Ctrl Pts',(1.25926119657258,-0.913193725215407,
9.83456731353236));
#266637=CARTESIAN_POINT('Ctrl Pts',(1.27814886649666,-0.886828093551,9.83690794903746));
#266638=CARTESIAN_POINT('Ctrl Pts',(1.29135354595389,-0.867487464491169,
9.83861424904));
#266639=CARTESIAN_POINT('Ctrl Pts',(1.39917182459066,-0.701648736084956,
9.85316505059864));
#266640=CARTESIAN_POINT('Ctrl Pts',(1.46895224824044,-0.54050297310002,
9.8669881214529));
#266641=CARTESIAN_POINT('Ctrl Pts',(1.51865727727712,-0.338250847533332,
9.88279201769263));
#266642=CARTESIAN_POINT('Ctrl Pts',(1.52568075238155,-0.305011875809233,
9.88533539302164));
#266643=CARTESIAN_POINT('Ctrl Pts',(1.5327928183653,-0.264900472378489,
9.88832049661821));
#266644=CARTESIAN_POINT('Ctrl Pts',(1.53393127173312,-0.258226533108866,
9.88881439758493));
#266645=CARTESIAN_POINT('Ctrl Pts',(1.53563348762522,-0.247838953554657,
9.88957859570405));
#266646=CARTESIAN_POINT('Ctrl Pts',(1.53622741708248,-0.244130454941157,
9.88985052883173));
#266647=CARTESIAN_POINT('Ctrl Pts',(1.53730595884031,-0.237236215816053,
9.89035435523716));
#266648=CARTESIAN_POINT('Ctrl Pts',(1.5377940999222,-0.234051147756886,
9.89058643647957));
#266649=CARTESIAN_POINT('Ctrl Pts',(1.53888431020765,-0.226786971484537,
9.89111421220874));
#266650=CARTESIAN_POINT('Ctrl Pts',(1.53948006016304,-0.222706973524559,
9.89140954872123));
#266651=CARTESIAN_POINT('Ctrl Pts',(1.54099201539908,-0.212056290805593,
9.89217777595388));
#266652=CARTESIAN_POINT('Ctrl Pts',(1.54188243379256,-0.205481937186603,
9.89264926517398));
#266653=CARTESIAN_POINT('Ctrl Pts',(1.54762235232947,-0.160961761497843,
9.89582498313843));
#266654=CARTESIAN_POINT('Ctrl Pts',(1.55111318153999,-0.122850056412527,
9.89845964745957));
#266655=CARTESIAN_POINT('Ctrl Pts',(1.56134100049507,0.0648263101851032,
9.91119418471039));
#266656=CARTESIAN_POINT('Ctrl Pts',(1.54786993121525,0.214693316810053,
9.92069523844469));
#266657=CARTESIAN_POINT('Ctrl Pts',(1.50404071096711,0.398749477501326,
9.93355995810379));
#266658=CARTESIAN_POINT('Ctrl Pts',(1.493434327872,0.436798654086403,9.93628159575215));
#266659=CARTESIAN_POINT('Ctrl Pts',(1.47817694821596,0.484442294591727,
9.9397895344268));
#266660=CARTESIAN_POINT('Ctrl Pts',(1.47485924787553,0.494450822895139,
9.94053210933116));
#266661=CARTESIAN_POINT('Ctrl Pts',(1.46936697264354,0.510472154154579,
9.94173028748855));
#266662=CARTESIAN_POINT('Ctrl Pts',(1.46725658702874,0.516506753167798,
9.94218377205813));
#266663=CARTESIAN_POINT('Ctrl Pts',(1.46316988138562,0.527965409064701,
9.94304909986741));
#266664=CARTESIAN_POINT('Ctrl Pts',(1.46120044398097,0.533391822043335,
9.94346070889015));
#266665=CARTESIAN_POINT('Ctrl Pts',(1.45663683796814,0.545751009800278,
9.94440241939294));
#266666=CARTESIAN_POINT('Ctrl Pts',(1.45402331359471,0.552676435575332,
9.94493315790384));
#266667=CARTESIAN_POINT('Ctrl Pts',(1.44708281771471,0.57067763389007,9.94632082704289));
#266668=CARTESIAN_POINT('Ctrl Pts',(1.44267816994791,0.581722723047897,
9.94718033638785));
#266669=CARTESIAN_POINT('Ctrl Pts',(1.43696565742733,0.595583384729583,
9.94826939717981));
#266670=CARTESIAN_POINT('Ctrl Pts',(1.43577539858722,0.598447049047754,
9.94849496736736));
#266671=CARTESIAN_POINT('Ctrl Pts',(1.4345766815454,0.601306905636538,9.94872080685755));
#266672=CARTESIAN_POINT('Origin',(0.,0.,-1.29405622560371));
#266673=CARTESIAN_POINT('',(1.43457669771236,0.601306867065985,10.7874266037958));
#266674=CARTESIAN_POINT('',(1.4345766806181,0.60130690784885,10.6508134549194));
#266675=CARTESIAN_POINT('',(1.43457668357355,0.601306900797845,-1.29405622560371));
#266676=CARTESIAN_POINT('',(-1.55549951249496,-0.000556301241264363,10.3953761425462));
#266677=CARTESIAN_POINT('Ctrl Pts',(1.43457669771236,0.601306867065985,
10.7874266037958));
#266678=CARTESIAN_POINT('Ctrl Pts',(1.45423156484639,0.554414978861378,
10.7835217661703));
#266679=CARTESIAN_POINT('Ctrl Pts',(1.47158201151098,0.506572022160425,
10.7796660057214));
#266680=CARTESIAN_POINT('Ctrl Pts',(1.48894631453756,0.450205259606307,
10.7753315281049));
#266681=CARTESIAN_POINT('Ctrl Pts',(1.49127132062371,0.442442944616008,
10.7747391284532));
#266682=CARTESIAN_POINT('Ctrl Pts',(1.49465467865279,0.430817454322671,
10.7738589749464));
#266683=CARTESIAN_POINT('Ctrl Pts',(1.49575889068674,0.426967948768711,
10.7735686866264));
#266684=CARTESIAN_POINT('Ctrl Pts',(1.49771233635579,0.420057256655038,
10.7730496755902));
#266685=CARTESIAN_POINT('Ctrl Pts',(1.49856706660349,0.416997708459551,
10.7728206417466));
#266686=CARTESIAN_POINT('Ctrl Pts',(1.5004116655524,0.410315955334787,10.7723220848118));
#266687=CARTESIAN_POINT('Ctrl Pts',(1.50139779219925,0.406692782963212,
10.7720527791139));
#266688=CARTESIAN_POINT('Ctrl Pts',(1.50415856681661,0.39640239146838,10.7712907504056));
#266689=CARTESIAN_POINT('Ctrl Pts',(1.50590202092662,0.38972677375402,10.7707997834689));
#266690=CARTESIAN_POINT('Ctrl Pts',(1.51687627530202,0.346533336744395,
10.7676435189769));
#266691=CARTESIAN_POINT('Ctrl Pts',(1.52482343111679,0.309698365693566,
10.7650460187595));
#266692=CARTESIAN_POINT('Ctrl Pts',(1.55028099038903,0.166685559859222,
10.755192700768));
#266693=CARTESIAN_POINT('Ctrl Pts',(1.55809744699292,0.0590862201464926,
10.7482481197342));
#266694=CARTESIAN_POINT('Ctrl Pts',(1.55229954441817,-0.126907574114333,
10.7359030453782));
#266695=CARTESIAN_POINT('Ctrl Pts',(1.54392189113161,-0.205041200641974,
10.7306151081072));
#266696=CARTESIAN_POINT('Ctrl Pts',(1.52755683722975,-0.293748557985828,
10.7243134914281));
#266697=CARTESIAN_POINT('Ctrl Pts',(1.52529610912158,-0.305270163163949,
10.7234893179022));
#266698=CARTESIAN_POINT('Ctrl Pts',(1.52141671298726,-0.323921075857665,
10.7221453592533));
#266699=CARTESIAN_POINT('Ctrl Pts',(1.51987780503289,-0.331066658570192,
10.7216281118342));
#266700=CARTESIAN_POINT('Ctrl Pts',(1.51704934517923,-0.343764486579375,
10.7207046467754));
#266701=CARTESIAN_POINT('Ctrl Pts',(1.51577952038416,-0.349321029917241,
10.7202990665875));
#266702=CARTESIAN_POINT('Ctrl Pts',(1.51303943261021,-0.361014893146869,
10.7194423424182));
#266703=CARTESIAN_POINT('Ctrl Pts',(1.51156230439561,-0.367150480687252,
10.7189909846686));
#266704=CARTESIAN_POINT('Ctrl Pts',(1.50755123974292,-0.383376775273461,
10.7177923180683));
#266705=CARTESIAN_POINT('Ctrl Pts',(1.50495337009474,-0.393451186720672,
10.717042965207));
#266706=CARTESIAN_POINT('Ctrl Pts',(1.49217747674197,-0.441016773887805,
10.7134799303669));
#266707=CARTESIAN_POINT('Ctrl Pts',(1.48069921710864,-0.478140929372599,
10.7106246429486));
#266708=CARTESIAN_POINT('Ctrl Pts',(1.41827547971653,-0.656131332688146,
10.6965558847399));
#266709=CARTESIAN_POINT('Ctrl Pts',(1.34855256554065,-0.789560131631482,
10.6847299266808));
#266710=CARTESIAN_POINT('Ctrl Pts',(1.23791751017579,-0.94269633478496,
10.6703291456549));
#266711=CARTESIAN_POINT('Ctrl Pts',(1.21377201115519,-0.973588356546316,
10.6673815396478));
#266712=CARTESIAN_POINT('Ctrl Pts',(1.18420383267967,-1.00860573210254,
10.6640186393697));
#266713=CARTESIAN_POINT('Ctrl Pts',(1.17989236849965,-1.01364601469693,
10.663534055731));
#266714=CARTESIAN_POINT('Ctrl Pts',(1.17286620103169,-1.02175432626998,
10.662753840621));
#266715=CARTESIAN_POINT('Ctrl Pts',(1.17017144758954,-1.02483940842595,
10.662456823813));
#266716=CARTESIAN_POINT('Ctrl Pts',(1.16536063210452,-1.03030334515677,
10.6619305570907));
#266717=CARTESIAN_POINT('Ctrl Pts',(1.16324942611813,-1.03268637990313,
10.6617009578816));
#266718=CARTESIAN_POINT('Ctrl Pts',(1.15867682209809,-1.0378159147098,10.661206589811));
#266719=CARTESIAN_POINT('Ctrl Pts',(1.15621297155535,-1.04056014533795,
10.6609420088091));
#266720=CARTESIAN_POINT('Ctrl Pts',(1.14931950436625,-1.04818335792989,
10.6602066578212));
#266721=CARTESIAN_POINT('Ctrl Pts',(1.14486853871365,-1.05304307041731,
10.6597374545337));
#266722=CARTESIAN_POINT('Ctrl Pts',(1.11876024108901,-1.08118776700141,
10.6570165531571));
#266723=CARTESIAN_POINT('Ctrl Pts',(1.09642194601422,-1.10383456618323,
10.65481289122));
#266724=CARTESIAN_POINT('Ctrl Pts',(0.967917785881114,-1.22635978958701,
10.6426962108693));
#266725=CARTESIAN_POINT('Ctrl Pts',(0.848814746059553,-1.31161924449267,
10.6334458568429));
#266726=CARTESIAN_POINT('Ctrl Pts',(0.675982332720464,-1.4018008306185,
10.6202961308335));
#266727=CARTESIAN_POINT('Ctrl Pts',(0.631342500743646,-1.42246388624232,
10.6169285277414));
#266728=CARTESIAN_POINT('Ctrl Pts',(0.575105366247022,-1.44532605818967,
10.6126793747554));
#266729=CARTESIAN_POINT('Ctrl Pts',(0.56436013137958,-1.44955552710602,
10.6118672651422));
#266730=CARTESIAN_POINT('Ctrl Pts',(0.547372449666443,-1.45602459372945,
10.6105825264636));
#266731=CARTESIAN_POINT('Ctrl Pts',(0.541160909247763,-1.45834463829094,
10.6101125891765));
#266732=CARTESIAN_POINT('Ctrl Pts',(0.529669175375238,-1.46255333597755,
10.6092427639186));
#266733=CARTESIAN_POINT('Ctrl Pts',(0.524393213671634,-1.46445329453189,
10.6088432597875));
#266734=CARTESIAN_POINT('Ctrl Pts',(0.51267685693432,-1.46860111035686,
10.6079556651249));
#266735=CARTESIAN_POINT('Ctrl Pts',(0.50623174893115,-1.47083520307617,
10.6074671280121));
#266736=CARTESIAN_POINT('Ctrl Pts',(0.487688518044741,-1.47712659723637,
10.6060606401153));
#266737=CARTESIAN_POINT('Ctrl Pts',(0.47555514305992,-1.48107743307225,
10.6051392143814));
#266738=CARTESIAN_POINT('Ctrl Pts',(0.380194303144987,-1.5108359742808,
10.5978868305215));
#266739=CARTESIAN_POINT('Ctrl Pts',(0.294995575051489,-1.52975343055046,
10.5913313192512));
#266740=CARTESIAN_POINT('Ctrl Pts',(0.117440681523819,-1.55379029920837,
10.5775589463255));
#266741=CARTESIAN_POINT('Ctrl Pts',(0.0252921300135777,-1.55801685828702,
10.5703521365794));
#266742=CARTESIAN_POINT('Ctrl Pts',(-0.0828976978068575,-1.55337421480202,
10.5620711461192));
#266743=CARTESIAN_POINT('Ctrl Pts',(-0.099095807129142,-1.55242504991223,
10.5608365252184));
#266744=CARTESIAN_POINT('Ctrl Pts',(-0.144255210267106,-1.5490691012917,
10.5574136872666));
#266745=CARTESIAN_POINT('Ctrl Pts',(-0.17317030581851,-1.54610380584979,
10.5552441312997));
#266746=CARTESIAN_POINT('Ctrl Pts',(-0.208585359246172,-1.5414657550715,
10.5526269787601));
#266747=CARTESIAN_POINT('Ctrl Pts',(-0.215177601349624,-1.54055935630778,
10.5521415363609));
#266748=CARTESIAN_POINT('Ctrl Pts',(-0.225468036437977,-1.53907713231616,
10.5513866633163));
#266749=CARTESIAN_POINT('Ctrl Pts',(-0.229170206918606,-1.53853023101168,
10.5511156713637));
#266750=CARTESIAN_POINT('Ctrl Pts',(-0.236012353000364,-1.53749423325551,
10.5506159699221));
#266751=CARTESIAN_POINT('Ctrl Pts',(-0.239152781415582,-1.53700887946959,
10.5503870616462));
#266752=CARTESIAN_POINT('Ctrl Pts',(-0.246263614445864,-1.53588757720398,
10.5498697415476));
#266753=CARTESIAN_POINT('Ctrl Pts',(-0.250233049780753,-1.53524585633393,
10.5495816586378));
#266754=CARTESIAN_POINT('Ctrl Pts',(-0.262274017403842,-1.53325130623887,
10.5487097760464));
#266755=CARTESIAN_POINT('Ctrl Pts',(-0.270337575309741,-1.53185013347118,
10.5481286195734));
#266756=CARTESIAN_POINT('Ctrl Pts',(-0.365255555363848,-1.51458375672526,
10.5413157704661));
#266757=CARTESIAN_POINT('Ctrl Pts',(-0.450633487045888,-1.49141217318771,
10.5354606363794));
#266758=CARTESIAN_POINT('Ctrl Pts',(-0.651402014909569,-1.41809205992767,
10.5213719735854));
#266759=CARTESIAN_POINT('Ctrl Pts',(-0.763557839278286,-1.36098661716113,
10.5131916845782));
#266760=CARTESIAN_POINT('Ctrl Pts',(-0.875587235721102,-1.28569786315884,
10.503823548588));
#266761=CARTESIAN_POINT('Ctrl Pts',(-0.883487782714621,-1.28028173990148,
10.5031561852251));
#266762=CARTESIAN_POINT('Ctrl Pts',(-0.900267479315245,-1.26854934545049,
10.5017239458047));
#266763=CARTESIAN_POINT('Ctrl Pts',(-0.909131245124481,-1.2622120838619,
10.5009583259423));
#266764=CARTESIAN_POINT('Ctrl Pts',(-0.923621547451472,-1.25162024290108,
10.4996912597618));
#266765=CARTESIAN_POINT('Ctrl Pts',(-0.92928712863231,-1.24741950640167,
10.4991918894905));
#266766=CARTESIAN_POINT('Ctrl Pts',(-0.939346742389795,-1.23985425473455,
10.4982980140685));
#266767=CARTESIAN_POINT('Ctrl Pts',(-0.943751787689046,-1.23650452373014,
10.4979040911938));
#266768=CARTESIAN_POINT('Ctrl Pts',(-0.948237323468547,-1.23305565317334,
10.4975003763098));
#266769=CARTESIAN_POINT('Ctrl Pts',(-0.9483358252886,-1.23297989761216,
10.4974915094956));
#266770=CARTESIAN_POINT('Ctrl Pts',(-0.948509900555364,-1.23284598699181,
10.4974758375341));
#266771=CARTESIAN_POINT('Ctrl Pts',(-0.948585477743541,-1.23278783677785,
10.4974690325783));
#266772=CARTESIAN_POINT('Ctrl Pts',(-0.948719391787902,-1.23268478171235,
10.4974569736416));
#266773=CARTESIAN_POINT('Ctrl Pts',(-0.948777730810681,-1.23263987966371,
10.4974517197715));
#266774=CARTESIAN_POINT('Ctrl Pts',(-0.948936255817107,-1.23251784911289,
10.4974374421699));
#266775=CARTESIAN_POINT('Ctrl Pts',(-0.949036435570715,-1.23244071254777,
10.4974284181197));
#266776=CARTESIAN_POINT('Ctrl Pts',(-0.949231601350095,-1.23229040058556,
10.4974108352688));
#266777=CARTESIAN_POINT('Ctrl Pts',(-0.949326588320262,-1.23221722641959,
10.497402276517));
#266778=CARTESIAN_POINT('Ctrl Pts',(-0.949511783623432,-1.2320745252345,
10.4973855872543));
#266779=CARTESIAN_POINT('Ctrl Pts',(-0.949601992787823,-1.23200499928569,
10.4973774567856));
#266780=CARTESIAN_POINT('Ctrl Pts',(-0.949778004265813,-1.23186931301664,
10.4973615909237));
#266781=CARTESIAN_POINT('Ctrl Pts',(-0.949863807306044,-1.23180315363669,
10.4973538555678));
#266782=CARTESIAN_POINT('Ctrl Pts',(-0.950031340495033,-1.23167394741138,
10.4973387501258));
#266783=CARTESIAN_POINT('Ctrl Pts',(-0.95011307128588,-1.23161090139152,
10.4973313800722));
#266784=CARTESIAN_POINT('Ctrl Pts',(-0.95027276081356,-1.2314876937074,
10.4973169783725));
#266785=CARTESIAN_POINT('Ctrl Pts',(-0.950350720114854,-1.23142753277412,
10.4973099467553));
#266786=CARTESIAN_POINT('Ctrl Pts',(-0.950503138376721,-1.23130988901431,
10.4972961976557));
#266787=CARTESIAN_POINT('Ctrl Pts',(-0.950577597837861,-1.23125240683509,
10.4972894801989));
#266788=CARTESIAN_POINT('Ctrl Pts',(-0.950723262457778,-1.23113993368578,
10.4972763374316));
#266789=CARTESIAN_POINT('Ctrl Pts',(-0.950794468061787,-1.23108494329079,
10.4972699121438));
#266790=CARTESIAN_POINT('Ctrl Pts',(-0.950933848294579,-1.23097728394535,
10.4972573337475));
#266791=CARTESIAN_POINT('Ctrl Pts',(-0.951002023322032,-1.23092461550625,
10.4972511806591));
#266792=CARTESIAN_POINT('Ctrl Pts',(-0.951135545596474,-1.23082144550847,
10.4972391284877));
#266793=CARTESIAN_POINT('Ctrl Pts',(-0.951200893196398,-1.23077094440966,
10.497233229423));
#266794=CARTESIAN_POINT('Ctrl Pts',(-0.951328945893783,-1.2306719680672,
10.4972216687212));
#266795=CARTESIAN_POINT('Ctrl Pts',(-0.951391651307561,-1.23062349323587,
10.4972160071006));
#266796=CARTESIAN_POINT('Ctrl Pts',(-0.951514588921246,-1.23052844049516,
10.4972049061347));
#266797=CARTESIAN_POINT('Ctrl Pts',(-0.95157482141183,-1.23048186295145,
10.4971994668036));
#266798=CARTESIAN_POINT('Ctrl Pts',(-0.957076944454097,-1.22622644763627,
10.4967025500275));
#266799=CARTESIAN_POINT('Ctrl Pts',(-0.962490774284427,-1.22198162223904,
10.4962096508706));
#266800=CARTESIAN_POINT('Ctrl Pts',(-0.973707354756502,-1.21306624778813,
10.4951800674235));
#266801=CARTESIAN_POINT('Ctrl Pts',(-0.979505058008557,-1.20838966065369,
10.4946431493827));
#266802=CARTESIAN_POINT('Ctrl Pts',(-0.994482310818171,-1.19612998810639,
10.4932436117579));
#266803=CARTESIAN_POINT('Ctrl Pts',(-1.00360862532356,-1.18848295213681,
10.4923784306437));
#266804=CARTESIAN_POINT('Ctrl Pts',(-1.03040524144025,-1.16550103536149,
10.4898005886437));
#266805=CARTESIAN_POINT('Ctrl Pts',(-1.04781764171479,-1.14987203934489,
10.4880761347964));
#266806=CARTESIAN_POINT('Ctrl Pts',(-1.16398244174426,-1.04077501920385,
10.476225214078));
#266807=CARTESIAN_POINT('Ctrl Pts',(-1.25045070465667,-0.935108740075265,
10.4655748212541));
#266808=CARTESIAN_POINT('Ctrl Pts',(-1.35161950553541,-0.771913652987544,
10.4507945694255));
#266809=CARTESIAN_POINT('Ctrl Pts',(-1.37857529808757,-0.722673998363168,
10.4465301019183));
#266810=CARTESIAN_POINT('Ctrl Pts',(-1.40621064075385,-0.66499147524461,
10.4418310332293));
#266811=CARTESIAN_POINT('Ctrl Pts',(-1.40955297142878,-0.657877234749755,
10.4412564719334));
#266812=CARTESIAN_POINT('Ctrl Pts',(-1.4145181939206,-0.647097052812373,
10.4403936880099));
#266813=CARTESIAN_POINT('Ctrl Pts',(-1.41618101010326,-0.643449814898415,
10.4401031306445));
#266814=CARTESIAN_POINT('Ctrl Pts',(-1.41913643646542,-0.636900398379603,
10.4395838335024));
#266815=CARTESIAN_POINT('Ctrl Pts',(-1.42043426527787,-0.634000663576762,
10.4393547810659));
#266816=CARTESIAN_POINT('Ctrl Pts',(-1.42324551271229,-0.627667538011124,
10.4388564098179));
#266817=CARTESIAN_POINT('Ctrl Pts',(-1.42475539376767,-0.624232646105482,
10.4385873071486));
#266818=CARTESIAN_POINT('Ctrl Pts',(-1.42900097619172,-0.614478539484409,
10.4378264313983));
#266819=CARTESIAN_POINT('Ctrl Pts',(-1.43170721266465,-0.608146468659603,
10.4373364060013));
#266820=CARTESIAN_POINT('Ctrl Pts',(-1.44883425489476,-0.567324463212259,
10.4342010367673));
#266821=CARTESIAN_POINT('Ctrl Pts',(-1.46205125233759,-0.532338664876566,
10.4316224594959));
#266822=CARTESIAN_POINT('Ctrl Pts',(-1.5279120355649,-0.336973133875317,
10.417633839255));
#266823=CARTESIAN_POINT('Ctrl Pts',(-1.5554393773208,-0.169340451667066,
10.4069999775086));
#266824=CARTESIAN_POINT('Ctrl Pts',(-1.55549989999529,-0.000557776525539587,
10.3953769175085));
#266825=CARTESIAN_POINT('Ctrl Pts',(-1.55549990054006,-0.000556255220122361,
10.3953768127452));
#266826=CARTESIAN_POINT('Ctrl Pts',(-1.55550868565946,0.0240102600394349,
10.3936850621365));
#266827=CARTESIAN_POINT('Ctrl Pts',(-1.55493549136123,0.0485725664847252,
10.3919773671645));
#266828=CARTESIAN_POINT('Ctrl Pts',(-1.55345097257562,0.0801224492624995,
10.3897584704002));
#266829=CARTESIAN_POINT('Ctrl Pts',(-1.55307356133013,0.0871323205925535,
10.3892638594744));
#266830=CARTESIAN_POINT('Ctrl Pts',(-1.55231571177791,0.099631608214045,
10.3883789309062));
#266831=CARTESIAN_POINT('Ctrl Pts',(-1.55195356875411,0.105122050068117,
10.3879891871315));
#266832=CARTESIAN_POINT('Ctrl Pts',(-1.55116860993205,0.116132882799388,
10.3872054483733));
#266833=CARTESIAN_POINT('Ctrl Pts',(-1.55074543641878,0.12165316634033,
10.3868114477975));
#266834=CARTESIAN_POINT('Ctrl Pts',(-1.54977582196752,0.133473362848572,
10.3859654443242));
#266835=CARTESIAN_POINT('Ctrl Pts',(-1.54922041869164,0.139772418854117,
10.3855131673219));
#266836=CARTESIAN_POINT('Ctrl Pts',(-1.54764428899439,0.156482713325616,
10.384309444217));
#266837=CARTESIAN_POINT('Ctrl Pts',(-1.54655693196448,0.166887180690696,
10.383555923194));
#266838=CARTESIAN_POINT('Ctrl Pts',(-1.54136714804898,0.212127053134722,
10.3802613356304));
#266839=CARTESIAN_POINT('Ctrl Pts',(-1.53619234332671,0.246826434431386,
10.3776869987059));
#266840=CARTESIAN_POINT('Ctrl Pts',(-1.50145063304191,0.43575653621164,
10.3633968995562));
#266841=CARTESIAN_POINT('Ctrl Pts',(-1.449827845268,0.584995434557289,10.3509748067582));
#266842=CARTESIAN_POINT('Ctrl Pts',(-1.35977738374537,0.756253455099173,
10.3362621216931));
#266843=CARTESIAN_POINT('Ctrl Pts',(-1.34164708027808,0.78797047579587,
10.3335223467886));
#266844=CARTESIAN_POINT('Ctrl Pts',(-1.31881158193795,0.824841258967402,
10.3303436974223));
#266845=CARTESIAN_POINT('Ctrl Pts',(-1.31516950369142,0.830636064929464,
10.3298443222486));
#266846=CARTESIAN_POINT('Ctrl Pts',(-1.30947654336594,0.839562649637762,
10.3290755932031));
#266847=CARTESIAN_POINT('Ctrl Pts',(-1.30745246664984,0.842711284216797,
10.3288045460241));
#266848=CARTESIAN_POINT('Ctrl Pts',(-1.30368905066121,0.848519420423827,
10.3283047937071));
#266849=CARTESIAN_POINT('Ctrl Pts',(-1.30195293989458,0.851180879904725,
10.3280758894511));
#266850=CARTESIAN_POINT('Ctrl Pts',(-1.29800203907194,0.857197244696896,
10.3275586427851));
#266851=CARTESIAN_POINT('Ctrl Pts',(-1.29578239472684,0.860548892422617,
10.3272706288879));
#266852=CARTESIAN_POINT('Ctrl Pts',(-1.2891542769947,0.870473513249677,
10.3264180762232));
#266853=CARTESIAN_POINT('Ctrl Pts',(-1.28470851609589,0.877021620517394,
10.3258559553043));
#266854=CARTESIAN_POINT('Ctrl Pts',(-1.2454890806787,0.933849234224909,
10.3209782069085));
#266855=CARTESIAN_POINT('Ctrl Pts',(-1.20782438305582,0.982079320103689,
10.3168417958582));
#266856=CARTESIAN_POINT('Ctrl Pts',(-1.089058024934,1.11695585114861,10.3048735161258));
#266857=CARTESIAN_POINT('Ctrl Pts',(-1.00078945260503,1.19668648460321,
10.29723070882));
#266858=CARTESIAN_POINT('Ctrl Pts',(-0.879712166781752,1.28319968722721,
10.2871627538557));
#266859=CARTESIAN_POINT('Ctrl Pts',(-0.854598475144424,1.30006007226175,
10.2850963465806));
#266860=CARTESIAN_POINT('Ctrl Pts',(-0.816925709653545,1.32378873608082,
10.2820160925));
#266861=CARTESIAN_POINT('Ctrl Pts',(-0.804736954557418,1.33123350467389,
10.2810224356398));
#266862=CARTESIAN_POINT('Ctrl Pts',(-0.785200706215637,1.34279969807468,
10.2794333336505));
#266863=CARTESIAN_POINT('Ctrl Pts',(-0.777919066964841,1.34703121661438,
10.2788418066149));
#266864=CARTESIAN_POINT('Ctrl Pts',(-0.764029017533328,1.35495283817906,
10.2777146668191));
#266865=CARTESIAN_POINT('Ctrl Pts',(-0.757427314795329,1.35865425788761,
10.2771794750982));
#266866=CARTESIAN_POINT('Ctrl Pts',(-0.745844118606342,1.36503802443247,
10.276241204718));
#266867=CARTESIAN_POINT('Ctrl Pts',(-0.740874470652498,1.3677416695397,
10.2758388934621));
#266868=CARTESIAN_POINT('Ctrl Pts',(-0.731163990606952,1.37295602526604,
10.2750532103122));
#266869=CARTESIAN_POINT('Ctrl Pts',(-0.726424695680042,1.37546944300873,
10.2746699413505));
#266870=CARTESIAN_POINT('Ctrl Pts',(-0.713888104391087,1.38203518161326,
10.2736565448411));
#266871=CARTESIAN_POINT('Ctrl Pts',(-0.706069404678794,1.38604598000914,
10.2730249684271));
#266872=CARTESIAN_POINT('Ctrl Pts',(-0.678245557197977,1.40002240284376,
10.2707786994315));
#266873=CARTESIAN_POINT('Ctrl Pts',(-0.658060950260043,1.40962245072208,
10.269151430898));
#266874=CARTESIAN_POINT('Ctrl Pts',(-0.476761938066386,1.49110793840217,
10.25454695146));
#266875=CARTESIAN_POINT('Ctrl Pts',(-0.30472376853314,1.5355188483371,10.2405573060793));
#266876=CARTESIAN_POINT('Ctrl Pts',(-0.0954235847670609,1.55293574567425,
10.2246241548186));
#266877=CARTESIAN_POINT('Ctrl Pts',(-0.0617670163658839,1.55463833700794,
10.2221018499259));
#266878=CARTESIAN_POINT('Ctrl Pts',(-0.0213826531515281,1.55536744330044,
10.2191425020006));
#266879=CARTESIAN_POINT('Ctrl Pts',(-0.0146857405561477,1.55544509222503,
10.2186539721346));
#266880=CARTESIAN_POINT('Ctrl Pts',(-0.00427714314134912,1.55549854697581,
10.2178983363767));
#266881=CARTESIAN_POINT('Ctrl Pts',(-0.000565803094649467,1.55550432472794,
10.2176296255618));
#266882=CARTESIAN_POINT('Ctrl Pts',(0.0063264062122905,1.55549038708562,
10.2171319962261));
#266883=CARTESIAN_POINT('Ctrl Pts',(0.00950716715387924,1.5554741983836,
10.2169028926674));
#266884=CARTESIAN_POINT('Ctrl Pts',(0.0167505299542766,1.55541511352609,
10.216382407332));
#266885=CARTESIAN_POINT('Ctrl Pts',(0.0208130249869358,1.55536605808523,
10.2160913715708));
#266886=CARTESIAN_POINT('Ctrl Pts',(0.0313956299772142,1.55519680086801,
10.2153354262995));
#266887=CARTESIAN_POINT('Ctrl Pts',(0.0379153478087279,1.55505151212667,
10.2148718693102));
#266888=CARTESIAN_POINT('Ctrl Pts',(0.0814357238219479,1.55380781000222,
10.2117908264832));
#266889=CARTESIAN_POINT('Ctrl Pts',(0.118391615239711,1.55142981376781,
10.2092385955489));
#266890=CARTESIAN_POINT('Ctrl Pts',(0.170475679911314,1.54620601174728,
10.2056876716411));
#266891=CARTESIAN_POINT('Ctrl Pts',(0.185697370728413,1.54445184470954,
10.2046555155841));
#266892=CARTESIAN_POINT('Ctrl Pts',(0.284967029825184,1.53152300422074,
10.1979467662469));
#266893=CARTESIAN_POINT('Ctrl Pts',(0.368009970509466,1.51371688609786,
10.1924332151657));
#266894=CARTESIAN_POINT('Ctrl Pts',(0.532008489798817,1.46425065810727,
10.1811003020359));
#266895=CARTESIAN_POINT('Ctrl Pts',(0.612585794477345,1.43240995287475,
10.1752946060289));
#266896=CARTESIAN_POINT('Ctrl Pts',(0.701514956133872,1.38838736140621,
10.1683596751497));
#266897=CARTESIAN_POINT('Ctrl Pts',(0.712867299509692,1.38259281614573,
10.1674642650704));
#266898=CARTESIAN_POINT('Ctrl Pts',(0.730181209905368,1.37348539832301,
10.1660823603076));
#266899=CARTESIAN_POINT('Ctrl Pts',(0.736194532796881,1.37027163216065,
10.1655993549946));
#266900=CARTESIAN_POINT('Ctrl Pts',(0.74711453404063,1.36434290695812,10.1647165472003));
#266901=CARTESIAN_POINT('Ctrl Pts',(0.752028057056082,1.36164073625601,
10.1643172045436));
#266902=CARTESIAN_POINT('Ctrl Pts',(0.762721903149051,1.35568416349133,
10.1634433734562));
#266903=CARTESIAN_POINT('Ctrl Pts',(0.768496211061508,1.35241924851249,
10.1629685143291));
#266904=CARTESIAN_POINT('Ctrl Pts',(0.784275318510369,1.34336372614142,
10.1616624688343));
#266905=CARTESIAN_POINT('Ctrl Pts',(0.794236549870784,1.33749847303368,
10.1608286047823));
#266906=CARTESIAN_POINT('Ctrl Pts',(0.846365062252937,1.30601710256412,
10.1564142768577));
#266907=CARTESIAN_POINT('Ctrl Pts',(0.887356654970115,1.27851932294011,
10.1527655450247));
#266908=CARTESIAN_POINT('Ctrl Pts',(1.04415641814986,1.16215893118084,10.1380716838586));
#266909=CARTESIAN_POINT('Ctrl Pts',(1.14850263419929,1.05915434891066,10.1265218396409));
#266910=CARTESIAN_POINT('Ctrl Pts',(1.25605792605177,0.918090689412616,
10.1130899706047));
#266911=CARTESIAN_POINT('Ctrl Pts',(1.27438937254133,0.892470792256993,
10.110735788307));
#266912=CARTESIAN_POINT('Ctrl Pts',(1.29559167976259,0.860851691204771,
10.1079473233843));
#266913=CARTESIAN_POINT('Ctrl Pts',(1.29921704342593,0.855370395282219,
10.1074680623674));
#266914=CARTESIAN_POINT('Ctrl Pts',(1.30482042377313,0.846780658309995,
10.1067236318135));
#266915=CARTESIAN_POINT('Ctrl Pts',(1.30682226218573,0.843687973960617,
10.1064569312944));
#266916=CARTESIAN_POINT('Ctrl Pts',(1.31053389849359,0.837908879611088,
10.1059610772914));
#266917=CARTESIAN_POINT('Ctrl Pts',(1.31224641838309,0.835224357510852,
10.1057317510052));
#266918=CARTESIAN_POINT('Ctrl Pts',(1.31614624573452,0.829069440312904,
10.1052082472807));
#266919=CARTESIAN_POINT('Ctrl Pts',(1.31832807651357,0.825595639971596,
10.1049144319132));
#266920=CARTESIAN_POINT('Ctrl Pts',(1.32401197095684,0.816466044553289,
10.1041464410459));
#266921=CARTESIAN_POINT('Ctrl Pts',(1.32749159018408,0.810796264991437,
10.1036736895829));
#266922=CARTESIAN_POINT('Ctrl Pts',(1.3514498300759,0.771190391188492,10.1003991098142));
#266923=CARTESIAN_POINT('Ctrl Pts',(1.37066332679176,0.736501170227816,
10.0976721869515));
#266924=CARTESIAN_POINT('Ctrl Pts',(1.40506730893587,0.668365085578623,
10.0925072917869));
#266925=CARTESIAN_POINT('Ctrl Pts',(1.4204227431959,0.635074885627405,10.0900670882858));
#266926=CARTESIAN_POINT('Ctrl Pts',(1.43457678342482,0.601306662576177,
10.0876445460468));
#266927=CARTESIAN_POINT('Ctrl Pts',(1.4345766815454,0.601306905636539,9.94872080685755));
#266928=CARTESIAN_POINT('Ctrl Pts',(1.39464986035857,0.69656289905012,9.95624305992229));
#266929=CARTESIAN_POINT('Ctrl Pts',(1.34534036199748,0.787592841149577,
9.96409078293215));
#266930=CARTESIAN_POINT('Ctrl Pts',(1.24095222318489,0.941520643270294,
9.97847524407404));
#266931=CARTESIAN_POINT('Ctrl Pts',(1.18913275716379,1.00617482597473,9.98493228383878));
#266932=CARTESIAN_POINT('Ctrl Pts',(1.10881976201145,1.09145938142171,9.99382504031493));
#266933=CARTESIAN_POINT('Ctrl Pts',(1.08439638207577,1.11572836726689,9.99640352829429));
#266934=CARTESIAN_POINT('Ctrl Pts',(1.05420923550547,1.14379600889694,9.99942416676281));
#266935=CARTESIAN_POINT('Ctrl Pts',(1.04920252577313,1.14839038948299,9.99991990651836));
#266936=CARTESIAN_POINT('Ctrl Pts',(1.04137798931262,1.1554766458844,10.000686325941));
#266937=CARTESIAN_POINT('Ctrl Pts',(1.0385810432954,1.15799128370229,10.0009586565537));
#266938=CARTESIAN_POINT('Ctrl Pts',(1.03337140330718,1.1626410331687,10.001462838238));
#266939=CARTESIAN_POINT('Ctrl Pts',(1.03096121709802,1.16477877657822,10.0016948797116));
#266940=CARTESIAN_POINT('Ctrl Pts',(1.02545687238681,1.16963045067171,10.002222078051));
#266941=CARTESIAN_POINT('Ctrl Pts',(1.02235857535066,1.17233959786527,10.002516880071));
#266942=CARTESIAN_POINT('Ctrl Pts',(1.01425702404123,1.17936704129483,10.0032827945205));
#266943=CARTESIAN_POINT('Ctrl Pts',(1.00923686757152,1.18366586423359,10.0037525192117));
#266944=CARTESIAN_POINT('Ctrl Pts',(0.975374681281018,1.2122904217217,10.0068896041933));
#266945=CARTESIAN_POINT('Ctrl Pts',(0.945680309356813,1.23559425786066,
10.0094893116133));
#266946=CARTESIAN_POINT('Ctrl Pts',(0.794622396906456,1.34550297979804,
10.0221527296009));
#266947=CARTESIAN_POINT('Ctrl Pts',(0.662096285572017,1.41542856750007,
10.0316152363526));
#266948=CARTESIAN_POINT('Ctrl Pts',(0.496438246775405,1.4743963622761,10.0435614534246));
#266949=CARTESIAN_POINT('Ctrl Pts',(0.471015719440541,1.48271360126234,
10.0453951352197));
#266950=CARTESIAN_POINT('Ctrl Pts',(0.42697878363117,1.49587389772509,10.0485813922596));
#266951=CARTESIAN_POINT('Ctrl Pts',(0.40846533711961,1.50103484675055,10.0499238569104));
#266952=CARTESIAN_POINT('Ctrl Pts',(0.382025576382251,1.50788004494536,
10.0518474689537));
#266953=CARTESIAN_POINT('Ctrl Pts',(0.374173856007484,1.50984757243412,
10.0524195059916));
#266954=CARTESIAN_POINT('Ctrl Pts',(0.360593369946202,1.51313820818275,
10.0534104394129));
#266955=CARTESIAN_POINT('Ctrl Pts',(0.354871740668333,1.51449029757679,
10.053828397696));
#266956=CARTESIAN_POINT('Ctrl Pts',(0.343889769620078,1.51701981959872,
10.0546315728696));
#266957=CARTESIAN_POINT('Ctrl Pts',(0.338630692480567,1.5182024105722,10.0550166179476));
#266958=CARTESIAN_POINT('Ctrl Pts',(0.326254977275459,1.52091779375944,
10.0559237465952));
#266959=CARTESIAN_POINT('Ctrl Pts',(0.319133568784506,1.5224279974781,10.0564465430711));
#266960=CARTESIAN_POINT('Ctrl Pts',(0.294442935494892,1.52748317517575,
10.0582620827262));
#266961=CARTESIAN_POINT('Ctrl Pts',(0.27682382777396,1.53077431752977,10.0595628245813));
#266962=CARTESIAN_POINT('Ctrl Pts',(0.135762045252824,1.55460888277475,
10.0700223573381));
#266963=CARTESIAN_POINT('Ctrl Pts',(0.0103314187981903,1.56048720632894,
10.0796562924481));
#266964=CARTESIAN_POINT('Ctrl Pts',(-0.199081856613034,1.54504168485567,
10.0959385487793));
#266965=CARTESIAN_POINT('Ctrl Pts',(-0.283103949734268,1.53187565082544,
10.1025091855824));
#266966=CARTESIAN_POINT('Ctrl Pts',(-0.37579258792469,1.50945993185414,
10.1095478713378));
#266967=CARTESIAN_POINT('Ctrl Pts',(-0.385920630206807,1.5069023319547,
10.1103139882301));
#266968=CARTESIAN_POINT('Ctrl Pts',(-0.400347308653118,1.50310421555012,
10.1114002492365));
#266969=CARTESIAN_POINT('Ctrl Pts',(-0.404667258260174,1.50194695704885,
10.1117248752355));
#266970=CARTESIAN_POINT('Ctrl Pts',(-0.41213379310469,1.49991221628383,
10.1122847645362));
#266971=CARTESIAN_POINT('Ctrl Pts',(-0.415282691695335,1.49904343059812,
10.1125205210313));
#266972=CARTESIAN_POINT('Ctrl Pts',(-0.4218602752194,1.49720634880885,10.1130121861267));
#266973=CARTESIAN_POINT('Ctrl Pts',(-0.425288384545355,1.49623618903792,
10.1132679854305));
#266974=CARTESIAN_POINT('Ctrl Pts',(-0.434378993801736,1.49362976676146,
10.113945197932));
#266975=CARTESIAN_POINT('Ctrl Pts',(-0.440035653118906,1.49197306188208,
10.1143654474963));
#266976=CARTESIAN_POINT('Ctrl Pts',(-0.464284288950538,1.48472128950693,
10.1161625644793));
#266977=CARTESIAN_POINT('Ctrl Pts',(-0.482781057108053,1.47881024862455,
10.1175223045462));
#266978=CARTESIAN_POINT('Ctrl Pts',(-0.659262807854901,1.41874712619837,
10.1304328637531));
#266979=CARTESIAN_POINT('Ctrl Pts',(-0.807683273884122,1.33982672490135,
10.1409098876283));
#266980=CARTESIAN_POINT('Ctrl Pts',(-0.975089262784055,1.21270068574397,
10.1551607716187));
#266981=CARTESIAN_POINT('Ctrl Pts',(-1.00834877594978,1.18518951783725,
10.1581282441116));
#266982=CARTESIAN_POINT('Ctrl Pts',(-1.04848212539614,1.14907924611275,
10.1619120696735));
#266983=CARTESIAN_POINT('Ctrl Pts',(-1.05646843059558,1.14174091882177,
10.1626756186984));
#266984=CARTESIAN_POINT('Ctrl Pts',(-1.06908762047572,1.12989983385748,
10.163899560269));
#266985=CARTESIAN_POINT('Ctrl Pts',(-1.07377042997215,1.12545059253557,
10.1643576663117));
#266986=CARTESIAN_POINT('Ctrl Pts',(-1.08257609821553,1.11697914766503,
10.1652266424887));
#266987=CARTESIAN_POINT('Ctrl Pts',(-1.08670460509117,1.11296294834169,
10.1656372481826));
#266988=CARTESIAN_POINT('Ctrl Pts',(-1.09600481999391,1.10381464429617,
10.1665695414669));
#266989=CARTESIAN_POINT('Ctrl Pts',(-1.10116293399881,1.09866897828989,
10.1670918194007));
#266990=CARTESIAN_POINT('Ctrl Pts',(-1.11437253156175,1.08530478638757,
10.1684429966065));
#266991=CARTESIAN_POINT('Ctrl Pts',(-1.12236919622339,1.07703295799389,
10.1692742567673));
#266992=CARTESIAN_POINT('Ctrl Pts',(-1.17646575132327,1.01981820408645,
10.1749908441597));
#266993=CARTESIAN_POINT('Ctrl Pts',(-1.2194351671807,0.968026999758387,
10.1800068724847));
#266994=CARTESIAN_POINT('Ctrl Pts',(-1.32794770583136,0.818504006184004,
10.194075021361));
#266995=CARTESIAN_POINT('Ctrl Pts',(-1.38597089553815,0.715874001236015,
10.2033193996353));
#266996=CARTESIAN_POINT('Ctrl Pts',(-1.44716184615487,0.571692611803612,
10.2152526904509));
#266997=CARTESIAN_POINT('Ctrl Pts',(-1.46107960670724,0.535123235047128,
10.2181923652023));
#266998=CARTESIAN_POINT('Ctrl Pts',(-1.4758551218457,0.491407455262296,
10.221575743023));
#266999=CARTESIAN_POINT('Ctrl Pts',(-1.4780600378127,0.484735141500817,
10.2220886071838));
#267000=CARTESIAN_POINT('Ctrl Pts',(-1.48139096232781,0.474421322198345,
10.2228756865157));
#267001=CARTESIAN_POINT('Ctrl Pts',(-1.48254889270473,0.470790352289202,
10.2231516948238));
#267002=CARTESIAN_POINT('Ctrl Pts',(-1.48465965686182,0.464086525332085,
10.223659246459));
#267003=CARTESIAN_POINT('Ctrl Pts',(-1.4856162972954,0.461014986000578,
10.223891002545));
#267004=CARTESIAN_POINT('Ctrl Pts',(-1.4877556515077,0.454070227034208,
10.2244132315157));
#267005=CARTESIAN_POINT('Ctrl Pts',(-1.48893277188251,0.450195348143785,
10.2247033768899));
#267006=CARTESIAN_POINT('Ctrl Pts',(-1.49236601180917,0.438732943758511,
10.225558140743));
#267007=CARTESIAN_POINT('Ctrl Pts',(-1.49457940735182,0.431132591298094,
10.2261203551612));
#267008=CARTESIAN_POINT('Ctrl Pts',(-1.51187526292265,0.370007767337685,
10.230607945371));
#267009=CARTESIAN_POINT('Ctrl Pts',(-1.52413761827353,0.315719351150575,
10.2343858584892));
#267010=CARTESIAN_POINT('Ctrl Pts',(-1.54805757830584,0.17511873879064,
10.2439157176547));
#267011=CARTESIAN_POINT('Ctrl Pts',(-1.55542813893534,0.0882786190245136,
10.2495683327449));
#267012=CARTESIAN_POINT('Ctrl Pts',(-1.55556419254695,-0.0776507360197793,
10.2605745051194));
#267013=CARTESIAN_POINT('Ctrl Pts',(-1.54962198720566,-0.156456241130258,
10.2658907513526));
#267014=CARTESIAN_POINT('Ctrl Pts',(-1.53594203793849,-0.24617611525238,
10.2722300465037));
#267015=CARTESIAN_POINT('Ctrl Pts',(-1.53402245979568,-0.257867607231571,
10.2730616198341));
#267016=CARTESIAN_POINT('Ctrl Pts',(-1.5306891459699,-0.27681327682575,
10.2744186468661));
#267017=CARTESIAN_POINT('Ctrl Pts',(-1.5293569129153,-0.284081469541231,
10.2749415250497));
#267018=CARTESIAN_POINT('Ctrl Pts',(-1.5268920309354,-0.297008893991048,
10.2758757213272));
#267019=CARTESIAN_POINT('Ctrl Pts',(-1.52577956852232,-0.302671874943031,
10.2762863916489));
#267020=CARTESIAN_POINT('Ctrl Pts',(-1.52336703235503,-0.314601485802336,
10.2771546063657));
#267021=CARTESIAN_POINT('Ctrl Pts',(-1.52205974849696,-0.320866529698587,
10.2776123734426));
#267022=CARTESIAN_POINT('Ctrl Pts',(-1.51848974320291,-0.337462588368844,
10.2788298992047));
#267023=CARTESIAN_POINT('Ctrl Pts',(-1.51616029397407,-0.347778739252849,
10.2795917734682));
#267024=CARTESIAN_POINT('Ctrl Pts',(-1.50455085403857,-0.396857144931691,
10.2832411836649));
#267025=CARTESIAN_POINT('Ctrl Pts',(-1.49388928610356,-0.435273628260907,
10.2861725227912));
#267026=CARTESIAN_POINT('Ctrl Pts',(-1.43628524530431,-0.615639856941075,
10.3003079185256));
#267027=CARTESIAN_POINT('Ctrl Pts',(-1.37051371152964,-0.750736944814589,
10.3121144984721));
#267028=CARTESIAN_POINT('Ctrl Pts',(-1.26511427957333,-0.905822977656985,
10.326395921319));
#267029=CARTESIAN_POINT('Ctrl Pts',(-1.24256571103544,-0.936515057905393,
10.3292569511393));
#267030=CARTESIAN_POINT('Ctrl Pts',(-1.21479543134976,-0.971543207076164,
10.3325367658213));
#267031=CARTESIAN_POINT('Ctrl Pts',(-1.21064631460267,-0.976708579031646,
10.3330207980656));
#267032=CARTESIAN_POINT('Ctrl Pts',(-1.20386332971184,-0.985043304530043,
10.3338022278515));
#267033=CARTESIAN_POINT('Ctrl Pts',(-1.20124970628607,-0.988228907001057,
10.3341009943053));
#267034=CARTESIAN_POINT('Ctrl Pts',(-1.19656983841324,-0.993886941911346,
10.3346317588914));
#267035=CARTESIAN_POINT('Ctrl Pts',(-1.19450854590318,-0.996363370448372,
10.3348641029391));
#267036=CARTESIAN_POINT('Ctrl Pts',(-1.19002663866141,-1.00171401551384,
10.3353661853621));
#267037=CARTESIAN_POINT('Ctrl Pts',(-1.18760330229603,-1.00458586829852,
10.3356357213107));
#267038=CARTESIAN_POINT('Ctrl Pts',(-1.18077904500518,-1.01261396928665,
10.3363894368417));
#267039=CARTESIAN_POINT('Ctrl Pts',(-1.17635471753991,-1.01775035589376,
10.3368719478006));
#267040=CARTESIAN_POINT('Ctrl Pts',(-1.14945929176624,-1.04856467363213,
10.339769538717));
#267041=CARTESIAN_POINT('Ctrl Pts',(-1.12617976056278,-1.07352882189692,
10.3421293104767));
#267042=CARTESIAN_POINT('Ctrl Pts',(-1.01426798997064,-1.18588779344111,
10.3529242729752));
#267043=CARTESIAN_POINT('Ctrl Pts',(-0.916169471450868,-1.26321352010279,
10.3609004667231));
#267044=CARTESIAN_POINT('Ctrl Pts',(-0.753694414430256,-1.36229888817716,
10.3736025517594));
#267045=CARTESIAN_POINT('Ctrl Pts',(-0.695381370771949,-1.39296680347772,
10.3780688738453));
#267046=CARTESIAN_POINT('Ctrl Pts',(-0.62485110076814,-1.42452537981127,
10.3834693352067));
#267047=CARTESIAN_POINT('Ctrl Pts',(-0.614344416196805,-1.42908795454396,
10.3842736644787));
#267048=CARTESIAN_POINT('Ctrl Pts',(-0.5970880679109,-1.43635613624648,
10.3855949479659));
#267049=CARTESIAN_POINT('Ctrl Pts',(-0.590367993864654,-1.43913124472895,
10.3861095483177));
#267050=CARTESIAN_POINT('Ctrl Pts',(-0.578291311789725,-1.44401958620469,
10.3870345659502));
#267051=CARTESIAN_POINT('Ctrl Pts',(-0.572941921310816,-1.44615039321894,
10.3874443832714));
#267052=CARTESIAN_POINT('Ctrl Pts',(-0.561558082033392,-1.45061180751835,
10.3883167324587));
#267053=CARTESIAN_POINT('Ctrl Pts',(-0.555520695701756,-1.45293456491392,
10.3887795181124));
#267054=CARTESIAN_POINT('Ctrl Pts',(-0.539282774045474,-1.4590657605718,
10.3900246812528));
#267055=CARTESIAN_POINT('Ctrl Pts',(-0.529056612271184,-1.46280480374804,
10.390809348187));
#267056=CARTESIAN_POINT('Ctrl Pts',(-0.477599061166027,-1.48100933389709,
10.3947610178785));
#267057=CARTESIAN_POINT('Ctrl Pts',(-0.435814267012427,-1.49383892505317,
10.3979811324152));
#267058=CARTESIAN_POINT('Ctrl Pts',(-0.243126762961555,-1.54422918050073,
10.4128964566057));
#267059=CARTESIAN_POINT('Ctrl Pts',(-0.0876918707412931,-1.56078535366454,
10.4252253702649));
#267060=CARTESIAN_POINT('Ctrl Pts',(0.0962735123591064,-1.55278314926884,
10.4391392515311));
#267061=CARTESIAN_POINT('Ctrl Pts',(0.12491161146944,-1.55074223002995,
10.4412817634017));
#267062=CARTESIAN_POINT('Ctrl Pts',(0.160127205521839,-1.54725051619652,
10.443874865253));
#267063=CARTESIAN_POINT('Ctrl Pts',(0.166771157396114,-1.5465485014074,
10.4443622614655));
#267064=CARTESIAN_POINT('Ctrl Pts',(0.177163521042644,-1.54538267071173,
10.4451215594705));
#267065=CARTESIAN_POINT('Ctrl Pts',(0.180915011287092,-1.54494798347355,
10.4453950257974));
#267066=CARTESIAN_POINT('Ctrl Pts',(0.187831694722515,-1.54412100438494,
10.4458980139329));
#267067=CARTESIAN_POINT('Ctrl Pts',(0.190997241653555,-1.54373264387433,
10.4461277440395));
#267068=CARTESIAN_POINT('Ctrl Pts',(0.198208031392311,-1.5428254789474,
10.4466499887457));
#267069=CARTESIAN_POINT('Ctrl Pts',(0.202252439393425,-1.54230050054513,
10.4469421537296));
#267070=CARTESIAN_POINT('Ctrl Pts',(0.214541910562755,-1.5406561106215,
10.4478277748135));
#267071=CARTESIAN_POINT('Ctrl Pts',(0.222780278108291,-1.53948642033404,
10.4484184994134));
#267072=CARTESIAN_POINT('Ctrl Pts',(0.241832981866239,-1.53662515190068,
10.4497786336488));
#267073=CARTESIAN_POINT('Ctrl Pts',(0.252639776186028,-1.53488540567801,
10.4505456036878));
#267074=CARTESIAN_POINT('Ctrl Pts',(0.289599371700655,-1.52853447342525,
10.4531560259521));
#267075=CARTESIAN_POINT('Ctrl Pts',(0.315653347597125,-1.5233675132306,
10.4549744646969));
#267076=CARTESIAN_POINT('Ctrl Pts',(0.460004865183639,-1.4908771634028,
10.4649923779096));
#267077=CARTESIAN_POINT('Ctrl Pts',(0.574923432398753,-1.45044352010272,
10.4727832366868));
#267078=CARTESIAN_POINT('Ctrl Pts',(0.740669605465649,-1.36929664955656,
10.4851193269967));
#267079=CARTESIAN_POINT('Ctrl Pts',(0.795613979223518,-1.33811867507471,
10.4894085406645));
#267080=CARTESIAN_POINT('Ctrl Pts',(0.858024250161843,-1.29749896124582,
10.4946138461831));
#267081=CARTESIAN_POINT('Ctrl Pts',(0.867472098024921,-1.29120150071172,
10.4954112278284));
#267082=CARTESIAN_POINT('Ctrl Pts',(0.882830063440128,-1.28072001155749,
10.4967233850599));
#267083=CARTESIAN_POINT('Ctrl Pts',(0.888781523963574,-1.27659706578813,
10.4972358618758));
#267084=CARTESIAN_POINT('Ctrl Pts',(0.899411747484894,-1.26912248441489,
10.4981585496682));
#267085=CARTESIAN_POINT('Ctrl Pts',(0.904101133471117,-1.26578612363553,
10.4985681729351));
#267086=CARTESIAN_POINT('Ctrl Pts',(0.914037243739115,-1.25863348852336,
10.4994417027001));
#267087=CARTESIAN_POINT('Ctrl Pts',(0.91927880801342,-1.25481026938627,
10.4999058714044));
#267088=CARTESIAN_POINT('Ctrl Pts',(0.933322070853899,-1.2444318388997,
10.5011586626093));
#267089=CARTESIAN_POINT('Ctrl Pts',(0.942078421389058,-1.23781619237101,
10.5019496235394));
#267090=CARTESIAN_POINT('Ctrl Pts',(0.986245343153725,-1.20370684429341,
10.5059902994799));
#267091=CARTESIAN_POINT('Ctrl Pts',(1.02052198049525,-1.17478686388855,
10.5092960539549));
#267092=CARTESIAN_POINT('Ctrl Pts',(1.11804221155345,-1.08501510988762,
10.5192312920522));
#267093=CARTESIAN_POINT('Ctrl Pts',(1.177435889796,-1.02025356956725,10.5260058840845));
#267094=CARTESIAN_POINT('Ctrl Pts',(1.28372048158515,-0.882647553728048,
10.5394891339913));
#267095=CARTESIAN_POINT('Ctrl Pts',(1.33064071179853,-0.810187338955744,
10.546171884293));
#267096=CARTESIAN_POINT('Ctrl Pts',(1.37715836679279,-0.723303554000018,
10.5534721554879));
#267097=CARTESIAN_POINT('Ctrl Pts',(1.38286579716953,-0.712330970263795,
10.5543816914596));
#267098=CARTESIAN_POINT('Ctrl Pts',(1.39066398095201,-0.696891836828856,
10.5556430317168));
#267099=CARTESIAN_POINT('Ctrl Pts',(1.39286509832849,-0.692482028503425,
10.5560012217619));
#267100=CARTESIAN_POINT('Ctrl Pts',(1.396380326652,-0.685354902790822,10.5565766932149));
#267101=CARTESIAN_POINT('Ctrl Pts',(1.39770752877413,-0.682644141463641,
10.5567947735125));
#267102=CARTESIAN_POINT('Ctrl Pts',(1.40048735842366,-0.676924348019211,
10.5572532265455));
#267103=CARTESIAN_POINT('Ctrl Pts',(1.40193819492123,-0.67391446940491,
10.5574934829998));
#267104=CARTESIAN_POINT('Ctrl Pts',(1.40548303788341,-0.666499414962702,
10.5580829940322));
#267105=CARTESIAN_POINT('Ctrl Pts',(1.40756606884171,-0.662088969467931,
10.5584315761637));
#267106=CARTESIAN_POINT('Ctrl Pts',(1.41511845772876,-0.645901394737934,
10.5597037222602));
#267107=CARTESIAN_POINT('Ctrl Pts',(1.4204612351256,-0.634065272658606,
10.5606199016087));
#267108=CARTESIAN_POINT('Ctrl Pts',(1.45525352133037,-0.554340504707602,
10.5667070284646));
#267109=CARTESIAN_POINT('Ctrl Pts',(1.47997839663625,-0.484482380529914,
10.5716382115629));
#267110=CARTESIAN_POINT('Ctrl Pts',(1.53515835677589,-0.284177835200355,
10.585359342164));
#267111=CARTESIAN_POINT('Ctrl Pts',(1.55389819801128,-0.151209515050148,
10.5940427568767));
#267112=CARTESIAN_POINT('Ctrl Pts',(1.55559805582344,-2.31852926990466E-5,
10.6045457699659));
#267113=CARTESIAN_POINT('Ctrl Pts',(1.55550024276892,0.0174431545606266,
10.6057675448385));
#267114=CARTESIAN_POINT('Ctrl Pts',(1.55495098829591,0.0419148854556453,
10.6074927050732));
#267115=CARTESIAN_POINT('Ctrl Pts',(1.55474621004683,0.0489249739294903,
10.6079884228675));
#267116=CARTESIAN_POINT('Ctrl Pts',(1.55428335251448,0.0617886671499064,
10.6089010100376));
#267117=CARTESIAN_POINT('Ctrl Pts',(1.55403958909289,0.0676426870412161,
10.6093174262123));
#267118=CARTESIAN_POINT('Ctrl Pts',(1.5534772801245,0.0795304799023775,
10.6101653781285));
#267119=CARTESIAN_POINT('Ctrl Pts',(1.55315664017382,0.0855640478401656,
10.6105969722121));
#267120=CARTESIAN_POINT('Ctrl Pts',(1.55227524764469,0.100506122771638,
10.6116689196459));
#267121=CARTESIAN_POINT('Ctrl Pts',(1.55167295628279,0.109411862899771,
10.6123105597758));
#267122=CARTESIAN_POINT('Ctrl Pts',(1.54911539442991,0.142939919334832,
10.6147368559119));
#267123=CARTESIAN_POINT('Ctrl Pts',(1.54665049890624,0.167518447209745,
10.6165372874127));
#267124=CARTESIAN_POINT('Ctrl Pts',(1.53899818124486,0.229031430577571,
10.6211009962873));
#267125=CARTESIAN_POINT('Ctrl Pts',(1.53306591292877,0.265855777746757,
10.6238858928683));
#267126=CARTESIAN_POINT('Ctrl Pts',(1.50548810790567,0.404991580091826,
10.634608373832));
#267127=CARTESIAN_POINT('Ctrl Pts',(1.47489605884916,0.505114366182903,
10.6427635453334));
#267128=CARTESIAN_POINT('Ctrl Pts',(1.43457668061803,0.601306907849032,
10.6508134549194));
#267129=CARTESIAN_POINT('Origin',(0.,0.,-1.29405622560371));
#267130=CARTESIAN_POINT('',(1.4345766883817,0.601306889326732,11.4896545509914));
#267131=CARTESIAN_POINT('',(1.43457668357355,0.601306900797848,11.3502242497076));
#267132=CARTESIAN_POINT('',(1.43457668357355,0.601306900797845,-1.29405622560371));
#267133=CARTESIAN_POINT('Ctrl Pts',(1.4345766883817,0.601306889326732,11.4896545509914));
#267134=CARTESIAN_POINT('Ctrl Pts',(1.44407323673688,0.578650360468923,
11.4878458824711));
#267135=CARTESIAN_POINT('Ctrl Pts',(1.45303230308892,0.555770666562326,
11.486019839339));
#267136=CARTESIAN_POINT('Ctrl Pts',(1.51303881084614,0.391140569784664,
11.4728827943302));
#267137=CARTESIAN_POINT('Ctrl Pts',(1.54378555080634,0.242881238893851,
11.4609546076149));
#267138=CARTESIAN_POINT('Ctrl Pts',(1.55466567521783,0.06030784464822,11.4470960617881));
#267139=CARTESIAN_POINT('Ctrl Pts',(1.55558260286277,0.0280276449396798,
11.4446814329925));
#267140=CARTESIAN_POINT('Ctrl Pts',(1.55547603854558,-0.0108784739935134,
11.4418313869187));
#267141=CARTESIAN_POINT('Ctrl Pts',(1.55541567678721,-0.0174964084788573,
11.4413486978236));
#267142=CARTESIAN_POINT('Ctrl Pts',(1.55525581052292,-0.0278075546564512,
11.4406001214563));
#267143=CARTESIAN_POINT('Ctrl Pts',(1.55518538509407,-0.0315010321067899,
11.4403326760263));
#267144=CARTESIAN_POINT('Ctrl Pts',(1.5550297856546,-0.0383763822669787,
11.4398361700344));
#267145=CARTESIAN_POINT('Ctrl Pts',(1.55494800430072,-0.0415582149089613,
11.4396069321225));
#267146=CARTESIAN_POINT('Ctrl Pts',(1.55473889694584,-0.048825377876731,
11.4390845733081));
#267147=CARTESIAN_POINT('Ctrl Pts',(1.55460523553539,-0.0529104704047821,
11.4387918084128));
#267148=CARTESIAN_POINT('Ctrl Pts',(1.55421354852023,-0.0635931526224319,
11.4380283766596));
#267149=CARTESIAN_POINT('Ctrl Pts',(1.553929612088,-0.0701898015677843,
11.4375591065679));
#267150=CARTESIAN_POINT('Ctrl Pts',(1.55169503418187,-0.115402625114617,
11.4343563135564));
#267151=CARTESIAN_POINT('Ctrl Pts',(1.54834695455523,-0.153940172523269,
11.4316940468738));
#267152=CARTESIAN_POINT('Ctrl Pts',(1.54228604730357,-0.202586017920447,
11.4283738711653));
#267153=CARTESIAN_POINT('Ctrl Pts',(1.54090408958628,-0.212842526626525,
11.4276761426403));
#267154=CARTESIAN_POINT('Ctrl Pts',(1.52547690141245,-0.319299504718612,
11.4204510722172));
#267155=CARTESIAN_POINT('Ctrl Pts',(1.50254410758542,-0.413998741802044,
11.414155311747));
#267156=CARTESIAN_POINT('Ctrl Pts',(1.45408005578147,-0.5548980010043,11.4042634206064));
#267157=CARTESIAN_POINT('Ctrl Pts',(1.43480839838853,-0.602979879718134,
11.4007904142757));
#267158=CARTESIAN_POINT('Ctrl Pts',(1.40015443874943,-0.678320687071308,
11.3951106087149));
#267159=CARTESIAN_POINT('Ctrl Pts',(1.38628492506799,-0.70623316468095,
11.3929516612066));
#267160=CARTESIAN_POINT('Ctrl Pts',(1.36703561190124,-0.742217626532354,
11.3900859592445));
#267161=CARTESIAN_POINT('Ctrl Pts',(1.3624049246891,-0.750683810293062,
11.3894056237435));
#267162=CARTESIAN_POINT('Ctrl Pts',(1.3546969688877,-0.764469838849435,
11.3882874544315));
#267163=CARTESIAN_POINT('Ctrl Pts',(1.35166636366483,-0.769815595703467,
11.3878512924443));
#267164=CARTESIAN_POINT('Ctrl Pts',(1.34573863050125,-0.780128743001058,
11.3870047651151));
#267165=CARTESIAN_POINT('Ctrl Pts',(1.34284547149433,-0.785098309342846,
11.3865945480933));
#267166=CARTESIAN_POINT('Ctrl Pts',(1.33609636553207,-0.796544769529156,
11.3856442839464));
#267167=CARTESIAN_POINT('Ctrl Pts',(1.33222078942502,-0.803009858200643,
11.3851035304211));
#267168=CARTESIAN_POINT('Ctrl Pts',(1.31953794558891,-0.823822355829706,
11.3833494461501));
#267169=CARTESIAN_POINT('Ctrl Pts',(1.31054498122841,-0.838054577330154,
11.3821293506623));
#267170=CARTESIAN_POINT('Ctrl Pts',(1.22533847775522,-0.968175817688255,
11.3707777778507));
#267171=CARTESIAN_POINT('Ctrl Pts',(1.13418955789108,-1.07350607508223,
11.360044561091));
#267172=CARTESIAN_POINT('Ctrl Pts',(0.977386715594308,-1.2121421210387,
11.3438318809266));
#267173=CARTESIAN_POINT('Ctrl Pts',(0.921314794587914,-1.25529067441546,
11.3383918477702));
#267174=CARTESIAN_POINT('Ctrl Pts',(0.851974596277352,-1.30149122473887,
11.332219528681));
#267175=CARTESIAN_POINT('Ctrl Pts',(0.84136676225202,-1.30837384554578,
11.3312897537226));
#267176=CARTESIAN_POINT('Ctrl Pts',(0.826625549404747,-1.31768486352746,
11.3300187403291));
#267177=CARTESIAN_POINT('Ctrl Pts',(0.822563496881006,-1.32022441037192,
11.3296706774395));
#267178=CARTESIAN_POINT('Ctrl Pts',(0.815688511890171,-1.324478521029,11.3290853278683));
#267179=CARTESIAN_POINT('Ctrl Pts',(0.812881774171896,-1.32620297204218,
11.3288474027228));
#267180=CARTESIAN_POINT('Ctrl Pts',(0.807522383677627,-1.32947235857583,
11.3283951108807));
#267181=CARTESIAN_POINT('Ctrl Pts',(0.804970742262437,-1.33101887923143,
11.3281806376976));
#267182=CARTESIAN_POINT('Ctrl Pts',(0.798229972451977,-1.3350779086275,
11.3276162913125));
#267183=CARTESIAN_POINT('Ctrl Pts',(0.794033385276217,-1.33757807092635,
11.3272672155987));
#267184=CARTESIAN_POINT('Ctrl Pts',(0.779216501427361,-1.34631108204241,
11.3260424403143));
#267185=CARTESIAN_POINT('Ctrl Pts',(0.768533674299746,-1.35243776283375,
11.3251732579917));
#267186=CARTESIAN_POINT('Ctrl Pts',(0.688036343535112,-1.3973416933008,
11.3187180951702));
#267187=CARTESIAN_POINT('Ctrl Pts',(0.615390781887192,-1.43082343273482,
11.3134156047808));
#267188=CARTESIAN_POINT('Ctrl Pts',(0.478582600796601,-1.48151849855804,
11.303794292087));
#267189=CARTESIAN_POINT('Ctrl Pts',(0.415283885472396,-1.50049238901889,
11.2994743813456));
#267190=CARTESIAN_POINT('Ctrl Pts',(0.288246899694262,-1.52991485862425,
11.2907889679189));
#267191=CARTESIAN_POINT('Ctrl Pts',(0.224687530253573,-1.54053227175699,
11.2864356435291));
#267192=CARTESIAN_POINT('Ctrl Pts',(0.144549789380137,-1.54885373694145,
11.2808302074974));
#267193=CARTESIAN_POINT('Ctrl Pts',(0.128416443673834,-1.5502747248807,
11.2796960868988));
#267194=CARTESIAN_POINT('Ctrl Pts',(0.104781346789404,-1.55198498967307,
11.2780250636582));
#267195=CARTESIAN_POINT('Ctrl Pts',(0.0972946267128872,-1.55247231565039,
11.2774943484672));
#267196=CARTESIAN_POINT('Ctrl Pts',(0.0840890679635162,-1.5532359953968,
11.2765556426064));
#267197=CARTESIAN_POINT('Ctrl Pts',(0.0783716345593125,-1.55353497354903,
11.2761483667232));
#267198=CARTESIAN_POINT('Ctrl Pts',(0.0672061926329519,-1.55405704770376,
11.2753512752644));
#267199=CARTESIAN_POINT('Ctrl Pts',(0.061758398629359,-1.55428307545546,
11.2749615574745));
#267200=CARTESIAN_POINT('Ctrl Pts',(0.0470666366396885,-1.55481527071458,
11.2739083236134));
#267201=CARTESIAN_POINT('Ctrl Pts',(0.0378210685758777,-1.55506763654793,
11.2732431377116));
#267202=CARTESIAN_POINT('Ctrl Pts',(0.0031911707828243,-1.55570388282549,
11.27074234781));
#267203=CARTESIAN_POINT('Ctrl Pts',(-0.0221977743906398,-1.55554873675841,
11.2688901144894));
#267204=CARTESIAN_POINT('Ctrl Pts',(-0.0507959154971018,-1.55467374063616,
11.2667812032219));
#267205=CARTESIAN_POINT('Ctrl Pts',(-0.0540212744564434,-1.55456500876575,
11.2665430336903));
#267206=CARTESIAN_POINT('Ctrl Pts',(-0.0629986478676237,-1.55423439523362,
11.2658792194824));
#267207=CARTESIAN_POINT('Ctrl Pts',(-0.0687497559886824,-1.55399062237622,
11.2654529363581));
#267208=CARTESIAN_POINT('Ctrl Pts',(-0.212927542232475,-1.5470774200656,
11.2547402956532));
#267209=CARTESIAN_POINT('Ctrl Pts',(-0.349831848842385,-1.52196936592823,
11.2438857029329));
#267210=CARTESIAN_POINT('Ctrl Pts',(-0.518444971914157,-1.46707173483673,
11.2302353683261));
#267211=CARTESIAN_POINT('Ctrl Pts',(-0.554867063694058,-1.45368760783786,
11.2272747462962));
#267212=CARTESIAN_POINT('Ctrl Pts',(-0.60380164124047,-1.43359784706473,
11.2233113733096));
#267213=CARTESIAN_POINT('Ctrl Pts',(-0.616777190795279,-1.42806342294545,
11.2222618923797));
#267214=CARTESIAN_POINT('Ctrl Pts',(-0.638925015790562,-1.41825857281392,
11.2204751350318));
#267215=CARTESIAN_POINT('Ctrl Pts',(-0.648134006366779,-1.41407385925245,
11.2197335912736));
#267216=CARTESIAN_POINT('Ctrl Pts',(-0.661273082173743,-1.40794792508543,
11.2186782375319));
#267217=CARTESIAN_POINT('Ctrl Pts',(-0.665236547327894,-1.40607958036795,
11.2183602344379));
#267218=CARTESIAN_POINT('Ctrl Pts',(-0.672098867875133,-1.40280922789103,
11.217810319532));
#267219=CARTESIAN_POINT('Ctrl Pts',(-0.675001339125067,-1.40141493179697,
11.2175779403438));
#267220=CARTESIAN_POINT('Ctrl Pts',(-0.681076971163145,-1.39847305035946,
11.217091976527));
#267221=CARTESIAN_POINT('Ctrl Pts',(-0.684249204104702,-1.39692367027999,
11.2168385052843));
#267222=CARTESIAN_POINT('Ctrl Pts',(-0.692686650013249,-1.39276702085703,
11.2161649529105));
#267223=CARTESIAN_POINT('Ctrl Pts',(-0.697942482336024,-1.39014066331589,
11.2157460369082));
#267224=CARTESIAN_POINT('Ctrl Pts',(-0.720706138202114,-1.37860393984384,
11.2139339433999));
#267225=CARTESIAN_POINT('Ctrl Pts',(-0.738060141838192,-1.36939164703411,
11.2125583737263));
#267226=CARTESIAN_POINT('Ctrl Pts',(-0.851175561927651,-1.30656951075313,
11.2036000671003));
#267227=CARTESIAN_POINT('Ctrl Pts',(-0.941219936408087,-1.24327602094947,
11.1964901497737));
#267228=CARTESIAN_POINT('Ctrl Pts',(-1.09643014097945,-1.10757107105275,
11.182888967164));
#267229=CARTESIAN_POINT('Ctrl Pts',(-1.16293430465464,-1.03752220304883,
11.1764562146549));
#267230=CARTESIAN_POINT('Ctrl Pts',(-1.23052721268062,-0.951604206502917,
11.168818201296));
#267231=CARTESIAN_POINT('Ctrl Pts',(-1.23840283314166,-0.941332136938379,
11.1679090591008));
#267232=CARTESIAN_POINT('Ctrl Pts',(-1.25025472662428,-0.9254676794188,
11.1665103906766));
#267233=CARTESIAN_POINT('Ctrl Pts',(-1.25432385285745,-0.919945094295435,
11.1660244892754));
#267234=CARTESIAN_POINT('Ctrl Pts',(-1.26136151039847,-0.910260141793547,
11.1651739842198));
#267235=CARTESIAN_POINT('Ctrl Pts',(-1.26434632226614,-0.906109685347741,
11.1648100160584));
#267236=CARTESIAN_POINT('Ctrl Pts',(-1.2710319110929,-0.896715852100479,
11.1639873428862));
#267237=CARTESIAN_POINT('Ctrl Pts',(-1.27472078673598,-0.891464161930384,
11.1635281909489));
#267238=CARTESIAN_POINT('Ctrl Pts',(-1.28458078595995,-0.877240577595905,
11.1622865958419));
#267239=CARTESIAN_POINT('Ctrl Pts',(-1.29069026893407,-0.868226609303773,
11.1615018402763));
#267240=CARTESIAN_POINT('Ctrl Pts',(-1.3184201045975,-0.826374284505443,
11.157867019056));
#267241=CARTESIAN_POINT('Ctrl Pts',(-1.33888334424869,-0.792790581932498,
11.1549746119441));
#267242=CARTESIAN_POINT('Ctrl Pts',(-1.43421910520561,-0.622090701509377,
11.1403767687332));
#267243=CARTESIAN_POINT('Ctrl Pts',(-1.48939342059203,-0.475050691549615,
11.1280030280243));
#267244=CARTESIAN_POINT('Ctrl Pts',(-1.52851215983715,-0.290339124693049,
11.1136920176644));
#267245=CARTESIAN_POINT('Ctrl Pts',(-1.53427002481038,-0.258190082007997,
11.1112492791146));
#267246=CARTESIAN_POINT('Ctrl Pts',(-1.5399761490847,-0.219312078202865,
11.1083706507332));
#267247=CARTESIAN_POINT('Ctrl Pts',(-1.5408981976906,-0.212737105385428,
11.1078864046954));
#267248=CARTESIAN_POINT('Ctrl Pts',(-1.54226834185423,-0.202490226695637,
11.1071359460143));
#267249=CARTESIAN_POINT('Ctrl Pts',(-1.54274547081239,-0.198822391234944,
11.1068681628043));
#267250=CARTESIAN_POINT('Ctrl Pts',(-1.54360877498709,-0.191995643337098,
11.1063713588623));
#267251=CARTESIAN_POINT('Ctrl Pts',(-1.54399833569566,-0.188837276424316,
11.1061421587234));
#267252=CARTESIAN_POINT('Ctrl Pts',(-1.54486530373876,-0.181626249050114,
11.105620308652));
#267253=CARTESIAN_POINT('Ctrl Pts',(-1.54533645842177,-0.177572893029326,
11.105328012022));
#267254=CARTESIAN_POINT('Ctrl Pts',(-1.54652572090355,-0.166978282939704,
11.1045666098808));
#267255=CARTESIAN_POINT('Ctrl Pts',(-1.54721829068781,-0.160434152887472,
11.1040988890746));
#267256=CARTESIAN_POINT('Ctrl Pts',(-1.55165291611642,-0.115828176337331,
11.1009271994944));
#267257=CARTESIAN_POINT('Ctrl Pts',(-1.55403203440442,-0.0776400661746127,
11.0982929362908));
#267258=CARTESIAN_POINT('Ctrl Pts',(-1.55532424691055,-0.026639391096279,
11.0948362395981));
#267259=CARTESIAN_POINT('Ctrl Pts',(-1.5554904855441,-0.0138756730603074,
11.0939762747276));
#267260=CARTESIAN_POINT('Ctrl Pts',(-1.55558217104781,0.114482777279392,
11.085366981832));
#267261=CARTESIAN_POINT('Ctrl Pts',(-1.54277988274089,0.229726903704349,
11.0779273206166));
#267262=CARTESIAN_POINT('Ctrl Pts',(-1.51279541076874,0.362565510575355,
11.0687948979185));
#267263=CARTESIAN_POINT('Ctrl Pts',(-1.50786677741873,0.382545991423653,
11.0674068982995));
#267264=CARTESIAN_POINT('Ctrl Pts',(-1.49229849522005,0.44067403895012,
11.0633178607757));
#267265=CARTESIAN_POINT('Ctrl Pts',(-1.48059747192315,0.478517587256855,
11.060590393756));
#267266=CARTESIAN_POINT('Ctrl Pts',(-1.4638461164133,0.52616913125099,11.0570508059872));
#267267=CARTESIAN_POINT('Ctrl Pts',(-1.4601177091598,0.536428626976604,
11.056282410341));
#267268=CARTESIAN_POINT('Ctrl Pts',(-1.45402424810548,0.552661740583099,
11.0550561429149));
#267269=CARTESIAN_POINT('Ctrl Pts',(-1.45172958267431,0.558661552393764,
11.0546006192035));
#267270=CARTESIAN_POINT('Ctrl Pts',(-1.44754235582564,0.569409787472199,
11.0537803750444));
#267271=CARTESIAN_POINT('Ctrl Pts',(-1.44566341540457,0.57416344902276,
11.0534161160298));
#267272=CARTESIAN_POINT('Ctrl Pts',(-1.44121105649753,0.585267365005433,
11.0525617211079));
#267273=CARTESIAN_POINT('Ctrl Pts',(-1.43861905941743,0.591610004150868,
11.0520709650014));
#267274=CARTESIAN_POINT('Ctrl Pts',(-1.43102437127428,0.609849204723922,
11.05065173194));
#267275=CARTESIAN_POINT('Ctrl Pts',(-1.42591552787011,0.621700645318622,
11.049719681143));
#267276=CARTESIAN_POINT('Ctrl Pts',(-1.38229536757299,0.719523382584035,
11.041942191734));
#267277=CARTESIAN_POINT('Ctrl Pts',(-1.33620236672565,0.801879836687392,
11.0348320434333));
#267278=CARTESIAN_POINT('Ctrl Pts',(-1.22750367541922,0.960433280597649,
11.0200160721238));
#267279=CARTESIAN_POINT('Ctrl Pts',(-1.16452767311637,1.03589252185072,
11.0123310771437));
#267280=CARTESIAN_POINT('Ctrl Pts',(-1.07236398676692,1.12721744724209,
11.0025004534834));
#267281=CARTESIAN_POINT('Ctrl Pts',(-1.04918473712791,1.14882350428654,
11.0001307017482));
#267282=CARTESIAN_POINT('Ctrl Pts',(-1.02067181916037,1.17381776763446,
10.997351212523));
#267283=CARTESIAN_POINT('Ctrl Pts',(-1.01595911612107,1.1778990584566,10.9968960808536));
#267284=CARTESIAN_POINT('Ctrl Pts',(-1.00820100259672,1.1845365313033,10.9961539745183));
#267285=CARTESIAN_POINT('Ctrl Pts',(-1.00517016372617,1.18710951413079,
10.9958658212058));
#267286=CARTESIAN_POINT('Ctrl Pts',(-0.999701081239196,1.19171644254419,
10.9953490674367));
#267287=CARTESIAN_POINT('Ctrl Pts',(-0.997266459579022,1.19375455620573,
10.9951201680369));
#267288=CARTESIAN_POINT('Ctrl Pts',(-0.991920916247426,1.19820174517085,
10.9946200783711));
#267289=CARTESIAN_POINT('Ctrl Pts',(-0.989007456346326,1.20060767044556,
10.994349115658));
#267290=CARTESIAN_POINT('Ctrl Pts',(-0.980664594257101,1.20744620122068,
10.9935776532084));
#267291=CARTESIAN_POINT('Ctrl Pts',(-0.975213866103736,1.21185283577421,
10.9930789788959));
#267292=CARTESIAN_POINT('Ctrl Pts',(-0.938377309305883,1.24122380776167,
10.989743218794));
#267293=CARTESIAN_POINT('Ctrl Pts',(-0.906062629495376,1.26500581859923,
10.9869831292336));
#267294=CARTESIAN_POINT('Ctrl Pts',(-0.768069859748684,1.35855705071681,
10.9757006456318));
#267295=CARTESIAN_POINT('Ctrl Pts',(-0.654993139874641,1.41654402629038,
10.9675940287547));
#267296=CARTESIAN_POINT('Ctrl Pts',(-0.515655655391122,1.46770408175223,
10.9576423940307));
#267297=CARTESIAN_POINT('Ctrl Pts',(-0.495024728406495,1.47479031893277,
10.9561710416941));
#267298=CARTESIAN_POINT('Ctrl Pts',(-0.43719224106788,1.4933041864229,10.952042502575));
#267299=CARTESIAN_POINT('Ctrl Pts',(-0.399703032479088,1.50377242428745,
10.9493612647338));
#267300=CARTESIAN_POINT('Ctrl Pts',(-0.351309944031713,1.51534792011397,
10.9458740173629));
#267301=CARTESIAN_POINT('Ctrl Pts',(-0.340730698574113,1.51776169942081,
10.9451101285128));
#267302=CARTESIAN_POINT('Ctrl Pts',(-0.323863890699692,1.521424829217,10.9438893965402));
#267303=CARTESIAN_POINT('Ctrl Pts',(-0.317592221534729,1.52274637062255,
10.9434348646361));
#267304=CARTESIAN_POINT('Ctrl Pts',(-0.306302687401168,1.52505247801854,
10.9426154723566));
#267305=CARTESIAN_POINT('Ctrl Pts',(-0.301287766335465,1.52605113863509,
10.9422510673386));
#267306=CARTESIAN_POINT('Ctrl Pts',(-0.289522475276183,1.52833379932475,
10.9413951131415));
#267307=CARTESIAN_POINT('Ctrl Pts',(-0.282768387655546,1.52959782360806,
10.94090293629));
#267308=CARTESIAN_POINT('Ctrl Pts',(-0.263213571276487,1.53312355615844,
10.9394755167559));
#267309=CARTESIAN_POINT('Ctrl Pts',(-0.250392860327313,1.53526955905738,
10.9385366360095));
#267310=CARTESIAN_POINT('Ctrl Pts',(-0.138710229148496,1.55252752479783,
10.9303296076239));
#267311=CARTESIAN_POINT('Ctrl Pts',(-0.0386513585304838,1.55823002918866,
10.9227609228349));
#267312=CARTESIAN_POINT('Ctrl Pts',(0.172465863355541,1.54991140647999,
10.9064468286025));
#267313=CARTESIAN_POINT('Ctrl Pts',(0.282901300586441,1.53360346747836,
10.8977099057263));
#267314=CARTESIAN_POINT('Ctrl Pts',(0.405596303157897,1.50176901048146,
10.888277423913));
#267315=CARTESIAN_POINT('Ctrl Pts',(0.420479874414671,1.49766993888031,
10.887138469811));
#267316=CARTESIAN_POINT('Ctrl Pts',(0.440440069687756,1.49185168580223,
10.8856203284504));
#267317=CARTESIAN_POINT('Ctrl Pts',(0.445571776325477,1.49032704526006,
10.8852308531077));
#267318=CARTESIAN_POINT('Ctrl Pts',(0.453638483437051,1.48788501925912,
10.8846200483424));
#267319=CARTESIAN_POINT('Ctrl Pts',(0.456578743310892,1.4869853919244,10.8843977132168));
#267320=CARTESIAN_POINT('Ctrl Pts',(0.462598888173646,1.48512387672494,
10.8839431255458));
#267321=CARTESIAN_POINT('Ctrl Pts',(0.465678452641179,1.48416112316659,
10.8837109335711));
#267322=CARTESIAN_POINT('Ctrl Pts',(0.472972262211009,1.48185594801787,
10.8831617854914));
#267323=CARTESIAN_POINT('Ctrl Pts',(0.477183859976159,1.48050510859362,
10.8828453189205));
#267324=CARTESIAN_POINT('Ctrl Pts',(0.491232995161731,1.47593277196518,
10.8817915451575));
#267325=CARTESIAN_POINT('Ctrl Pts',(0.501044410423555,1.47263095070723,
10.8810587501095));
#267326=CARTESIAN_POINT('Ctrl Pts',(0.590995037240804,1.44135690833052,
10.8743629192792));
#267327=CARTESIAN_POINT('Ctrl Pts',(0.668764723103699,1.40696237549458,
10.868734006899));
#267328=CARTESIAN_POINT('Ctrl Pts',(0.853659543376579,1.30637496902906,
10.8548593246367));
#267329=CARTESIAN_POINT('Ctrl Pts',(0.956283033878582,1.23323493667614,
10.8466693205959));
#267330=CARTESIAN_POINT('Ctrl Pts',(1.05605398054823,1.14211279316921,10.8372912555581));
#267331=CARTESIAN_POINT('Ctrl Pts',(1.06305317632791,1.13560097725169,10.8366252071394));
#267332=CARTESIAN_POINT('Ctrl Pts',(1.07790584279944,1.12152491303635,10.8351937877764));
#267333=CARTESIAN_POINT('Ctrl Pts',(1.08574064998974,1.11394181481536,10.8344276579514));
#267334=CARTESIAN_POINT('Ctrl Pts',(1.09851266645072,1.10131736970719,10.8331599207525));
#267335=CARTESIAN_POINT('Ctrl Pts',(1.10349653823666,1.09632359014344,10.8326603932683));
#267336=CARTESIAN_POINT('Ctrl Pts',(1.11242695528036,1.08725282897042,10.8317564165027));
#267337=CARTESIAN_POINT('Ctrl Pts',(1.11638551674112,1.08318780522391,10.8313525036097));
#267338=CARTESIAN_POINT('Ctrl Pts',(1.12480786157488,1.07444373641828,10.8304861593299));
#267339=CARTESIAN_POINT('Ctrl Pts',(1.12926487047949,1.06975834568157,10.8300234455558));
#267340=CARTESIAN_POINT('Ctrl Pts',(1.14130080463768,1.05694663980147,10.8287621655614));
#267341=CARTESIAN_POINT('Ctrl Pts',(1.14882194752271,1.04876682204764,10.8279611592821));
#267342=CARTESIAN_POINT('Ctrl Pts',(1.1883878531437,1.00479955658845,10.8236773523445));
#267343=CARTESIAN_POINT('Ctrl Pts',(1.21884616070218,0.967626451145882,
10.8201296762553));
#267344=CARTESIAN_POINT('Ctrl Pts',(1.31101578117956,0.843868250753702,
10.8085355798078));
#267345=CARTESIAN_POINT('Ctrl Pts',(1.36558856985246,0.75235531415365,10.8002588317065));
#267346=CARTESIAN_POINT('Ctrl Pts',(1.4188108695178,0.637929180241413,10.7904961005974));
#267347=CARTESIAN_POINT('Ctrl Pts',(1.42687088569456,0.619691121367997,
10.788957519497));
#267348=CARTESIAN_POINT('Ctrl Pts',(1.43457669771236,0.601306867065985,
10.7874266037958));
#267349=CARTESIAN_POINT('',(-1.55549978056836,-0.000826227440647477,10.9559437744364));
#267350=CARTESIAN_POINT('Ctrl Pts',(1.43457668061803,0.601306907849032,
10.6508134549194));
#267351=CARTESIAN_POINT('Ctrl Pts',(1.41619620423421,0.645158396090189,
10.6544831834601));
#267352=CARTESIAN_POINT('Ctrl Pts',(1.39579412672923,0.688193435945673,
10.6581266992052));
#267353=CARTESIAN_POINT('Ctrl Pts',(1.36438025897942,0.747273394627868,
10.66313110101));
#267354=CARTESIAN_POINT('Ctrl Pts',(1.35502484783335,0.764106517541768,
10.664557133452));
#267355=CARTESIAN_POINT('Ctrl Pts',(1.34240944669324,0.785844546997109,
10.6663948398768));
#267356=CARTESIAN_POINT('Ctrl Pts',(1.33943134897283,0.790909880445301,
10.6668227782386));
#267357=CARTESIAN_POINT('Ctrl Pts',(1.33460359699645,0.799015739870661,
10.6675069953127));
#267358=CARTESIAN_POINT('Ctrl Pts',(1.3327721261639,0.802066938659978,10.6677644108619));
#267359=CARTESIAN_POINT('Ctrl Pts',(1.32923864623555,0.807908133224289,
10.6682569032129));
#267360=CARTESIAN_POINT('Ctrl Pts',(1.32753830870945,0.810699062234914,
10.6684920785131));
#267361=CARTESIAN_POINT('Ctrl Pts',(1.32348534594304,0.817304640257065,
10.6690484062855));
#267362=CARTESIAN_POINT('Ctrl Pts',(1.32112498360486,0.821114556534951,
10.6693690562206));
#267363=CARTESIAN_POINT('Ctrl Pts',(1.31317939338839,0.833816764043849,
10.6704375349543));
#267364=CARTESIAN_POINT('Ctrl Pts',(1.30752043314011,0.84266295045385,10.6711807266092));
#267365=CARTESIAN_POINT('Ctrl Pts',(1.27544013593418,0.891710063610714,
10.6753001603434));
#267366=CARTESIAN_POINT('Ctrl Pts',(1.24725167629116,0.930730189131567,
10.678573390205));
#267367=CARTESIAN_POINT('Ctrl Pts',(1.13870618721888,1.06717600073408,10.6902522847122));
#267368=CARTESIAN_POINT('Ctrl Pts',(1.04838333350197,1.15603226635772,10.6983550752257));
#267369=CARTESIAN_POINT('Ctrl Pts',(0.911642673098545,1.26120099364639,
10.7100154772344));
#267370=CARTESIAN_POINT('Ctrl Pts',(0.873736669563318,1.28775146965589,
10.7131890168183));
#267371=CARTESIAN_POINT('Ctrl Pts',(0.825057760966379,1.31870796655941,
10.7172277215283));
#267372=CARTESIAN_POINT('Ctrl Pts',(0.815341442936844,1.32473745666391,
10.7180320394218));
#267373=CARTESIAN_POINT('Ctrl Pts',(0.799866058557581,1.33410600684216,
10.7193107236626));
#267374=CARTESIAN_POINT('Ctrl Pts',(0.794150378480177,1.33751625148603,
10.7197824880266));
#267375=CARTESIAN_POINT('Ctrl Pts',(0.783467090048704,1.34379778564043,
10.7206634307065));
#267376=CARTESIAN_POINT('Ctrl Pts',(0.778505121588518,1.34667848572849,
10.7210722594634));
#267377=CARTESIAN_POINT('Ctrl Pts',(0.767449830053376,1.35301518106417,
10.7219824570715));
#267378=CARTESIAN_POINT('Ctrl Pts',(0.761348901513619,1.35645758099316,
10.7224843036137));
#267379=CARTESIAN_POINT('Ctrl Pts',(0.743520845129856,1.3663587532309,10.7239496227149));
#267380=CARTESIAN_POINT('Ctrl Pts',(0.731733590657187,1.37270733266515,
10.7249169800991));
#267381=CARTESIAN_POINT('Ctrl Pts',(0.704910433859287,1.3867105560066,10.7271156282808));
#267382=CARTESIAN_POINT('Ctrl Pts',(0.689829203029044,1.39427418944725,
10.7283499498588));
#267383=CARTESIAN_POINT('Ctrl Pts',(0.640219855864595,1.41815268420438,
10.7324052391445));
#267384=CARTESIAN_POINT('Ctrl Pts',(0.605215845889956,1.43344056071235,
10.7352592707501));
#267385=CARTESIAN_POINT('Ctrl Pts',(0.495389114658614,1.47666693979708,
10.7441894641905));
#267386=CARTESIAN_POINT('Ctrl Pts',(0.418955618688625,1.50014320523994,
10.7503773161104));
#267387=CARTESIAN_POINT('Ctrl Pts',(0.323987695278868,1.52148566292954,
10.75792399371));
#267388=CARTESIAN_POINT('Ctrl Pts',(0.306845677700836,1.52503520927365,
10.7592802964974));
#267389=CARTESIAN_POINT('Ctrl Pts',(0.222367522555693,1.54104577788857,
10.7659275088472));
#267390=CARTESIAN_POINT('Ctrl Pts',(0.154309765543913,1.54934192275926,
10.771171496261));
#267391=CARTESIAN_POINT('Ctrl Pts',(0.0778710378401672,1.55357050533948,
10.7767980922308));
#267392=CARTESIAN_POINT('Ctrl Pts',(0.069819771137083,1.55395315908165,
10.7773874525756));
#267393=CARTESIAN_POINT('Ctrl Pts',(0.057688532344503,1.5544352455154,10.7782701666098));
#267394=CARTESIAN_POINT('Ctrl Pts',(0.0536107142970978,1.5545812270859,
10.7785659816501));
#267395=CARTESIAN_POINT('Ctrl Pts',(0.04631493491922,1.55481366690318,10.7790935665395));
#267396=CARTESIAN_POINT('Ctrl Pts',(0.0430972478866489,1.55490618362709,
10.7793256653622));
#267397=CARTESIAN_POINT('Ctrl Pts',(0.0360933107500557,1.55508580640662,
10.779829598358));
#267398=CARTESIAN_POINT('Ctrl Pts',(0.0323070271114213,1.55516907415071,
10.7801012169415));
#267399=CARTESIAN_POINT('Ctrl Pts',(0.0216060525305109,1.55536531177897,
10.7808667017652));
#267400=CARTESIAN_POINT('Ctrl Pts',(0.0146907420575159,1.55544600081099,
10.7813588146593));
#267401=CARTESIAN_POINT('Ctrl Pts',(-0.0289771161113971,1.55566427131,10.7844514434209));
#267402=CARTESIAN_POINT('Ctrl Pts',(-0.0657279399814517,1.55454539425717,
10.7869876301598));
#267403=CARTESIAN_POINT('Ctrl Pts',(-0.155184050603876,1.54864314198138,
10.7930740252757));
#267404=CARTESIAN_POINT('Ctrl Pts',(-0.207751720116059,1.54247128097895,
10.796577285723));
#267405=CARTESIAN_POINT('Ctrl Pts',(-0.384102111429581,1.51258504509691,
10.8083702762409));
#267406=CARTESIAN_POINT('Ctrl Pts',(-0.505265310789401,1.47653324469058,
10.816584091007));
#267407=CARTESIAN_POINT('Ctrl Pts',(-0.637115133483651,1.41914871414357,
10.8265641689815));
#267408=CARTESIAN_POINT('Ctrl Pts',(-0.653355044431452,1.41174569468414,
10.8278116380983));
#267409=CARTESIAN_POINT('Ctrl Pts',(-0.676022702163713,1.40093767222303,
10.8295804468908));
#267410=CARTESIAN_POINT('Ctrl Pts',(-0.682559881241098,1.39776430795671,
10.8300938323111));
#267411=CARTESIAN_POINT('Ctrl Pts',(-0.693904235807884,1.39215882114782,
10.8309905847092));
#267412=CARTESIAN_POINT('Ctrl Pts',(-0.698721498509973,1.38974729284195,
10.8313732321887));
#267413=CARTESIAN_POINT('Ctrl Pts',(-0.708667277923455,1.38470363921932,
10.8321671459282));
#267414=CARTESIAN_POINT('Ctrl Pts',(-0.71379387648419,1.38206793592603,
10.8325785327186));
#267415=CARTESIAN_POINT('Ctrl Pts',(-0.725868218104618,1.37577513599158,
10.8335526302688));
#267416=CARTESIAN_POINT('Ctrl Pts',(-0.732803098461349,1.37209384138383,
10.8341161865886));
#267417=CARTESIAN_POINT('Ctrl Pts',(-0.747448672841228,1.36417672069205,
10.835315176103));
#267418=CARTESIAN_POINT('Ctrl Pts',(-0.755151868301836,1.35992767958414,
10.8359510643873));
#267419=CARTESIAN_POINT('Ctrl Pts',(-0.776007003449739,1.34819226909533,
10.8376871758941));
#267420=CARTESIAN_POINT('Ctrl Pts',(-0.789086095040736,1.34057911688083,
10.838791871823));
#267421=CARTESIAN_POINT('Ctrl Pts',(-0.830058397803283,1.31592239523502,
10.8423040084776));
#267422=CARTESIAN_POINT('Ctrl Pts',(-0.857524971854549,1.29819079262242,
10.8447353642989));
#267423=CARTESIAN_POINT('Ctrl Pts',(-0.977590337987496,1.21520671318003,
10.8557146768537));
#267424=CARTESIAN_POINT('Ctrl Pts',(-1.06344862377193,1.14082484694671,
10.8645642374876));
#267425=CARTESIAN_POINT('Ctrl Pts',(-1.18253181884092,1.0124359648641,10.878074107562));
#267426=CARTESIAN_POINT('Ctrl Pts',(-1.22186727572909,0.964598587834279,
10.882794261092));
#267427=CARTESIAN_POINT('Ctrl Pts',(-1.26295003261908,0.908075608173471,
10.8879291829592));
#267428=CARTESIAN_POINT('Ctrl Pts',(-1.26759811018072,0.901575916603189,
10.8885133850766));
#267429=CARTESIAN_POINT('Ctrl Pts',(-1.27453536002879,0.891715422511863,
10.8893899022158));
#267430=CARTESIAN_POINT('Ctrl Pts',(-1.27686168479867,0.888381121829058,
10.8896846289766));
#267431=CARTESIAN_POINT('Ctrl Pts',(-1.28100591737691,0.882391322119793,
10.8902110514531));
#267432=CARTESIAN_POINT('Ctrl Pts',(-1.28282867426031,0.879739278912409,
10.8904430698793));
#267433=CARTESIAN_POINT('Ctrl Pts',(-1.28678506910476,0.873944428817586,
10.8909477306516));
#267434=CARTESIAN_POINT('Ctrl Pts',(-1.28891542699547,0.870799461196348,
10.8912201523769));
#267435=CARTESIAN_POINT('Ctrl Pts',(-1.29492122314751,0.861863002509983,
10.8919901923896));
#267436=CARTESIAN_POINT('Ctrl Pts',(-1.29876936068532,0.856053130275553,
10.8924860240214));
#267437=CARTESIAN_POINT('Ctrl Pts',(-1.32326487319759,0.818524700312995,
10.8956594763472));
#267438=CARTESIAN_POINT('Ctrl Pts',(-1.34278994909062,0.786084190293236,
10.8982688178962));
#267439=CARTESIAN_POINT('Ctrl Pts',(-1.4308626495039,0.626876648683413,
10.9106078912675));
#267440=CARTESIAN_POINT('Ctrl Pts',(-1.48275758416514,0.491709700680271,
10.9197701759167));
#267441=CARTESIAN_POINT('Ctrl Pts',(-1.52401123281862,0.313776118444744,
10.9321330785903));
#267442=CARTESIAN_POINT('Ctrl Pts',(-1.5313170344172,0.275922870364973,
10.9347746967179));
#267443=CARTESIAN_POINT('Ctrl Pts',(-1.53949692490965,0.223054491725705,
10.93850249068));
#267444=CARTESIAN_POINT('Ctrl Pts',(-1.5415710276318,0.208237430823827,
10.9395513283463));
#267445=CARTESIAN_POINT('Ctrl Pts',(-1.54434140756813,0.186127602853223,
10.9411234913082));
#267446=CARTESIAN_POINT('Ctrl Pts',(-1.54520046363276,0.178855784234435,
10.9416417062508));
#267447=CARTESIAN_POINT('Ctrl Pts',(-1.5466163139368,0.166098248394197,
10.9425529684043));
#267448=CARTESIAN_POINT('Ctrl Pts',(-1.54719534759494,0.160615085230751,
10.9429453107873));
#267449=CARTESIAN_POINT('Ctrl Pts',(-1.5482816790177,0.149776595957513,
10.9437222515601));
#267450=CARTESIAN_POINT('Ctrl Pts',(-1.54879037307705,0.144421484556476,
10.9441068003859));
#267451=CARTESIAN_POINT('Ctrl Pts',(-1.54982941478438,0.13284581735533,
10.9449395534471));
#267452=CARTESIAN_POINT('Ctrl Pts',(-1.55035010782426,0.126624512560305,
10.9453880537738));
#267453=CARTESIAN_POINT('Ctrl Pts',(-1.55152314351844,0.1115150612476,10.9464796663673));
#267454=CARTESIAN_POINT('Ctrl Pts',(-1.55213657237751,0.102624209138309,
10.9471239819166));
#267455=CARTESIAN_POINT('Ctrl Pts',(-1.55457598776545,0.0622138129656635,
10.9500618284598));
#267456=CARTESIAN_POINT('Ctrl Pts',(-1.55551832872089,0.0306508940191186,
10.9523824318058));
#267457=CARTESIAN_POINT('Ctrl Pts',(-1.55549973002184,-0.000916461665043444,
10.954730847374));
#267458=CARTESIAN_POINT('Ctrl Pts',(-1.55549978056836,-0.000826227440647477,
10.9559437744364));
#267459=CARTESIAN_POINT('Ctrl Pts',(-1.55546565861298,-0.0650660378110669,
10.9605241758682));
#267460=CARTESIAN_POINT('Ctrl Pts',(-1.55144787772679,-0.129166249084525,
10.9651045773));
#267461=CARTESIAN_POINT('Ctrl Pts',(-1.54352279076948,-0.19265939991392,
10.9696849787318));
#267462=CARTESIAN_POINT('Ctrl Pts',(-1.53556587820097,-0.256407526914957,
10.9742837741668));
#267463=CARTESIAN_POINT('Ctrl Pts',(-1.52367036163636,-0.319543413071712,
10.9788825696018));
#267464=CARTESIAN_POINT('Ctrl Pts',(-1.50796326206369,-0.381611124400532,
10.9834813650368));
#267465=CARTESIAN_POINT('Ctrl Pts',(-1.49217853217136,-0.443985597410511,
10.9881028894269));
#267466=CARTESIAN_POINT('Ctrl Pts',(-1.47254460406452,-0.505281027035107,
10.9927244138169));
#267467=CARTESIAN_POINT('Ctrl Pts',(-1.44923826450197,-0.565056371261592,
10.997345938207));
#267468=CARTESIAN_POINT('Ctrl Pts',(-1.44472395673645,-0.576634521485644,
10.9982411016618));
#267469=CARTESIAN_POINT('Ctrl Pts',(-1.44007200844342,-0.588155714178932,
10.9991362651166));
#267470=CARTESIAN_POINT('Ctrl Pts',(-1.43528390274065,-0.599616851442292,
11.0000314285715));
#267471=CARTESIAN_POINT('Ctrl Pts',(-1.41309670781834,-0.652725638565867,
11.0041794502094));
#267472=CARTESIAN_POINT('Ctrl Pts',(-1.38791123557696,-0.704712790082137,
11.0083274718473));
#267473=CARTESIAN_POINT('Ctrl Pts',(-1.35986268358359,-0.755217671798561,
11.0124754934853));
#267474=CARTESIAN_POINT('Ctrl Pts',(-1.33186400318891,-0.805632753542662,
11.0166161397525));
#267475=CARTESIAN_POINT('Ctrl Pts',(-1.30101259808066,-0.854570345106836,
11.0207567860196));
#267476=CARTESIAN_POINT('Ctrl Pts',(-1.2674912840762,-0.901690686871537,
11.0248974322868));
#267477=CARTESIAN_POINT('Ctrl Pts',(-1.23400331523107,-0.948764155912103,
11.0290339596668));
#267478=CARTESIAN_POINT('Ctrl Pts',(-1.1978509999251,-0.994023534493074,
11.0331704870468));
#267479=CARTESIAN_POINT('Ctrl Pts',(-1.15926163198756,-1.03715607244115,
11.0373070144269));
#267480=CARTESIAN_POINT('Ctrl Pts',(-1.12069581533763,-1.08026228638183,
11.0414410172632));
#267481=CARTESIAN_POINT('Ctrl Pts',(-1.07969624093573,-1.12124384537538,
11.0455750200995));
#267482=CARTESIAN_POINT('Ctrl Pts',(-1.03653046940682,-1.15982103619105,
11.0497090229358));
#267483=CARTESIAN_POINT('Ctrl Pts',(-0.993374448377873,-1.19838951299827,
11.0538420919629));
#267484=CARTESIAN_POINT('Ctrl Pts',(-0.948053589772702,-1.23455435295824,
11.05797516099));
#267485=CARTESIAN_POINT('Ctrl Pts',(-0.900870680298012,-1.26807423575254,
11.0621082300171));
#267486=CARTESIAN_POINT('Ctrl Pts',(-0.853645123206089,-1.30162441644808,
11.0662450348364));
#267487=CARTESIAN_POINT('Ctrl Pts',(-0.80455457673083,-1.33252455904199,
11.0703818396558));
#267488=CARTESIAN_POINT('Ctrl Pts',(-0.753932043950639,-1.36057587921601,
11.0745186444751));
#267489=CARTESIAN_POINT('Ctrl Pts',(-0.703288596590755,-1.38863878872661,
11.0786571584055));
#267490=CARTESIAN_POINT('Ctrl Pts',(-0.651112370525066,-1.41385030117597,
11.082795672336));
#267491=CARTESIAN_POINT('Ctrl Pts',(-0.597759394860077,-1.43605847926069,
11.0869341862665));
#267492=CARTESIAN_POINT('Ctrl Pts',(-0.544302397442401,-1.45830995640379,
11.0910807690153));
#267493=CARTESIAN_POINT('Ctrl Pts',(-0.489664558226208,-1.47754622284655,
11.0952273517642));
#267494=CARTESIAN_POINT('Ctrl Pts',(-0.434219362892345,-1.49366455233073,
11.0993739345131));
#267495=CARTESIAN_POINT('Ctrl Pts',(-0.381764104060325,-1.50891368509943,
11.103296908723));
#267496=CARTESIAN_POINT('Ctrl Pts',(-0.328586705854618,-1.52137244781314,
11.107219882933));
#267497=CARTESIAN_POINT('Ctrl Pts',(-0.27500985724936,-1.53099635153572,
11.1111428571429));
#267498=CARTESIAN_POINT('Ctrl Pts',(-0.2183594906108,-1.54117234524515,
11.1152908787808));
#267499=CARTESIAN_POINT('Ctrl Pts',(-0.161024631712135,-1.54822116712312,
11.1194389004188));
#267500=CARTESIAN_POINT('Ctrl Pts',(-0.103381573792702,-1.55206072696919,
11.1235869220567));
#267501=CARTESIAN_POINT('Ctrl Pts',(-0.0458410078468976,-1.55589345990357,
11.1277275683239));
#267502=CARTESIAN_POINT('Ctrl Pts',(0.0120061540690754,-1.55652822247625,
11.1318682145911));
#267503=CARTESIAN_POINT('Ctrl Pts',(0.0697753189408187,-1.55393425049669,
11.1360088608582));
#267504=CARTESIAN_POINT('Ctrl Pts',(0.127487018224909,-1.55134285885777,
11.1401453882382));
#267505=CARTESIAN_POINT('Ctrl Pts',(0.185120356531842,-1.5455291193456,
11.1442819156183));
#267506=CARTESIAN_POINT('Ctrl Pts',(0.242289298251249,-1.53651428433091,
11.1484184429983));
#267507=CARTESIAN_POINT('Ctrl Pts',(0.299423349474618,-1.5275049511159,
11.1525524458346));
#267508=CARTESIAN_POINT('Ctrl Pts',(0.356093052529829,-1.51529847601814,
11.1566864486709));
#267509=CARTESIAN_POINT('Ctrl Pts',(0.411918277242572,-1.49996786061352,
11.1608204515072));
#267510=CARTESIAN_POINT('Ctrl Pts',(0.467730891874893,-1.48464070816484,
11.1649535205343));
#267511=CARTESIAN_POINT('Ctrl Pts',(0.522698904886622,-1.46619095424824,
11.1690865895614));
#267512=CARTESIAN_POINT('Ctrl Pts',(0.576455325509742,-1.44474202115515,
11.1732196585885));
#267513=CARTESIAN_POINT('Ctrl Pts',(0.630260335405474,-1.42327370083267,
11.1773564634079));
#267514=CARTESIAN_POINT('Ctrl Pts',(0.682851079059476,-1.39880097627071,
11.1814932682272));
#267515=CARTESIAN_POINT('Ctrl Pts',(0.733879903405016,-1.37149572998907,
11.1856300730465));
#267516=CARTESIAN_POINT('Ctrl Pts',(0.784929810188654,-1.3441792026095,
11.189768586977));
#267517=CARTESIAN_POINT('Ctrl Pts',(0.834416064806619,-1.31402809101586,
11.1939071009074));
#267518=CARTESIAN_POINT('Ctrl Pts',(0.882017874341116,-1.28125903678483,
11.1980456148379));
#267519=CARTESIAN_POINT('Ctrl Pts',(0.929712492638306,-1.24842609306287,
11.2021921975868));
#267520=CARTESIAN_POINT('Ctrl Pts',(0.975514909601415,-1.21296532571064,
11.2063387803356));
#267521=CARTESIAN_POINT('Ctrl Pts',(1.01913619998497,-1.17513473945765,
11.2104853630845));
#267522=CARTESIAN_POINT('Ctrl Pts',(1.06040516952995,-1.13934420464734,
11.2144083372944));
#267523=CARTESIAN_POINT('Ctrl Pts',(1.0997219438703,-1.10143315475768,11.2183313115044));
#267524=CARTESIAN_POINT('Ctrl Pts',(1.13687407815269,-1.06164852019134,
11.2222542857143));
#267525=CARTESIAN_POINT('Ctrl Pts',(1.17615750155851,-1.01958157908816,
11.2264023073522));
#267526=CARTESIAN_POINT('Ctrl Pts',(1.21318538180509,-0.975243017775855,
11.2305503289902));
#267527=CARTESIAN_POINT('Ctrl Pts',(1.24768460527871,-0.928904395376887,
11.2346983506281));
#267528=CARTESIAN_POINT('Ctrl Pts',(1.28212248756693,-0.882648165152056,
11.2388389968953));
#267529=CARTESIAN_POINT('Ctrl Pts',(1.31404032867007,-0.834399346673556,
11.2429796431625));
#267530=CARTESIAN_POINT('Ctrl Pts',(1.34320362724052,-0.78446431771491,
11.2471202894296));
#267531=CARTESIAN_POINT('Ctrl Pts',(1.37233791576565,-0.734578961376423,
11.2512568168096));
#267532=CARTESIAN_POINT('Ctrl Pts',(1.39872282929431,-0.683011165324985,
11.2553933441897));
#267533=CARTESIAN_POINT('Ctrl Pts',(1.42216677914759,-0.630096740420842,
11.2595298715697));
#267534=CARTESIAN_POINT('Ctrl Pts',(1.44559642103898,-0.577214609459475,
11.263663874406));
#267535=CARTESIAN_POINT('Ctrl Pts',(1.46608844667386,-0.522987953983979,
11.2677978772423));
#267536=CARTESIAN_POINT('Ctrl Pts',(1.48349794208529,-0.467775700340131,
11.2719318800786));
#267537=CARTESIAN_POINT('Ctrl Pts',(1.500903504953,-0.412575918315756,11.2760649491057));
#267538=CARTESIAN_POINT('Ctrl Pts',(1.51522776338046,-0.356391476567678,
11.2801980181328));
#267539=CARTESIAN_POINT('Ctrl Pts',(1.52637528689117,-0.299597619429611,
11.2843310871599));
#267540=CARTESIAN_POINT('Ctrl Pts',(1.53753288640867,-0.242752427545375,
11.2884678919793));
#267541=CARTESIAN_POINT('Ctrl Pts',(1.54550791113036,-0.185297231555324,
11.2926046967986));
#267542=CARTESIAN_POINT('Ctrl Pts',(1.55025613005402,-0.127617323392752,
11.2967415016179));
#267543=CARTESIAN_POINT('Ctrl Pts',(1.5550063106931,-0.0699135849125411,
11.3008800155484));
#267544=CARTESIAN_POINT('Ctrl Pts',(1.55652701283117,-0.0119854709137854,
11.3050185294789));
#267545=CARTESIAN_POINT('Ctrl Pts',(1.55482617711243,0.0457800061812131,
11.3091570434093));
#267546=CARTESIAN_POINT('Ctrl Pts',(1.55312202529163,0.103658108037933,
11.3133036261582));
#267547=CARTESIAN_POINT('Ctrl Pts',(1.54818382720234,0.161372418399441,
11.317450208907));
#267548=CARTESIAN_POINT('Ctrl Pts',(1.54007155928367,0.218540253238526,
11.3215967916559));
#267549=CARTESIAN_POINT('Ctrl Pts',(1.53239675336362,0.272625256551814,
11.3255197658659));
#267550=CARTESIAN_POINT('Ctrl Pts',(1.52188150498649,0.326220834726039,
11.3294427400758));
#267551=CARTESIAN_POINT('Ctrl Pts',(1.50861798182058,0.379014557672403,
11.3333657142857));
#267552=CARTESIAN_POINT('Ctrl Pts',(1.49459539648248,0.434829628530324,
11.3375131975713));
#267553=CARTESIAN_POINT('Ctrl Pts',(1.4774416706778,0.489982606874012,11.3416606808568));
#267554=CARTESIAN_POINT('Ctrl Pts',(1.45723671095245,0.544096883149017,
11.3458081641423));
#267555=CARTESIAN_POINT('Ctrl Pts',(1.45006554835835,0.563303171065727,
11.3472801926641));
#267556=CARTESIAN_POINT('Ctrl Pts',(1.4425104980916,0.582378687427456,11.3487522211859));
#267557=CARTESIAN_POINT('Ctrl Pts',(1.43457668357355,0.601306900797849,
11.3502242497077));
#267558=CARTESIAN_POINT('Origin',(0.,0.,-1.29405622560371));
#267559=CARTESIAN_POINT('',(1.4345767274609,0.601306796092946,12.1885981050115));
#267560=CARTESIAN_POINT('',(1.43231976391824,0.600353038565383,12.0501913886179));
#267561=CARTESIAN_POINT('',(1.43457668357355,0.601306900797845,-1.29405622560371));
#267562=CARTESIAN_POINT('',(-1.55549949371246,0.00125501405145053,11.7935273087615));
#267563=CARTESIAN_POINT('Ctrl Pts',(1.43457672746074,0.601306796093334,
12.1885981050115));
#267564=CARTESIAN_POINT('Ctrl Pts',(1.45158204059095,0.56073611467368,12.1856920715499));
#267565=CARTESIAN_POINT('Ctrl Pts',(1.46687680900277,0.519419120084027,
12.1827654785763));
#267566=CARTESIAN_POINT('Ctrl Pts',(1.49549833502048,0.430675741285502,
12.1764757733554));
#267567=CARTESIAN_POINT('Ctrl Pts',(1.50835993112976,0.383205376732718,
12.1731087244595));
#267568=CARTESIAN_POINT('Ctrl Pts',(1.52144025862211,0.323933824353823,
12.1688601916985));
#267569=CARTESIAN_POINT('Ctrl Pts',(1.52380293781175,0.312631055912539,
12.168048123122));
#267570=CARTESIAN_POINT('Ctrl Pts',(1.527323859471,0.294798308515377,12.1667634352161));
#267571=CARTESIAN_POINT('Ctrl Pts',(1.52856658848981,0.288285269302204,
12.1662935073094));
#267572=CARTESIAN_POINT('Ctrl Pts',(1.53078339948072,0.27624966941998,12.1654236909974));
#267573=CARTESIAN_POINT('Ctrl Pts',(1.5317693356534,0.270729379308468,12.1650241863763));
#267574=CARTESIAN_POINT('Ctrl Pts',(1.53388841843068,0.258482306658949,
12.1641365802209));
#267575=CARTESIAN_POINT('Ctrl Pts',(1.53500720214617,0.25175319197037,12.1636480320448));
#267576=CARTESIAN_POINT('Ctrl Pts',(1.53809174235351,0.232415329622212,
12.1622414807255));
#267577=CARTESIAN_POINT('Ctrl Pts',(1.53994660646182,0.219789727999229,
12.1613200021437));
#267578=CARTESIAN_POINT('Ctrl Pts',(1.55325386263287,0.120751532516686,
12.1540652905653));
#267579=CARTESIAN_POINT('Ctrl Pts',(1.55757745999443,0.0335535934348645,
12.1475073349953));
#267580=CARTESIAN_POINT('Ctrl Pts',(1.55140191647346,-0.145780576912626,
12.1337143431608));
#267581=CARTESIAN_POINT('Ctrl Pts',(1.54002114670295,-0.237559200622337,
12.1264887818188));
#267582=CARTESIAN_POINT('Ctrl Pts',(1.51674661293645,-0.345527624136952,
12.1180440353607));
#267583=CARTESIAN_POINT('Ctrl Pts',(1.512611826786,-0.363201236993375,12.1166640550951));
#267584=CARTESIAN_POINT('Ctrl Pts',(1.50152803910009,-0.407098978642287,
12.113248257347));
#267585=CARTESIAN_POINT('Ctrl Pts',(1.49420019446831,-0.433222860636483,
12.1112260707693));
#267586=CARTESIAN_POINT('Ctrl Pts',(1.48427072885522,-0.465363330377416,
12.1087620280064));
#267587=CARTESIAN_POINT('Ctrl Pts',(1.48231017142485,-0.471570976102156,
12.1082872406096));
#267588=CARTESIAN_POINT('Ctrl Pts',(1.47917134528659,-0.481296312540366,
12.1075453632342));
#267589=CARTESIAN_POINT('Ctrl Pts',(1.47801939612779,-0.484822312434049,
12.1072767953699));
#267590=CARTESIAN_POINT('Ctrl Pts',(1.47585614512653,-0.491364435052166,
12.1067792939064));
#267591=CARTESIAN_POINT('Ctrl Pts',(1.47484821326013,-0.494381550339857,
12.1065501761354));
#267592=CARTESIAN_POINT('Ctrl Pts',(1.47253101675,-0.501247625872965,12.1060294835219));
#267593=CARTESIAN_POINT('Ctrl Pts',(1.47121591472639,-0.505094556499425,
12.1057382558047));
#267594=CARTESIAN_POINT('Ctrl Pts',(1.46713426563989,-0.51688298107644,
12.1048472520649));
#267595=CARTESIAN_POINT('Ctrl Pts',(1.46431832670959,-0.524807408475454,
12.1042502918418));
#267596=CARTESIAN_POINT('Ctrl Pts',(1.42882683372046,-0.622175085968407,
12.0969354181743));
#267597=CARTESIAN_POINT('Ctrl Pts',(1.38806298754657,-0.708473954905476,
12.0906540911223));
#267598=CARTESIAN_POINT('Ctrl Pts',(1.27999483179161,-0.891613013130005,
12.0766529068945));
#267599=CARTESIAN_POINT('Ctrl Pts',(1.20909331202946,-0.985621329517202,
12.0689615847856));
#267600=CARTESIAN_POINT('Ctrl Pts',(1.11567365197953,-1.08406132597586,
12.059548017591));
#267601=CARTESIAN_POINT('Ctrl Pts',(1.10281419048869,-1.09714058715052,
12.0582664915187));
#267602=CARTESIAN_POINT('Ctrl Pts',(1.08451914954465,-1.11510166583624,
12.0564609634516));
#267603=CARTESIAN_POINT('Ctrl Pts',(1.0792755318422,-1.12017759037847,12.0559454456617));
#267604=CARTESIAN_POINT('Ctrl Pts',(1.07012639839581,-1.1289102549915,12.0550492329253));
#267605=CARTESIAN_POINT('Ctrl Pts',(1.06623734177724,-1.13258412582228,
12.0546692836316));
#267606=CARTESIAN_POINT('Ctrl Pts',(1.0581051801526,-1.14018731827884,12.0538768278583));
#267607=CARTESIAN_POINT('Ctrl Pts',(1.05385896777574,-1.14411317945634,
12.0534641822785));
#267608=CARTESIAN_POINT('Ctrl Pts',(1.04378462695974,-1.15332380435742,
12.0524877582621));
#267609=CARTESIAN_POINT('Ctrl Pts',(1.03793814955025,-1.15858816611638,
12.0519231324301));
#267610=CARTESIAN_POINT('Ctrl Pts',(1.01841055371683,-1.17590502458872,
12.0500437070847));
#267611=CARTESIAN_POINT('Ctrl Pts',(1.00455794571759,-1.18776090351007,
12.0487208354279));
#267612=CARTESIAN_POINT('Ctrl Pts',(0.971178085517181,-1.21532768558087,
12.0455560488411));
#267613=CARTESIAN_POINT('Ctrl Pts',(0.951473759381031,-1.23081510007813,
12.0437057400017));
#267614=CARTESIAN_POINT('Ctrl Pts',(0.810956354033189,-1.33586936761816,
12.0306297007018));
#267615=CARTESIAN_POINT('Ctrl Pts',(0.678090337225914,-1.40796866756557,
12.0187571993409));
#267616=CARTESIAN_POINT('Ctrl Pts',(0.499803415034939,-1.47354912648907,
12.0042721454798));
#267617=CARTESIAN_POINT('Ctrl Pts',(0.46210021024975,-1.4858043403824,12.0012908798576));
#267618=CARTESIAN_POINT('Ctrl Pts',(0.417566453962252,-1.49842008525386,
11.9978944336353));
#267619=CARTESIAN_POINT('Ctrl Pts',(0.411154858918472,-1.50019204823291,
11.9974084291805));
#267620=CARTESIAN_POINT('Ctrl Pts',(0.400771283344013,-1.50299017109325,
11.9966263804856));
#267621=CARTESIAN_POINT('Ctrl Pts',(0.396806355850358,-1.50404181888666,
11.9963289405809));
#267622=CARTESIAN_POINT('Ctrl Pts',(0.389756246341952,-1.50588195345002,
11.9958022111291));
#267623=CARTESIAN_POINT('Ctrl Pts',(0.386672761823889,-1.50667666247869,
11.9955725698963));
#267624=CARTESIAN_POINT('Ctrl Pts',(0.380016490173102,-1.50837040856132,
11.9950784358204));
#267625=CARTESIAN_POINT('Ctrl Pts',(0.376442946894745,-1.5092662226142,
11.9948141290924));
#267626=CARTESIAN_POINT('Ctrl Pts',(0.366485884725922,-1.51172468938218,
11.9940803176299));
#267627=CARTESIAN_POINT('Ctrl Pts',(0.360095493960803,-1.51325962066001,
11.9936123689661));
#267628=CARTESIAN_POINT('Ctrl Pts',(0.323021315754391,-1.52191644977286,
11.9909139031385));
#267629=CARTESIAN_POINT('Ctrl Pts',(0.292133916195586,-1.52814612673749,
11.9887305008976));
#267630=CARTESIAN_POINT('Ctrl Pts',(0.117250866611674,-1.55792096940701,
11.9766204561852));
#267631=CARTESIAN_POINT('Ctrl Pts',(-0.0293126270151572,-1.56205465328092,
11.9673618405338));
#267632=CARTESIAN_POINT('Ctrl Pts',(-0.223339881178667,-1.5401731539439,
11.9541926636323));
#267633=CARTESIAN_POINT('Ctrl Pts',(-0.272067078029229,-1.53231612997555,
11.9508140042706));
#267634=CARTESIAN_POINT('Ctrl Pts',(-0.331646544503724,-1.51977775977022,
11.9465524758041));
#267635=CARTESIAN_POINT('Ctrl Pts',(-0.342931000125702,-1.51727129610168,
11.9457395465846));
#267636=CARTESIAN_POINT('Ctrl Pts',(-0.360645349920121,-1.51312893814528,
11.9444537938638));
#267637=CARTESIAN_POINT('Ctrl Pts',(-0.36709467127881,-1.51157723974608,
11.9439836692483));
#267638=CARTESIAN_POINT('Ctrl Pts',(-0.378977260688168,-1.50863777317442,
11.94311366523));
#267639=CARTESIAN_POINT('Ctrl Pts',(-0.384413352792178,-1.50726177801037,
11.9427141707757));
#267640=CARTESIAN_POINT('Ctrl Pts',(-0.39644254662691,-1.50414761472061,
11.9418268051065));
#267641=CARTESIAN_POINT('Ctrl Pts',(-0.403031866176009,-1.50239543787667,
11.9413384885164));
#267642=CARTESIAN_POINT('Ctrl Pts',(-0.421905386813321,-1.49724365156291,
11.9399332645514));
#267643=CARTESIAN_POINT('Ctrl Pts',(-0.434159346805522,-1.49373637271134,
11.9390128919615));
#267644=CARTESIAN_POINT('Ctrl Pts',(-0.50412808035066,-1.47277651889407,
11.9337103078438));
#267645=CARTESIAN_POINT('Ctrl Pts',(-0.560824812037048,-1.45213275769606,
11.9292248993702));
#267646=CARTESIAN_POINT('Ctrl Pts',(-0.736672458551097,-1.37626893498022,
11.9146979491392));
#267647=CARTESIAN_POINT('Ctrl Pts',(-0.850092936226315,-1.30925151295815,
11.9043396242968));
#267648=CARTESIAN_POINT('Ctrl Pts',(-0.979530552695255,-1.20878670771401,
11.8919146289656));
#267649=CARTESIAN_POINT('Ctrl Pts',(-1.0046788888164,-1.18796722702655,
11.8894713610034));
#267650=CARTESIAN_POINT('Ctrl Pts',(-1.03387257401732,-1.16220795157377,
11.8866169625753));
#267651=CARTESIAN_POINT('Ctrl Pts',(-1.03856433069995,-1.15801725228821,
11.8861576538563));
#267652=CARTESIAN_POINT('Ctrl Pts',(-1.0461923680452,-1.15112020313484,
11.8854101312503));
#267653=CARTESIAN_POINT('Ctrl Pts',(-1.04914381880209,-1.14843086054787,
11.8851207102606));
#267654=CARTESIAN_POINT('Ctrl Pts',(-1.05442426453674,-1.14358200726755,
11.8846026190701));
#267655=CARTESIAN_POINT('Ctrl Pts',(-1.05675701877295,-1.14142671288253,
11.8843736426868));
#267656=CARTESIAN_POINT('Ctrl Pts',(-1.06129282473143,-1.13721013527475,
11.8839282317697));
#267657=CARTESIAN_POINT('Ctrl Pts',(-1.06349646771223,-1.13514960035315,
11.8837117442681));
#267658=CARTESIAN_POINT('Ctrl Pts',(-1.06984292218618,-1.1291805924429,
11.8830879467235));
#267659=CARTESIAN_POINT('Ctrl Pts',(-1.07397034085452,-1.12525570345684,
11.8826818672655));
#267660=CARTESIAN_POINT('Ctrl Pts',(-1.09331004413161,-1.10666164108773,
11.8807767078342));
#267661=CARTESIAN_POINT('Ctrl Pts',(-1.10824484635721,-1.09170523433954,
11.8792984012521));
#267662=CARTESIAN_POINT('Ctrl Pts',(-1.14984497320157,-1.04831105564144,
11.8751432625112));
#267663=CARTESIAN_POINT('Ctrl Pts',(-1.17575386580629,-1.01916773046994,
11.8725096059014));
#267664=CARTESIAN_POINT('Ctrl Pts',(-1.2359450804774,-0.946107782794096,
11.8661877984875));
#267665=CARTESIAN_POINT('Ctrl Pts',(-1.26901637162586,-0.901264703617742,
11.8625349099386));
#267666=CARTESIAN_POINT('Ctrl Pts',(-1.35490827479823,-0.770668540126365,
11.8522449840749));
#267667=CARTESIAN_POINT('Ctrl Pts',(-1.40190742087495,-0.681438298097991,
11.8455890219725));
#267668=CARTESIAN_POINT('Ctrl Pts',(-1.44702596352617,-0.571003745377852,
11.8373174846453));
#267669=CARTESIAN_POINT('Ctrl Pts',(-1.45378059771936,-0.553580470949328,
11.8360122478373));
#267670=CARTESIAN_POINT('Ctrl Pts',(-1.46275448749065,-0.529134833582684,
11.8341786028953));
#267671=CARTESIAN_POINT('Ctrl Pts',(-1.46524042696315,-0.522211499911363,
11.8336590352217));
#267672=CARTESIAN_POINT('Ctrl Pts',(-1.46945426056182,-0.510208983951964,
11.8327577288438));
#267673=CARTESIAN_POINT('Ctrl Pts',(-1.47120517393833,-0.505137967342879,
11.8323767565876));
#267674=CARTESIAN_POINT('Ctrl Pts',(-1.47478559083017,-0.494591786325402,
11.8315840356302));
#267675=CARTESIAN_POINT('Ctrl Pts',(-1.4766109150612,-0.489115301221913,
11.8311721561985));
#267676=CARTESIAN_POINT('Ctrl Pts',(-1.48083291888741,-0.476209051969776,
11.83020088385));
#267677=CARTESIAN_POINT('Ctrl Pts',(-1.48320421352683,-0.468771214659952,
11.8296406684617));
#267678=CARTESIAN_POINT('Ctrl Pts',(-1.48807310557398,-0.453092517158042,
11.8284586276957));
#267679=CARTESIAN_POINT('Ctrl Pts',(-1.49055845382412,-0.444848161535628,
11.8278364227426));
#267680=CARTESIAN_POINT('Ctrl Pts',(-1.50050315548437,-0.410840499083276,
11.8252668929519));
#267681=CARTESIAN_POINT('Ctrl Pts',(-1.50736358380977,-0.384908426387242,
11.8233004664417));
#267682=CARTESIAN_POINT('Ctrl Pts',(-1.54152424155393,-0.240811636859674,
11.812328617889));
#267683=CARTESIAN_POINT('Ctrl Pts',(-1.55559729728022,-0.119965461492677,
11.8029143200534));
#267684=CARTESIAN_POINT('Ctrl Pts',(-1.55549949371246,0.00125501405145053,
11.7935273087615));
#267685=CARTESIAN_POINT('Ctrl Pts',(-1.55549949256107,0.00125644030590557,
11.793527198316));
#267686=CARTESIAN_POINT('Ctrl Pts',(-1.55543827476008,0.0770453639235173,
11.7876582936078));
#267687=CARTESIAN_POINT('Ctrl Pts',(-1.5498380746614,0.152741214403535,
11.7818321000103));
#267688=CARTESIAN_POINT('Ctrl Pts',(-1.53791872494753,0.233275774147497,
11.775851467811));
#267689=CARTESIAN_POINT('Ctrl Pts',(-1.53706917578888,0.238809427517005,
11.7754416727001));
#267690=CARTESIAN_POINT('Ctrl Pts',(-1.53560595715123,0.248008884992335,
11.7747624411622));
#267691=CARTESIAN_POINT('Ctrl Pts',(-1.53500900097402,0.251677234498533,
11.7744921321761));
#267692=CARTESIAN_POINT('Ctrl Pts',(-1.53390385571041,0.258318225709805,
11.774003798637));
#267693=CARTESIAN_POINT('Ctrl Pts',(-1.5334001613056,0.261291580473112,
11.7737855291795));
#267694=CARTESIAN_POINT('Ctrl Pts',(-1.53234817902121,0.267393713056188,
11.7733383686218));
#267695=CARTESIAN_POINT('Ctrl Pts',(-1.53179896062522,0.27052224333861,
11.7731095425681));
#267696=CARTESIAN_POINT('Ctrl Pts',(-1.53053654987904,0.277586229865394,
11.7725938285275));
#267697=CARTESIAN_POINT('Ctrl Pts',(-1.52981776157695,0.281520625991666,
11.7723072606542));
#267698=CARTESIAN_POINT('Ctrl Pts',(-1.5276016529063,0.293391668079941,
11.7714445086636));
#267699=CARTESIAN_POINT('Ctrl Pts',(-1.52605765506662,0.301319633833431,
11.770870887273));
#267700=CARTESIAN_POINT('Ctrl Pts',(-1.51121779730803,0.374476351867772,
11.7655983195444));
#267701=CARTESIAN_POINT('Ctrl Pts',(-1.49380714537275,0.438810412518146,
11.7611122629698));
#267702=CARTESIAN_POINT('Ctrl Pts',(-1.45370456831319,0.556465673460301,
11.7528579526875));
#267703=CARTESIAN_POINT('Ctrl Pts',(-1.43205907766077,0.610014816728726,
11.7490800359503));
#267704=CARTESIAN_POINT('Ctrl Pts',(-1.37969947215315,0.72129729323195,
11.7409688696035));
#267705=CARTESIAN_POINT('Ctrl Pts',(-1.34822414890071,0.778544112823092,
11.7366347880482));
#267706=CARTESIAN_POINT('Ctrl Pts',(-1.29337733083871,0.864945141752854,
11.7296625366397));
#267707=CARTESIAN_POINT('Ctrl Pts',(-1.27239475243753,0.89552567501197,
11.727103408162));
#267708=CARTESIAN_POINT('Ctrl Pts',(-1.24421543415836,0.933602828860798,
11.7237805921658));
#267709=CARTESIAN_POINT('Ctrl Pts',(-1.23800781260553,0.941818950493964,
11.7230551921094));
#267710=CARTESIAN_POINT('Ctrl Pts',(-1.2278793428984,0.954951360685005,
11.7218817361772));
#267711=CARTESIAN_POINT('Ctrl Pts',(-1.22400938351031,0.959906666795737,
11.7214356867553));
#267712=CARTESIAN_POINT('Ctrl Pts',(-1.21657069394242,0.96931344098426,
11.720582603928));
#267713=CARTESIAN_POINT('Ctrl Pts',(-1.2130072985851,0.973769013789738,
11.7201757877134));
#267714=CARTESIAN_POINT('Ctrl Pts',(-1.20479492207426,0.983922519613457,
11.7192423373674));
#267715=CARTESIAN_POINT('Ctrl Pts',(-1.20012991525647,0.989607251349276,
11.7187150634646));
#267716=CARTESIAN_POINT('Ctrl Pts',(-1.18781758867245,1.00439583103383,
11.7173309918827));
#267717=CARTESIAN_POINT('Ctrl Pts',(-1.18010602177053,1.01344529804828,
11.7164715921882));
#267718=CARTESIAN_POINT('Ctrl Pts',(-1.11557181185831,1.08744033771526,
11.7093391710308));
#267719=CARTESIAN_POINT('Ctrl Pts',(-1.05354923356515,1.14763061224681,
11.7028457507348));
#267720=CARTESIAN_POINT('Ctrl Pts',(-0.920477103875181,1.25685294142414,
11.6896133472452));
#267721=CARTESIAN_POINT('Ctrl Pts',(-0.849689080786751,1.30575089228336,
11.6828990233396));
#267722=CARTESIAN_POINT('Ctrl Pts',(-0.745583186768539,1.36559700999893,
11.6736841640721));
#267723=CARTESIAN_POINT('Ctrl Pts',(-0.715382226259641,1.38165773382522,
11.6710835797942));
#267724=CARTESIAN_POINT('Ctrl Pts',(-0.667305151858946,1.40522534427645,
11.6670802130565));
#267725=CARTESIAN_POINT('Ctrl Pts',(-0.649777569366639,1.413415592456,11.6656481795102));
#267726=CARTESIAN_POINT('Ctrl Pts',(-0.627090073541303,1.42350565929894,
11.6638336137261));
#267727=CARTESIAN_POINT('Ctrl Pts',(-0.622067587670371,1.42570762822903,
11.6634343354659));
#267728=CARTESIAN_POINT('Ctrl Pts',(-0.614275784233497,1.4290747131572,
11.6628187614712));
#267729=CARTESIAN_POINT('Ctrl Pts',(-0.61151462909365,1.43025841500837,
11.6626013692067));
#267730=CARTESIAN_POINT('Ctrl Pts',(-0.60582242021112,1.43267915674698,
11.6621547690777));
#267731=CARTESIAN_POINT('Ctrl Pts',(-0.602891038114204,1.43391518839084,
11.6619256324742));
#267732=CARTESIAN_POINT('Ctrl Pts',(-0.596201654091225,1.43671166010294,
11.6614046688441));
#267733=CARTESIAN_POINT('Ctrl Pts',(-0.59244131047902,1.43826635268745,
11.6611131903921));
#267734=CARTESIAN_POINT('Ctrl Pts',(-0.582619488955455,1.44228207296019,
11.6603553305582));
#267735=CARTESIAN_POINT('Ctrl Pts',(-0.57654842669666,1.44471968303848,
11.6598903129488));
#267736=CARTESIAN_POINT('Ctrl Pts',(-0.5356247164776,1.46085202807501,11.6567775543695));
#267737=CARTESIAN_POINT('Ctrl Pts',(-0.500299239638685,1.47332404016643,
11.6541966090801));
#267738=CARTESIAN_POINT('Ctrl Pts',(-0.455800175436651,1.48724933807806,
11.6510349228867));
#267739=CARTESIAN_POINT('Ctrl Pts',(-0.447021619980684,1.48991143046835,
11.6504154678147));
#267740=CARTESIAN_POINT('Ctrl Pts',(-0.352900817635657,1.51754675641406,
11.6438143804556));
#267741=CARTESIAN_POINT('Ctrl Pts',(-0.265586708613,1.53523697968682,11.6380369984889));
#267742=CARTESIAN_POINT('Ctrl Pts',(-0.118576690159297,1.55209726425564,
11.6282520010717));
#267743=CARTESIAN_POINT('Ctrl Pts',(-0.059587436677704,1.55547893964097,
11.6243123453095));
#267744=CARTESIAN_POINT('Ctrl Pts',(0.0327683210596626,1.55551173349886,
11.6180033995987));
#267745=CARTESIAN_POINT('Ctrl Pts',(0.0660784657661782,1.55445291811311,
11.6156998037777));
#267746=CARTESIAN_POINT('Ctrl Pts',(0.109642075689366,1.55166546088532,
11.6126379520989));
#267747=CARTESIAN_POINT('Ctrl Pts',(0.119950130040805,1.55090265471277,
11.6119098601358));
#267748=CARTESIAN_POINT('Ctrl Pts',(0.136523469858874,1.54950999724567,
11.6107330983032));
#267749=CARTESIAN_POINT('Ctrl Pts',(0.142793996735838,1.54894472521255,
11.6102864556283));
#267750=CARTESIAN_POINT('Ctrl Pts',(0.154737828945701,1.5477948769901,11.6094329311594));
#267751=CARTESIAN_POINT('Ctrl Pts',(0.160411702453959,1.54721713442772,
11.6090262704917));
#267752=CARTESIAN_POINT('Ctrl Pts',(0.173377735378919,1.54582477967243,
11.608094158825));
#267753=CARTESIAN_POINT('Ctrl Pts',(0.180667516446653,1.54498975195845,
11.607568074564));
#267754=CARTESIAN_POINT('Ctrl Pts',(0.199699069317484,1.54267319730258,
11.60618916652));
#267755=CARTESIAN_POINT('Ctrl Pts',(0.211430122289766,1.54110921123343,
11.6053337722227));
#267756=CARTESIAN_POINT('Ctrl Pts',(0.329677276358081,1.52396896471315,
11.5966547709806));
#267757=CARTESIAN_POINT('Ctrl Pts',(0.434298895567302,1.49751253877421,
11.5884785693645));
#267758=CARTESIAN_POINT('Ctrl Pts',(0.612358274561361,1.43224572763298,
11.5738061700983));
#267759=CARTESIAN_POINT('Ctrl Pts',(0.687032838892333,1.39796185575089,
11.5674035894142));
#267760=CARTESIAN_POINT('Ctrl Pts',(0.78851268001489,1.34126715350211,11.5585811930183));
#267761=CARTESIAN_POINT('Ctrl Pts',(0.817813109994618,1.32360567811974,
11.5560196353514));
#267762=CARTESIAN_POINT('Ctrl Pts',(0.852151860316267,1.30133111890856,
11.5530205637455));
#267763=CARTESIAN_POINT('Ctrl Pts',(0.85777006686341,1.29763476791207,11.5525299853492));
#267764=CARTESIAN_POINT('Ctrl Pts',(0.866456394970757,1.29183876079708,
11.5517718749555));
#267765=CARTESIAN_POINT('Ctrl Pts',(0.869541167959608,1.28976440728287,
11.551502721495));
#267766=CARTESIAN_POINT('Ctrl Pts',(0.87525113978003,1.28589494353712,11.5510046946817));
#267767=CARTESIAN_POINT('Ctrl Pts',(0.87787824824078,1.28410285612381,11.5507756336121));
#267768=CARTESIAN_POINT('Ctrl Pts',(0.883842210878091,1.28000766958513,
11.5502557832441));
#267769=CARTESIAN_POINT('Ctrl Pts',(0.887175565891035,1.27769957510366,
11.5499653365535));
#267770=CARTESIAN_POINT('Ctrl Pts',(0.895823995414858,1.271661033543,11.5492119366804));
#267771=CARTESIAN_POINT('Ctrl Pts',(0.901124875053817,1.26791024069463,
11.548750321127));
#267772=CARTESIAN_POINT('Ctrl Pts',(0.936027864489046,1.24288414308738,
11.5457108299805));
#267773=CARTESIAN_POINT('Ctrl Pts',(0.964900622201271,1.22060496353759,
11.5431962190013));
#267774=CARTESIAN_POINT('Ctrl Pts',(1.00555814454436,1.18688696401468,11.539611120718));
#267775=CARTESIAN_POINT('Ctrl Pts',(1.01798471773903,1.17624614493162,11.5385090748479));
#267776=CARTESIAN_POINT('Ctrl Pts',(1.0564829365996,1.14221311911377,11.5350665459296));
#267777=CARTESIAN_POINT('Ctrl Pts',(1.08193435620354,1.11813470954132,11.5327486011254));
#267778=CARTESIAN_POINT('Ctrl Pts',(1.16259766892338,1.03648745647425,11.5251800595548));
#267779=CARTESIAN_POINT('Ctrl Pts',(1.21419561020457,0.975534706193046,
11.51996903195));
#267780=CARTESIAN_POINT('Ctrl Pts',(1.28327766639522,0.879909085401753,
11.5120538558977));
#267781=CARTESIAN_POINT('Ctrl Pts',(1.30451201813904,0.848109434627519,
11.509461091908));
#267782=CARTESIAN_POINT('Ctrl Pts',(1.33337797176438,0.801228290341209,
11.5056682333747));
#267783=CARTESIAN_POINT('Ctrl Pts',(1.34196994117998,0.786752965749487,
11.5045010874051));
#267784=CARTESIAN_POINT('Ctrl Pts',(1.35694320883465,0.760567638537831,
11.5023946877119));
#267785=CARTESIAN_POINT('Ctrl Pts',(1.36341210969027,0.748909476842886,
11.5014585941772));
#267786=CARTESIAN_POINT('Ctrl Pts',(1.37301943071061,0.731058181902767,
11.5000270684353));
#267787=CARTESIAN_POINT('Ctrl Pts',(1.37626768900546,0.724924594567943,
11.4995355338475));
#267788=CARTESIAN_POINT('Ctrl Pts',(1.38209299733483,0.71374456396407,11.498640073186));
#267789=CARTESIAN_POINT('Ctrl Pts',(1.38468374345685,0.708705358325314,
11.4982366378726));
#267790=CARTESIAN_POINT('Ctrl Pts',(1.39021051287214,0.697809359022167,
11.49736463231));
#267791=CARTESIAN_POINT('Ctrl Pts',(1.39313717239279,0.6919479663299,11.496895743849));
#267792=CARTESIAN_POINT('Ctrl Pts',(1.40096698220504,0.676015700266734,
11.4956216520789));
#267793=CARTESIAN_POINT('Ctrl Pts',(1.40579843873033,0.665910241467936,
11.494813982745));
#267794=CARTESIAN_POINT('Ctrl Pts',(1.41888691716792,0.637757044987237,
11.4925646705203));
#267795=CARTESIAN_POINT('Ctrl Pts',(1.42690708914345,0.619604747661188,
11.4911152672628));
#267796=CARTESIAN_POINT('Ctrl Pts',(1.4345766883817,0.601306889326732,11.4896545509914));
#267797=CARTESIAN_POINT('',(-1.55549976470477,-0.000855571976022074,11.6559437432627));
#267798=CARTESIAN_POINT('Ctrl Pts',(1.43457668357355,0.601306900797849,
11.3502242497077));
#267799=CARTESIAN_POINT('Ctrl Pts',(1.41226865130244,0.654528613221381,
11.3543632498939));
#267800=CARTESIAN_POINT('Ctrl Pts',(1.38696253154565,0.706584446038729,
11.3585022500801));
#267801=CARTESIAN_POINT('Ctrl Pts',(1.35880582970744,0.757117538532215,
11.3626412502663));
#267802=CARTESIAN_POINT('Ctrl Pts',(1.33067329122353,0.80760726483087,11.3667766984695));
#267803=CARTESIAN_POINT('Ctrl Pts',(1.29969527071767,0.856576387070337,
11.3709121466726));
#267804=CARTESIAN_POINT('Ctrl Pts',(1.26606623022454,0.903690517093667,
11.3750475948758));
#267805=CARTESIAN_POINT('Ctrl Pts',(1.23245312122716,0.950782327165226,
11.3791810839426));
#267806=CARTESIAN_POINT('Ctrl Pts',(1.19619178468126,0.996020464185237,
11.3833145730094));
#267807=CARTESIAN_POINT('Ctrl Pts',(1.15752003742474,1.03909942400149,11.3874480620763));
#267808=CARTESIAN_POINT('Ctrl Pts',(1.11885174464237,1.08217453565562,11.3915811819063));
#267809=CARTESIAN_POINT('Ctrl Pts',(1.07777381780718,1.12309046680136,11.3957143017364));
#267810=CARTESIAN_POINT('Ctrl Pts',(1.03456293596234,1.16157642087509,11.3998474215664));
#267811=CARTESIAN_POINT('Ctrl Pts',(0.991308894315491,1.20010081540842,
11.4039846696305));
#267812=CARTESIAN_POINT('Ctrl Pts',(0.945918034130839,1.23619004022242,
11.4081219176946));
#267813=CARTESIAN_POINT('Ctrl Pts',(0.898701275092304,1.26961264492264,
11.4122591657587));
#267814=CARTESIAN_POINT('Ctrl Pts',(0.851459226604644,1.30305315087824,
11.4163986297462));
#267815=CARTESIAN_POINT('Ctrl Pts',(0.802389773687353,1.33382391591129,
11.4205380937338));
#267816=CARTESIAN_POINT('Ctrl Pts',(0.75183136726111,1.36173780339766,11.4246775577214));
#267817=CARTESIAN_POINT('Ctrl Pts',(0.701180318458949,1.38970283982327,
11.4288246067933));
#267818=CARTESIAN_POINT('Ctrl Pts',(0.649035338870661,1.41480032145479,
11.4329716558652));
#267819=CARTESIAN_POINT('Ctrl Pts',(0.595756836526051,1.43689040700134,
11.4371187049372));
#267820=CARTESIAN_POINT('Ctrl Pts',(0.564244746428948,1.44995580365031,
11.4395715175772));
#267821=CARTESIAN_POINT('Ctrl Pts',(0.532336468268933,1.46197007338129,
11.4420243302172));
#267822=CARTESIAN_POINT('Ctrl Pts',(0.500108798853076,1.47291257015131,
11.4444771428572));
#267823=CARTESIAN_POINT('Ctrl Pts',(0.445607664972614,1.49141773953708,
11.4486251644952));
#267824=CARTESIAN_POINT('Ctrl Pts',(0.389963628830703,1.50693267352437,
11.4527731861331));
#267825=CARTESIAN_POINT('Ctrl Pts',(0.33353654704593,1.51932011827155,11.456921207771));
#267826=CARTESIAN_POINT('Ctrl Pts',(0.277209795174015,1.53168553757966,
11.4610618540382));
#267827=CARTESIAN_POINT('Ctrl Pts',(0.220103265647797,1.54093439430489,
11.4652025003054));
#267828=CARTESIAN_POINT('Ctrl Pts',(0.162592671480833,1.54697895046466,
11.4693431465725));
#267829=CARTESIAN_POINT('Ctrl Pts',(0.105139285689614,1.55301749383243,
11.4734796739526));
#267830=CARTESIAN_POINT('Ctrl Pts',(0.0472831469573348,1.55585799774962,
11.4776162013326));
#267831=CARTESIAN_POINT('Ctrl Pts',(-0.0105908529907744,1.55546394488362,
11.4817527287126));
#267832=CARTESIAN_POINT('Ctrl Pts',(-0.0684295321422135,1.5550701325101,
11.4858867315489));
#267833=CARTESIAN_POINT('Ctrl Pts',(-0.126285531165076,1.55144568003564,
11.4900207343852));
#267834=CARTESIAN_POINT('Ctrl Pts',(-0.183772085437503,1.54460612151252,
11.4941547372215));
#267835=CARTESIAN_POINT('Ctrl Pts',(-0.241245654360086,1.53776810794302,
11.4982878062486));
#267836=CARTESIAN_POINT('Ctrl Pts',(-0.298349427291833,1.52771649160558,
11.5024208752757));
#267837=CARTESIAN_POINT('Ctrl Pts',(-0.354702117886104,1.51451862239033,
11.5065539443028));
#267838=CARTESIAN_POINT('Ctrl Pts',(-0.411105744465599,1.50130882390491,
11.5106907491222));
#267839=CARTESIAN_POINT('Ctrl Pts',(-0.466756423426883,1.48494720733713,
11.5148275539415));
#267840=CARTESIAN_POINT('Ctrl Pts',(-0.521284767950481,1.46555192357788,
11.5189643587608));
#267841=CARTESIAN_POINT('Ctrl Pts',(-0.575835640730655,1.44614862670301,
11.5231028726913));
#267842=CARTESIAN_POINT('Ctrl Pts',(-0.629262772949708,1.42370936492172,
11.5272413866217));
#267843=CARTESIAN_POINT('Ctrl Pts',(-0.681216667352735,1.39840055138749,
11.5313799005522));
#267844=CARTESIAN_POINT('Ctrl Pts',(-0.733271855733956,1.37304239351756,
11.535526483301));
#267845=CARTESIAN_POINT('Ctrl Pts',(-0.783847609271613,1.34480375730816,
11.5396730660499));
#267846=CARTESIAN_POINT('Ctrl Pts',(-0.832619777979761,1.31389670648683,
11.5438196487988));
#267847=CARTESIAN_POINT('Ctrl Pts',(-0.878761859687165,1.28465634867402,
11.5477426230087));
#267848=CARTESIAN_POINT('Ctrl Pts',(-0.923289576558216,1.25302821438636,
11.5516655972186));
#267849=CARTESIAN_POINT('Ctrl Pts',(-0.965956055322932,1.21922481486597,
11.5555885714286));
#267850=CARTESIAN_POINT('Ctrl Pts',(-1.0114338992033,1.18319405323478,11.5597700369217));
#267851=CARTESIAN_POINT('Ctrl Pts',(-1.05500203629591,1.14452862400283,
11.5639515024147));
#267852=CARTESIAN_POINT('Ctrl Pts',(-1.09633493644636,1.10346271215984,
11.5681329679078));
#267853=CARTESIAN_POINT('Ctrl Pts',(-1.13676231568373,1.06329647205179,
11.5722228258815));
#267854=CARTESIAN_POINT('Ctrl Pts',(-1.17505098592424,1.02083424380586,
11.5763126838553));
#267855=CARTESIAN_POINT('Ctrl Pts',(-1.21092769215217,0.976337223698363,
11.580402541829));
#267856=CARTESIAN_POINT('Ctrl Pts',(-1.2467695817939,0.931883385769461,
11.5844884307958));
#267857=CARTESIAN_POINT('Ctrl Pts',(-1.28020380750838,0.885399079675038,
11.5885743197627));
#267858=CARTESIAN_POINT('Ctrl Pts',(-1.3109950352659,0.837181143784403,
11.5926602087296));
#267859=CARTESIAN_POINT('Ctrl Pts',(-1.34176891796273,0.788990369624073,
11.5967437960671));
#267860=CARTESIAN_POINT('Ctrl Pts',(-1.36990246527459,0.739068350541516,
11.6008273834047));
#267861=CARTESIAN_POINT('Ctrl Pts',(-1.39520305183881,0.687741735057339,
11.6049109707423));
#267862=CARTESIAN_POINT('Ctrl Pts',(-1.42155159810529,0.634289152076536,
11.6091637017856));
#267863=CARTESIAN_POINT('Ctrl Pts',(-1.4448270044127,0.579313576673076,
11.613416432829));
#267864=CARTESIAN_POINT('Ctrl Pts',(-1.46486537546916,0.523210934281381,
11.6176691638724));
#267865=CARTESIAN_POINT('Ctrl Pts',(-1.48411993315168,0.46930278171604,
11.6217555466902));
#267866=CARTESIAN_POINT('Ctrl Pts',(-1.50038591659663,0.414354664111797,
11.6258419295081));
#267867=CARTESIAN_POINT('Ctrl Pts',(-1.51356867128985,0.35873406207089,
11.6299283123259));
#267868=CARTESIAN_POINT('Ctrl Pts',(-1.52675850798256,0.303083579698876,
11.6340168904179));
#267869=CARTESIAN_POINT('Ctrl Pts',(-1.53686172842426,0.246760420744384,
11.63810546851));
#267870=CARTESIAN_POINT('Ctrl Pts',(-1.54383509081983,0.190140638353125,
11.642194046602));
#267871=CARTESIAN_POINT('Ctrl Pts',(-1.55081899955752,0.133435225592786,
11.6462888081592));
#267872=CARTESIAN_POINT('Ctrl Pts',(-1.55466358298914,0.076432827428913,
11.6503835697164));
#267873=CARTESIAN_POINT('Ctrl Pts',(-1.55537762736568,0.0195111837242169,
11.6544783312735));
#267874=CARTESIAN_POINT('Ctrl Pts',(-1.55546280686274,0.0127209096986689,
11.6549668019366));
#267875=CARTESIAN_POINT('Ctrl Pts',(-1.55550349795349,0.00593177925652502,
11.6554552725996));
#267876=CARTESIAN_POINT('Ctrl Pts',(-1.55549976470477,-0.000855571976022074,
11.6559437432627));
#267877=CARTESIAN_POINT('Ctrl Pts',(-1.55745359230764,-0.000857079788619507,
11.6559437743963));
#267878=CARTESIAN_POINT('Ctrl Pts',(-1.55778429450171,-0.0507394822719253,
11.6595291829309));
#267879=CARTESIAN_POINT('Ctrl Pts',(-1.53298428568849,-0.61557232946888,
11.7001517343226));
#267880=CARTESIAN_POINT('Ctrl Pts',(-0.843887408158428,-1.63323853987322,
11.7778114285714));
#267881=CARTESIAN_POINT('Ctrl Pts',(0.914119296723934,-1.59499216209124,
11.8889228571429));
#267882=CARTESIAN_POINT('Ctrl Pts',(1.66724862260157,-0.371308863304057,
11.9797161771584));
#267883=CARTESIAN_POINT('Ctrl Pts',(1.52345377446436,0.384508855915243,
12.0334723543167));
#267884=CARTESIAN_POINT('Ctrl Pts',(1.43231976391824,0.600353038565383,
12.0501913886179));
#267885=CARTESIAN_POINT('Origin',(0.,0.,-1.29405622560371));
#267886=CARTESIAN_POINT('',(1.43457668357408,0.601306900796593,12.8868295753666));
#267887=CARTESIAN_POINT('',(1.43457658310325,0.601307140496281,12.749909041778));
#267888=CARTESIAN_POINT('',(1.43457668357355,0.601306900797845,-1.29405622560371));
#267889=CARTESIAN_POINT('Ctrl Pts',(1.43457668357408,0.601306900796593,
12.8868295753666));
#267890=CARTESIAN_POINT('Ctrl Pts',(1.43630803386767,0.597176306654078,
12.8865025089062));
#267891=CARTESIAN_POINT('Ctrl Pts',(1.43802156797068,0.593038178282737,
12.8861764329062));
#267892=CARTESIAN_POINT('Ctrl Pts',(1.4410954682343,0.585523145905051,12.8855872095809));
#267893=CARTESIAN_POINT('Ctrl Pts',(1.44246188697645,0.582148785377978,
12.8853237112177));
#267894=CARTESIAN_POINT('Ctrl Pts',(1.44500388949606,0.575807427749637,
12.884830574421));
#267895=CARTESIAN_POINT('Ctrl Pts',(1.44618217616257,0.572841643151802,
12.8846007829389));
#267896=CARTESIAN_POINT('Ctrl Pts',(1.44885376338895,0.56605639265347,12.8840769538399));
#267897=CARTESIAN_POINT('Ctrl Pts',(1.45034109317028,0.562234632383855,
12.883783275206));
#267898=CARTESIAN_POINT('Ctrl Pts',(1.45425306680089,0.552063814954083,
12.8830052188027));
#267899=CARTESIAN_POINT('Ctrl Pts',(1.45665128087403,0.545704579846847,
12.8825223643004));
#267900=CARTESIAN_POINT('Ctrl Pts',(1.47397588503568,0.498837638219103,
12.8789888702182));
#267901=CARTESIAN_POINT('Ctrl Pts',(1.48725353464925,0.457735361294269,
12.8760272387744));
#267902=CARTESIAN_POINT('Ctrl Pts',(1.52863014621185,0.308706085240282,
12.8655946795542));
#267903=CARTESIAN_POINT('Ctrl Pts',(1.54682145612325,0.198383237105034,
12.8584125802658));
#267904=CARTESIAN_POINT('Ctrl Pts',(1.55660052978561,0.0239302771643157,
12.8467669169518));
#267905=CARTESIAN_POINT('Ctrl Pts',(1.5562866564253,-0.0393471128764939,
12.8424887910578));
#267906=CARTESIAN_POINT('Ctrl Pts',(1.5510677913964,-0.118432824939837,
12.836973522802));
#267907=CARTESIAN_POINT('Ctrl Pts',(1.54976385617614,-0.134423153233905,
12.8358499251551));
#267908=CARTESIAN_POINT('Ctrl Pts',(1.54749025593567,-0.157829087226317,
12.8341915418417));
#267909=CARTESIAN_POINT('Ctrl Pts',(1.54671403800262,-0.165262803190695,
12.8336628091812));
#267910=CARTESIAN_POINT('Ctrl Pts',(1.54524911786642,-0.178376418299592,
12.8327263659454));
#267911=CARTESIAN_POINT('Ctrl Pts',(1.54458258992354,-0.184058697639912,
12.8323193587251));
#267912=CARTESIAN_POINT('Ctrl Pts',(1.54321848998383,-0.195158335282571,
12.8315218439678));
#267913=CARTESIAN_POINT('Ctrl Pts',(1.54252370083522,-0.200575957220771,
12.8311314297177));
#267914=CARTESIAN_POINT('Ctrl Pts',(1.54056908483936,-0.215205946379475,
12.8300739494174));
#267915=CARTESIAN_POINT('Ctrl Pts',(1.5392551837623,-0.224410732376552,
12.8294051893792));
#267916=CARTESIAN_POINT('Ctrl Pts',(1.53399549161855,-0.259036418208121,
12.8268762261096));
#267917=CARTESIAN_POINT('Ctrl Pts',(1.529502010323,-0.284368577793769,12.824998908354));
#267918=CARTESIAN_POINT('Ctrl Pts',(1.52398551699384,-0.311532305912606,
12.8229551370473));
#267919=CARTESIAN_POINT('Ctrl Pts',(1.52358452857621,-0.313487508284854,
12.8228078577438));
#267920=CARTESIAN_POINT('Ctrl Pts',(1.52198148458363,-0.321228154025933,
12.8222240969608));
#267921=CARTESIAN_POINT('Ctrl Pts',(1.52075024302148,-0.32700743568416,
12.8217867421423));
#267922=CARTESIAN_POINT('Ctrl Pts',(1.48978889966949,-0.468378321187837,
12.8110511573063));
#267923=CARTESIAN_POINT('Ctrl Pts',(1.44207641665855,-0.599375531415827,
12.8001811203944));
#267924=CARTESIAN_POINT('Ctrl Pts',(1.35950012202056,-0.756879461573442,
12.7864889022573));
#267925=CARTESIAN_POINT('Ctrl Pts',(1.34005725765543,-0.790793342407725,
12.7835056388749));
#267926=CARTESIAN_POINT('Ctrl Pts',(1.31184820494531,-0.835963784946403,
12.7795150063747));
#267927=CARTESIAN_POINT('Ctrl Pts',(1.30417580189023,-0.847883644583293,
12.7784602780913));
#267928=CARTESIAN_POINT('Ctrl Pts',(1.2907299311169,-0.86815872653338,12.7766654847704));
#267929=CARTESIAN_POINT('Ctrl Pts',(1.28503574504065,-0.876565159090118,
12.7759211035816));
#267930=CARTESIAN_POINT('Ctrl Pts',(1.27676295003602,-0.88852455059335,
12.7748624561391));
#267931=CARTESIAN_POINT('Ctrl Pts',(1.27425114019557,-0.892123052373519,
12.7745439615408));
#267932=CARTESIAN_POINT('Ctrl Pts',(1.26986933526257,-0.898344308237728,
12.7739934790093));
#267933=CARTESIAN_POINT('Ctrl Pts',(1.26800637511454,-0.900971951995269,
12.7737610209342));
#267934=CARTESIAN_POINT('Ctrl Pts',(1.26408617194305,-0.906465025305012,
12.7732751896025));
#267935=CARTESIAN_POINT('Ctrl Pts',(1.26202733731474,-0.909329254309723,
12.7730219282269));
#267936=CARTESIAN_POINT('Ctrl Pts',(1.25652115694188,-0.916934672921012,
12.772349536477));
#267937=CARTESIAN_POINT('Ctrl Pts',(1.253056677899,-0.921663483686224,12.7719315641689));
#267938=CARTESIAN_POINT('Ctrl Pts',(1.2379373998346,-0.942057573383563,
12.7701288464441));
#267939=CARTESIAN_POINT('Ctrl Pts',(1.22601431547814,-0.957523090808126,
12.7687614858435));
#267940=CARTESIAN_POINT('Ctrl Pts',(1.19976006815747,-0.990282907704105,
12.7658543679145));
#267941=CARTESIAN_POINT('Ctrl Pts',(1.18533915034077,-1.00749970940668,
12.7643198488392));
#267942=CARTESIAN_POINT('Ctrl Pts',(1.07182044809957,-1.13721408385789,
12.7526525542086));
#267943=CARTESIAN_POINT('Ctrl Pts',(0.957300501113441,-1.23516669992363,
12.7431369642283));
#267944=CARTESIAN_POINT('Ctrl Pts',(0.797890359839658,-1.33582968469954,
12.7303078577488));
#267945=CARTESIAN_POINT('Ctrl Pts',(0.764502373532948,-1.3552142526981,
12.7276460873808));
#267946=CARTESIAN_POINT('Ctrl Pts',(0.721264224917749,-1.37821114234835,
12.724211289038));
#267947=CARTESIAN_POINT('Ctrl Pts',(0.712049719733451,-1.38299429585679,
12.7234800155666));
#267948=CARTESIAN_POINT('Ctrl Pts',(0.697162481163887,-1.39053388717173,
12.72229934632));
#267949=CARTESIAN_POINT('Ctrl Pts',(0.691519545084185,-1.39334874785641,
12.7218520023628));
#267950=CARTESIAN_POINT('Ctrl Pts',(0.680742908817956,-1.3986428573648,
12.7209979498659));
#267951=CARTESIAN_POINT('Ctrl Pts',(0.675612377307309,-1.40112835400685,
12.7205914670816));
#267952=CARTESIAN_POINT('Ctrl Pts',(0.663864638601112,-1.4067400440466,
12.719660908738));
#267953=CARTESIAN_POINT('Ctrl Pts',(0.65723884301869,-1.40984783212392,
12.7191362074789));
#267954=CARTESIAN_POINT('Ctrl Pts',(0.639899226007944,-1.41783207545981,
12.7177632945459));
#267955=CARTESIAN_POINT('Ctrl Pts',(0.629151724697672,-1.42263379222711,
12.7169125487042));
#267956=CARTESIAN_POINT('Ctrl Pts',(0.545226050390564,-1.45899269118711,
12.7102695031969));
#267957=CARTESIAN_POINT('Ctrl Pts',(0.469787643090025,-1.48500058473315,
12.7042906659553));
#267958=CARTESIAN_POINT('Ctrl Pts',(0.289643495969261,-1.53200218576918,
12.6900219387361));
#267959=CARTESIAN_POINT('Ctrl Pts',(0.184102071200889,-1.54823434186491,
12.6816588031931));
#267960=CARTESIAN_POINT('Ctrl Pts',(0.0402743406402426,-1.55543075149596,
12.6707003078938));
#267961=CARTESIAN_POINT('Ctrl Pts',(0.00275707545095223,-1.55594981291119,
12.6678845757238));
#267962=CARTESIAN_POINT('Ctrl Pts',(-0.0416357872520772,-1.55495794351881,
12.6646297598777));
#267963=CARTESIAN_POINT('Ctrl Pts',(-0.0485247956830509,-1.55475821073372,
12.6641268709908));
#267964=CARTESIAN_POINT('Ctrl Pts',(-0.059163306185866,-1.55437898860908,
12.6633539041798));
#267965=CARTESIAN_POINT('Ctrl Pts',(-0.0629137507359866,-1.55423170660157,
12.663082103881));
#267966=CARTESIAN_POINT('Ctrl Pts',(-0.0698376003415167,-1.55393470000887,
12.6625816545831));
#267967=CARTESIAN_POINT('Ctrl Pts',(-0.073011059152898,-1.55378882990267,
12.662352801957));
#267968=CARTESIAN_POINT('Ctrl Pts',(-0.0801860862681806,-1.55343699441159,
12.6618365423015));
#267969=CARTESIAN_POINT('Ctrl Pts',(-0.0841873142209091,-1.55322528988408,
12.6615494583852));
#267970=CARTESIAN_POINT('Ctrl Pts',(-0.0960276280279973,-1.55255293201059,
12.6607022171312));
#267971=CARTESIAN_POINT('Ctrl Pts',(-0.103864250696702,-1.55204836790932,
12.6601444332513));
#267972=CARTESIAN_POINT('Ctrl Pts',(-0.167335707890344,-1.54747882997415,
12.6556483679543));
#267973=CARTESIAN_POINT('Ctrl Pts',(-0.222726367074404,-1.54048258065713,
12.6518588651193));
#267974=CARTESIAN_POINT('Ctrl Pts',(-0.410811867645751,-1.50636497978527,
12.6390875249788));
#267975=CARTESIAN_POINT('Ctrl Pts',(-0.540267839730735,-1.46492782110384,
12.6304116167841));
#267976=CARTESIAN_POINT('Ctrl Pts',(-0.695402089092766,-1.39186942844944,
12.618718676366));
#267977=CARTESIAN_POINT('Ctrl Pts',(-0.727527365184992,-1.37535019306935,
12.6162243236083));
#267978=CARTESIAN_POINT('Ctrl Pts',(-0.767910920675648,-1.35277352142793,
12.6129782187025));
#267979=CARTESIAN_POINT('Ctrl Pts',(-0.776726207233167,-1.34773134290876,
12.6122627026434));
#267980=CARTESIAN_POINT('Ctrl Pts',(-0.790891172584244,-1.33944411686298,
12.6111013830782));
#267981=CARTESIAN_POINT('Ctrl Pts',(-0.796271857019717,-1.33625241504336,
12.6106575106051));
#267982=CARTESIAN_POINT('Ctrl Pts',(-0.806529278766559,-1.33008398787893,
12.6098060067984));
#267983=CARTESIAN_POINT('Ctrl Pts',(-0.811409166832632,-1.32711267596163,
12.6093985780495));
#267984=CARTESIAN_POINT('Ctrl Pts',(-0.822480755730538,-1.32028741035984,
12.6084688028307));
#267985=CARTESIAN_POINT('Ctrl Pts',(-0.828661903223299,-1.3164166841432,
12.6079458460296));
#267986=CARTESIAN_POINT('Ctrl Pts',(-0.844899437422479,-1.30608882318844,
12.6065616640811));
#267987=CARTESIAN_POINT('Ctrl Pts',(-0.854908847816922,-1.29955912543796,
12.6056977661122));
#267988=CARTESIAN_POINT('Ctrl Pts',(-0.943520601362143,-1.24028597035465,
12.5979525768149));
#267989=CARTESIAN_POINT('Ctrl Pts',(-1.01721558217201,-1.18059580870191,
12.5908033683006));
#267990=CARTESIAN_POINT('Ctrl Pts',(-1.1513053586924,-1.05006382595058,
12.5763755618778));
#267991=CARTESIAN_POINT('Ctrl Pts',(-1.21170373049357,-0.979751296507427,
12.569134214758));
#267992=CARTESIAN_POINT('Ctrl Pts',(-1.28660532725679,-0.87495416411567,
12.5593411702552));
#267993=CARTESIAN_POINT('Ctrl Pts',(-1.30667574881821,-0.844687559676874,
12.5566180522283));
#267994=CARTESIAN_POINT('Ctrl Pts',(-1.32924517351526,-0.807919682708667,
12.5534561345351));
#267995=CARTESIAN_POINT('Ctrl Pts',(-1.33278165642756,-0.802072319646806,
12.552957548061));
#267996=CARTESIAN_POINT('Ctrl Pts',(-1.33819431581306,-0.792988156403571,
12.5521897705286));
#267997=CARTESIAN_POINT('Ctrl Pts',(-1.34009748406117,-0.789767672853815,
12.5519188926589));
#267998=CARTESIAN_POINT('Ctrl Pts',(-1.34359594194522,-0.783798630843553,
12.5514192962093));
#267999=CARTESIAN_POINT('Ctrl Pts',(-1.34519441523558,-0.781052069010605,
12.551190379527));
#268000=CARTESIAN_POINT('Ctrl Pts',(-1.34879739290478,-0.774817415126494,
12.5506729072732));
#268001=CARTESIAN_POINT('Ctrl Pts',(-1.35079678769415,-0.771326437528438,
12.5503846814438));
#268002=CARTESIAN_POINT('Ctrl Pts',(-1.35669631720515,-0.760932463389,12.5495309161395));
#268003=CARTESIAN_POINT('Ctrl Pts',(-1.36055732214704,-0.754007222224728,
12.5489678047051));
#268004=CARTESIAN_POINT('Ctrl Pts',(-1.3942431952972,-0.692485665568443,
12.5440130145136));
#268005=CARTESIAN_POINT('Ctrl Pts',(-1.42082499068629,-0.636167442836501,
12.5398070162856));
#268006=CARTESIAN_POINT('Ctrl Pts',(-1.47151872124608,-0.509611696999284,
12.5307333446788));
#268007=CARTESIAN_POINT('Ctrl Pts',(-1.49412287672159,-0.438940492438061,
12.52590187724));
#268008=CARTESIAN_POINT('Ctrl Pts',(-1.5300089804147,-0.29110256943578,
12.5158353021519));
#268009=CARTESIAN_POINT('Ctrl Pts',(-1.54268101829008,-0.214011724475579,
12.5106051451062));
#268010=CARTESIAN_POINT('Ctrl Pts',(-1.55108315050351,-0.118494252877623,
12.5039474662107));
#268011=CARTESIAN_POINT('Ctrl Pts',(-1.55234245265071,-0.100661270788728,
12.5026973619671));
#268012=CARTESIAN_POINT('Ctrl Pts',(-1.5537096531494,-0.0750166086789068,
12.5008876467063));
#268013=CARTESIAN_POINT('Ctrl Pts',(-1.55406652312781,-0.0672191606709169,
12.5003358010362));
#268014=CARTESIAN_POINT('Ctrl Pts',(-1.55458519307445,-0.0536511825652345,
12.4993726472811));
#268015=CARTESIAN_POINT('Ctrl Pts',(-1.55477358681539,-0.04788177122694,
12.4989621771955));
#268016=CARTESIAN_POINT('Ctrl Pts',(-1.5550751072852,-0.0367483988363213,
12.4981682570041));
#268017=CARTESIAN_POINT('Ctrl Pts',(-1.55519260473,-0.031384629643052,12.4977849494411));
#268018=CARTESIAN_POINT('Ctrl Pts',(-1.5554293939188,-0.0172313597589847,
12.4967713069122));
#268019=CARTESIAN_POINT('Ctrl Pts',(-1.55550193094502,-0.00844137850564686,
12.4961395216324));
#268020=CARTESIAN_POINT('Ctrl Pts',(-1.5554945369244,0.0245530928688604,
12.4937592320721));
#268021=CARTESIAN_POINT('Ctrl Pts',(-1.55492416102653,0.0487528198289879,
12.4919955828552));
#268022=CARTESIAN_POINT('Ctrl Pts',(-1.55208285740592,0.109288947594619,
12.4875362748412));
#268023=CARTESIAN_POINT('Ctrl Pts',(-1.54910057074156,0.145575781188323,
12.4848200657217));
#268024=CARTESIAN_POINT('Ctrl Pts',(-1.52851922446572,0.320541083888283,
12.4715152711997));
#268025=CARTESIAN_POINT('Ctrl Pts',(-1.49355764573315,0.456503787206729,
12.4604642924911));
#268026=CARTESIAN_POINT('Ctrl Pts',(-1.42905275071181,0.615125929149876,
12.4474923462506));
#268027=CARTESIAN_POINT('Ctrl Pts',(-1.41630761673484,0.643929161521702,
12.4451371633041));
#268028=CARTESIAN_POINT('Ctrl Pts',(-1.40000603838808,0.677939574099746,
12.4423725326169));
#268029=CARTESIAN_POINT('Ctrl Pts',(-1.39728265577096,0.683535044468746,
12.4419182337002));
#268030=CARTESIAN_POINT('Ctrl Pts',(-1.39276595690463,0.692675261253849,
12.4411772076144));
#268031=CARTESIAN_POINT('Ctrl Pts',(-1.39099254675416,0.696229677688026,
12.4408893074381));
#268032=CARTESIAN_POINT('Ctrl Pts',(-1.38777719660975,0.70261282565802,
12.4403728197065));
#268033=CARTESIAN_POINT('Ctrl Pts',(-1.38634020330007,0.705443953494621,
12.4401439346554));
#268034=CARTESIAN_POINT('Ctrl Pts',(-1.383172778194,0.711637276654677,12.4396436560727));
#268035=CARTESIAN_POINT('Ctrl Pts',(-1.38143875449403,0.714997563818882,
12.4393724913268));
#268036=CARTESIAN_POINT('Ctrl Pts',(-1.37644944839085,0.724580209153862,
12.4385998756825));
#268037=CARTESIAN_POINT('Ctrl Pts',(-1.37316420321775,0.730787000052084,
12.4381002587719));
#268038=CARTESIAN_POINT('Ctrl Pts',(-1.35068804593067,0.772564289207047,
12.434741440879));
#268039=CARTESIAN_POINT('Ctrl Pts',(-1.33015706013255,0.807401190602827,
12.4319604626095));
#268040=CARTESIAN_POINT('Ctrl Pts',(-1.2382332657067,0.950332811755104,
12.4204630777161));
#268041=CARTESIAN_POINT('Ctrl Pts',(-1.15484438834402,1.0500919243436,12.4121792712782));
#268042=CARTESIAN_POINT('Ctrl Pts',(-1.04178226039845,1.15537569561948,
12.4018018576025));
#268043=CARTESIAN_POINT('Ctrl Pts',(-1.02310931585939,1.17194304882542,
12.4001130309193));
#268044=CARTESIAN_POINT('Ctrl Pts',(-0.999862656680437,1.19158924342775,
12.3980341583902));
#268045=CARTESIAN_POINT('Ctrl Pts',(-0.995660168197325,1.19510296025012,
12.3976592610984));
#268046=CARTESIAN_POINT('Ctrl Pts',(-0.987583130098101,1.20178402997367,
12.3969403773389));
#268047=CARTESIAN_POINT('Ctrl Pts',(-0.983711678178769,1.20495503105514,
12.3965965241109));
#268048=CARTESIAN_POINT('Ctrl Pts',(-0.960203267982165,1.22402132531571,
12.3945126838423));
#268049=CARTESIAN_POINT('Ctrl Pts',(-0.94019774938797,1.23945414885604,
12.3927565572023));
#268050=CARTESIAN_POINT('Ctrl Pts',(-0.912382122166189,1.25985091384744,
12.3903326658022));
#268051=CARTESIAN_POINT('Ctrl Pts',(-0.904889700561335,1.26524309333065,
12.3896814884863));
#268052=CARTESIAN_POINT('Ctrl Pts',(-0.892898978778593,1.27371164539533,
12.3886418415372));
#268053=CARTESIAN_POINT('Ctrl Pts',(-0.888431651697082,1.27683168068718,
12.3882550464476));
#268054=CARTESIAN_POINT('Ctrl Pts',(-0.879235843593155,1.28318251913938,
12.3874598947281));
#268055=CARTESIAN_POINT('Ctrl Pts',(-0.874505735270798,1.28641080664344,
12.3870514507153));
#268056=CARTESIAN_POINT('Ctrl Pts',(-0.863529041839809,1.2938138551353,
12.3861048461946));
#268057=CARTESIAN_POINT('Ctrl Pts',(-0.857269866607893,1.29796959516599,
12.3855659822328));
#268058=CARTESIAN_POINT('Ctrl Pts',(-0.837376369323995,1.31097109273508,
12.3838560067863));
#268059=CARTESIAN_POINT('Ctrl Pts',(-0.823633793998572,1.31964833421932,
12.3826786944117));
#268060=CARTESIAN_POINT('Ctrl Pts',(-0.754410675375549,1.36185422149185,
12.3767657719777));
#268061=CARTESIAN_POINT('Ctrl Pts',(-0.697015739094113,1.39210247571934,
12.3719140591416));
#268062=CARTESIAN_POINT('Ctrl Pts',(-0.577998342048428,1.44561859389717,
12.3619601799778));
#268063=CARTESIAN_POINT('Ctrl Pts',(-0.51644491965093,1.46873376392769,
12.3568653268197));
#268064=CARTESIAN_POINT('Ctrl Pts',(-0.438410659311208,1.49252441701657,
12.3505396051291));
#268065=CARTESIAN_POINT('Ctrl Pts',(-0.423132024362915,1.49692763313344,
12.349307454213));
#268066=CARTESIAN_POINT('Ctrl Pts',(-0.340047883931425,1.51949831308055,
12.3426480818876));
#268067=CARTESIAN_POINT('Ctrl Pts',(-0.271129746806319,1.53329677022921,
12.3372674099411));
#268068=CARTESIAN_POINT('Ctrl Pts',(-0.193474224065011,1.54344212718842,
12.331512053412));
#268069=CARTESIAN_POINT('Ctrl Pts',(-0.185433228320604,1.54442882671571,
12.3309197816025));
#268070=CARTESIAN_POINT('Ctrl Pts',(-0.173406460593269,1.54580932977666,
12.3300397800865));
#268071=CARTESIAN_POINT('Ctrl Pts',(-0.16942645091503,1.54625061465036,
12.3297495171734));
#268072=CARTESIAN_POINT('Ctrl Pts',(-0.162286074448352,1.5470144056371,
12.3292305331364));
#268073=CARTESIAN_POINT('Ctrl Pts',(-0.159126398395019,1.54734260303603,
12.32900150103));
#268074=CARTESIAN_POINT('Ctrl Pts',(-0.152229386695192,1.54803764980117,
12.3285029264759));
#268075=CARTESIAN_POINT('Ctrl Pts',(-0.148491726274141,1.54840064563759,
12.3282336015401));
#268076=CARTESIAN_POINT('Ctrl Pts',(-0.137882127124026,1.54939226364097,
12.3274714635509));
#268077=CARTESIAN_POINT('Ctrl Pts',(-0.13100715221249,1.54998870912158,
12.3269804073676));
#268078=CARTESIAN_POINT('Ctrl Pts',(-0.0865553451291839,1.5535472937897,
12.323822151199));
#268079=CARTESIAN_POINT('Ctrl Pts',(-0.0488815495785679,1.55518879973118,
12.3212228472374));
#268080=CARTESIAN_POINT('Ctrl Pts',(0.0965865640621532,1.55623451500756,
12.3113554818272));
#268081=CARTESIAN_POINT('Ctrl Pts',(0.204150612941537,1.54580754830162,
12.3043996192563));
#268082=CARTESIAN_POINT('Ctrl Pts',(0.386488362420709,1.50875256398428,
12.2920547747426));
#268083=CARTESIAN_POINT('Ctrl Pts',(0.461900598502809,1.4873979624635,12.2867799282199));
#268084=CARTESIAN_POINT('Ctrl Pts',(0.546397930219472,1.45642277019431,
12.2804928178577));
#268085=CARTESIAN_POINT('Ctrl Pts',(0.557370543630846,1.45225894644588,
12.2796690059345));
#268086=CARTESIAN_POINT('Ctrl Pts',(0.575097428552243,1.44530156116565,
12.2783255211351));
#268087=CARTESIAN_POINT('Ctrl Pts',(0.581881118511559,1.44258379848928,
12.2778083829847));
#268088=CARTESIAN_POINT('Ctrl Pts',(0.593921055616238,1.43766147458029,
12.27688504024));
#268089=CARTESIAN_POINT('Ctrl Pts',(0.599184848635445,1.43547561852478,
12.2764794724726));
#268090=CARTESIAN_POINT('Ctrl Pts',(0.610252201690894,1.43080828161097,
12.2756226993501));
#268091=CARTESIAN_POINT('Ctrl Pts',(0.616052894984619,1.42832031309741,
12.2751712798409));
#268092=CARTESIAN_POINT('Ctrl Pts',(0.631378164445106,1.4216364463678,12.2739722735484));
#268093=CARTESIAN_POINT('Ctrl Pts',(0.640875901169038,1.41738020364727,
12.2732226406837));
#268094=CARTESIAN_POINT('Ctrl Pts',(0.685659775415312,1.39676895250205,
12.269656125898));
#268095=CARTESIAN_POINT('Ctrl Pts',(0.720364112563305,1.37919102408313,
12.2667975395383));
#268096=CARTESIAN_POINT('Ctrl Pts',(0.885331155445646,1.28770876644346,
12.2527271104533));
#268097=CARTESIAN_POINT('Ctrl Pts',(1.00510973220499,1.19655552789888,12.2409033206742));
#268098=CARTESIAN_POINT('Ctrl Pts',(1.1374259359383,1.06177997478218,12.2265065524647));
#268099=CARTESIAN_POINT('Ctrl Pts',(1.16380398059014,1.03279979177485,12.223560589531));
#268100=CARTESIAN_POINT('Ctrl Pts',(1.193337604329,0.997782335858556,12.2201993275371));
#268101=CARTESIAN_POINT('Ctrl Pts',(1.19758070379005,0.992685594615127,
12.21971481363));
#268102=CARTESIAN_POINT('Ctrl Pts',(1.20439160302388,0.984397223190089,
12.2189346885213));
#268103=CARTESIAN_POINT('Ctrl Pts',(1.20697955963501,0.981222385662177,
12.2186376924891));
#268104=CARTESIAN_POINT('Ctrl Pts',(1.2115567502596,0.975561698016046,12.2181114484705));
#268105=CARTESIAN_POINT('Ctrl Pts',(1.21355091970713,0.973079930794289,
12.2178818513066));
#268106=CARTESIAN_POINT('Ctrl Pts',(1.21783881333861,0.967709913679408,
12.2173874716625));
#268107=CARTESIAN_POINT('Ctrl Pts',(1.22012988688721,0.964819626768871,
12.2171228771278));
#268108=CARTESIAN_POINT('Ctrl Pts',(1.22648634399336,0.956741832763743,
12.2163874501555));
#268109=CARTESIAN_POINT('Ctrl Pts',(1.23052913546826,0.951536513991988,
12.2159181849416));
#268110=CARTESIAN_POINT('Ctrl Pts',(1.25389352929578,0.921055606847856,
12.2131961695598));
#268111=CARTESIAN_POINT('Ctrl Pts',(1.27247082443883,0.895215495728091,
12.2109915015328));
#268112=CARTESIAN_POINT('Ctrl Pts',(1.34702900787913,0.784492801423282,
12.2018823334935));
#268113=CARTESIAN_POINT('Ctrl Pts',(1.39535328556851,0.694884712183891,
12.1953009886188));
#268114=CARTESIAN_POINT('Ctrl Pts',(1.43457672746074,0.601306796093332,
12.1885981050115));
#268115=CARTESIAN_POINT('',(-1.55596490018789,0.0013805236815898,12.3559437743963));
#268116=CARTESIAN_POINT('Ctrl Pts',(1.43231976391824,0.600353038565383,
12.0501913886179));
#268117=CARTESIAN_POINT('Ctrl Pts',(1.32156751076454,0.862661581944224,
12.0705094971739));
#268118=CARTESIAN_POINT('Ctrl Pts',(0.815438458427758,1.52296397998904,
12.127864748587));
#268119=CARTESIAN_POINT('Ctrl Pts',(-0.666202740309759,1.7134141339966,
12.2222571428571));
#268120=CARTESIAN_POINT('Ctrl Pts',(-1.49941198544797,0.726802141234669,
12.3038564962274));
#268121=CARTESIAN_POINT('Ctrl Pts',(-1.55693100729208,0.106334549516482,
12.3484187067404));
#268122=CARTESIAN_POINT('Ctrl Pts',(-1.55596490018789,0.0013805236815898,
12.3559437743963));
#268123=CARTESIAN_POINT('Ctrl Pts',(-1.55549937226897,0.00139745155209831,
12.3562113151331));
#268124=CARTESIAN_POINT('Ctrl Pts',(-1.55560015022923,-0.110778211126,12.363603217017));
#268125=CARTESIAN_POINT('Ctrl Pts',(-1.54356710252479,-0.222627877494369,
12.3709328968758));
#268126=CARTESIAN_POINT('Ctrl Pts',(-1.51586618162988,-0.349338442814302,
12.3798584345126));
#268127=CARTESIAN_POINT('Ctrl Pts',(-1.51183262656993,-0.366401004801656,
12.3810729896259));
#268128=CARTESIAN_POINT('Ctrl Pts',(-1.50510967085173,-0.392835973703192,
12.3829765578517));
#268129=CARTESIAN_POINT('Ctrl Pts',(-1.50261901115177,-0.402257782188188,
12.3836593733796));
#268130=CARTESIAN_POINT('Ctrl Pts',(-1.49829769540081,-0.418004318998284,
12.3848081980143));
#268131=CARTESIAN_POINT('Ctrl Pts',(-1.49651509301103,-0.424342042170239,
12.3852726683186));
#268132=CARTESIAN_POINT('Ctrl Pts',(-1.49292509230952,-0.436801626793386,
12.3861900133275));
#268133=CARTESIAN_POINT('Ctrl Pts',(-1.49112013799867,-0.442924061511792,
12.3866428013252));
#268134=CARTESIAN_POINT('Ctrl Pts',(-1.48761046176979,-0.454564313554196,
12.3875076011396));
#268135=CARTESIAN_POINT('Ctrl Pts',(-1.48591258877012,-0.460084098841065,
12.3879193833788));
#268136=CARTESIAN_POINT('Ctrl Pts',(-1.48196280840128,-0.472674892616054,
12.3888626199935));
#268137=CARTESIAN_POINT('Ctrl Pts',(-1.47969097327655,-0.479739449769033,
12.389394718922));
#268138=CARTESIAN_POINT('Ctrl Pts',(-1.47362798022986,-0.498140248149313,
12.3907882834518));
#268139=CARTESIAN_POINT('Ctrl Pts',(-1.46975661181773,-0.509449328330971,
12.3916523638042));
#268140=CARTESIAN_POINT('Ctrl Pts',(-1.43078718406095,-0.619144528455941,
12.4001098086086));
#268141=CARTESIAN_POINT('Ctrl Pts',(-1.38600037386035,-0.713783199183425,
12.4080332552461));
#268142=CARTESIAN_POINT('Ctrl Pts',(-1.30096844084808,-0.854805318301572,
12.4207640374016));
#268143=CARTESIAN_POINT('Ctrl Pts',(-1.26688248342074,-0.904555059984803,
12.4254551433798));
#268144=CARTESIAN_POINT('Ctrl Pts',(-1.20606190559064,-0.983119351874199,
12.4331046737486));
#268145=CARTESIAN_POINT('Ctrl Pts',(-1.18096831486752,-1.01312550119775,
12.4360898880484));
#268146=CARTESIAN_POINT('Ctrl Pts',(-1.14055748614195,-1.05790301861601,
12.4406100633039));
#268147=CARTESIAN_POINT('Ctrl Pts',(-1.12602462218836,-1.07335867547891,
12.4421830873412));
#268148=CARTESIAN_POINT('Ctrl Pts',(-1.10715837982193,-1.09261776779837,
12.4441545208049));
#268149=CARTESIAN_POINT('Ctrl Pts',(-1.10311474859451,-1.09670010428365,
12.4445730684628));
#268150=CARTESIAN_POINT('Ctrl Pts',(-1.09688579431638,-1.10291937344725,
12.445211600245));
#268151=CARTESIAN_POINT('Ctrl Pts',(-1.09471669942804,-1.10507236800551,
12.4454328135893));
#268152=CARTESIAN_POINT('Ctrl Pts',(-1.09025148295789,-1.10947839179932,
12.4458858327158));
#268153=CARTESIAN_POINT('Ctrl Pts',(-1.08795474135719,-1.11173066842782,
12.4461175725733));
#268154=CARTESIAN_POINT('Ctrl Pts',(-1.08275423116946,-1.11679894593777,
12.4466394439839));
#268155=CARTESIAN_POINT('Ctrl Pts',(-1.07984645959039,-1.11961075176768,
12.4469292500253));
#268156=CARTESIAN_POINT('Ctrl Pts',(-1.07123211024121,-1.12787602147472,
12.4477820825379));
#268157=CARTESIAN_POINT('Ctrl Pts',(-1.06549483917688,-1.13329753748813,
12.4483427210811));
#268158=CARTESIAN_POINT('Ctrl Pts',(-1.01967757513187,-1.17593770515855,
12.4527644420004));
#268159=CARTESIAN_POINT('Ctrl Pts',(-0.977695839382554,-1.2110674012157,
12.456482916874));
#268160=CARTESIAN_POINT('Ctrl Pts',(-0.826268070246201,-1.32476095302283,
12.4691433913733));
#268161=CARTESIAN_POINT('Ctrl Pts',(-0.708554042657932,-1.39128103360543,
12.4777736621562));
#268162=CARTESIAN_POINT('Ctrl Pts',(-0.560840067834145,-1.45108550805223,
12.4886284562226));
#268163=CARTESIAN_POINT('Ctrl Pts',(-0.537721348907002,-1.45981039046095,
12.4903260643206));
#268164=CARTESIAN_POINT('Ctrl Pts',(-0.4975278368748,-1.4738948877594,12.4932824857116));
#268165=CARTESIAN_POINT('Ctrl Pts',(-0.480549933961462,-1.47951742255689,
12.4945327801255));
#268166=CARTESIAN_POINT('Ctrl Pts',(-0.455867104797492,-1.48722191573576,
12.4963544344436));
#268167=CARTESIAN_POINT('Ctrl Pts',(-0.448236720553013,-1.48953941940832,
12.4969181124094));
#268168=CARTESIAN_POINT('Ctrl Pts',(-0.434970716162959,-1.49345741293552,
12.4978991989121));
#268169=CARTESIAN_POINT('Ctrl Pts',(-0.429343195071929,-1.49508494317291,
12.4983157198108));
#268170=CARTESIAN_POINT('Ctrl Pts',(-0.418494099513277,-1.4981562960236,
12.49911942811));
#268171=CARTESIAN_POINT('Ctrl Pts',(-0.413273902823672,-1.499604707421,
12.499506459898));
#268172=CARTESIAN_POINT('Ctrl Pts',(-0.400917527316907,-1.50296372588632,
12.5004233782777));
#268173=CARTESIAN_POINT('Ctrl Pts',(-0.393775149091655,-1.50485080772348,
12.500954016322));
#268174=CARTESIAN_POINT('Ctrl Pts',(-0.36864354507519,-1.51129964155113,
12.5028235433987));
#268175=CARTESIAN_POINT('Ctrl Pts',(-0.350587023565802,-1.51559010073253,
12.5041710728761));
#268176=CARTESIAN_POINT('Ctrl Pts',(-0.221607200207151,-1.54380917537687,
12.5138313979138));
#268177=CARTESIAN_POINT('Ctrl Pts',(-0.108456652023515,-1.55585465976143,
12.5225259285749));
#268178=CARTESIAN_POINT('Ctrl Pts',(0.0758711805864795,-1.5552654049063,
12.5368163144409));
#268179=CARTESIAN_POINT('Ctrl Pts',(0.14667540519007,-1.55019173375234,
12.5423257713841));
#268180=CARTESIAN_POINT('Ctrl Pts',(0.237206617356653,-1.53744405456127,
12.5492439391433));
#268181=CARTESIAN_POINT('Ctrl Pts',(0.257465832132295,-1.53418142313367,
12.5507834746384));
#268182=CARTESIAN_POINT('Ctrl Pts',(0.290914021506309,-1.52811349442264,
12.5533049174963));
#268183=CARTESIAN_POINT('Ctrl Pts',(0.304141196931125,-1.52553596650936,
12.55429670792));
#268184=CARTESIAN_POINT('Ctrl Pts',(0.322178311086359,-1.52177720918438,
12.5556403758097));
#268185=CARTESIAN_POINT('Ctrl Pts',(0.327018071872729,-1.52074452851333,
12.5560000435315));
#268186=CARTESIAN_POINT('Ctrl Pts',(0.335131466829362,-1.51897281458054,
12.5566014408929));
#268187=CARTESIAN_POINT('Ctrl Pts',(0.338407748220145,-1.51824626070349,
12.5568438664806));
#268188=CARTESIAN_POINT('Ctrl Pts',(0.34461377601422,-1.51684891412099,
12.5573022363793));
#268189=CARTESIAN_POINT('Ctrl Pts',(0.347543962521087,-1.51618022590472,
12.5575183020249));
#268190=CARTESIAN_POINT('Ctrl Pts',(0.355206673937327,-1.51440816246543,
12.5580824503047));
#268191=CARTESIAN_POINT('Ctrl Pts',(0.359936050032937,-1.51329108414137,
12.5584297557633));
#268192=CARTESIAN_POINT('Ctrl Pts',(0.376282149870901,-1.5093491704708,
12.559627334812));
#268193=CARTESIAN_POINT('Ctrl Pts',(0.387871873844865,-1.50641249571743,
12.5604715234795));
#268194=CARTESIAN_POINT('Ctrl Pts',(0.497139595461702,-1.4773808628683,
12.5683940268733));
#268195=CARTESIAN_POINT('Ctrl Pts',(0.592104563507977,-1.44195031690323,
12.5750124333734));
#268196=CARTESIAN_POINT('Ctrl Pts',(0.785088731277806,-1.34764042850243,
12.589150483299));
#268197=CARTESIAN_POINT('Ctrl Pts',(0.881414400348714,-1.28670213965037,
12.59665331513));
#268198=CARTESIAN_POINT('Ctrl Pts',(0.980874254483286,-1.2073322528372,
12.6055359588512));
#268199=CARTESIAN_POINT('Ctrl Pts',(0.991399732746898,-1.19870430929726,
12.6064912615979));
#268200=CARTESIAN_POINT('Ctrl Pts',(1.00720419160567,-1.18539853262973,
12.6079499239553));
#268201=CARTESIAN_POINT('Ctrl Pts',(1.01256700482454,-1.18082091043928,
12.6084492122276));
#268202=CARTESIAN_POINT('Ctrl Pts',(1.02182186106105,-1.17281168823464,
12.6093185257271));
#268203=CARTESIAN_POINT('Ctrl Pts',(1.02572823297761,-1.16939675161193,
12.6096878596056));
#268204=CARTESIAN_POINT('Ctrl Pts',(1.03443682908957,-1.16170651878011,
12.6105166884413));
#268205=CARTESIAN_POINT('Ctrl Pts',(1.03922975382705,-1.157420885254,12.6109766105641));
#268206=CARTESIAN_POINT('Ctrl Pts',(1.05193526253678,-1.14591760428703,
12.6122059977293));
#268207=CARTESIAN_POINT('Ctrl Pts',(1.05979998088015,-1.13864785700074,
12.6129776522848));
#268208=CARTESIAN_POINT('Ctrl Pts',(1.09425187249814,-1.10613611732601,
12.6164061873442));
#268209=CARTESIAN_POINT('Ctrl Pts',(1.12001480381902,-1.08004198616461,
12.6190995049003));
#268210=CARTESIAN_POINT('Ctrl Pts',(1.24544129781082,-0.943685596223638,
12.6329017122115));
#268211=CARTESIAN_POINT('Ctrl Pts',(1.32984968312786,-0.820458237612204,
12.6446209043491));
#268212=CARTESIAN_POINT('Ctrl Pts',(1.41412675134025,-0.649312762034147,
12.6591871112096));
#268213=CARTESIAN_POINT('Ctrl Pts',(1.43122522815361,-0.61070177855176,
12.6623660977481));
#268214=CARTESIAN_POINT('Ctrl Pts',(1.44936349252139,-0.564780462295209,
12.6659872522042));
#268215=CARTESIAN_POINT('Ctrl Pts',(1.45194761012485,-0.558103616540816,
12.6665098856312));
#268216=CARTESIAN_POINT('Ctrl Pts',(1.45584659743324,-0.547819016650909,
12.6673087286485));
#268217=CARTESIAN_POINT('Ctrl Pts',(1.45719431623729,-0.544223957440305,
12.6675868147411));
#268218=CARTESIAN_POINT('Ctrl Pts',(1.45964624908201,-0.537608980658181,
12.668096330654));
#268219=CARTESIAN_POINT('Ctrl Pts',(1.46075440580217,-0.534590642363316,
12.6683279857228));
#268220=CARTESIAN_POINT('Ctrl Pts',(1.46322541888445,-0.527795174897882,
12.6688476787133));
#268221=CARTESIAN_POINT('Ctrl Pts',(1.46458301178637,-0.524016197918953,
12.6691354034082));
#268222=CARTESIAN_POINT('Ctrl Pts',(1.46802586889457,-0.514314806686216,
12.6698708830791));
#268223=CARTESIAN_POINT('Ctrl Pts',(1.47008996253747,-0.508384871633926,
12.6703174255542));
#268224=CARTESIAN_POINT('Ctrl Pts',(1.48231793395388,-0.472557847312886,
12.6729981019342));
#268225=CARTESIAN_POINT('Ctrl Pts',(1.49160628561459,-0.442366842251715,
12.6751850659997));
#268226=CARTESIAN_POINT('Ctrl Pts',(1.50358408076105,-0.398749859390128,
12.6782706054195));
#268227=CARTESIAN_POINT('Ctrl Pts',(1.50702511613622,-0.385540994223214,
12.6791954556755));
#268228=CARTESIAN_POINT('Ctrl Pts',(1.53473127644131,-0.273143149108765,
12.6869975334167));
#268229=CARTESIAN_POINT('Ctrl Pts',(1.54934979569201,-0.171828086244541,
12.6936003016814));
#268230=CARTESIAN_POINT('Ctrl Pts',(1.55707109430422,5.27306946508915E-5,
12.7050265026763));
#268231=CARTESIAN_POINT('Ctrl Pts',(1.55549462106469,0.0700354402682524,
12.7097378005632));
#268232=CARTESIAN_POINT('Ctrl Pts',(1.54769163906902,0.156586642653441,
12.7157780457768));
#268233=CARTESIAN_POINT('Ctrl Pts',(1.54588946824115,0.173477660584556,
12.7169667435368));
#268234=CARTESIAN_POINT('Ctrl Pts',(1.54286830441444,0.197982354900983,
12.7187072047668));
#268235=CARTESIAN_POINT('Ctrl Pts',(1.54186870435193,0.205622256365373,
12.7192520934816));
#268236=CARTESIAN_POINT('Ctrl Pts',(1.54001527695707,0.219013704964218,
12.720211305066));
#268237=CARTESIAN_POINT('Ctrl Pts',(1.53918587668273,0.224768528860726,
12.7206248519073));
#268238=CARTESIAN_POINT('Ctrl Pts',(1.53751073696963,0.235947276184699,
12.7214308290482));
#268239=CARTESIAN_POINT('Ctrl Pts',(1.53666851026494,0.2413716461636,12.7218231426811));
#268240=CARTESIAN_POINT('Ctrl Pts',(1.53433843416575,0.255871849796493,
12.7228751951929));
#268241=CARTESIAN_POINT('Ctrl Pts',(1.5327987951335,0.26493901368328,12.7235365611952));
#268242=CARTESIAN_POINT('Ctrl Pts',(1.52685157232671,0.298174539208212,
12.7259740270748));
#268243=CARTESIAN_POINT('Ctrl Pts',(1.52195223056001,0.322249995993279,
12.727765552245));
#268244=CARTESIAN_POINT('Ctrl Pts',(1.51537870829572,0.351044631417397,
12.7299408405132));
#268245=CARTESIAN_POINT('Ctrl Pts',(1.51424908402265,0.355885758789841,
12.7303076758378));
#268246=CARTESIAN_POINT('Ctrl Pts',(1.4934680278206,0.443054815944682,12.7369330502946));
#268247=CARTESIAN_POINT('Ctrl Pts',(1.46718470041356,0.523511886852931,
12.743384755441));
#268248=CARTESIAN_POINT('Ctrl Pts',(1.43457658310325,0.601307140496281,
12.749909041778));
#268249=CARTESIAN_POINT('Origin',(0.,0.,-1.29405622560371));
#268250=CARTESIAN_POINT('',(1.43457670670211,0.601306845618552,13.5890749702576));
#268251=CARTESIAN_POINT('',(1.43457668314421,0.601306901822156,13.4515605039018));
#268252=CARTESIAN_POINT('',(1.43457668357355,0.601306900797845,-1.29405622560371));
#268253=CARTESIAN_POINT('',(-1.55549936700331,-0.00142192595573973,13.1940429763088));
#268254=CARTESIAN_POINT('Ctrl Pts',(1.43457670670211,0.601306845618552,
13.5890749702576));
#268255=CARTESIAN_POINT('Ctrl Pts',(1.45865647660418,0.543858178177025,
13.5843171061907));
#268256=CARTESIAN_POINT('Ctrl Pts',(1.47926802300138,0.485004505948749,
13.5794850661721));
#268257=CARTESIAN_POINT('Ctrl Pts',(1.52008574292279,0.341318809516777,
13.5679023622844));
#268258=CARTESIAN_POINT('Ctrl Pts',(1.53680621093689,0.255714392750175,
13.5611697067846));
#268259=CARTESIAN_POINT('Ctrl Pts',(1.54713080553736,0.161333096143716,
13.5541942793966));
#268260=CARTESIAN_POINT('Ctrl Pts',(1.54792672424916,0.153508829286314,
13.553619393256));
#268261=CARTESIAN_POINT('Ctrl Pts',(1.5490387721051,0.141687002620586,13.5527562187289));
#268262=CARTESIAN_POINT('Ctrl Pts',(1.54939882710123,0.137693862439449,
13.5524655925377));
#268263=CARTESIAN_POINT('Ctrl Pts',(1.55001651315244,0.130534103140939,
13.5519462221477));
#268264=CARTESIAN_POINT('Ctrl Pts',(1.55027988470742,0.127368060485406,
13.5517171648972));
#268265=CARTESIAN_POINT('Ctrl Pts',(1.5508330899526,0.120461816918602,13.5512188408898));
#268266=CARTESIAN_POINT('Ctrl Pts',(1.55111909413622,0.116721372670901,
13.550949789956));
#268267=CARTESIAN_POINT('Ctrl Pts',(1.55189145955195,0.106115579625303,
13.5501892079015));
#268268=CARTESIAN_POINT('Ctrl Pts',(1.55234580020136,0.0992478702810322,
13.5496994223305));
#268269=CARTESIAN_POINT('Ctrl Pts',(1.55497038625052,0.0551315965832953,
13.5465693417098));
#268270=CARTESIAN_POINT('Ctrl Pts',(1.55584562602841,0.0178144299041783,
13.5439955536589));
#268271=CARTESIAN_POINT('Ctrl Pts',(1.55405865316281,-0.124707051753495,
13.5343239609659));
#268272=CARTESIAN_POINT('Ctrl Pts',(1.5420690022035,-0.229514357431623,
13.5275250686444));
#268273=CARTESIAN_POINT('Ctrl Pts',(1.5022580284579,-0.41155925816425,13.5151756968029));
#268274=CARTESIAN_POINT('Ctrl Pts',(1.47875894083323,-0.489315115857666,
13.5097181953477));
#268275=CARTESIAN_POINT('Ctrl Pts',(1.44502094592174,-0.575876790834559,
13.5032286048885));
#268276=CARTESIAN_POINT('Ctrl Pts',(1.44060894138887,-0.586826615692031,
13.502400002413));
#268277=CARTESIAN_POINT('Ctrl Pts',(1.43325670151859,-0.60449084873319,
13.5010502410663));
#268278=CARTESIAN_POINT('Ctrl Pts',(1.43039283032183,-0.611236702346225,
13.5005316565034));
#268279=CARTESIAN_POINT('Ctrl Pts',(1.42521611655373,-0.623194821552002,
13.4996066927768));
#268280=CARTESIAN_POINT('Ctrl Pts',(1.42292206433732,-0.628415118954393,
13.4992009587135));
#268281=CARTESIAN_POINT('Ctrl Pts',(1.4180328568701,-0.639376856903346,
13.4983448244155));
#268282=CARTESIAN_POINT('Ctrl Pts',(1.41543142234358,-0.645115365489947,
13.4978942151));
#268283=CARTESIAN_POINT('Ctrl Pts',(1.40846157284832,-0.660245048516545,
13.4966996648346));
#268284=CARTESIAN_POINT('Ctrl Pts',(1.40403416509097,-0.669608527343406,
13.4959537049001));
#268285=CARTESIAN_POINT('Ctrl Pts',(1.38278833447639,-0.713403862462427,
13.4924325196657));
#268286=CARTESIAN_POINT('Ctrl Pts',(1.36479619656187,-0.74724795975849,
13.4896168695039));
#268287=CARTESIAN_POINT('Ctrl Pts',(1.27025692406576,-0.910255563427451,
13.4755678538875));
#268288=CARTESIAN_POINT('Ctrl Pts',(1.17653771174988,-1.02852426048133,
13.4637154610322));
#268289=CARTESIAN_POINT('Ctrl Pts',(1.03867740986663,-1.15857033205153,
13.4492663910669));
#268290=CARTESIAN_POINT('Ctrl Pts',(1.00896372847602,-1.18453738778254,
13.4462993004457));
#268291=CARTESIAN_POINT('Ctrl Pts',(0.973126711431908,-1.21352741692326,
13.4429169777336));
#268292=CARTESIAN_POINT('Ctrl Pts',(0.967934653940546,-1.2176727384809,
13.4424315698324));
#268293=CARTESIAN_POINT('Ctrl Pts',(0.959496052635796,-1.22432200875417,
13.4416502909437));
#268294=CARTESIAN_POINT('Ctrl Pts',(0.956265963444916,-1.22684655289302,
13.441353028632));
#268295=CARTESIAN_POINT('Ctrl Pts',(0.950509470250032,-1.23130911424539,
13.4408264934953));
#268296=CARTESIAN_POINT('Ctrl Pts',(0.947987063070771,-1.23325217081216,
13.440596869988));
#268297=CARTESIAN_POINT('Ctrl Pts',(0.942531918220844,-1.23742774227772,
13.4401026380868));
#268298=CARTESIAN_POINT('Ctrl Pts',(0.939597210115723,-1.23965758083888,
13.4398382165388));
#268299=CARTESIAN_POINT('Ctrl Pts',(0.931401722497112,-1.24583882171926,
13.4391037606934));
#268300=CARTESIAN_POINT('Ctrl Pts',(0.926123673893443,-1.24976737161002,
13.4386352869109));
#268301=CARTESIAN_POINT('Ctrl Pts',(0.895332820379853,-1.27238339338094,
13.4359274617279));
#268302=CARTESIAN_POINT('Ctrl Pts',(0.869277570227663,-1.29032446616473,
13.4337356084054));
#268303=CARTESIAN_POINT('Ctrl Pts',(0.720112008040473,-1.38646543964895,
13.4216228284471));
#268304=CARTESIAN_POINT('Ctrl Pts',(0.587024807379808,-1.44784598767101,
13.412367685377));
#268305=CARTESIAN_POINT('Ctrl Pts',(0.400140260560503,-1.50395978040451,
13.3992066305443));
#268306=CARTESIAN_POINT('Ctrl Pts',(0.352314943247857,-1.51587618345896,
13.3958325591057));
#268307=CARTESIAN_POINT('Ctrl Pts',(0.292676964265228,-1.52776109089081,
13.3915761664699));
#268308=CARTESIAN_POINT('Ctrl Pts',(0.281320765834508,-1.52989292769967,
13.3907635776079));
#268309=CARTESIAN_POINT('Ctrl Pts',(0.263410496588431,-1.53304897095434,
13.3894782459837));
#268310=CARTESIAN_POINT('Ctrl Pts',(0.256871654844472,-1.53415813641352,
13.3890081991548));
#268311=CARTESIAN_POINT('Ctrl Pts',(0.244791494970911,-1.53612786552186,
13.3881382693904));
#268312=CARTESIAN_POINT('Ctrl Pts',(0.23925220739389,-1.53700034970343,
13.3877387709431));
#268313=CARTESIAN_POINT('Ctrl Pts',(0.226966212681123,-1.53886747158078,
13.3868513103064));
#268314=CARTESIAN_POINT('Ctrl Pts',(0.220217472080572,-1.53984772592532,
13.3863629022416));
#268315=CARTESIAN_POINT('Ctrl Pts',(0.201296294613768,-1.54246909591618,
13.3849908658806));
#268316=CARTESIAN_POINT('Ctrl Pts',(0.189110784996112,-1.54401042903936,
13.3841041200772));
#268317=CARTESIAN_POINT('Ctrl Pts',(0.16152054228375,-1.54716878856753,
13.3820888176029));
#268318=CARTESIAN_POINT('Ctrl Pts',(0.146107547853411,-1.54870032554592,
13.3809576847575));
#268319=CARTESIAN_POINT('Ctrl Pts',(0.0968600525073427,-1.55285219559935,
13.377325733894));
#268320=CARTESIAN_POINT('Ctrl Pts',(0.0629636142149593,-1.5545954713363,
13.3747989674912));
#268321=CARTESIAN_POINT('Ctrl Pts',(-0.0953325866465109,-1.55755120588528,
13.3628732576448));
#268322=CARTESIAN_POINT('Ctrl Pts',(-0.219527562206013,-1.5449449237587,
13.3531061291233));
#268323=CARTESIAN_POINT('Ctrl Pts',(-0.352018721021943,-1.51518765062239,
13.342687590316));
#268324=CARTESIAN_POINT('Ctrl Pts',(-0.363139000214201,-1.51256103130583,
13.3418135695069));
#268325=CARTESIAN_POINT('Ctrl Pts',(-0.411836161330166,-1.50049071033415,
13.3379904815714));
#268326=CARTESIAN_POINT('Ctrl Pts',(-0.449085440557114,-1.48976652035185,
13.3350773271913));
#268327=CARTESIAN_POINT('Ctrl Pts',(-0.492175702757902,-1.47559716263511,
13.3317491872374));
#268328=CARTESIAN_POINT('Ctrl Pts',(-0.498439469931759,-1.4734931312073,
13.3312664547501));
#268329=CARTESIAN_POINT('Ctrl Pts',(-0.508557276873416,-1.47002260644851,
13.3304886292608));
#268330=CARTESIAN_POINT('Ctrl Pts',(-0.512419581614434,-1.46868074840852,
13.3301921643284));
#268331=CARTESIAN_POINT('Ctrl Pts',(-0.519279189064021,-1.46626720122315,
13.3296665001026));
#268332=CARTESIAN_POINT('Ctrl Pts',(-0.522278531743087,-1.465201527966,
13.3294369546342));
#268333=CARTESIAN_POINT('Ctrl Pts',(-0.528750797503353,-1.46287951754892,
13.3289422764567));
#268334=CARTESIAN_POINT('Ctrl Pts',(-0.532222520104307,-1.4616200185369,
13.3286773339011));
#268335=CARTESIAN_POINT('Ctrl Pts',(-0.541535111472556,-1.45820394274807,
13.3279676467945));
#268336=CARTESIAN_POINT('Ctrl Pts',(-0.547367654961516,-1.4560246115361,
13.3275242221131));
#268337=CARTESIAN_POINT('Ctrl Pts',(-0.579679529621522,-1.44372967031622,
13.3250727221209));
#268338=CARTESIAN_POINT('Ctrl Pts',(-0.605893714508587,-1.43292595510251,
13.3231026946037));
#268339=CARTESIAN_POINT('Ctrl Pts',(-0.766692546522229,-1.36145280517023,
13.3110482023596));
#268340=CARTESIAN_POINT('Ctrl Pts',(-0.892374016857767,-1.28259484816741,
13.3016908299711));
#268341=CARTESIAN_POINT('Ctrl Pts',(-1.04390505051855,-1.15431033337945,
13.2883149588975));
#268342=CARTESIAN_POINT('Ctrl Pts',(-1.08110490532008,-1.11954516731242,
13.2848327703219));
#268343=CARTESIAN_POINT('Ctrl Pts',(-1.12465509032343,-1.0746475286691,
13.28045542583));
#268344=CARTESIAN_POINT('Ctrl Pts',(-1.13268401615312,-1.06618164001697,
13.2796349847631));
#268345=CARTESIAN_POINT('Ctrl Pts',(-1.14514371580149,-1.05274424683791,
13.2783399397987));
#268346=CARTESIAN_POINT('Ctrl Pts',(-1.1496392187029,-1.04783311811135,
13.2778681003129));
#268347=CARTESIAN_POINT('Ctrl Pts',(-1.15751891709497,-1.03911316271139,
13.2770328255442));
#268348=CARTESIAN_POINT('Ctrl Pts',(-1.16091621203529,-1.03531625885682,
13.2766699490089));
#268349=CARTESIAN_POINT('Ctrl Pts',(-1.16866084484423,-1.02657460969551,
13.2758363287833));
#268350=CARTESIAN_POINT('Ctrl Pts',(-1.1729955378379,-1.02161884540701,
13.2753650678692));
#268351=CARTESIAN_POINT('Ctrl Pts',(-1.18180904725329,-1.01141250377658,
13.2743971375996));
#268352=CARTESIAN_POINT('Ctrl Pts',(-1.18628463796444,-1.00615934714186,
13.273900349496));
#268353=CARTESIAN_POINT('Ctrl Pts',(-1.20780594330266,-0.980555835174825,
13.2714855962354));
#268354=CARTESIAN_POINT('Ctrl Pts',(-1.22436279966232,-0.959802331887778,
13.2695480587677));
#268355=CARTESIAN_POINT('Ctrl Pts',(-1.27644531427125,-0.890976870139557,
13.2631810105464));
#268356=CARTESIAN_POINT('Ctrl Pts',(-1.30972975110126,-0.841284036024207,
13.2586708795457));
#268357=CARTESIAN_POINT('Ctrl Pts',(-1.36744771550181,-0.743353417773102,
13.2499609303454));
#268358=CARTESIAN_POINT('Ctrl Pts',(-1.39239043495957,-0.695511298393266,
13.2457800708118));
#268359=CARTESIAN_POINT('Ctrl Pts',(-1.44893884953429,-0.571755834475074,
13.2352284161469));
#268360=CARTESIAN_POINT('Ctrl Pts',(-1.47711133093812,-0.494442798788441,
13.2288690966019));
#268361=CARTESIAN_POINT('Ctrl Pts',(-1.50233780352053,-0.403377446876232,
13.2218699021356));
#268362=CARTESIAN_POINT('Ctrl Pts',(-1.50548779756471,-0.391457223010544,
13.2209632748028));
#268363=CARTESIAN_POINT('Ctrl Pts',(-1.50968822552226,-0.374760719961676,
13.2197078315613));
#268364=CARTESIAN_POINT('Ctrl Pts',(-1.51085826887459,-0.370015443763787,
13.2193526469601));
#268365=CARTESIAN_POINT('Ctrl Pts',(-1.51270669089005,-0.362363936520089,
13.218782625625));
#268366=CARTESIAN_POINT('Ctrl Pts',(-1.51339909257423,-0.359461183108582,
13.2185669996639));
#268367=CARTESIAN_POINT('Ctrl Pts',(-1.51483812258624,-0.35335047817249,
13.218114412214));
#268368=CARTESIAN_POINT('Ctrl Pts',(-1.51558292238446,-0.350142119451603,
13.2178775611972));
#268369=CARTESIAN_POINT('Ctrl Pts',(-1.51705901456637,-0.343690629268269,
13.2174028042245));
#268370=CARTESIAN_POINT('Ctrl Pts',(-1.51779011399703,-0.340447459570058,
13.2171649094264));
#268371=CARTESIAN_POINT('Ctrl Pts',(-1.51951374458998,-0.33268548827976,
13.2165973242223));
#268372=CARTESIAN_POINT('Ctrl Pts',(-1.52049653203074,-0.328164519125983,
13.2162681699804));
#268373=CARTESIAN_POINT('Ctrl Pts',(-1.52308642920974,-0.315989160648673,
13.2153854226322));
#268374=CARTESIAN_POINT('Ctrl Pts',(-1.52465603060778,-0.308326799373177,
13.2148337991552));
#268375=CARTESIAN_POINT('Ctrl Pts',(-1.54558199302605,-0.202102815742466,
13.2072365938642));
#268376=CARTESIAN_POINT('Ctrl Pts',(-1.55540751071694,-0.101891035777499,
13.2006549036526));
#268377=CARTESIAN_POINT('Ctrl Pts',(-1.55549935012108,-0.00142189060349853,
13.1940429475177));
#268378=CARTESIAN_POINT('Ctrl Pts',(-1.5554993500872,-0.00142192767448274,
13.1940429499574));
#268379=CARTESIAN_POINT('Ctrl Pts',(-1.55560532666497,0.114509776029417,
13.1864133902736));
#268380=CARTESIAN_POINT('Ctrl Pts',(-1.54275149737557,0.230076481554751,
13.1787694472679));
#268381=CARTESIAN_POINT('Ctrl Pts',(-1.51509323349481,0.352366628040915,
13.1700144932057));
#268382=CARTESIAN_POINT('Ctrl Pts',(-1.51292222855975,0.361574432401795,
13.1693513464451));
#268383=CARTESIAN_POINT('Ctrl Pts',(-1.50913380558097,0.377010350794123,
13.1682327101714));
#268384=CARTESIAN_POINT('Ctrl Pts',(-1.50756146729406,0.383249354671272,
13.1677786567778));
#268385=CARTESIAN_POINT('Ctrl Pts',(-1.50438393824964,0.395535535725688,
13.166880629426));
#268386=CARTESIAN_POINT('Ctrl Pts',(-1.50278087943554,0.401583142086659,
13.1664367313259));
#268387=CARTESIAN_POINT('Ctrl Pts',(-1.49964423762699,0.413134423311204,
13.1655852093262));
#268388=CARTESIAN_POINT('Ctrl Pts',(-1.49811672757471,0.418639654275458,
13.1651777881848));
#268389=CARTESIAN_POINT('Ctrl Pts',(-1.49457053617927,0.431152341152361,
13.1642480731838));
#268390=CARTESIAN_POINT('Ctrl Pts',(-1.49253284844343,0.438154221544365,
13.1637251692766));
#268391=CARTESIAN_POINT('Ctrl Pts',(-1.48702672798701,0.456590105710933,
13.1623412197185));
#268392=CARTESIAN_POINT('Ctrl Pts',(-1.48347571470457,0.467998721624268,
13.161477502689));
#268393=CARTESIAN_POINT('Ctrl Pts',(-1.45067209494675,0.569263081057521,
13.1537442097845));
#268394=CARTESIAN_POINT('Ctrl Pts',(-1.41342513761139,0.656302509391999,
13.146607677695));
#268395=CARTESIAN_POINT('Ctrl Pts',(-1.34146758101601,0.789483469408031,
13.134937233164));
#268396=CARTESIAN_POINT('Ctrl Pts',(-1.31168601895308,0.838032817961845,
13.1305093920219));
#268397=CARTESIAN_POINT('Ctrl Pts',(-1.24454219641953,0.935110167357172,
13.1213801067369));
#268398=CARTESIAN_POINT('Ctrl Pts',(-1.20683566660835,0.983293241526527,
13.1166901917138));
#268399=CARTESIAN_POINT('Ctrl Pts',(-1.15705682664943,1.03971083680104,
13.1111023098393));
#268400=CARTESIAN_POINT('Ctrl Pts',(-1.14758278044537,1.0501585232005,13.1100632427421));
#268401=CARTESIAN_POINT('Ctrl Pts',(-1.13532145456876,1.0633158085424,13.1087507584632));
#268402=CARTESIAN_POINT('Ctrl Pts',(-1.13266473845105,1.06614534892473,
13.1084682657019));
#268403=CARTESIAN_POINT('Ctrl Pts',(-1.12747518450364,1.07163120002392,
13.107920164797));
#268404=CARTESIAN_POINT('Ctrl Pts',(-1.12494348322294,1.07428854636398,
13.1076544755705));
#268405=CARTESIAN_POINT('Ctrl Pts',(-1.12019636800393,1.07923607219256,
13.107159495127));
#268406=CARTESIAN_POINT('Ctrl Pts',(-1.11798334561292,1.08152838226147,
13.1069300373096));
#268407=CARTESIAN_POINT('Ctrl Pts',(-1.11289058649208,1.08677126864311,
13.1064049268886));
#268408=CARTESIAN_POINT('Ctrl Pts',(-1.1100061521652,1.08971720692291,13.1061096448164));
#268409=CARTESIAN_POINT('Ctrl Pts',(-1.1023884202592,1.0974357390234,13.1053352742));
#268410=CARTESIAN_POINT('Ctrl Pts',(-1.09763577379955,1.10218924999249,
13.1048576482712));
#268411=CARTESIAN_POINT('Ctrl Pts',(-1.06349102594555,1.1359003044778,13.1014638391734));
#268412=CARTESIAN_POINT('Ctrl Pts',(-1.03298465154647,1.16371221366005,
13.0986288910756));
#268413=CARTESIAN_POINT('Ctrl Pts',(-0.986915767935382,1.20247081242974,
13.0945611493805));
#268414=CARTESIAN_POINT('Ctrl Pts',(-0.972204664422465,1.21439570218504,
13.0932919754945));
#268415=CARTESIAN_POINT('Ctrl Pts',(-0.872144057891693,1.29252136973191,
13.0848289421818));
#268416=CARTESIAN_POINT('Ctrl Pts',(-0.780318232993791,1.34994478672804,
13.0778515516041));
#268417=CARTESIAN_POINT('Ctrl Pts',(-0.64948818760217,1.41391670476706,
13.0680745669525));
#268418=CARTESIAN_POINT('Ctrl Pts',(-0.615107885555045,1.42920862997314,
13.06552176588));
#268419=CARTESIAN_POINT('Ctrl Pts',(-0.564764787435561,1.44944750182462,
13.0617826480369));
#268420=CARTESIAN_POINT('Ctrl Pts',(-0.549222369575856,1.45540787372533,
13.0606281985852));
#268421=CARTESIAN_POINT('Ctrl Pts',(-0.521376076388962,1.46557710503839,
13.0585577064921));
#268422=CARTESIAN_POINT('Ctrl Pts',(-0.509109280853314,1.46988332393,13.0576448914661));
#268423=CARTESIAN_POINT('Ctrl Pts',(-0.491435989831771,1.47583970761921,
13.0563280784612));
#268424=CARTESIAN_POINT('Ctrl Pts',(-0.486071981170295,1.47761503859665,
13.0559281939286));
#268425=CARTESIAN_POINT('Ctrl Pts',(-0.475223985267353,1.48113994892571,
13.055118973102));
#268426=CARTESIAN_POINT('Ctrl Pts',(-0.469739724351119,1.48288838899446,
13.0547096068622));
#268427=CARTESIAN_POINT('Ctrl Pts',(-0.459100580465859,1.48621531774945,
13.0539148968668));
#268428=CARTESIAN_POINT('Ctrl Pts',(-0.453946939829438,1.48779752929173,
13.0535296816134));
#268429=CARTESIAN_POINT('Ctrl Pts',(-0.44164454600721,1.49150459746582,
13.0526094627482));
#268430=CARTESIAN_POINT('Ctrl Pts',(-0.434488589985751,1.49360487775552,
13.0520736669071));
#268431=CARTESIAN_POINT('Ctrl Pts',(-0.408750275005844,1.50095848114298,
13.0501444417567));
#268432=CARTESIAN_POINT('Ctrl Pts',(-0.390086268774325,1.50591692664642,
13.0487415466751));
#268433=CARTESIAN_POINT('Ctrl Pts',(-0.231012431485575,1.54502234670856,
13.0367459444016));
#268434=CARTESIAN_POINT('Ctrl Pts',(-0.0865916555847983,1.55978968356651,
13.0255025276203));
#268435=CARTESIAN_POINT('Ctrl Pts',(0.104580207163462,1.55268793576817,
13.010716817981));
#268436=CARTESIAN_POINT('Ctrl Pts',(0.151316968064041,1.54883204359739,
13.0071192403454));
#268437=CARTESIAN_POINT('Ctrl Pts',(0.213631181874183,1.54084273850421,
13.002397335285));
#268438=CARTESIAN_POINT('Ctrl Pts',(0.229419505095176,1.53857120893022,
13.0012075346182));
#268439=CARTESIAN_POINT('Ctrl Pts',(0.256073786931493,1.53431690627593,
12.9992129705051));
#268440=CARTESIAN_POINT('Ctrl Pts',(0.266958344467703,1.53246057508004,
12.9984024702484));
#268441=CARTESIAN_POINT('Ctrl Pts',(0.282278053802187,1.52967965775119,
12.9972682135915));
#268442=CARTESIAN_POINT('Ctrl Pts',(0.286730009584213,1.52885141789327,
12.9969393718969));
#268443=CARTESIAN_POINT('Ctrl Pts',(0.2943819094531,1.52739326199613,12.9963755778687));
#268444=CARTESIAN_POINT('Ctrl Pts',(0.297583585667985,1.52677270599082,
12.9961401035246));
#268445=CARTESIAN_POINT('Ctrl Pts',(0.303746662533513,1.52555804127153,
12.9956876750254));
#268446=CARTESIAN_POINT('Ctrl Pts',(0.306708298186996,1.52496537420939,
12.9954706377838));
#268447=CARTESIAN_POINT('Ctrl Pts',(0.314642991614519,1.52335347423595,
12.9948901198869));
#268448=CARTESIAN_POINT('Ctrl Pts',(0.319612876292937,1.52231850507107,
12.99452752485));
#268449=CARTESIAN_POINT('Ctrl Pts',(0.337809312421182,1.51843609151781,
12.9932033508101));
#268450=CARTESIAN_POINT('Ctrl Pts',(0.351004128039468,1.51544034215433,
12.9922497638899));
#268451=CARTESIAN_POINT('Ctrl Pts',(0.519034662137245,1.47497820036408,
12.9801710586475));
#268452=CARTESIAN_POINT('Ctrl Pts',(0.66728645537411,1.41410911376194,12.9701384119536));
#268453=CARTESIAN_POINT('Ctrl Pts',(0.852479784879324,1.30234451359323,
12.9556166853679));
#268454=CARTESIAN_POINT('Ctrl Pts',(0.89957653346717,1.27026920346239,12.9517306723403));
#268455=CARTESIAN_POINT('Ctrl Pts',(0.954059686325388,1.22861144325625,
12.9469298716769));
#268456=CARTESIAN_POINT('Ctrl Pts',(0.963234115898543,1.22143194181302,
12.9461105072023));
#268457=CARTESIAN_POINT('Ctrl Pts',(0.977465937982646,1.21003468478247,
12.9448216800265));
#268458=CARTESIAN_POINT('Ctrl Pts',(0.9825787994208,1.20588660279634,12.9443549993826));
#268459=CARTESIAN_POINT('Ctrl Pts',(0.991601206928114,1.19847121565272,
12.9435248545138));
#268460=CARTESIAN_POINT('Ctrl Pts',(0.995521350429314,1.19521690417903,
12.9431619195307));
#268461=CARTESIAN_POINT('Ctrl Pts',(1.00452734580211,1.1876655219114,12.9423228769869));
#268462=CARTESIAN_POINT('Ctrl Pts',(1.00960170512964,1.18335496570163,12.9418462227313));
#268463=CARTESIAN_POINT('Ctrl Pts',(1.02349211450505,1.17140099234914,12.9405305301814));
#268464=CARTESIAN_POINT('Ctrl Pts',(1.03224991886995,1.1636908887341,12.9396887487776));
#268465=CARTESIAN_POINT('Ctrl Pts',(1.07874143173811,1.12182338561223,12.935152800035));
#268466=CARTESIAN_POINT('Ctrl Pts',(1.11486400381476,1.08593183256602,12.9313857880437));
#268467=CARTESIAN_POINT('Ctrl Pts',(1.24867531701197,0.939251589313107,
12.9164274177818));
#268468=CARTESIAN_POINT('Ctrl Pts',(1.33213542888772,0.816571739045674,
12.9047271564757));
#268469=CARTESIAN_POINT('Ctrl Pts',(1.40952661595457,0.658498329059338,
12.8914388014644));
#268470=CARTESIAN_POINT('Ctrl Pts',(1.42130463026261,0.632675864308015,
12.889322724023));
#268471=CARTESIAN_POINT('Ctrl Pts',(1.4331090631311,0.604799347628273,12.8871063962525));
#268472=CARTESIAN_POINT('Ctrl Pts',(1.43384446664119,0.603053797993081,
12.8869678972309));
#268473=CARTESIAN_POINT('Ctrl Pts',(1.43457668357408,0.601306900796593,
12.8868295753666));
#268474=CARTESIAN_POINT('Ctrl Pts',(1.43457658310325,0.601307140496281,
12.749909041778));
#268475=CARTESIAN_POINT('Ctrl Pts',(1.40228372079604,0.6783502702836,12.7563702513696));
#268476=CARTESIAN_POINT('Ctrl Pts',(1.36378817913178,0.752783104809556,
12.7629010726667));
#268477=CARTESIAN_POINT('Ctrl Pts',(1.30172901177612,0.852171572957744,
12.7717880182731));
#268478=CARTESIAN_POINT('Ctrl Pts',(1.2831381829391,0.879915697305408,12.7742872593444));
#268479=CARTESIAN_POINT('Ctrl Pts',(1.25973790685436,0.912516333320734,
12.7772276251402));
#268480=CARTESIAN_POINT('Ctrl Pts',(1.25577314197408,0.917964853837816,
12.7777191667732));
#268481=CARTESIAN_POINT('Ctrl Pts',(1.24954763807542,0.926404341162586,
12.7784805139681));
#268482=CARTESIAN_POINT('Ctrl Pts',(1.24731134518913,0.929413100894063,
12.7787519363812));
#268483=CARTESIAN_POINT('Ctrl Pts',(1.24313212303325,0.934993670167423,
12.7792553090446));
#268484=CARTESIAN_POINT('Ctrl Pts',(1.2411920948355,0.937567502968436,12.7794874441212));
#268485=CARTESIAN_POINT('Ctrl Pts',(1.23674603205329,0.943428102332941,
12.7800159740925));
#268486=CARTESIAN_POINT('Ctrl Pts',(1.23423488992615,0.946710921889629,
12.7803120069392));
#268487=CARTESIAN_POINT('Ctrl Pts',(1.2276389665983,0.955262930364784,12.7810832504053));
#268488=CARTESIAN_POINT('Ctrl Pts',(1.22353328455597,0.960516009361563,
12.7815570414815));
#268489=CARTESIAN_POINT('Ctrl Pts',(1.19524232048095,0.996237562853903,
12.7847805233195));
#268490=CARTESIAN_POINT('Ctrl Pts',(1.16995276655549,1.02581901059186,12.7874582599539));
#268491=CARTESIAN_POINT('Ctrl Pts',(1.04152227898642,1.16510860655659,12.8002870147671));
#268492=CARTESIAN_POINT('Ctrl Pts',(0.923937739193306,1.26039358871116,
12.8098415741555));
#268493=CARTESIAN_POINT('Ctrl Pts',(0.772806328867017,1.35018016463913,
12.8218075618696));
#268494=CARTESIAN_POINT('Ctrl Pts',(0.750818561725533,1.36252980584718,
12.8235391458762));
#268495=CARTESIAN_POINT('Ctrl Pts',(0.712315887237081,1.38294019052209,
12.8265631473355));
#268496=CARTESIAN_POINT('Ctrl Pts',(0.695940054740942,1.39125299074903,
12.8278468097822));
#268497=CARTESIAN_POINT('Ctrl Pts',(0.672270587057553,1.40274577125392,
12.829700605158));
#268498=CARTESIAN_POINT('Ctrl Pts',(0.665093305691609,1.40616298184091,
12.8302625195112));
#268499=CARTESIAN_POINT('Ctrl Pts',(0.652585778977298,1.41200082098948,
12.8312415366845));
#268500=CARTESIAN_POINT('Ctrl Pts',(0.647267426161632,1.41444667439876,
12.8316577624454));
#268501=CARTESIAN_POINT('Ctrl Pts',(0.636995343196801,1.41910062965395,
12.8324616174887));
#268502=CARTESIAN_POINT('Ctrl Pts',(0.63204361292717,1.42131296142817,12.832849094657));
#268503=CARTESIAN_POINT('Ctrl Pts',(0.6202980466784,1.42648712279473,12.8337681877066));
#268504=CARTESIAN_POINT('Ctrl Pts',(0.613494466018343,1.42942635866672,
12.8343005636465));
#268505=CARTESIAN_POINT('Ctrl Pts',(0.58945120747819,1.439610089999,12.8361820993049));
#268506=CARTESIAN_POINT('Ctrl Pts',(0.57210278054025,1.44659195667141,12.8375400454521));
#268507=CARTESIAN_POINT('Ctrl Pts',(0.45366101912095,1.49179501438343,12.8468173264569));
#268508=CARTESIAN_POINT('Ctrl Pts',(0.34896724615083,1.51969531058973,12.8550794889915));
#268509=CARTESIAN_POINT('Ctrl Pts',(0.168152024005762,1.54820285716115,
12.8692633673445));
#268510=CARTESIAN_POINT('Ctrl Pts',(0.093302731761542,1.55451052067063,
12.8751018308152));
#268511=CARTESIAN_POINT('Ctrl Pts',(-0.0134353899226439,1.5557654713372,
12.8831863143454));
#268512=CARTESIAN_POINT('Ctrl Pts',(-0.0451649484647025,1.55516790270789,
12.8855583847279));
#268513=CARTESIAN_POINT('Ctrl Pts',(-0.0834904111891236,1.55327193833299,
12.8883693715831));
#268514=CARTESIAN_POINT('Ctrl Pts',(-0.0901220650063386,1.55290127852089,
12.8888538007289));
#268515=CARTESIAN_POINT('Ctrl Pts',(-0.100471855152008,1.55225627800856,
12.8896065482265));
#268516=CARTESIAN_POINT('Ctrl Pts',(-0.104191618366901,1.55201103531839,
12.8898764263521));
#268517=CARTESIAN_POINT('Ctrl Pts',(-0.111128678421574,1.55152862476989,
12.8903784465026));
#268518=CARTESIAN_POINT('Ctrl Pts',(-0.114346088047813,1.55129482340083,
12.8906107638171));
#268519=CARTESIAN_POINT('Ctrl Pts',(-0.121714770198221,1.55073630970753,
12.8911416624902));
#268520=CARTESIAN_POINT('Ctrl Pts',(-0.125865481649582,1.55040493715256,
12.8914398690967));
#268521=CARTESIAN_POINT('Ctrl Pts',(-0.136760923365318,1.54949105487974,
12.8922205517017));
#268522=CARTESIAN_POINT('Ctrl Pts',(-0.143503365503485,1.54888116645628,
12.8927015509941));
#268523=CARTESIAN_POINT('Ctrl Pts',(-0.1911323947483,1.54425919012869,12.896085804839));
#268524=CARTESIAN_POINT('Ctrl Pts',(-0.231854302044268,1.53867226965545,
12.8989087314909));
#268525=CARTESIAN_POINT('Ctrl Pts',(-0.31308739480184,1.52422825958511,
12.9044841285828));
#268526=CARTESIAN_POINT('Ctrl Pts',(-0.35355983257934,1.51535187651162,
12.9072336623691));
#268527=CARTESIAN_POINT('Ctrl Pts',(-0.439317677535034,1.4929200410687,
12.9130868951461));
#268528=CARTESIAN_POINT('Ctrl Pts',(-0.484435839807965,1.47889560521561,
12.9161833770986));
#268529=CARTESIAN_POINT('Ctrl Pts',(-0.616204196510021,1.43125870218765,
12.925435586729));
#268530=CARTESIAN_POINT('Ctrl Pts',(-0.700544290145323,1.39192056937093,
12.9316466269394));
#268531=CARTESIAN_POINT('Ctrl Pts',(-0.792103182272308,1.33877617675636,
12.9390429035172));
#268532=CARTESIAN_POINT('Ctrl Pts',(-0.803259054430659,1.33211259895255,
12.9399555749378));
#268533=CARTESIAN_POINT('Ctrl Pts',(-0.820228387576899,1.3216858820524,
12.9413622624499));
#268534=CARTESIAN_POINT('Ctrl Pts',(-0.826102583131821,1.3180222676205,
12.9418526437559));
#268535=CARTESIAN_POINT('Ctrl Pts',(-0.836751465092908,1.31128162479135,
12.9427480034049));
#268536=CARTESIAN_POINT('Ctrl Pts',(-0.841534152912501,1.30821740615402,
12.9431525034268));
#268537=CARTESIAN_POINT('Ctrl Pts',(-0.851924833250524,1.30147964730193,
12.944036554533));
#268538=CARTESIAN_POINT('Ctrl Pts',(-0.857526051997652,1.29779592440225,
12.9445164793394));
#268539=CARTESIAN_POINT('Ctrl Pts',(-0.87279218017388,1.28761395480967,
12.9458338847357));
#268540=CARTESIAN_POINT('Ctrl Pts',(-0.882408024098973,1.28104330593842,
12.9466740718866));
#268541=CARTESIAN_POINT('Ctrl Pts',(-0.932315867409602,1.24611200146705,
12.9510904273366));
#268542=CARTESIAN_POINT('Ctrl Pts',(-0.971312976945295,1.21595974625617,
12.9547345262802));
#268543=CARTESIAN_POINT('Ctrl Pts',(-1.1206553678197,1.08871590608621,12.9694993093467));
#268544=CARTESIAN_POINT('Ctrl Pts',(-1.21841436714455,0.978073296096773,
12.9811327007383));
#268545=CARTESIAN_POINT('Ctrl Pts',(-1.31032144964198,0.838479084850347,
12.9937749190824));
#268546=CARTESIAN_POINT('Ctrl Pts',(-1.32111561701813,0.821366601300952,
12.9952923480351));
#268547=CARTESIAN_POINT('Ctrl Pts',(-1.3384657430439,0.792633265348912,
12.9977814551326));
#268548=CARTESIAN_POINT('Ctrl Pts',(-1.3452113011274,0.781130351486874,
12.9987627146716));
#268549=CARTESIAN_POINT('Ctrl Pts',(-1.35424656077656,0.765258643229806,
13.0000945341625));
#268550=CARTESIAN_POINT('Ctrl Pts',(-1.35666439424859,0.760964034351721,
13.000452711198));
#268551=CARTESIAN_POINT('Ctrl Pts',(-1.36069218683463,0.75372956429974,
13.0010523159055));
#268552=CARTESIAN_POINT('Ctrl Pts',(-1.36231311079477,0.75079589256053,
13.001294430726));
#268553=CARTESIAN_POINT('Ctrl Pts',(-1.36537122967589,0.745218564666876,
13.0017527367919));
#268554=CARTESIAN_POINT('Ctrl Pts',(-1.3668102515783,0.742575949350076,
13.00196904677));
#268555=CARTESIAN_POINT('Ctrl Pts',(-1.37056229000855,0.735637859191506,
13.0025348024319));
#268556=CARTESIAN_POINT('Ctrl Pts',(-1.37286280772509,0.731335602550337,
13.0028834622806));
#268557=CARTESIAN_POINT('Ctrl Pts',(-1.3807844238112,0.716352083656887,
13.0040905093476));
#268558=CARTESIAN_POINT('Ctrl Pts',(-1.38630160289683,0.70561591698935,
13.0049426829418));
#268559=CARTESIAN_POINT('Ctrl Pts',(-1.43569331840376,0.606685970181726,
13.0126895163759));
#268560=CARTESIAN_POINT('Ctrl Pts',(-1.47122953742331,0.514560931490708,
13.019148654988));
#268561=CARTESIAN_POINT('Ctrl Pts',(-1.52836752342796,0.310638897373222,
13.0330874556989));
#268562=CARTESIAN_POINT('Ctrl Pts',(-1.54691801183598,0.198603903938476,
13.0405499501285));
#268563=CARTESIAN_POINT('Ctrl Pts',(-1.55399221543649,0.0701820582762164,
13.0495071809115));
#268564=CARTESIAN_POINT('Ctrl Pts',(-1.55461075640187,0.0547968371795999,
13.0505861641577));
#268565=CARTESIAN_POINT('Ctrl Pts',(-1.55518843906608,0.0320005674855285,
13.0521947456539));
#268566=CARTESIAN_POINT('Ctrl Pts',(-1.55532318863349,0.0245945685074745,
13.052718874717));
#268567=CARTESIAN_POINT('Ctrl Pts',(-1.55546882978987,0.0114149699964946,
13.0536544703676));
#268568=CARTESIAN_POINT('Ctrl Pts',(-1.55550048266985,0.00564169813958446,
13.0540652819445));
#268569=CARTESIAN_POINT('Ctrl Pts',(-1.55549945402464,-0.00652181833482271,
13.0549329319355));
#268570=CARTESIAN_POINT('Ctrl Pts',(-1.55545953505878,-0.0129119375274382,
13.0553899885487));
#268571=CARTESIAN_POINT('Ctrl Pts',(-1.55524955990949,-0.0298324091756489,
13.0566036052685));
#268572=CARTESIAN_POINT('Ctrl Pts',(-1.55501193277288,-0.0403614300648564,
13.0573622568114));
#268573=CARTESIAN_POINT('Ctrl Pts',(-1.55338021559916,-0.0902126302264806,
13.060971255883));
#268574=CARTESIAN_POINT('Ctrl Pts',(-1.5506014901205,-0.129471681614499,
13.0638642355735));
#268575=CARTESIAN_POINT('Ctrl Pts',(-1.53010224199153,-0.317505513036257,
13.0779791742268));
#268576=CARTESIAN_POINT('Ctrl Pts',(-1.4924357582644,-0.463296811112938,
13.0898098144486));
#268577=CARTESIAN_POINT('Ctrl Pts',(-1.41971519652966,-0.636755720839577,
13.1041377016585));
#268578=CARTESIAN_POINT('Ctrl Pts',(-1.40359444342355,-0.671544733435485,
13.1070186084021));
#268579=CARTESIAN_POINT('Ctrl Pts',(-1.38319186676609,-0.711621084039836,
13.110318338441));
#268580=CARTESIAN_POINT('Ctrl Pts',(-1.38014259583502,-0.717517056865483,
13.1108032868958));
#268581=CARTESIAN_POINT('Ctrl Pts',(-1.37513761686939,-0.727044561098761,
13.1115859003218));
#268582=CARTESIAN_POINT('Ctrl Pts',(-1.3732050856552,-0.730688068156672,
13.1118849408291));
#268583=CARTESIAN_POINT('Ctrl Pts',(-1.36973684543953,-0.737164573033759,
13.1124160025907));
#268584=CARTESIAN_POINT('Ctrl Pts',(-1.36820680607999,-0.740000520266559,
13.1126483713304));
#268585=CARTESIAN_POINT('Ctrl Pts',(-1.36487473067632,-0.746130899563447,
13.1131502906357));
#268586=CARTESIAN_POINT('Ctrl Pts',(-1.36306957720293,-0.749423563969802,
13.1134196399628));
#268587=CARTESIAN_POINT('Ctrl Pts',(-1.35797805621914,-0.758631424012251,
13.1141723037586));
#268588=CARTESIAN_POINT('Ctrl Pts',(-1.35466493426856,-0.764531856101368,
13.1146539570812));
#268589=CARTESIAN_POINT('Ctrl Pts',(-1.33452370832511,-0.799859908895218,
13.1175350047483));
#268590=CARTESIAN_POINT('Ctrl Pts',(-1.3167742547823,-0.828755333186258,
13.1198798229291));
#268591=CARTESIAN_POINT('Ctrl Pts',(-1.19860182111201,-1.00773995271303,
13.1344828563475));
#268592=CARTESIAN_POINT('Ctrl Pts',(-1.07363450604211,-1.13995934047877,
13.1458004310081));
#268593=CARTESIAN_POINT('Ctrl Pts',(-0.913524684104517,-1.25913202035108,
13.1596344340926));
#268594=CARTESIAN_POINT('Ctrl Pts',(-0.898087159556186,-1.27018903801665,
13.1609604101024));
#268595=CARTESIAN_POINT('Ctrl Pts',(-0.876308517177886,-1.28519231286381,
13.1628223429951));
#268596=CARTESIAN_POINT('Ctrl Pts',(-0.870135092921735,-1.28938001183234,
13.1633491748046));
#268597=CARTESIAN_POINT('Ctrl Pts',(-0.859411517584092,-1.29654218679491,
13.1642627994264));
#268598=CARTESIAN_POINT('Ctrl Pts',(-0.854875412625818,-1.29953754321188,
13.1646488033143));
#268599=CARTESIAN_POINT('Ctrl Pts',(-0.845429072877646,-1.3057044463902,
13.1654517482956));
#268600=CARTESIAN_POINT('Ctrl Pts',(-0.840516482678021,-1.30887220889639,
13.165868822067));
#268601=CARTESIAN_POINT('Ctrl Pts',(-0.828923445072133,-1.31625551116972,
13.1668519598735));
#268602=CARTESIAN_POINT('Ctrl Pts',(-0.822228564445755,-1.32044796641858,
13.1674188635305));
#268603=CARTESIAN_POINT('Ctrl Pts',(-0.800109270553225,-1.33406602411455,
13.1692892962143));
#268604=CARTESIAN_POINT('Ctrl Pts',(-0.784552993855251,-1.34327344579654,
13.170600704567));
#268605=CARTESIAN_POINT('Ctrl Pts',(-0.700157411333412,-1.39125923226449,
13.1776968519611));
#268606=CARTESIAN_POINT('Ctrl Pts',(-0.628610409128113,-1.42501505368135,
13.1836563499679));
#268607=CARTESIAN_POINT('Ctrl Pts',(-0.467641120586529,-1.4864723626952,
13.1969004302794));
#268608=CARTESIAN_POINT('Ctrl Pts',(-0.377646270198764,-1.5118436641429,
13.2042063044731));
#268609=CARTESIAN_POINT('Ctrl Pts',(-0.244307568042703,-1.53677789588288,
13.2145691006185));
#268610=CARTESIAN_POINT('Ctrl Pts',(-0.202388976565711,-1.54285837769939,
13.2177601288857));
#268611=CARTESIAN_POINT('Ctrl Pts',(-0.153485974857522,-1.54792403750036,
13.2213691483664));
#268612=CARTESIAN_POINT('Ctrl Pts',(-0.146696977286281,-1.54858218114044,
13.2218676346047));
#268613=CARTESIAN_POINT('Ctrl Pts',(-0.135741630765942,-1.54957152910898,
13.2226677156232));
#268614=CARTESIAN_POINT('Ctrl Pts',(-0.131577991333384,-1.5499306266571,
13.2229707853996));
#268615=CARTESIAN_POINT('Ctrl Pts',(-0.124196362446616,-1.55053730348172,
13.2235062512743));
#268616=CARTESIAN_POINT('Ctrl Pts',(-0.12097900062946,-1.55079165205646,
13.2237390178965));
#268617=CARTESIAN_POINT('Ctrl Pts',(-0.114053647445887,-1.55131745220483,
13.2242386974867));
#268618=CARTESIAN_POINT('Ctrl Pts',(-0.1103454706002,-1.55158562442216,
13.2245054260738));
#268619=CARTESIAN_POINT('Ctrl Pts',(-0.100055748635186,-1.55229269324437,
13.2252433668086));
#268620=CARTESIAN_POINT('Ctrl Pts',(-0.0934722156499973,-1.55270303257786,
13.2257130208875));
#268621=CARTESIAN_POINT('Ctrl Pts',(-0.0559602116824918,-1.55480163031358,
13.2283758781633));
#268622=CARTESIAN_POINT('Ctrl Pts',(-0.0249867336084995,-1.55560781052316,
13.2305236779858));
#268623=CARTESIAN_POINT('Ctrl Pts',(0.077771935132967,-1.5552119128537,
13.2375422152561));
#268624=CARTESIAN_POINT('Ctrl Pts',(0.149452456779749,-1.54996721677447,
13.2422675205366));
#268625=CARTESIAN_POINT('Ctrl Pts',(0.331671817486694,-1.52387080190935,
13.2543847265251));
#268626=CARTESIAN_POINT('Ctrl Pts',(0.440758015238778,-1.49596672539899,
13.2617628725647));
#268627=CARTESIAN_POINT('Ctrl Pts',(0.563299726462704,-1.45004122688803,
13.2708374029218));
#268628=CARTESIAN_POINT('Ctrl Pts',(0.580595879495543,-1.44320286680382,
13.2721365701282));
#268629=CARTESIAN_POINT('Ctrl Pts',(0.604590995475178,-1.43321479595762,
13.2739667132268));
#268630=CARTESIAN_POINT('Ctrl Pts',(0.611396890022277,-1.43032470531911,
13.2744889727128));
#268631=CARTESIAN_POINT('Ctrl Pts',(0.623154609822524,-1.425232594751,13.2753968456621));
#268632=CARTESIAN_POINT('Ctrl Pts',(0.628116056753881,-1.42305299788104,
13.2757816939791));
#268633=CARTESIAN_POINT('Ctrl Pts',(0.63841590050243,-1.41846384934235,
13.2765843346048));
#268634=CARTESIAN_POINT('Ctrl Pts',(0.643752270606257,-1.41604998720707,
13.2770022691362));
#268635=CARTESIAN_POINT('Ctrl Pts',(0.656315508413264,-1.41028142028259,
13.2779912033803));
#268636=CARTESIAN_POINT('Ctrl Pts',(0.663530424017184,-1.40690124138273,
13.278563071082));
#268637=CARTESIAN_POINT('Ctrl Pts',(0.687383602986294,-1.39550176287826,
13.2804670420124));
#268638=CARTESIAN_POINT('Ctrl Pts',(0.70390440777325,-1.38724183832221,
13.2818074200295));
#268639=CARTESIAN_POINT('Ctrl Pts',(0.742789816014992,-1.3669268061881,
13.2850156524628));
#268640=CARTESIAN_POINT('Ctrl Pts',(0.765013231729733,-1.3546144184417,
13.2868921262663));
#268641=CARTESIAN_POINT('Ctrl Pts',(0.916648346407024,-1.2656827440796,
13.3000002758974));
#268642=CARTESIAN_POINT('Ctrl Pts',(1.0346452553648,-1.17119236350077,13.3118750782068));
#268643=CARTESIAN_POINT('Ctrl Pts',(1.16366683825793,-1.03293874591521,
13.3262852912839));
#268644=CARTESIAN_POINT('Ctrl Pts',(1.18904931408387,-1.00361611867614,
13.32920012223));
#268645=CARTESIAN_POINT('Ctrl Pts',(1.21747914611102,-0.968178251894301,
13.3325338878714));
#268646=CARTESIAN_POINT('Ctrl Pts',(1.22161309324011,-0.962956932221121,
13.333020455665));
#268647=CARTESIAN_POINT('Ctrl Pts',(1.22825677660456,-0.954454087009126,
13.3338051606405));
#268648=CARTESIAN_POINT('Ctrl Pts',(1.23078713955892,-0.951188904291931,
13.3341046850991));
#268649=CARTESIAN_POINT('Ctrl Pts',(1.2352685219935,-0.945358300140465,
13.3346362724096));
#268650=CARTESIAN_POINT('Ctrl Pts',(1.23722460088262,-0.942796862932915,
13.3348686855186));
#268651=CARTESIAN_POINT('Ctrl Pts',(1.24143966535341,-0.937241629584523,
13.3353703202518));
#268652=CARTESIAN_POINT('Ctrl Pts',(1.24369578712206,-0.934245741140031,
13.3356393427225));
#268653=CARTESIAN_POINT('Ctrl Pts',(1.2499793873529,-0.925838690796355,
13.3363901655692));
#268654=CARTESIAN_POINT('Ctrl Pts',(1.25398260134742,-0.920409360077848,
13.3368703178509));
#268655=CARTESIAN_POINT('Ctrl Pts',(1.27766374703624,-0.887850666032035,
13.3397227338609));
#268656=CARTESIAN_POINT('Ctrl Pts',(1.29649783208754,-0.860114673723011,
13.3420416761633));
#268657=CARTESIAN_POINT('Ctrl Pts',(1.40594706755979,-0.687159132722282,
13.3559831089664));
#268658=CARTESIAN_POINT('Ctrl Pts',(1.47297832753361,-0.528413330252782,
13.3667433474358));
#268659=CARTESIAN_POINT('Ctrl Pts',(1.51304023146319,-0.360957743978504,
13.3785859300394));
#268660=CARTESIAN_POINT('Ctrl Pts',(1.513270224476,-0.359992309183792,13.3786542167928));
#268661=CARTESIAN_POINT('Ctrl Pts',(1.51936667205013,-0.334292353703326,
13.3804723022116));
#268662=CARTESIAN_POINT('Ctrl Pts',(1.52462653278502,-0.30941924589726,
13.3822390451271));
#268663=CARTESIAN_POINT('Ctrl Pts',(1.53097905397723,-0.275264054449133,
13.3846801459928));
#268664=CARTESIAN_POINT('Ctrl Pts',(1.53260128702239,-0.266083542612564,
13.3853377482856));
#268665=CARTESIAN_POINT('Ctrl Pts',(1.53505142806947,-0.251451312763804,
13.3863884277084));
#268666=CARTESIAN_POINT('Ctrl Pts',(1.53593305956365,-0.246008708431925,
13.3867798019021));
#268667=CARTESIAN_POINT('Ctrl Pts',(1.53768313315552,-0.234828669009878,
13.3875849649422));
#268668=CARTESIAN_POINT('Ctrl Pts',(1.53854844178735,-0.229090838701217,
13.3879988459015));
#268669=CARTESIAN_POINT('Ctrl Pts',(1.54047677735189,-0.215800191937193,
13.3889591088162));
#268670=CARTESIAN_POINT('Ctrl Pts',(1.54151638962109,-0.20824418621481,
13.3895062187461));
#268671=CARTESIAN_POINT('Ctrl Pts',(1.54463708680179,-0.184257473754559,
13.3912469609415));
#268672=CARTESIAN_POINT('Ctrl Pts',(1.54651128561639,-0.167801521536852,
13.3924470380808));
#268673=CARTESIAN_POINT('Ctrl Pts',(1.55459948495729,-0.0850525451355771,
13.3985132266329));
#268674=CARTESIAN_POINT('Ctrl Pts',(1.55681433074755,-0.0184479522290053,
13.4035018149905));
#268675=CARTESIAN_POINT('Ctrl Pts',(1.55183858713221,0.142433535765555,
13.4157927330419));
#268676=CARTESIAN_POINT('Ctrl Pts',(1.54033839074952,0.236318001884554,
13.4231738493771));
#268677=CARTESIAN_POINT('Ctrl Pts',(1.50874237150909,0.382522225760758,
13.4346829770609));
#268678=CARTESIAN_POINT('Ctrl Pts',(1.49421843576441,0.43582058583104,13.4388775548485));
#268679=CARTESIAN_POINT('Ctrl Pts',(1.47440688443156,0.495749071166107,
13.4435151061474));
#268680=CARTESIAN_POINT('Ctrl Pts',(1.47186710097608,0.503239551856673,
13.4440932914642));
#268681=CARTESIAN_POINT('Ctrl Pts',(1.46794109286813,0.514534338862254,
13.4449625738269));
#268682=CARTESIAN_POINT('Ctrl Pts',(1.46659701925061,0.518352989893866,
13.4452560253135));
#268683=CARTESIAN_POINT('Ctrl Pts',(1.46415812027924,0.525196722987202,
13.4457810929504));
#268684=CARTESIAN_POINT('Ctrl Pts',(1.46306881013627,0.528223680334259,
13.4460130244597));
#268685=CARTESIAN_POINT('Ctrl Pts',(1.460668102007,0.534830327114244,13.446518571043));
#268686=CARTESIAN_POINT('Ctrl Pts',(1.45935293452879,0.538408577520192,
13.4467919594709));
#268687=CARTESIAN_POINT('Ctrl Pts',(1.4555743387941,0.548573648448143,13.4475674951338));
#268688=CARTESIAN_POINT('Ctrl Pts',(1.45307933713432,0.555148762501953,
13.4480678151394));
#268689=CARTESIAN_POINT('Ctrl Pts',(1.44539993475487,0.574979885537125,
13.4495734757298));
#268690=CARTESIAN_POINT('Ctrl Pts',(1.44007838871623,0.588181127766952,
13.4505712215658));
#268691=CARTESIAN_POINT('Ctrl Pts',(1.43457668314421,0.601306901822155,
13.4515605039018));
#268692=CARTESIAN_POINT('Origin',(0.,0.,-1.29405622560371));
#268693=CARTESIAN_POINT('',(1.43457668360422,0.601306900724687,14.2893889670083));
#268694=CARTESIAN_POINT('',(1.43457666475166,0.601306945702447,14.1492791259731));
#268695=CARTESIAN_POINT('',(1.43457668357355,0.601306900797845,-1.29405622560371));
#268696=CARTESIAN_POINT('Ctrl Pts',(1.43457668360422,0.601306900724687,
14.2893889670083));
#268697=CARTESIAN_POINT('Ctrl Pts',(1.43510642363156,0.600043065750092,
14.2892958059463));
#268698=CARTESIAN_POINT('Ctrl Pts',(1.43563451927348,0.598778469337572,
14.2892025954736));
#268699=CARTESIAN_POINT('Ctrl Pts',(1.45097763803968,0.561900302523962,
14.2864845633064));
#268700=CARTESIAN_POINT('Ctrl Pts',(1.46446337624145,0.525751513059345,
14.2838244665163));
#268701=CARTESIAN_POINT('Ctrl Pts',(1.47985501929301,0.479288129934118,
14.2803915511198));
#268702=CARTESIAN_POINT('Ctrl Pts',(1.48302025483501,0.469402709922828,
14.2796604297811));
#268703=CARTESIAN_POINT('Ctrl Pts',(1.48794888988238,0.453462359550888,
14.2784799473835));
#268704=CARTESIAN_POINT('Ctrl Pts',(1.48977485404067,0.447426968980638,
14.2780326369627));
#268705=CARTESIAN_POINT('Ctrl Pts',(1.49318173919188,0.435914034364007,
14.2771786098615));
#268706=CARTESIAN_POINT('Ctrl Pts',(1.49476934501179,0.430438561508871,
14.2767721187157));
#268707=CARTESIAN_POINT('Ctrl Pts',(1.49832640831333,0.417913624157321,
14.2758414867958));
#268708=CARTESIAN_POINT('Ctrl Pts',(1.50027626746597,0.410858784730702,
14.2753167199634));
#268709=CARTESIAN_POINT('Ctrl Pts',(1.50523271448447,0.392419876782316,
14.2739435229652));
#268710=CARTESIAN_POINT('Ctrl Pts',(1.50815991158616,0.381015158950399,
14.273092556915));
#268711=CARTESIAN_POINT('Ctrl Pts',(1.52992096659911,0.292048901328185,
14.2664403349478));
#268712=CARTESIAN_POINT('Ctrl Pts',(1.54288608418305,0.213188381740176,
14.2604519398788));
#268713=CARTESIAN_POINT('Ctrl Pts',(1.55888861657664,0.0276904145284185,
14.2461814623007));
#268714=CARTESIAN_POINT('Ctrl Pts',(1.55713325312661,-0.0789659695126312,
14.2378271995628));
#268715=CARTESIAN_POINT('Ctrl Pts',(1.5400575459802,-0.221829575670318,
14.2268785210513));
#268716=CARTESIAN_POINT('Ctrl Pts',(1.5342638068842,-0.258883665635753,
14.2240640623603));
#268717=CARTESIAN_POINT('Ctrl Pts',(1.52582604833923,-0.302460913689011,
14.220810521741));
#268718=CARTESIAN_POINT('Ctrl Pts',(1.52447114190434,-0.3092175227038,14.2203076906654));
#268719=CARTESIAN_POINT('Ctrl Pts',(1.52230898694001,-0.319639928743608,
14.2195347935613));
#268720=CARTESIAN_POINT('Ctrl Pts',(1.52153331987344,-0.323312067652006,
14.2192630056382));
#268721=CARTESIAN_POINT('Ctrl Pts',(1.5200765526474,-0.330087286165561,
14.218762567841));
#268722=CARTESIAN_POINT('Ctrl Pts',(1.5193992418032,-0.333191066476965,
14.2185337144139));
#268723=CARTESIAN_POINT('Ctrl Pts',(1.51784611682222,-0.340205043173597,
14.2180174387534));
#268724=CARTESIAN_POINT('Ctrl Pts',(1.51696470090874,-0.344113938868705,
14.217730339721));
#268725=CARTESIAN_POINT('Ctrl Pts',(1.51431107086636,-0.3556738793492,14.2168830122607));
#268726=CARTESIAN_POINT('Ctrl Pts',(1.51249597187433,-0.36331511079172,
14.2163251580079));
#268727=CARTESIAN_POINT('Ctrl Pts',(1.49731099727027,-0.425154273493698,
14.21182623971));
#268728=CARTESIAN_POINT('Ctrl Pts',(1.4810885217557,-0.478617613667169,
14.2080341671923));
#268729=CARTESIAN_POINT('Ctrl Pts',(1.41578279436657,-0.658392935595339,
14.1952554988008));
#268730=CARTESIAN_POINT('Ctrl Pts',(1.35311839352551,-0.779098067013249,
14.1865748042326));
#268731=CARTESIAN_POINT('Ctrl Pts',(1.25500069965703,-0.919701455304375,
14.1748824273492));
#268732=CARTESIAN_POINT('Ctrl Pts',(1.23337076002019,-0.948511330104299,
14.1723946758144));
#268733=CARTESIAN_POINT('Ctrl Pts',(1.20439214639933,-0.98444032425386,
14.1691560255389));
#268734=CARTESIAN_POINT('Ctrl Pts',(1.19794541529606,-0.992275147130088,
14.1684411538262));
#268735=CARTESIAN_POINT('Ctrl Pts',(1.18740182208363,-1.00483644263579,
14.1672806253067));
#268736=CARTESIAN_POINT('Ctrl Pts',(1.18335221288825,-1.00960234830909,
14.166836894656));
#268737=CARTESIAN_POINT('Ctrl Pts',(1.17554798188747,-1.01867553272687,
14.1659854913553));
#268738=CARTESIAN_POINT('Ctrl Pts',(1.17179814339994,-1.02298680745084,
14.1655780203292));
#268739=CARTESIAN_POINT('Ctrl Pts',(1.16320552875811,-1.03275669749077,
14.1646479110233));
#268740=CARTESIAN_POINT('Ctrl Pts',(1.15834795537023,-1.03820205609117,
14.1641246608388));
#268741=CARTESIAN_POINT('Ctrl Pts',(1.14542507174974,-1.05248506220085,
14.1627391896757));
#268742=CARTESIAN_POINT('Ctrl Pts',(1.13729593924475,-1.06126402598284,
14.1618742878627));
#268743=CARTESIAN_POINT('Ctrl Pts',(1.06344518721115,-1.13919529438871,
14.1540739772809));
#268744=CARTESIAN_POINT('Ctrl Pts',(0.991605851365938,-1.20224492947703,
14.146866192723));
#268745=CARTESIAN_POINT('Ctrl Pts',(0.840141542172154,-1.31231958673576,
14.1324267164581));
#268746=CARTESIAN_POINT('Ctrl Pts',(0.761184553683046,-1.35963932549793,
14.125236452795));
#268747=CARTESIAN_POINT('Ctrl Pts',(0.645953894423232,-1.41549742045255,
14.1155018825313));
#268748=CARTESIAN_POINT('Ctrl Pts',(0.612851497056703,-1.4301408838063,
14.1127879729051));
#268749=CARTESIAN_POINT('Ctrl Pts',(0.572928962189321,-1.44616018064728,
14.1096353094923));
#268750=CARTESIAN_POINT('Ctrl Pts',(0.566575779084717,-1.4486610214193,
14.1091371619));
#268751=CARTESIAN_POINT('Ctrl Pts',(0.556717660917583,-1.45246675676604,
14.1083699138952));
#268752=CARTESIAN_POINT('Ctrl Pts',(0.553224246933727,-1.45380093784985,
14.1080991302809));
#268753=CARTESIAN_POINT('Ctrl Pts',(0.546753090118514,-1.45624565513195,
14.107599620471));
#268754=CARTESIAN_POINT('Ctrl Pts',(0.543776776856625,-1.45735965600731,
14.1073706967387));
#268755=CARTESIAN_POINT('Ctrl Pts',(0.537023444886674,-1.45986378372471,
14.1068530983014));
#268756=CARTESIAN_POINT('Ctrl Pts',(0.533244436396847,-1.46124837704856,
14.1065647540256));
#268757=CARTESIAN_POINT('Ctrl Pts',(0.523446873793777,-1.46479504253782,
14.1058204183328));
#268758=CARTESIAN_POINT('Ctrl Pts',(0.517420204688105,-1.46693472310291,
14.1053657121367));
#268759=CARTESIAN_POINT('Ctrl Pts',(0.478761759015114,-1.48039195215472,
14.1024680292886));
#268760=CARTESIAN_POINT('Ctrl Pts',(0.445770819136474,-1.49065824034146,
14.1000817686897));
#268761=CARTESIAN_POINT('Ctrl Pts',(0.393489843388598,-1.50503593705312,
14.0963943809113));
#268762=CARTESIAN_POINT('Ctrl Pts',(0.374419364428812,-1.50989324912639,
14.0950686171438));
#268763=CARTESIAN_POINT('Ctrl Pts',(0.274226625088214,-1.53339753127321,
14.0881796074168));
#268764=CARTESIAN_POINT('Ctrl Pts',(0.191794339524217,-1.5458732989144,
14.0827648639141));
#268765=CARTESIAN_POINT('Ctrl Pts',(0.0225543798508679,-1.55773519677699,
14.0715401863919));
#268766=CARTESIAN_POINT('Ctrl Pts',(-0.063988810093637,-1.55658269572875,
14.0657401640109));
#268767=CARTESIAN_POINT('Ctrl Pts',(-0.162664829078716,-1.54702385202516,
14.0588115741827));
#268768=CARTESIAN_POINT('Ctrl Pts',(-0.175332975959581,-1.54563934211039,
14.0579163100236));
#268769=CARTESIAN_POINT('Ctrl Pts',(-0.194750207432216,-1.54327544183502,
14.0565345834734));
#268770=CARTESIAN_POINT('Ctrl Pts',(-0.201512468268516,-1.54240703289295,
14.0560516090263));
#268771=CARTESIAN_POINT('Ctrl Pts',(-0.213825760922436,-1.54074340451008,
14.0551688329878));
#268772=CARTESIAN_POINT('Ctrl Pts',(-0.219378648311558,-1.53996256504178,
14.0547694910442));
#268773=CARTESIAN_POINT('Ctrl Pts',(-0.231491250414504,-1.53819246484057,
14.0538956321503));
#268774=CARTESIAN_POINT('Ctrl Pts',(-0.238049075273868,-1.53719123506156,
14.0534207443418));
#268775=CARTESIAN_POINT('Ctrl Pts',(-0.256017765360416,-1.53433008826178,
14.0521145448663));
#268776=CARTESIAN_POINT('Ctrl Pts',(-0.267414409566224,-1.53238488509148,
14.0512805544763));
#268777=CARTESIAN_POINT('Ctrl Pts',(-0.327351064457082,-1.5214657963856,
14.0468643284272));
#268778=CARTESIAN_POINT('Ctrl Pts',(-0.375459893498453,-1.51031313222582,
14.0432137546576));
#268779=CARTESIAN_POINT('Ctrl Pts',(-0.563406098753759,-1.45720826746905,
14.0285161612423));
#268780=CARTESIAN_POINT('Ctrl Pts',(-0.697549418085453,-1.39796187754212,
14.0169644034898));
#268781=CARTESIAN_POINT('Ctrl Pts',(-0.848166289265676,-1.3042941307266,
14.0035347745476));
#268782=CARTESIAN_POINT('Ctrl Pts',(-0.874364157900145,-1.28687874797435,
14.0011839877682));
#268783=CARTESIAN_POINT('Ctrl Pts',(-0.905375794037493,-1.26487867861151,
13.9983989869758));
#268784=CARTESIAN_POINT('Ctrl Pts',(-0.910709420163506,-1.26104391525003,
13.9979199218419));
#268785=CARTESIAN_POINT('Ctrl Pts',(-0.918995678434938,-1.25500627900246,
13.9971757282376));
#268786=CARTESIAN_POINT('Ctrl Pts',(-0.921964965607764,-1.25282657230593,
13.9969090703319));
#268787=CARTESIAN_POINT('Ctrl Pts',(-0.927486778227432,-1.24874283435745,
13.9964132534112));
#268788=CARTESIAN_POINT('Ctrl Pts',(-0.930041174895956,-1.24684153100951,
13.9961839218546));
#268789=CARTESIAN_POINT('Ctrl Pts',(-0.93587354453081,-1.24247245150107,
13.9956603516606));
#268790=CARTESIAN_POINT('Ctrl Pts',(-0.939147603576829,-1.23999954186706,
13.9953664754453));
#268791=CARTESIAN_POINT('Ctrl Pts',(-0.94770645285149,-1.23348166531379,
13.9945982202367));
#268792=CARTESIAN_POINT('Ctrl Pts',(-0.952975210616525,-1.22941563012079,
13.9941252668691));
#268793=CARTESIAN_POINT('Ctrl Pts',(-0.989492067658269,-1.20085882590092,
13.9908458626741));
#268794=CARTESIAN_POINT('Ctrl Pts',(-1.01982188986394,-1.17521081263067,
13.9881145682104));
#268795=CARTESIAN_POINT('Ctrl Pts',(-1.16023542700811,-1.04693676537881,
13.9752463257933));
#268796=CARTESIAN_POINT('Ctrl Pts',(-1.25601908796069,-0.929862827458389,
13.9656960119448));
#268797=CARTESIAN_POINT('Ctrl Pts',(-1.35294289368544,-0.768473671828879,
13.952876749384));
#268798=CARTESIAN_POINT('Ctrl Pts',(-1.37119805597474,-0.735405841287683,
13.9502712236113));
#268799=CARTESIAN_POINT('Ctrl Pts',(-1.39288081512394,-0.692509589513686,
13.9468997415392));
#268800=CARTESIAN_POINT('Ctrl Pts',(-1.39743907059523,-0.683264613150348,
13.9461736392021));
#268801=CARTESIAN_POINT('Ctrl Pts',(-1.40463023514552,-0.668306600677126,
13.9449993208265));
#268802=CARTESIAN_POINT('Ctrl Pts',(-1.40732101430308,-0.662621589281365,
13.9445531166446));
#268803=CARTESIAN_POINT('Ctrl Pts',(-1.41238643843066,-0.651749447734409,
13.9436999190605));
#268804=CARTESIAN_POINT('Ctrl Pts',(-1.4147671764514,-0.646565254963968,
13.9432931438775));
#268805=CARTESIAN_POINT('Ctrl Pts',(-1.42014969815926,-0.634672435659164,
13.9423600449609));
#268806=CARTESIAN_POINT('Ctrl Pts',(-1.42313254027963,-0.627955440400696,
13.9418330831641));
#268807=CARTESIAN_POINT('Ctrl Pts',(-1.4308101664857,-0.610330677333528,
13.9404503668461));
#268808=CARTESIAN_POINT('Ctrl Pts',(-1.43542775780959,-0.599390028089579,
13.9395920185953));
#268809=CARTESIAN_POINT('Ctrl Pts',(-1.47209461872559,-0.509659367487536,
13.9325505508937));
#268810=CARTESIAN_POINT('Ctrl Pts',(-1.49775130286952,-0.428429134032381,
13.9261536139243));
#268811=CARTESIAN_POINT('Ctrl Pts',(-1.53228263841126,-0.276857080910632,
13.9142108919993));
#268812=CARTESIAN_POINT('Ctrl Pts',(-1.54324448647616,-0.207209614375265,
13.9087240440755));
#268813=CARTESIAN_POINT('Ctrl Pts',(-1.55349617243896,-0.0913174537903301,
13.8997352703765));
#268814=CARTESIAN_POINT('Ctrl Pts',(-1.55551523355228,-0.0454119413306816,
13.8962123141049));
#268815=CARTESIAN_POINT('Ctrl Pts',(-1.55549869742765,0.00416514605386303,
13.8924873319056));
#268816=CARTESIAN_POINT('Ctrl Pts',(-1.55548466003159,0.00781139927385783,
13.8922138397129));
#268817=CARTESIAN_POINT('Ctrl Pts',(-1.55530944731517,0.0315978658981645,
13.8904329013735));
#268818=CARTESIAN_POINT('Ctrl Pts',(-1.55476992860723,0.0517346559627735,
13.8889401577351));
#268819=CARTESIAN_POINT('Ctrl Pts',(-1.55356545931134,0.0777803327808232,
13.8870333551244));
#268820=CARTESIAN_POINT('Ctrl Pts',(-1.55325763646708,0.0837026544015386,
13.8866013896784));
#268821=CARTESIAN_POINT('Ctrl Pts',(-1.55271183589274,0.0931598309754612,
13.885914316331));
#268822=CARTESIAN_POINT('Ctrl Pts',(-1.55249564301516,0.0966958041096516,
13.8856580319886));
#268823=CARTESIAN_POINT('Ctrl Pts',(-1.55206014726408,0.103440279047142,
13.8851703964523));
#268824=CARTESIAN_POINT('Ctrl Pts',(-1.55184297704861,0.10664880147417,
13.884938938198));
#268825=CARTESIAN_POINT('Ctrl Pts',(-1.55130828652724,0.114200768753752,
13.8843953433217));
#268826=CARTESIAN_POINT('Ctrl Pts',(-1.55098247404556,0.118543586394214,
13.8840836718114));
#268827=CARTESIAN_POINT('Ctrl Pts',(-1.54985135725508,0.132816707213509,
13.8830622087196));
#268828=CARTESIAN_POINT('Ctrl Pts',(-1.54896886718134,0.142740917409205,
13.882356559669));
#268829=CARTESIAN_POINT('Ctrl Pts',(-1.546633599569,0.166421389750078,13.8806822542213));
#268830=CARTESIAN_POINT('Ctrl Pts',(-1.54509254556125,0.180168331531759,
13.8797179345087));
#268831=CARTESIAN_POINT('Ctrl Pts',(-1.53867436904587,0.231256235348058,
13.8761565459136));
#268832=CARTESIAN_POINT('Ctrl Pts',(-1.53262489373753,0.268439267809651,
13.8736088610586));
#268833=CARTESIAN_POINT('Ctrl Pts',(-1.49826252131152,0.440069658214332,
13.8619052633682));
#268834=CARTESIAN_POINT('Ctrl Pts',(-1.45357114256359,0.570599769147444,
13.8531082460646));
#268835=CARTESIAN_POINT('Ctrl Pts',(-1.37680317210424,0.724709481668072,
13.841361226969));
#268836=CARTESIAN_POINT('Ctrl Pts',(-1.36025022100336,0.755321011010828,
13.8389578045322));
#268837=CARTESIAN_POINT('Ctrl Pts',(-1.33741841882751,0.794355760157811,
13.8357863967801));
#268838=CARTESIAN_POINT('Ctrl Pts',(-1.33206051093637,0.803308089395746,
13.8350515628939));
#268839=CARTESIAN_POINT('Ctrl Pts',(-1.32331445159441,0.817593432724739,
13.8338665206161));
#268840=CARTESIAN_POINT('Ctrl Pts',(-1.3199830903128,0.822960994325506,
13.8334183917417));
#268841=CARTESIAN_POINT('Ctrl Pts',(-1.31358475367028,0.833131332217873,
13.8325637407926));
#268842=CARTESIAN_POINT('Ctrl Pts',(-1.31052389448628,0.837937851030816,
13.8321574496257));
#268843=CARTESIAN_POINT('Ctrl Pts',(-1.30348310073282,0.848861184646816,
13.8312285935015));
#268844=CARTESIAN_POINT('Ctrl Pts',(-1.29948641831693,0.85496698763336,
13.8307054111437));
#268845=CARTESIAN_POINT('Ctrl Pts',(-1.28707968511959,0.873633000769312,
13.8290935498743));
#268846=CARTESIAN_POINT('Ctrl Pts',(-1.27852962089448,0.886098591796523,
13.8279996375153));
#268847=CARTESIAN_POINT('Ctrl Pts',(-1.25840919810705,0.914535641405829,
13.8254626644934));
#268848=CARTESIAN_POINT('Ctrl Pts',(-1.24671425993316,0.930415304044121,
13.8240150046247));
#268849=CARTESIAN_POINT('Ctrl Pts',(-1.20543176783678,0.984293438906693,
13.8189937299405));
#268850=CARTESIAN_POINT('Ctrl Pts',(-1.17438601061904,1.021134656924,13.8153666864828));
#268851=CARTESIAN_POINT('Ctrl Pts',(-1.0811288902787,1.1219135072548,13.8048860701825));
#268852=CARTESIAN_POINT('Ctrl Pts',(-1.01506091612326,1.18202336306852,
13.7979248322068));
#268853=CARTESIAN_POINT('Ctrl Pts',(-0.895377679050786,1.27344245844416,
13.7863069990047));
#268854=CARTESIAN_POINT('Ctrl Pts',(-0.844366127486653,1.30782441175503,
13.7816197385012));
#268855=CARTESIAN_POINT('Ctrl Pts',(-0.784630385465915,1.34312996941277,
13.7765212468718));
#268856=CARTESIAN_POINT('Ctrl Pts',(-0.777782423342916,1.34710707279357,
13.7759423328059));
#268857=CARTESIAN_POINT('Ctrl Pts',(-0.767411880095811,1.3530245465355,
13.775074316669));
#268858=CARTESIAN_POINT('Ctrl Pts',(-0.763911797365107,1.35500375795572,
13.7747828386143));
#268859=CARTESIAN_POINT('Ctrl Pts',(-0.757631889322544,1.35852282577063,
13.7742625597066));
#268860=CARTESIAN_POINT('Ctrl Pts',(-0.75485499515718,1.36006775007228,
13.774033440954));
#268861=CARTESIAN_POINT('Ctrl Pts',(-0.748797470660418,1.36341358467278,
13.7735356929672));
#268862=CARTESIAN_POINT('Ctrl Pts',(-0.745515074148207,1.36521116679979,
13.7732672756406));
#268863=CARTESIAN_POINT('Ctrl Pts',(-0.736214431294065,1.37026105427154,
13.7725102872313));
#268864=CARTESIAN_POINT('Ctrl Pts',(-0.730181072184381,1.37348558497319,
13.7720234356829));
#268865=CARTESIAN_POINT('Ctrl Pts',(-0.691866477595388,1.39363900378096,
13.7689569757977));
#268866=CARTESIAN_POINT('Ctrl Pts',(-0.659016668405864,1.40947027716365,
13.7664407937663));
#268867=CARTESIAN_POINT('Ctrl Pts',(-0.577698982879933,1.44519402812156,
13.760408867415));
#268868=CARTESIAN_POINT('Ctrl Pts',(-0.528724072290274,1.4638215390211,
13.7569393300948));
#268869=CARTESIAN_POINT('Ctrl Pts',(-0.357779981470167,1.51913788168171,
13.7450920664581));
#268870=CARTESIAN_POINT('Ctrl Pts',(-0.232323442074437,1.54331064014915,
13.7367975492238));
#268871=CARTESIAN_POINT('Ctrl Pts',(-0.0876692729125478,1.55312835300434,
13.7267329859269));
#268872=CARTESIAN_POINT('Ctrl Pts',(-0.0699901918887989,1.55402538935513,
13.725495536695));
#268873=CARTESIAN_POINT('Ctrl Pts',(-0.0451148681929885,1.55486224052582,
13.7237422908924));
#268874=CARTESIAN_POINT('Ctrl Pts',(-0.0379279934085873,1.55505414778454,
13.7232343353313));
#268875=CARTESIAN_POINT('Ctrl Pts',(-0.0254184584830591,1.55530141241899,
13.7223476022687));
#268876=CARTESIAN_POINT('Ctrl Pts',(-0.0200963196289022,1.55537928434101,
13.7219695319587));
#268877=CARTESIAN_POINT('Ctrl Pts',(-0.00897005928959219,1.55548496494596,
13.7211774011916));
#268878=CARTESIAN_POINT('Ctrl Pts',(-0.00316598331366182,1.55550760621891,
13.7207631854895));
#268879=CARTESIAN_POINT('Ctrl Pts',(0.0106258773889423,1.55548421622053,
13.7197764733789));
#268880=CARTESIAN_POINT('Ctrl Pts',(0.0186133790661768,1.55540914035031,
13.7192030796356));
#268881=CARTESIAN_POINT('Ctrl Pts',(0.0455390572294313,1.55494863072896,
13.7172634051839));
#268882=CARTESIAN_POINT('Ctrl Pts',(0.0644699897829865,1.55427880749964,
13.7158883246744));
#268883=CARTESIAN_POINT('Ctrl Pts',(0.10967387793181,1.55185214542411,13.7125762551443));
#268884=CARTESIAN_POINT('Ctrl Pts',(0.135922932076452,1.54977361096245,
13.7106297922839));
#268885=CARTESIAN_POINT('Ctrl Pts',(0.310417488702593,1.53148923671992,
13.6975320383032));
#268886=CARTESIAN_POINT('Ctrl Pts',(0.455716652937254,1.49469953382833,
13.685755728808));
#268887=CARTESIAN_POINT('Ctrl Pts',(0.629278418229681,1.42305510441386,
13.6714481623336));
#268888=CARTESIAN_POINT('Ctrl Pts',(0.664481824163188,1.40696186281549,
13.6685392375838));
#268889=CARTESIAN_POINT('Ctrl Pts',(0.70495127858869,1.38660288399937,13.6652153954514));
#268890=CARTESIAN_POINT('Ctrl Pts',(0.710832011863789,1.38359738296306,
13.6647329185618));
#268891=CARTESIAN_POINT('Ctrl Pts',(0.720321475707622,1.37867107407236,
13.6639554230796));
#268892=CARTESIAN_POINT('Ctrl Pts',(0.723942006627118,1.37677337674962,
13.6636590344032));
#268893=CARTESIAN_POINT('Ctrl Pts',(0.730368362679882,1.37337265000639,
13.6631334533313));
#268894=CARTESIAN_POINT('Ctrl Pts',(0.733177091196946,1.37187526205131,
13.6629039151919));
#268895=CARTESIAN_POINT('Ctrl Pts',(0.739235442990032,1.36862151591274,
13.6624091937249));
#268896=CARTESIAN_POINT('Ctrl Pts',(0.742483408793337,1.36686220316036,
13.6621442008693));
#268897=CARTESIAN_POINT('Ctrl Pts',(0.751531759605301,1.36191924992618,
13.6614065363533));
#268898=CARTESIAN_POINT('Ctrl Pts',(0.757318236863859,1.35871009465218,
13.6609354474234));
#268899=CARTESIAN_POINT('Ctrl Pts',(0.791193813306958,1.33963919614724,
13.6581803409233));
#268900=CARTESIAN_POINT('Ctrl Pts',(0.818806991269441,1.32294229676711,
13.6559457822308));
#268901=CARTESIAN_POINT('Ctrl Pts',(0.971991577838283,1.22368033191457,
13.6434955326567));
#268902=CARTESIAN_POINT('Ctrl Pts',(1.08560070714567,1.12411788947292,13.6339761488987));
#268903=CARTESIAN_POINT('Ctrl Pts',(1.21222105476563,0.975757562258376,
13.6207765181854));
#268904=CARTESIAN_POINT('Ctrl Pts',(1.23978604282488,0.940485320867346,
13.6177037630854));
#268905=CARTESIAN_POINT('Ctrl Pts',(1.2723151556437,0.894941571335043,13.6137844018349));
#268906=CARTESIAN_POINT('Ctrl Pts',(1.27874056979808,0.885736312250796,
13.6129946273594));
#268907=CARTESIAN_POINT('Ctrl Pts',(1.28876034967867,0.871045353410482,
13.6117375346395));
#268908=CARTESIAN_POINT('Ctrl Pts',(1.29242071696767,0.865604952946545,
13.6112727176601));
#268909=CARTESIAN_POINT('Ctrl Pts',(1.29917953367074,0.855420885069376,
13.61040384407));
#268910=CARTESIAN_POINT('Ctrl Pts',(1.30228668646884,0.850683099637103,
13.6100001225079));
#268911=CARTESIAN_POINT('Ctrl Pts',(1.30913843912789,0.840110033934366,
13.6091001848727));
#268912=CARTESIAN_POINT('Ctrl Pts',(1.31287002766012,0.834266509881198,
13.608603495805));
#268913=CARTESIAN_POINT('Ctrl Pts',(1.3236440530544,0.81714349543857,13.607149936131));
#268914=CARTESIAN_POINT('Ctrl Pts',(1.330580913642,0.805798661670588,13.6061892187042));
#268915=CARTESIAN_POINT('Ctrl Pts',(1.34593906480333,0.779942149024446,
13.6040042634589));
#268916=CARTESIAN_POINT('Ctrl Pts',(1.35427260094002,0.765380561398834,
13.6027770111668));
#268917=CARTESIAN_POINT('Ctrl Pts',(1.38072989315217,0.7173651296398,13.5987397398097));
#268918=CARTESIAN_POINT('Ctrl Pts',(1.39786086528448,0.683383006565913,
13.5958968047415));
#268919=CARTESIAN_POINT('Ctrl Pts',(1.42094296181424,0.633088123108505,
13.5917105661335));
#268920=CARTESIAN_POINT('Ctrl Pts',(1.42789341460871,0.617251608647841,
13.5903955059367));
#268921=CARTESIAN_POINT('Ctrl Pts',(1.43457670670211,0.601306845618552,
13.5890749702576));
#268922=CARTESIAN_POINT('',(-1.55549951545175,-0.00134136213463568,13.7562673034149));
#268923=CARTESIAN_POINT('Ctrl Pts',(1.43457668314421,0.601306901822155,
13.4515605039018));
#268924=CARTESIAN_POINT('Ctrl Pts',(1.42491482403355,0.624357822664694,
13.4532978390657));
#268925=CARTESIAN_POINT('Ctrl Pts',(1.41469733731682,0.647175991875524,
13.4550090885635));
#268926=CARTESIAN_POINT('Ctrl Pts',(1.35292712151481,0.776660653332891,
13.4647256675113));
#268927=CARTESIAN_POINT('Ctrl Pts',(1.28987237647954,0.877409177485551,
13.4723368859934));
#268928=CARTESIAN_POINT('Ctrl Pts',(1.17468647016616,1.02180141387318,13.4846626878756));
#268929=CARTESIAN_POINT('Ctrl Pts',(1.13012664881844,1.07087739654077,13.4891551949743));
#268930=CARTESIAN_POINT('Ctrl Pts',(1.07434407638805,1.12494292997761,13.4945845415706));
#268931=CARTESIAN_POINT('Ctrl Pts',(1.06602061085322,1.13283354251355,13.4953898810427));
#268932=CARTESIAN_POINT('Ctrl Pts',(1.05227617988597,1.14557759080823,13.4967124911391));
#268933=CARTESIAN_POINT('Ctrl Pts',(1.04690696526504,1.15048640937279,13.4972273998412));
#268934=CARTESIAN_POINT('Ctrl Pts',(1.03722633739703,1.1592130679131,13.4981527566677));
#268935=CARTESIAN_POINT('Ctrl Pts',(1.03292775444979,1.16304499666431,13.4985626030537));
#268936=CARTESIAN_POINT('Ctrl Pts',(1.02375751441355,1.17112877698053,13.4994347851006));
#268937=CARTESIAN_POINT('Ctrl Pts',(1.01888043804736,1.1753742855888,13.4998973733425));
#268938=CARTESIAN_POINT('Ctrl Pts',(1.00572949336778,1.18667886239086,13.501141448177));
#268939=CARTESIAN_POINT('Ctrl Pts',(0.997407957952652,1.1936816537615,13.5019252172642));
#268940=CARTESIAN_POINT('Ctrl Pts',(0.955411117453664,1.22827733973371,
13.5058643974196));
#268941=CARTESIAN_POINT('Ctrl Pts',(0.92066447964419,1.254532522117,13.5090725162834));
#268942=CARTESIAN_POINT('Ctrl Pts',(0.742060889928688,1.37806955984452,
13.5253335989984));
#268943=CARTESIAN_POINT('Ctrl Pts',(0.583761386538825,1.45221755675548,
13.5392159625137));
#268944=CARTESIAN_POINT('Ctrl Pts',(0.403116580464746,1.50242156626473,
13.5531371381978));
#268945=CARTESIAN_POINT('Ctrl Pts',(0.38967143678975,1.50596472321581,13.5541613548444));
#268946=CARTESIAN_POINT('Ctrl Pts',(0.371163106854808,1.510577681094,13.5555533471034));
#268947=CARTESIAN_POINT('Ctrl Pts',(0.366139932036013,1.51180307405809,
13.5559293338634));
#268948=CARTESIAN_POINT('Ctrl Pts',(0.358129953326154,1.51371482689133,
13.5565259192799));
#268949=CARTESIAN_POINT('Ctrl Pts',(0.355147130667341,1.51441743143822,
13.5567474276248));
#268950=CARTESIAN_POINT('Ctrl Pts',(0.348948164385919,1.51585827727611,
13.5572063882515));
#268951=CARTESIAN_POINT('Ctrl Pts',(0.345731731505761,1.51659510361663,
13.5574437519777));
#268952=CARTESIAN_POINT('Ctrl Pts',(0.337963820233271,1.5183485947983,13.5580151822512));
#268953=CARTESIAN_POINT('Ctrl Pts',(0.333410015257791,1.5193550481537,13.5583486695394));
#268954=CARTESIAN_POINT('Ctrl Pts',(0.317519410930875,1.52279220583716,
13.5595073655911));
#268955=CARTESIAN_POINT('Ctrl Pts',(0.306159649201728,1.52511670663915,
13.5603268032607));
#268956=CARTESIAN_POINT('Ctrl Pts',(0.237248552546934,1.53841667915043,
13.5652500041482));
#268957=CARTESIAN_POINT('Ctrl Pts',(0.179133733721364,1.54626180991327,
13.5692018582337));
#268958=CARTESIAN_POINT('Ctrl Pts',(0.0185697998232404,1.55875939697581,
13.5799122249702));
#268959=CARTESIAN_POINT('Ctrl Pts',(-0.0841022821022617,1.55659974997274,
13.5865459877373));
#268960=CARTESIAN_POINT('Ctrl Pts',(-0.203457621590718,1.54223893461175,
13.5946132004922));
#268961=CARTESIAN_POINT('Ctrl Pts',(-0.221059791182818,1.53981442767176,
13.5958115598582));
#268962=CARTESIAN_POINT('Ctrl Pts',(-0.27913610129727,1.53079872051998,
13.5998004262197));
#268963=CARTESIAN_POINT('Ctrl Pts',(-0.319388137313364,1.52290919163844,
13.6026221209597));
#268964=CARTESIAN_POINT('Ctrl Pts',(-0.370107750335763,1.51086874961113,
13.6062740927559));
#268965=CARTESIAN_POINT('Ctrl Pts',(-0.380908571754019,1.50818194325879,
13.6070573859803));
#268966=CARTESIAN_POINT('Ctrl Pts',(-0.39799116808154,1.50373728279574,
13.6083055786646));
#268967=CARTESIAN_POINT('Ctrl Pts',(-0.404292470219306,1.50205538570144,
13.6087680288113));
#268968=CARTESIAN_POINT('Ctrl Pts',(-0.415574630332352,1.49896789819568,
13.6095997475955));
#268969=CARTESIAN_POINT('Ctrl Pts',(-0.420559433272976,1.49757697468096,
13.6099685364776));
#268970=CARTESIAN_POINT('Ctrl Pts',(-0.432192535520679,1.4942682957153,
13.6108323005173));
#268971=CARTESIAN_POINT('Ctrl Pts',(-0.438835117795961,1.49233101685513,
13.6113279032667));
#268972=CARTESIAN_POINT('Ctrl Pts',(-0.457380899882402,1.48678769520407,
13.6127184234272));
#268973=CARTESIAN_POINT('Ctrl Pts',(-0.469253864524501,1.48308318449054,
13.6136165280138));
#268974=CARTESIAN_POINT('Ctrl Pts',(-0.534842717663971,1.46175222579179,
13.6186229929478));
#268975=CARTESIAN_POINT('Ctrl Pts',(-0.587604483824374,1.44135207249496,
13.6228215111518));
#268976=CARTESIAN_POINT('Ctrl Pts',(-0.751116181933909,1.36765930924143,
13.6363935101631));
#268977=CARTESIAN_POINT('Ctrl Pts',(-0.856723480656026,1.30410393245719,
13.6460516803294));
#268978=CARTESIAN_POINT('Ctrl Pts',(-0.96664430687877,1.21878870492784,
13.65669105786));
#268979=CARTESIAN_POINT('Ctrl Pts',(-0.979391380448577,1.20856927108453,
13.6579340177806));
#268980=CARTESIAN_POINT('Ctrl Pts',(-1.01418380355451,1.17976385065839,
13.6613475059728));
#268981=CARTESIAN_POINT('Ctrl Pts',(-1.03587852485889,1.16076160029383,
13.6634998755578));
#268982=CARTESIAN_POINT('Ctrl Pts',(-1.06194243707086,1.13661922900806,
13.6661032157693));
#268983=CARTESIAN_POINT('Ctrl Pts',(-1.06682146717324,1.132041065035,13.6665913274712));
#268984=CARTESIAN_POINT('Ctrl Pts',(-1.0744097607285,1.1248280734704,13.6673514978763));
#268985=CARTESIAN_POINT('Ctrl Pts',(-1.07713914210445,1.1222146845356,13.6676251267921));
#268986=CARTESIAN_POINT('Ctrl Pts',(-1.08217652191016,1.11735607247166,
13.668130481512));
#268987=CARTESIAN_POINT('Ctrl Pts',(-1.08448705553333,1.11511364622996,
13.6683624056499));
#268988=CARTESIAN_POINT('Ctrl Pts',(-1.08902927520813,1.11067784630976,
13.6688186115888));
#268989=CARTESIAN_POINT('Ctrl Pts',(-1.09126129507027,1.10848492406989,
13.6690429224655));
#268990=CARTESIAN_POINT('Ctrl Pts',(-1.09801008749208,1.10181420801552,
13.6697216205818));
#268991=CARTESIAN_POINT('Ctrl Pts',(-1.10250610512266,1.09731535717561,
13.6701744032067));
#268992=CARTESIAN_POINT('Ctrl Pts',(-1.12848152482335,1.07100274917494,
13.6727949887573));
#268993=CARTESIAN_POINT('Ctrl Pts',(-1.14934262608573,1.04858442651917,
13.6749183423942));
#268994=CARTESIAN_POINT('Ctrl Pts',(-1.21594893668811,0.972628012759765,
13.6818208369414));
#268995=CARTESIAN_POINT('Ctrl Pts',(-1.25872456846244,0.916597678142573,
13.6864598008834));
#268996=CARTESIAN_POINT('Ctrl Pts',(-1.36049882817829,0.762658125252066,
13.6986087720395));
#268997=CARTESIAN_POINT('Ctrl Pts',(-1.41276211104518,0.660835304177493,
13.7060999184273));
#268998=CARTESIAN_POINT('Ctrl Pts',(-1.46002081698805,0.536901277587853,
13.7152981382997));
#268999=CARTESIAN_POINT('Ctrl Pts',(-1.46631419443058,0.519467419739277,
13.7165929077524));
#269000=CARTESIAN_POINT('Ctrl Pts',(-1.47467681327628,0.494937431694128,
13.7184178410167));
#269001=CARTESIAN_POINT('Ctrl Pts',(-1.47700945658193,0.487932194779434,
13.7189393546206));
#269002=CARTESIAN_POINT('Ctrl Pts',(-1.48096668264113,0.475759679229069,
13.7198462906411));
#269003=CARTESIAN_POINT('Ctrl Pts',(-1.48261432658778,0.470599983763692,
13.7202309517733));
#269004=CARTESIAN_POINT('Ctrl Pts',(-1.48598805829119,0.459841350453832,
13.7210335500361));
#269005=CARTESIAN_POINT('Ctrl Pts',(-1.48770952472348,0.454241065174517,
13.7214516309685));
#269006=CARTESIAN_POINT('Ctrl Pts',(-1.49170054395539,0.440991383826819,
13.7224415394216));
#269007=CARTESIAN_POINT('Ctrl Pts',(-1.49394294040363,0.433334051129318,
13.723014239705));
#269008=CARTESIAN_POINT('Ctrl Pts',(-1.4985407327796,0.417173549614107,
13.7242243169945));
#269009=CARTESIAN_POINT('Ctrl Pts',(-1.50088288159451,0.408666940270814,
13.7248621014086));
#269010=CARTESIAN_POINT('Ctrl Pts',(-1.51057966231786,0.372240432773733,
13.7275969994662));
#269011=CARTESIAN_POINT('Ctrl Pts',(-1.51722809949493,0.34414029899846,
13.7297164446371));
#269012=CARTESIAN_POINT('Ctrl Pts',(-1.54473528368205,0.21150498246949,
13.7397716978657));
#269013=CARTESIAN_POINT('Ctrl Pts',(-1.55559124031108,0.105207658855261,
13.7480058999189));
#269014=CARTESIAN_POINT('Ctrl Pts',(-1.55549942243246,-0.00134045226759553,
13.7562673955592));
#269015=CARTESIAN_POINT('Ctrl Pts',(-1.555499421659,-0.00134134951378047,
13.7562674651297));
#269016=CARTESIAN_POINT('Ctrl Pts',(-1.55542394797204,-0.0888646051650332,
13.7630538171062));
#269017=CARTESIAN_POINT('Ctrl Pts',(-1.54796158042164,-0.176239683107133,
13.769824279052));
#269018=CARTESIAN_POINT('Ctrl Pts',(-1.53222541744419,-0.268137709402849,
13.7766750956072));
#269019=CARTESIAN_POINT('Ctrl Pts',(-1.53123530937207,-0.273735257118771,
13.7770912617309));
#269020=CARTESIAN_POINT('Ctrl Pts',(-1.52953758398736,-0.283035756747498,
13.7777807331157));
#269021=CARTESIAN_POINT('Ctrl Pts',(-1.52884716097948,-0.286741729761807,
13.7780549372045));
#269022=CARTESIAN_POINT('Ctrl Pts',(-1.52757271702178,-0.293447066589199,
13.7785500596778));
#269023=CARTESIAN_POINT('Ctrl Pts',(-1.5269933206881,-0.296447273035847,
13.7787712305849));
#269024=CARTESIAN_POINT('Ctrl Pts',(-1.52578578452506,-0.302602608692982,
13.7792242176254));
#269025=CARTESIAN_POINT('Ctrl Pts',(-1.52515670426852,-0.305757464130997,
13.7794559675518));
#269026=CARTESIAN_POINT('Ctrl Pts',(-1.52371394955127,-0.312877667828354,
13.7799780624258));
#269027=CARTESIAN_POINT('Ctrl Pts',(-1.52289458257793,-0.316841800336313,
13.7802680806119));
#269028=CARTESIAN_POINT('Ctrl Pts',(-1.52037515790309,-0.328795297816436,
13.7811407524533));
#269029=CARTESIAN_POINT('Ctrl Pts',(-1.51862760042459,-0.336774683673459,
13.7817207901984));
#269030=CARTESIAN_POINT('Ctrl Pts',(-1.50002669118191,-0.418616553269739,
13.7876478157671));
#269031=CARTESIAN_POINT('Ctrl Pts',(-1.47785858246025,-0.491179692018681,
13.7927186950357));
#269032=CARTESIAN_POINT('Ctrl Pts',(-1.42971047402387,-0.615480554534184,
13.8015367829861));
#269033=CARTESIAN_POINT('Ctrl Pts',(-1.40597689187837,-0.667920211683963,
13.805301279978));
#269034=CARTESIAN_POINT('Ctrl Pts',(-1.34490607878004,-0.785096086708805,
13.8140380613771));
#269035=CARTESIAN_POINT('Ctrl Pts',(-1.30570601163146,-0.848691935995779,
13.8190280247341));
#269036=CARTESIAN_POINT('Ctrl Pts',(-1.24924637175966,-0.927063712846012,
13.8257022261241));
#269037=CARTESIAN_POINT('Ctrl Pts',(-1.23601901106091,-0.944627199154691,
13.8272344172082));
#269038=CARTESIAN_POINT('Ctrl Pts',(-1.21834382729615,-0.967089505732215,
13.829245279046));
#269039=CARTESIAN_POINT('Ctrl Pts',(-1.21423032916878,-0.972249195904546,
13.8297107932177));
#269040=CARTESIAN_POINT('Ctrl Pts',(-1.20606691872174,-0.982356205174639,
13.8306299122717));
#269041=CARTESIAN_POINT('Ctrl Pts',(-1.2020190850422,-0.987305040632434,
13.8310834284625));
#269042=CARTESIAN_POINT('Ctrl Pts',(-1.19425861286853,-0.996674440019329,
13.8319487803847));
#269043=CARTESIAN_POINT('Ctrl Pts',(-1.19055164083243,-1.00109957679535,
13.8323603816892));
#269044=CARTESIAN_POINT('Ctrl Pts',(-1.18203579936579,-1.01115102679588,
13.8333020236178));
#269045=CARTESIAN_POINT('Ctrl Pts',(-1.1772112645467,-1.01676381972,13.8338327009346));
#269046=CARTESIAN_POINT('Ctrl Pts',(-1.16453357234536,-1.03130167038854,
13.8352201050721));
#269047=CARTESIAN_POINT('Ctrl Pts',(-1.15661796188794,-1.04017135709515,
13.8360794089955));
#269048=CARTESIAN_POINT('Ctrl Pts',(-1.09426903235366,-1.10844356984625,
13.8427959279096));
#269049=CARTESIAN_POINT('Ctrl Pts',(-1.03540586685138,-1.1636161245161,
13.848843685773));
#269050=CARTESIAN_POINT('Ctrl Pts',(-0.897708902440449,-1.27392848768245,
13.8623716080388));
#269051=CARTESIAN_POINT('Ctrl Pts',(-0.817493066480184,-1.32683052556791,
13.8698808194894));
#269052=CARTESIAN_POINT('Ctrl Pts',(-0.705432959993615,-1.38669234473495,
13.8796062008373));
#269053=CARTESIAN_POINT('Ctrl Pts',(-0.677509894960468,-1.4005470125059,
13.8819700809562));
#269054=CARTESIAN_POINT('Ctrl Pts',(-0.632673719022722,-1.42113843186653,
13.8856537936808));
#269055=CARTESIAN_POINT('Ctrl Pts',(-0.61602722266824,-1.42843306309832,
13.8869977175083));
#269056=CARTESIAN_POINT('Ctrl Pts',(-0.594271376189781,-1.43751554964689,
13.8887201536663));
#269057=CARTESIAN_POINT('Ctrl Pts',(-0.589276085943536,-1.43957046402505,
13.8891133392763));
#269058=CARTESIAN_POINT('Ctrl Pts',(-0.581460023397564,-1.44273825927916,
13.8897248604344));
#269059=CARTESIAN_POINT('Ctrl Pts',(-0.578646595453798,-1.44386895582517,
13.889944236981));
#269060=CARTESIAN_POINT('Ctrl Pts',(-0.572829285119295,-1.44618715705759,
13.8903962810099));
#269061=CARTESIAN_POINT('Ctrl Pts',(-0.569825053464294,-1.44737351497923,
13.8906288685618));
#269062=CARTESIAN_POINT('Ctrl Pts',(-0.562966613211537,-1.45005721901695,
13.8911579136427));
#269063=CARTESIAN_POINT('Ctrl Pts',(-0.559110114859249,-1.45154856155106,
13.8914540109092));
#269064=CARTESIAN_POINT('Ctrl Pts',(-0.54887583830307,-1.45545940953836,
13.8922362408763));
#269065=CARTESIAN_POINT('Ctrl Pts',(-0.54248791948583,-1.45785240693218,
13.8927208488526));
#269066=CARTESIAN_POINT('Ctrl Pts',(-0.49632850963146,-1.47479890636588,
13.8961979446267));
#269067=CARTESIAN_POINT('Ctrl Pts',(-0.455988706641099,-1.48776641226626,
13.8991050194487));
#269068=CARTESIAN_POINT('Ctrl Pts',(-0.31782043230741,-1.52603188908608,
13.9087822336986));
#269069=CARTESIAN_POINT('Ctrl Pts',(-0.218075711322604,-1.54344701824852,
13.9153173802451));
#269070=CARTESIAN_POINT('Ctrl Pts',(-0.0642819751277782,-1.55508183062603,
13.9255477747706));
#269071=CARTESIAN_POINT('Ctrl Pts',(-0.0110557105183446,-1.55637035341085,
13.9291132382103));
#269072=CARTESIAN_POINT('Ctrl Pts',(0.0632624219517054,-1.55435680552894,
13.9342018805486));
#269073=CARTESIAN_POINT('Ctrl Pts',(0.0843814181962754,-1.55335344310347,
13.9356601720196));
#269074=CARTESIAN_POINT('Ctrl Pts',(0.121065411833475,-1.5508603014553,
13.9382188935981));
#269075=CARTESIAN_POINT('Ctrl Pts',(0.136640844848652,-1.54956566726711,
13.9393133453624));
#269076=CARTESIAN_POINT('Ctrl Pts',(0.159817376257911,-1.54728709012976,
13.9409551451811));
#269077=CARTESIAN_POINT('Ctrl Pts',(0.167435339975332,-1.54648127572977,
13.9414969280022));
#269078=CARTESIAN_POINT('Ctrl Pts',(0.180817647551001,-1.5449656814214,
13.9424525645731));
#269079=CARTESIAN_POINT('Ctrl Pts',(0.186584597428597,-1.54427982074695,
13.9428656605312));
#269080=CARTESIAN_POINT('Ctrl Pts',(0.197808293237889,-1.54288120490314,
13.9436721794718));
#269081=CARTESIAN_POINT('Ctrl Pts',(0.20326537082163,-1.54217175467155,
13.944065492624));
#269082=CARTESIAN_POINT('Ctrl Pts',(0.217902694031781,-1.54018978109164,
13.9451236843625));
#269083=CARTESIAN_POINT('Ctrl Pts',(0.227075396453182,-1.53886416010994,
13.9457902248465));
#269084=CARTESIAN_POINT('Ctrl Pts',(0.260995846663186,-1.53365216587991,
13.9482680823758));
#269085=CARTESIAN_POINT('Ctrl Pts',(0.285659229486592,-1.52925029577789,
13.9500954971752));
#269086=CARTESIAN_POINT('Ctrl Pts',(0.479353219575773,-1.48983123210039,
13.964660750462));
#269087=CARTESIAN_POINT('Ctrl Pts',(0.641580781174021,-1.42748861649259,
13.9783450837591));
#269088=CARTESIAN_POINT('Ctrl Pts',(0.819120240931761,-1.32278107627788,
13.9939805151973));
#269089=CARTESIAN_POINT('Ctrl Pts',(0.847485929812238,-1.30478955056603,
13.9964945686221));
#269090=CARTESIAN_POINT('Ctrl Pts',(0.880828612054437,-1.28209467455352,
13.999449958471));
#269091=CARTESIAN_POINT('Ctrl Pts',(0.886383160992166,-1.2782608085616,
13.9999422980049));
#269092=CARTESIAN_POINT('Ctrl Pts',(0.894985918576415,-1.27223996411929,
14.0007046094499));
#269093=CARTESIAN_POINT('Ctrl Pts',(0.898051375772499,-1.27007796927322,
14.0009762046691));
#269094=CARTESIAN_POINT('Ctrl Pts',(0.903735999749112,-1.26603786652385,
14.0014797305121));
#269095=CARTESIAN_POINT('Ctrl Pts',(0.906357127918199,-1.26416272438452,
14.0017118470248));
#269096=CARTESIAN_POINT('Ctrl Pts',(0.91232370999698,-1.25986616453107,
14.0022401202137));
#269097=CARTESIAN_POINT('Ctrl Pts',(0.9156653598114,-1.2574395628645,14.0025359162271));
#269098=CARTESIAN_POINT('Ctrl Pts',(0.924367352814728,-1.25106736298631,
14.0033061334268));
#269099=CARTESIAN_POINT('Ctrl Pts',(0.929712180830482,-1.2471005631822,
14.0037791412212));
#269100=CARTESIAN_POINT('Ctrl Pts',(0.965954529295828,-1.21983988279399,
14.0069873430414));
#269101=CARTESIAN_POINT('Ctrl Pts',(0.996002166994366,-1.19543205529874,
14.0096513480871));
#269102=CARTESIAN_POINT('Ctrl Pts',(1.13812891129731,-1.07089798544751,
14.0224491256689));
#269103=CARTESIAN_POINT('Ctrl Pts',(1.23620420906182,-0.956015343843199,
14.0319857622665));
#269104=CARTESIAN_POINT('Ctrl Pts',(1.33684677620992,-0.796184803320936,
14.0448378869267));
#269105=CARTESIAN_POINT('Ctrl Pts',(1.35618599479533,-0.7627769461492,14.0474991020282));
#269106=CARTESIAN_POINT('Ctrl Pts',(1.37916437902502,-0.719441022950661,
14.0509390434279));
#269107=CARTESIAN_POINT('Ctrl Pts',(1.38397333559117,-0.710146158717262,
14.0516761341921));
#269108=CARTESIAN_POINT('Ctrl Pts',(1.39156045790689,-0.695111782705513,
14.0528675768741));
#269109=CARTESIAN_POINT('Ctrl Pts',(1.39439782002678,-0.689402361304805,
14.053319853124));
#269110=CARTESIAN_POINT('Ctrl Pts',(1.39973897550416,-0.67848686165099,
14.0541842689806));
#269111=CARTESIAN_POINT('Ctrl Pts',(1.40224902971585,-0.673283950488848,
14.0545961824337));
#269112=CARTESIAN_POINT('Ctrl Pts',(1.40792318031783,-0.661353041222404,
14.0555405594739));
#269113=CARTESIAN_POINT('Ctrl Pts',(1.41106811619982,-0.654616143019086,
14.0560736732287));
#269114=CARTESIAN_POINT('Ctrl Pts',(1.41916247491842,-0.636947499641706,
14.0574716406558));
#269115=CARTESIAN_POINT('Ctrl Pts',(1.42403382068632,-0.625980758538256,
14.0583391361447));
#269116=CARTESIAN_POINT('Ctrl Pts',(1.46362193219472,-0.534002908640036,
14.0656146311728));
#269117=CARTESIAN_POINT('Ctrl Pts',(1.49151614713888,-0.450247279612979,
14.0722526854534));
#269118=CARTESIAN_POINT('Ctrl Pts',(1.51437955710908,-0.355420693444977,
14.0797556027548));
#269119=CARTESIAN_POINT('Ctrl Pts',(1.51650801132852,-0.346226458405174,
14.0804827849193));
#269120=CARTESIAN_POINT('Ctrl Pts',(1.53799900059489,-0.249389988913261,
14.0881371409923));
#269121=CARTESIAN_POINT('Ctrl Pts',(1.54982507646817,-0.160247161293668,
14.0951572699393));
#269122=CARTESIAN_POINT('Ctrl Pts',(1.55552459876715,-0.034766945670613,
14.104703441249));
#269123=CARTESIAN_POINT('Ctrl Pts',(1.55591285957617,0.00109598353668149,
14.1073920035592));
#269124=CARTESIAN_POINT('Ctrl Pts',(1.55489805662046,0.0438119126565924,
14.1105237168089));
#269125=CARTESIAN_POINT('Ctrl Pts',(1.5546893807644,0.0506792285990876,
14.1110250102522));
#269126=CARTESIAN_POINT('Ctrl Pts',(1.55429546432879,0.0613198828896375,
14.1117981353413));
#269127=CARTESIAN_POINT('Ctrl Pts',(1.55414197076843,0.0650941932193456,
14.1120716634984));
#269128=CARTESIAN_POINT('Ctrl Pts',(1.5538321676789,0.0720847613072222,
14.1125769265078));
#269129=CARTESIAN_POINT('Ctrl Pts',(1.55367962191105,0.0753010687049443,
14.11280885908));
#269130=CARTESIAN_POINT('Ctrl Pts',(1.55331046554904,0.082605103211132,
14.1133343671755));
#269131=CARTESIAN_POINT('Ctrl Pts',(1.55308770642234,0.0866924602037214,
14.1136275970647));
#269132=CARTESIAN_POINT('Ctrl Pts',(1.55246741763863,0.0973030110623689,
14.1143867208042));
#269133=CARTESIAN_POINT('Ctrl Pts',(1.55204490385286,0.10382475230554,14.1148512669579));
#269134=CARTESIAN_POINT('Ctrl Pts',(1.54901116597825,0.146483165649293,
14.1178775920443));
#269135=CARTESIAN_POINT('Ctrl Pts',(1.54517892804341,0.182525373289272,
14.1203770470608));
#269136=CARTESIAN_POINT('Ctrl Pts',(1.53875895622177,0.227796197206829,
14.1234810896471));
#269137=CARTESIAN_POINT('Ctrl Pts',(1.53734114932868,0.237175947248667,
14.124122286209));
#269138=CARTESIAN_POINT('Ctrl Pts',(1.51983133250108,0.346253514021789,
14.1315622405307));
#269139=CARTESIAN_POINT('Ctrl Pts',(1.4941523090723,0.444173292909463,14.1380947421775));
#269140=CARTESIAN_POINT('Ctrl Pts',(1.45141285026689,0.559893776997534,
14.1462866907977));
#269141=CARTESIAN_POINT('Ctrl Pts',(1.44321615033215,0.58069516914172,14.1477780500171));
#269142=CARTESIAN_POINT('Ctrl Pts',(1.43457666475166,0.601306945702447,
14.1492791259731));
#269143=CARTESIAN_POINT('Origin',(0.,0.,-1.29405622560371));
#269144=CARTESIAN_POINT('',(1.4345766844093,0.601306898803946,14.987048570644));
#269145=CARTESIAN_POINT('',(1.43457662445949,0.601307041830064,14.8491341039362));
#269146=CARTESIAN_POINT('',(1.43457668357355,0.601306900797845,-1.29405622560371));
#269147=CARTESIAN_POINT('',(-1.55549959649185,0.00112040782065311,14.5950894464761));
#269148=CARTESIAN_POINT('Ctrl Pts',(1.4345766844093,0.601306898803942,14.987048570644));
#269149=CARTESIAN_POINT('Ctrl Pts',(1.49486490206182,0.457473406188229,
14.976439209092));
#269150=CARTESIAN_POINT('Ctrl Pts',(1.53318843830475,0.305373873929638,
14.9665756914561));
#269151=CARTESIAN_POINT('Ctrl Pts',(1.55186059850538,0.112762420484539,
14.9534032965279));
#269152=CARTESIAN_POINT('Ctrl Pts',(1.55412782937726,0.0753192035225039,
14.9508170288459));
#269153=CARTESIAN_POINT('Ctrl Pts',(1.55530042438738,0.0271224202641314,
14.9474374879375));
#269154=CARTESIAN_POINT('Ctrl Pts',(1.55545033675133,0.0164096155206039,
14.9466831401705));
#269155=CARTESIAN_POINT('Ctrl Pts',(1.55551293087773,-0.000682820512163463,
14.9454741278517));
#269156=CARTESIAN_POINT('Ctrl Pts',(1.55549704933952,-0.00706198732699898,
14.9450216973144));
#269157=CARTESIAN_POINT('Ctrl Pts',(1.55539770759106,-0.0185583587751548,
14.9442040810712));
#269158=CARTESIAN_POINT('Ctrl Pts',(1.55532823072722,-0.0236756206461456,
14.9438393377651));
#269159=CARTESIAN_POINT('Ctrl Pts',(1.55510551932437,-0.0357054738714125,
14.9429799409452));
#269160=CARTESIAN_POINT('Ctrl Pts',(1.55493144578642,-0.0426175215637954,
14.9424846433416));
#269161=CARTESIAN_POINT('Ctrl Pts',(1.55429084062506,-0.0627264404817726,
14.9410391678639));
#269162=CARTESIAN_POINT('Ctrl Pts',(1.55370234646703,-0.0759185232106978,
14.9400852083322));
#269163=CARTESIAN_POINT('Ctrl Pts',(1.55199334469202,-0.105704756185604,
14.9379178593878));
#269164=CARTESIAN_POINT('Ctrl Pts',(1.55077451958072,-0.122291403380222,
14.9367015250704));
#269165=CARTESIAN_POINT('Ctrl Pts',(1.54593622038812,-0.17627536209115,
14.9327109837878));
#269166=CARTESIAN_POINT('Ctrl Pts',(1.54122803732576,-0.213559167661376,
14.9299047078128));
#269167=CARTESIAN_POINT('Ctrl Pts',(1.50962398916305,-0.407139761776606,
14.9150739528187));
#269168=CARTESIAN_POINT('Ctrl Pts',(1.46029687605994,-0.55879555238969,
14.9024383936853));
#269169=CARTESIAN_POINT('Ctrl Pts',(1.3825376542555,-0.713000734108949,
14.8896108510062));
#269170=CARTESIAN_POINT('Ctrl Pts',(1.37599517880621,-0.725546496153935,
14.8885683386006));
#269171=CARTESIAN_POINT('Ctrl Pts',(1.36682924517354,-0.74255288928872,
14.8871583950433));
#269172=CARTESIAN_POINT('Ctrl Pts',(1.36435363637782,-0.747091785398318,
14.8867824091287));
#269173=CARTESIAN_POINT('Ctrl Pts',(1.36038715102502,-0.754278650312392,
14.8861876821429));
#269174=CARTESIAN_POINT('Ctrl Pts',(1.35891109661614,-0.756934683390036,
14.8859680227311));
#269175=CARTESIAN_POINT('Ctrl Pts',(1.35584117107055,-0.762420827647948,
14.8855146083494));
#269176=CARTESIAN_POINT('Ctrl Pts',(1.3542462126083,-0.765250282898886,
14.8852809324592));
#269177=CARTESIAN_POINT('Ctrl Pts',(1.35039637250112,-0.772030165909536,
14.8847213672156));
#269178=CARTESIAN_POINT('Ctrl Pts',(1.34813297822836,-0.775975782069383,
14.8843960196119));
#269179=CARTESIAN_POINT('Ctrl Pts',(1.34028754759362,-0.789514229579249,
14.8832804854181));
#269180=CARTESIAN_POINT('Ctrl Pts',(1.33461999815095,-0.799057512441261,
14.8824955637599));
#269181=CARTESIAN_POINT('Ctrl Pts',(1.30067556034983,-0.854845851685494,
14.8779103999651));
#269182=CARTESIAN_POINT('Ctrl Pts',(1.270095811652,-0.899653488003313,14.874240872608));
#269183=CARTESIAN_POINT('Ctrl Pts',(1.18031980704884,-1.0174692048576,14.8643632437778));
#269184=CARTESIAN_POINT('Ctrl Pts',(1.11675754865631,-1.08685408867507,
14.8582744560472));
#269185=CARTESIAN_POINT('Ctrl Pts',(0.995846956086833,-1.19696136337736,
14.8473810357873));
#269186=CARTESIAN_POINT('Ctrl Pts',(0.941287329985927,-1.24032406775073,
14.8426667396948));
#269187=CARTESIAN_POINT('Ctrl Pts',(0.874552777073934,-1.28641745353404,
14.8369986175241));
#269188=CARTESIAN_POINT('Ctrl Pts',(0.865021222204317,-1.29284596813049,
14.8361913775601));
#269189=CARTESIAN_POINT('Ctrl Pts',(0.84937607011585,-1.30314730509912,
14.8348696227709));
#269190=CARTESIAN_POINT('Ctrl Pts',(0.843305037361686,-1.30708424289972,
14.8343575078911));
#269191=CARTESIAN_POINT('Ctrl Pts',(0.832410176387109,-1.31404183327217,
14.833439761891));
#269192=CARTESIAN_POINT('Ctrl Pts',(0.827596787547885,-1.31707866014364,
14.8330347389075));
#269193=CARTESIAN_POINT('Ctrl Pts',(0.817376138388073,-1.32344884581364,
14.8321755877951));
#269194=CARTESIAN_POINT('Ctrl Pts',(0.811964922446482,-1.32677562594298,
14.8317212273248));
#269195=CARTESIAN_POINT('Ctrl Pts',(0.797477704479851,-1.33556045313757,
14.8305060392756));
#269196=CARTESIAN_POINT('Ctrl Pts',(0.788366222054037,-1.34095902351144,
14.8297430660026));
#269197=CARTESIAN_POINT('Ctrl Pts',(0.743669932872061,-1.36682866862723,
14.8260059052544));
#269198=CARTESIAN_POINT('Ctrl Pts',(0.707342550418044,-1.3859767350806,
14.8229850016968));
#269199=CARTESIAN_POINT('Ctrl Pts',(0.536369388325766,-1.4676229683982,
14.8088271239949));
#269200=CARTESIAN_POINT('Ctrl Pts',(0.393975421402373,-1.51207780353708,
14.7971040263131));
#269201=CARTESIAN_POINT('Ctrl Pts',(0.209887098955397,-1.54174519951429,
14.7829022388443));
#269202=CARTESIAN_POINT('Ctrl Pts',(0.172071569920612,-1.54642258921192,
14.7800398705558));
#269203=CARTESIAN_POINT('Ctrl Pts',(0.127570565130129,-1.5502739118521,
14.7767628341066));
#269204=CARTESIAN_POINT('Ctrl Pts',(0.121018624993018,-1.5507991318482,
14.7762826707616));
#269205=CARTESIAN_POINT('Ctrl Pts',(0.110396207315975,-1.55158292060797,
14.7755081630059));
#269206=CARTESIAN_POINT('Ctrl Pts',(0.106327787713946,-1.55186703190108,
14.7752124651791));
#269207=CARTESIAN_POINT('Ctrl Pts',(0.0990830193210822,-1.5523443339152,
14.7746876363614));
#269208=CARTESIAN_POINT('Ctrl Pts',(0.0959071563343846,-1.55254378160758,
14.7744581635346));
#269209=CARTESIAN_POINT('Ctrl Pts',(0.0890368977889373,-1.55295407948584,
14.7739630449436));
#269210=CARTESIAN_POINT('Ctrl Pts',(0.0853423595391087,-1.55316149340679,
14.773697592557));
#269211=CARTESIAN_POINT('Ctrl Pts',(0.0750097057204092,-1.55370459556713,
14.7729573441526));
#269212=CARTESIAN_POINT('Ctrl Pts',(0.0683700202281368,-1.55401093008039,
14.7724841488582));
#269213=CARTESIAN_POINT('Ctrl Pts',(0.0289741863571047,-1.55557554567858,
14.7696901239696));
#269214=CARTESIAN_POINT('Ctrl Pts',(-0.00381608135986826,-1.55584080807551,
14.7674203988275));
#269215=CARTESIAN_POINT('Ctrl Pts',(-0.194838050308205,-1.55134576804175,
14.7543948445618));
#269216=CARTESIAN_POINT('Ctrl Pts',(-0.351594185123817,-1.52349160191971,
14.7443993367283));
#269217=CARTESIAN_POINT('Ctrl Pts',(-0.536872277991188,-1.46039304176426,
14.7310752183441));
#269218=CARTESIAN_POINT('Ctrl Pts',(-0.571834710660903,-1.44706059220272,
14.7284952494209));
#269219=CARTESIAN_POINT('Ctrl Pts',(-0.616138326706858,-1.42830962991474,
14.7251228610801));
#269220=CARTESIAN_POINT('Ctrl Pts',(-0.625952705227407,-1.42403582721424,
14.7243691599743));
#269221=CARTESIAN_POINT('Ctrl Pts',(-0.641542237557301,-1.41705485979598,
14.7231609419995));
#269222=CARTESIAN_POINT('Ctrl Pts',(-0.647346334614583,-1.41441282485061,
14.722708653952));
#269223=CARTESIAN_POINT('Ctrl Pts',(-0.658184564721687,-1.40939855877366,
14.7218593758202));
#269224=CARTESIAN_POINT('Ctrl Pts',(-0.663222548960715,-1.40703484952657,
14.7214626844791));
#269225=CARTESIAN_POINT('Ctrl Pts',(-0.67455919067198,-1.40164153738495,
14.7205656396141));
#269226=CARTESIAN_POINT('Ctrl Pts',(-0.680850293412602,-1.39859643072956,
14.7200647553006));
#269227=CARTESIAN_POINT('Ctrl Pts',(-0.699458354821174,-1.3894341960119,
14.7185739050948));
#269228=CARTESIAN_POINT('Ctrl Pts',(-0.711714656474277,-1.38319615396487,
14.7175797482935));
#269229=CARTESIAN_POINT('Ctrl Pts',(-0.739531135586624,-1.36857092359856,
14.7152947410611));
#269230=CARTESIAN_POINT('Ctrl Pts',(-0.755034030115011,-1.36007949747804,
14.7140003393474));
#269231=CARTESIAN_POINT('Ctrl Pts',(-0.806025673564585,-1.3310092631534,
14.709671635109));
#269232=CARTESIAN_POINT('Ctrl Pts',(-0.840842318597159,-1.30929244409194,
14.7065988758501));
#269233=CARTESIAN_POINT('Ctrl Pts',(-0.963608840547663,-1.22579944926369,
14.695335402881));
#269234=CARTESIAN_POINT('Ctrl Pts',(-1.04595565381527,-1.15633015067891,
14.6869212469262));
#269235=CARTESIAN_POINT('Ctrl Pts',(-1.15829691523965,-1.03966416688124,
14.6744628789054));
#269236=CARTESIAN_POINT('Ctrl Pts',(-1.19403128661577,-0.998420798811307,
14.6703210304767));
#269237=CARTESIAN_POINT('Ctrl Pts',(-1.23233290277162,-0.949208637463735,
14.6657398916192));
#269238=CARTESIAN_POINT('Ctrl Pts',(-1.23709014440016,-0.943000213237792,
14.6651681972039));
#269239=CARTESIAN_POINT('Ctrl Pts',(-1.24420940695368,-0.933562639616464,
14.6643088613918));
#269240=CARTESIAN_POINT('Ctrl Pts',(-1.2466060371625,-0.930359951590167,
14.6640189122466));
#269241=CARTESIAN_POINT('Ctrl Pts',(-1.25088360745399,-0.924597501727867,
14.6635002613761));
#269242=CARTESIAN_POINT('Ctrl Pts',(-1.25276907636123,-0.922041203816691,
14.6632712504563));
#269243=CARTESIAN_POINT('Ctrl Pts',(-1.25686849950748,-0.916447462607108,
14.6627724571021));
#269244=CARTESIAN_POINT('Ctrl Pts',(-1.25907927652511,-0.913407769294506,
14.6625028936473));
#269245=CARTESIAN_POINT('Ctrl Pts',(-1.26532682650846,-0.904751959004491,
14.6617394002847));
#269246=CARTESIAN_POINT('Ctrl Pts',(-1.26933725965174,-0.899116795093998,
14.6612472371353));
#269247=CARTESIAN_POINT('Ctrl Pts',(-1.29515400094594,-0.86232398593046,
14.6580641158906));
#269248=CARTESIAN_POINT('Ctrl Pts',(-1.31585122304527,-0.830399122665444,
14.6554422922447));
#269249=CARTESIAN_POINT('Ctrl Pts',(-1.40070831188263,-0.688355256619558,
14.6442227513191));
#269250=CARTESIAN_POINT('Ctrl Pts',(-1.45237240917423,-0.571345816022819,
14.6360675361225));
#269251=CARTESIAN_POINT('Ctrl Pts',(-1.49991869317795,-0.413768607775255,
14.625041205455));
#269252=CARTESIAN_POINT('Ctrl Pts',(-1.50937247641969,-0.377829277982698,
14.6225269189865));
#269253=CARTESIAN_POINT('Ctrl Pts',(-1.51809288682723,-0.33908819225072,
14.6197992313694));
#269254=CARTESIAN_POINT('Ctrl Pts',(-1.51864937869788,-0.33658710554306,
14.6196230597135));
#269255=CARTESIAN_POINT('Ctrl Pts',(-1.52468852810913,-0.309124983517292,
14.6176878101906));
#269256=CARTESIAN_POINT('Ctrl Pts',(-1.52956113490112,-0.284035152648691,
14.6159117445361));
#269257=CARTESIAN_POINT('Ctrl Pts',(-1.53535643518452,-0.249693546340576,
14.6134645256988));
#269258=CARTESIAN_POINT('Ctrl Pts',(-1.53681774573789,-0.24053577670269,
14.612810382294));
#269259=CARTESIAN_POINT('Ctrl Pts',(-1.53900877225638,-0.225969092511054,
14.611767177405));
#269260=CARTESIAN_POINT('Ctrl Pts',(-1.53979207450111,-0.220568351705099,
14.6113798114108));
#269261=CARTESIAN_POINT('Ctrl Pts',(-1.54130551109226,-0.209732320819259,
14.6106013692436));
#269262=CARTESIAN_POINT('Ctrl Pts',(-1.54203535326286,-0.204297069951322,
14.6102102898128));
#269263=CARTESIAN_POINT('Ctrl Pts',(-1.54344536599304,-0.193358226605947,
14.609421916275));
#269264=CARTESIAN_POINT('Ctrl Pts',(-1.54412487755364,-0.187854631687998,
14.6090246074517));
#269265=CARTESIAN_POINT('Ctrl Pts',(-1.54561366289956,-0.175242244892861,
14.6081125469229));
#269266=CARTESIAN_POINT('Ctrl Pts',(-1.54640334242745,-0.168131313815164,
14.607597187089));
#269267=CARTESIAN_POINT('Ctrl Pts',(-1.54915474553508,-0.14169397103447,
14.6056767814503));
#269268=CARTESIAN_POINT('Ctrl Pts',(-1.55080336398481,-0.122337524634641,
14.6042620218949));
#269269=CARTESIAN_POINT('Ctrl Pts',(-1.55438730032399,-0.0683087702370583,
14.6002871583492));
#269270=CARTESIAN_POINT('Ctrl Pts',(-1.5555246032339,-0.03359728732884,
14.5977035516453));
#269271=CARTESIAN_POINT('Ctrl Pts',(-1.55549959649185,0.00112040782065311,
14.5950894464761));
#269272=CARTESIAN_POINT('Ctrl Pts',(-1.55549959789313,0.00111846069355959,
14.595089593087));
#269273=CARTESIAN_POINT('Ctrl Pts',(-1.55548425053835,0.0224627996720666,
14.5934824494409));
#269274=CARTESIAN_POINT('Ctrl Pts',(-1.55502958043063,0.0438039458821249,
14.5918642772033));
#269275=CARTESIAN_POINT('Ctrl Pts',(-1.54822857536825,0.206093876730948,
14.5794785918082));
#269276=CARTESIAN_POINT('Ctrl Pts',(-1.52317170858574,0.345589628889972,
14.5682926697141));
#269277=CARTESIAN_POINT('Ctrl Pts',(-1.47623606221595,0.490336843701623,
14.5569574948509));
#269278=CARTESIAN_POINT('Ctrl Pts',(-1.47270410090153,0.500845066095354,
14.556136665006));
#269279=CARTESIAN_POINT('Ctrl Pts',(-1.46630393991913,0.519233379449804,
14.5547049940083));
#269280=CARTESIAN_POINT('Ctrl Pts',(-1.4634838404652,0.527129589049032,
14.5540917494566));
#269281=CARTESIAN_POINT('Ctrl Pts',(-1.45920337267358,0.53881560366164,
14.553186856077));
#269282=CARTESIAN_POINT('Ctrl Pts',(-1.45779185164148,0.542622940793565,
14.552892463875));
#269283=CARTESIAN_POINT('Ctrl Pts',(-1.4552481092326,0.549402681953135,
14.5523690512611));
#269284=CARTESIAN_POINT('Ctrl Pts',(-1.45412166770451,0.552377174174578,
14.5521396964069));
#269285=CARTESIAN_POINT('Ctrl Pts',(-1.4516604967155,0.558816461569717,
14.5516438024714));
#269286=CARTESIAN_POINT('Ctrl Pts',(-1.45032248508607,0.562279935157498,
14.5513774623542));
#269287=CARTESIAN_POINT('Ctrl Pts',(-1.44659886112226,0.571816895843875,
14.5506450453363));
#269288=CARTESIAN_POINT('Ctrl Pts',(-1.44418737740314,0.577880307963531,
14.5501804797453));
#269289=CARTESIAN_POINT('Ctrl Pts',(-1.43148204040952,0.609250182459884,
14.5477817516802));
#269290=CARTESIAN_POINT('Ctrl Pts',(-1.42056017349597,0.634299338453912,
14.5458824696654));
#269291=CARTESIAN_POINT('Ctrl Pts',(-1.40137663391961,0.675311851633021,
14.5427786767828));
#269292=CARTESIAN_POINT('Ctrl Pts',(-1.39348878267914,0.691441703119032,
14.5415595310115));
#269293=CARTESIAN_POINT('Ctrl Pts',(-1.37812298516231,0.721531656444259,
14.5392815105495));
#269294=CARTESIAN_POINT('Ctrl Pts',(-1.37070779423519,0.735520945336393,
14.5382208704523));
#269295=CARTESIAN_POINT('Ctrl Pts',(-1.3128730877119,0.840716934861597,
14.5302153703065));
#269296=CARTESIAN_POINT('Ctrl Pts',(-1.25361624668274,0.926762009243754,
14.523477239618));
#269297=CARTESIAN_POINT('Ctrl Pts',(-1.1601289333121,1.03696926908142,14.5137991470962));
#269298=CARTESIAN_POINT('Ctrl Pts',(-1.13287604875944,1.06667514548298,
14.5110706280556));
#269299=CARTESIAN_POINT('Ctrl Pts',(-1.09220755453749,1.10768577517916,
14.5070956276272));
#269300=CARTESIAN_POINT('Ctrl Pts',(-1.0797054981399,1.11987549097028,14.5058859072131));
#269301=CARTESIAN_POINT('Ctrl Pts',(-1.05711322117367,1.14117332294881,
14.5037189025745));
#269302=CARTESIAN_POINT('Ctrl Pts',(-1.04710369134614,1.15036461802958,
14.502765204596));
#269303=CARTESIAN_POINT('Ctrl Pts',(-1.03177921489796,1.16407065873604,
14.5013138782989));
#269304=CARTESIAN_POINT('Ctrl Pts',(-1.0265520285847,1.16868292388205,14.5008203401368));
#269305=CARTESIAN_POINT('Ctrl Pts',(-1.01709071019442,1.17691877098868,
14.4999296178954));
#269306=CARTESIAN_POINT('Ctrl Pts',(-1.01286774664155,1.18055505276195,
14.4995329684991));
#269307=CARTESIAN_POINT('Ctrl Pts',(-1.00375940665784,1.18831315708249,
14.4986793481202));
#269308=CARTESIAN_POINT('Ctrl Pts',(-0.998867997074274,1.19242770343379,
14.4982220891621));
#269309=CARTESIAN_POINT('Ctrl Pts',(-0.985666066209812,1.20339464642037,
14.4969909351986));
#269310=CARTESIAN_POINT('Ctrl Pts',(-0.977309631316976,1.21019095302896,
14.4962147943293));
#269311=CARTESIAN_POINT('Ctrl Pts',(-0.939088544590627,1.24062220169355,
14.4926783033393));
#269312=CARTESIAN_POINT('Ctrl Pts',(-0.908435058600292,1.26324028518734,
14.4898783585339));
#269313=CARTESIAN_POINT('Ctrl Pts',(-0.746840842708807,1.3735498360812,
14.4752854896071));
#269314=CARTESIAN_POINT('Ctrl Pts',(-0.603987886157338,1.44207934776766,
14.4628021748968));
#269315=CARTESIAN_POINT('Ctrl Pts',(-0.42198731154876,1.49752411697499,
14.4483801948711));
#269316=CARTESIAN_POINT('Ctrl Pts',(-0.390377653254265,1.50607352411901,
14.4459309631188));
#269317=CARTESIAN_POINT('Ctrl Pts',(-0.352053900359383,1.51515096369368,
14.4430457372718));
#269318=CARTESIAN_POINT('Ctrl Pts',(-0.345578969477129,1.51664088421181,
14.4425611348744));
#269319=CARTESIAN_POINT('Ctrl Pts',(-0.335483792140536,1.51889583684061,
14.4418102454153));
#269320=CARTESIAN_POINT('Ctrl Pts',(-0.331870130960391,1.51968949292715,
14.4415423849408));
#269321=CARTESIAN_POINT('Ctrl Pts',(-0.325143076801083,1.52114179354025,
14.4410455126465));
#269322=CARTESIAN_POINT('Ctrl Pts',(-0.322030522570498,1.52180377161487,
14.4408163209499));
#269323=CARTESIAN_POINT('Ctrl Pts',(-0.31492345624512,1.52329252130051,
14.4402945863532));
#269324=CARTESIAN_POINT('Ctrl Pts',(-0.310927711278263,1.52411313495032,
14.4400023961408));
#269325=CARTESIAN_POINT('Ctrl Pts',(-0.298616267675917,1.52659112759011,
14.4391054935858));
#269326=CARTESIAN_POINT('Ctrl Pts',(-0.290290022620433,1.52819627584766,
14.4385036513972));
#269327=CARTESIAN_POINT('Ctrl Pts',(-0.273236051650089,1.53133955650659,
14.4372798288425));
#269328=CARTESIAN_POINT('Ctrl Pts',(-0.264507469498146,1.53287135294408,
14.4366581863243));
#269329=CARTESIAN_POINT('Ctrl Pts',(-0.0999070888177371,1.56030953543648,
14.4250162901345));
#269330=CARTESIAN_POINT('Ctrl Pts',(0.0590233411496406,1.56239584489408,
14.4150581402861));
#269331=CARTESIAN_POINT('Ctrl Pts',(0.271872446521253,1.53261167114947,
14.4006284059027));
#269332=CARTESIAN_POINT('Ctrl Pts',(0.327701868486181,1.5216515452454,14.3967481133074));
#269333=CARTESIAN_POINT('Ctrl Pts',(0.39408833510564,1.50479574678,14.3919536637725));
#269334=CARTESIAN_POINT('Ctrl Pts',(0.40534235679344,1.50180338797677,14.3911346217553));
#269335=CARTESIAN_POINT('Ctrl Pts',(0.422903946645971,1.49692212120169,
14.3898461900224));
#269336=CARTESIAN_POINT('Ctrl Pts',(0.42923509350274,1.49511899764551,14.3893795795179));
#269337=CARTESIAN_POINT('Ctrl Pts',(0.440445613630258,1.49184914435426,
14.3885495061347));
#269338=CARTESIAN_POINT('Ctrl Pts',(0.445329617618472,1.49039851671121,
14.3881865721065));
#269339=CARTESIAN_POINT('Ctrl Pts',(0.456580491852915,1.48699658667121,
14.3873474548923));
#269340=CARTESIAN_POINT('Ctrl Pts',(0.462942094221371,1.48502835298161,
14.386870724586));
#269341=CARTESIAN_POINT('Ctrl Pts',(0.480419513925493,1.47949774966963,
14.3855546228983));
#269342=CARTESIAN_POINT('Ctrl Pts',(0.491507972831767,1.47585107631614,
14.384712505617));
#269343=CARTESIAN_POINT('Ctrl Pts',(0.550780845115496,1.4556158839497,14.3801716684024));
#269344=CARTESIAN_POINT('Ctrl Pts',(0.598163740691983,1.43679371633505,
14.3763999178132));
#269345=CARTESIAN_POINT('Ctrl Pts',(0.755750221888889,1.36504762113438,
14.3633542651999));
#269346=CARTESIAN_POINT('Ctrl Pts',(0.860606315382178,1.30148514922372,
14.3537661588909));
#269347=CARTESIAN_POINT('Ctrl Pts',(0.984670651486607,1.20467523565277,
14.341681222052));
#269348=CARTESIAN_POINT('Ctrl Pts',(1.01167461188462,1.18208864292561,14.3390025534003));
#269349=CARTESIAN_POINT('Ctrl Pts',(1.04773862492915,1.14978207713126,14.3353806394628));
#269350=CARTESIAN_POINT('Ctrl Pts',(1.05747390685733,1.14083478899139,14.3343982469418));
#269351=CARTESIAN_POINT('Ctrl Pts',(1.07409403817436,1.12516434364419,14.3327146580435));
#269352=CARTESIAN_POINT('Ctrl Pts',(1.08103262876914,1.1184995624049,14.3320097947228));
#269353=CARTESIAN_POINT('Ctrl Pts',(1.09097799732966,1.10876764691982,14.3309971478179));
#269354=CARTESIAN_POINT('Ctrl Pts',(1.09403443020287,1.10575193974056,14.330685614288));
#269355=CARTESIAN_POINT('Ctrl Pts',(1.09935182797519,1.10046176336163,14.3301431205011));
#269356=CARTESIAN_POINT('Ctrl Pts',(1.10161829732988,1.09819290750213,14.3299117292382));
#269357=CARTESIAN_POINT('Ctrl Pts',(1.10639456503801,1.09338194473567,14.3294237829629));
#269358=CARTESIAN_POINT('Ctrl Pts',(1.10890262941845,1.09083819597026,14.3291673620266));
#269359=CARTESIAN_POINT('Ctrl Pts',(1.11564441217541,1.08395321181499,14.3284774847724));
#269360=CARTESIAN_POINT('Ctrl Pts',(1.11986160421642,1.07959576252823,14.3280452947567));
#269361=CARTESIAN_POINT('Ctrl Pts',(1.13884623476006,1.05974878955028,14.3260960940857));
#269362=CARTESIAN_POINT('Ctrl Pts',(1.15331943010993,1.043979241614,14.3246001274156));
#269363=CARTESIAN_POINT('Ctrl Pts',(1.17030921405807,1.02468294497131,14.3228244102407));
#269364=CARTESIAN_POINT('Ctrl Pts',(1.17314152807511,1.02143905846759,14.3225277091567));
#269365=CARTESIAN_POINT('Ctrl Pts',(1.18637016239279,1.00616052474135,14.3211385094828));
#269366=CARTESIAN_POINT('Ctrl Pts',(1.19659534262965,0.993978262325523,
14.3200547128902));
#269367=CARTESIAN_POINT('Ctrl Pts',(1.30038614212316,0.866398690485069,
14.3089227094254));
#269368=CARTESIAN_POINT('Ctrl Pts',(1.37714534498762,0.738324552090829,
14.2994889485436));
#269369=CARTESIAN_POINT('Ctrl Pts',(1.43457668360422,0.601306900724686,
14.2893889670083));
#269370=CARTESIAN_POINT('Ctrl Pts',(1.43457666475166,0.601306945702447,
14.1492791259731));
#269371=CARTESIAN_POINT('Ctrl Pts',(1.41615095798171,0.645266339740121,
14.1524805185963));
#269372=CARTESIAN_POINT('Ctrl Pts',(1.39571127249006,0.688363216504817,
14.1557269862668));
#269373=CARTESIAN_POINT('Ctrl Pts',(1.36533555092534,0.745471761040895,
14.1602228695212));
#269374=CARTESIAN_POINT('Ctrl Pts',(1.3571062184931,0.760349909706468,14.1614126364628));
#269375=CARTESIAN_POINT('Ctrl Pts',(1.34479420304447,0.781772481299565,
14.1631543778237));
#269376=CARTESIAN_POINT('Ctrl Pts',(1.34090390144716,0.788426524346289,
14.1636994630176));
#269377=CARTESIAN_POINT('Ctrl Pts',(1.33399232294111,0.800049088212788,
14.1646589011918));
#269378=CARTESIAN_POINT('Ctrl Pts',(1.33099231371677,0.805030136308535,
14.1650724769881));
#269379=CARTESIAN_POINT('Ctrl Pts',(1.32510643631638,0.814679879830104,
14.1658784216071));
#269380=CARTESIAN_POINT('Ctrl Pts',(1.32222364325466,0.819350358492522,
14.1662706733348));
#269381=CARTESIAN_POINT('Ctrl Pts',(1.31444659519299,0.831802200864574,
14.1673223448837));
#269382=CARTESIAN_POINT('Ctrl Pts',(1.30950804419281,0.839555494556103,
14.1679833896785));
#269383=CARTESIAN_POINT('Ctrl Pts',(1.29113768537945,0.867839645452182,
14.1704181551143));
#269384=CARTESIAN_POINT('Ctrl Pts',(1.27729005128138,0.888094685551313,
14.1722072558396));
#269385=CARTESIAN_POINT('Ctrl Pts',(1.26033577187772,0.911676672489267,
14.174346283534));
#269386=CARTESIAN_POINT('Ctrl Pts',(1.25768569959545,0.915329062849927,
14.1746792037951));
#269387=CARTESIAN_POINT('Ctrl Pts',(1.15521085351981,1.0552770301321,14.1874984922414));
#269388=CARTESIAN_POINT('Ctrl Pts',(1.03386376484364,1.1744034179853,14.2008904314514));
#269389=CARTESIAN_POINT('Ctrl Pts',(0.86849596856837,1.29089546984202,14.2162325932811));
#269390=CARTESIAN_POINT('Ctrl Pts',(0.840568560973116,1.30925218258257,
14.2187336155123));
#269391=CARTESIAN_POINT('Ctrl Pts',(0.806320926591495,1.33021510796637,
14.2216757884163));
#269392=CARTESIAN_POINT('Ctrl Pts',(0.800549860318849,1.33369621567632,
14.2221674263225));
#269393=CARTESIAN_POINT('Ctrl Pts',(0.791533462962841,1.33905529470563,
14.2229288898673));
#269394=CARTESIAN_POINT('Ctrl Pts',(0.788303753806995,1.34095917082117,
14.2232003331356));
#269395=CARTESIAN_POINT('Ctrl Pts',(0.782284672796656,1.34447808797766,
14.2237037242665));
#269396=CARTESIAN_POINT('Ctrl Pts',(0.779497189324543,1.34609612231607,
14.2239358570836));
#269397=CARTESIAN_POINT('Ctrl Pts',(0.773124038606977,1.3497690727102,14.2244643559788));
#269398=CARTESIAN_POINT('Ctrl Pts',(0.769535199760015,1.35181837023764,
14.2247603601764));
#269399=CARTESIAN_POINT('Ctrl Pts',(0.760136659553227,1.3571355640577,14.2255314794755));
#269400=CARTESIAN_POINT('Ctrl Pts',(0.754313963980703,1.36038050867561,
14.2260051757787));
#269401=CARTESIAN_POINT('Ctrl Pts',(0.714390058465094,1.38229465252935,
14.2292269138871));
#269402=CARTESIAN_POINT('Ctrl Pts',(0.679616700559208,1.39971905520224,
14.2319030886684));
#269403=CARTESIAN_POINT('Ctrl Pts',(0.557680721110371,1.45520196238738,
14.2409742755611));
#269404=CARTESIAN_POINT('Ctrl Pts',(0.467704087879769,1.48656518539461,
14.2471443532155));
#269405=CARTESIAN_POINT('Ctrl Pts',(0.297105345708217,1.52899358283808,
14.2587657909073));
#269406=CARTESIAN_POINT('Ctrl Pts',(0.217402974511302,1.5423444173344,14.2641658962156));
#269407=CARTESIAN_POINT('Ctrl Pts',(0.118831885331883,1.55106190972053,
14.2710334748072));
#269408=CARTESIAN_POINT('Ctrl Pts',(0.100606077109826,1.55235061536784,
14.272310690932));
#269409=CARTESIAN_POINT('Ctrl Pts',(0.0744404945306592,1.55373800769298,
14.2741568161015));
#269410=CARTESIAN_POINT('Ctrl Pts',(0.0665155791580642,1.55409744138275,
14.2747176015493));
#269411=CARTESIAN_POINT('Ctrl Pts',(0.0527414603637865,1.5546166162528,
14.2756952957193));
#269412=CARTESIAN_POINT('Ctrl Pts',(0.0468934065256717,1.55480400433193,
14.2761113341421));
#269413=CARTESIAN_POINT('Ctrl Pts',(0.0356189492305106,1.55510160363929,
14.2769152897417));
#269414=CARTESIAN_POINT('Ctrl Pts',(0.0301927434527061,1.55521641711133,
14.2773030570594));
#269415=CARTESIAN_POINT('Ctrl Pts',(0.0173401977181681,1.55542107665724,
14.2782235632367));
#269416=CARTESIAN_POINT('Ctrl Pts',(0.00991365484985559,1.55548613753573,
14.2787570677559));
#269417=CARTESIAN_POINT('Ctrl Pts',(-0.0163044721599605,1.55552805707598,
14.2806463886457));
#269418=CARTESIAN_POINT('Ctrl Pts',(-0.0350941927334791,1.55521757717389,
14.2820110866454));
#269419=CARTESIAN_POINT('Ctrl Pts',(-0.155588080260383,1.55104190617281,
14.2908350002324));
#269420=CARTESIAN_POINT('Ctrl Pts',(-0.256692252927695,1.53754360718377,
14.2985947740687));
#269421=CARTESIAN_POINT('Ctrl Pts',(-0.401040464613895,1.50363312636605,
14.3100734624229));
#269422=CARTESIAN_POINT('Ctrl Pts',(-0.445844737903421,1.49096228745882,
14.3136906990146));
#269423=CARTESIAN_POINT('Ctrl Pts',(-0.545740143620875,1.45780503420672,
14.3218166073789));
#269424=CARTESIAN_POINT('Ctrl Pts',(-0.600381412745239,1.43616558094254,
14.3263052277747));
#269425=CARTESIAN_POINT('Ctrl Pts',(-0.664205836612502,1.4066078258431,
14.3315070239361));
#269426=CARTESIAN_POINT('Ctrl Pts',(-0.674683584151132,1.40161230441675,
14.332359535248));
#269427=CARTESIAN_POINT('Ctrl Pts',(-0.689293537626307,1.39444484898514,
14.33354524951));
#269428=CARTESIAN_POINT('Ctrl Pts',(-0.693473040825964,1.39237105724174,
14.3338841005771));
#269429=CARTESIAN_POINT('Ctrl Pts',(-0.700592755273029,1.38879837688395,
14.3344606518894));
#269430=CARTESIAN_POINT('Ctrl Pts',(-0.70353762133428,1.38730889011528,
14.334698926757));
#269431=CARTESIAN_POINT('Ctrl Pts',(-0.709207460892252,1.38441843927126,
14.335157271851));
#269432=CARTESIAN_POINT('Ctrl Pts',(-0.711933047831652,1.38301878997667,
14.3353774245943));
#269433=CARTESIAN_POINT('Ctrl Pts',(-0.718480108061998,1.37963224638834,
14.3359058540576));
#269434=CARTESIAN_POINT('Ctrl Pts',(-0.722297528208144,1.37763750053657,
14.3362136437028));
#269435=CARTESIAN_POINT('Ctrl Pts',(-0.736257871888219,1.37026871559943,
14.337338228532));
#269436=CARTESIAN_POINT('Ctrl Pts',(-0.746349844426033,1.36479813053238,
14.3381492425614));
#269437=CARTESIAN_POINT('Ctrl Pts',(-0.851897287926064,1.3060627679079,
14.3466206333362));
#269438=CARTESIAN_POINT('Ctrl Pts',(-0.941561329325435,1.24297994671131,
14.353738743941));
#269439=CARTESIAN_POINT('Ctrl Pts',(-1.10359824444006,1.10130144245127,
14.3679136434628));
#269440=CARTESIAN_POINT('Ctrl Pts',(-1.17597910480945,1.02365144088429,
14.3749353706486));
#269441=CARTESIAN_POINT('Ctrl Pts',(-1.2482033916897,0.928308826371025,
14.3832834447503));
#269442=CARTESIAN_POINT('Ctrl Pts',(-1.25635317904375,0.91724895881205,
14.3842476420301));
#269443=CARTESIAN_POINT('Ctrl Pts',(-1.26847768455944,0.900330328751975,
14.3857171296547));
#269444=CARTESIAN_POINT('Ctrl Pts',(-1.27256081592829,0.894549777188648,
14.3862182546709));
#269445=CARTESIAN_POINT('Ctrl Pts',(-1.27988490520559,0.884029325193976,
14.3871286875832));
#269446=CARTESIAN_POINT('Ctrl Pts',(-1.28313935497527,0.879298932372164,
14.387537473274));
#269447=CARTESIAN_POINT('Ctrl Pts',(-1.29007807956924,0.869092834607,14.3884182765239));
#269448=CARTESIAN_POINT('Ctrl Pts',(-1.29375383228069,0.863611501503633,
14.3888906048745));
#269449=CARTESIAN_POINT('Ctrl Pts',(-1.30356805931941,0.848773113891189,
14.3901674117379));
#269450=CARTESIAN_POINT('Ctrl Pts',(-1.30964051764068,0.839373091380753,
14.3909743276963));
#269451=CARTESIAN_POINT('Ctrl Pts',(-1.33861049025997,0.793448502152106,
14.394908063641));
#269452=CARTESIAN_POINT('Ctrl Pts',(-1.36008223339606,0.756051728565129,
14.3980862297483));
#269453=CARTESIAN_POINT('Ctrl Pts',(-1.44996338279417,0.583258649341762,
14.4126746345461));
#269454=CARTESIAN_POINT('Ctrl Pts',(-1.49988575723115,0.439220128545266,
14.424682208944));
#269455=CARTESIAN_POINT('Ctrl Pts',(-1.53422623095591,0.258418640860106,
14.4386285103538));
#269456=CARTESIAN_POINT('Ctrl Pts',(-1.53927720453619,0.226398758163,14.4410526389676));
#269457=CARTESIAN_POINT('Ctrl Pts',(-1.54415888398919,0.187611940616024,
14.4439166738966));
#269458=CARTESIAN_POINT('Ctrl Pts',(-1.5449505865198,0.180976763181725,
14.4444040725565));
#269459=CARTESIAN_POINT('Ctrl Pts',(-1.54611830821319,0.170623529340433,
14.4451604114354));
#269460=CARTESIAN_POINT('Ctrl Pts',(-1.54652371647945,0.166908977954843,
14.4454309351536));
#269461=CARTESIAN_POINT('Ctrl Pts',(-1.54725405719984,0.159986034503915,
14.4459335170802));
#269462=CARTESIAN_POINT('Ctrl Pts',(-1.54758239499378,0.156778122789219,
14.4461657545738));
#269463=CARTESIAN_POINT('Ctrl Pts',(-1.54831055686672,0.149438611141913,
14.4466956465444));
#269464=CARTESIAN_POINT('Ctrl Pts',(-1.5487038209897,0.145306417391493,
14.4469929316527));
#269465=CARTESIAN_POINT('Ctrl Pts',(-1.54969098754791,0.134474286099981,
14.4477696084757));
#269466=CARTESIAN_POINT('Ctrl Pts',(-1.55025799118575,0.127771888903843,
14.4482475478732));
#269467=CARTESIAN_POINT('Ctrl Pts',(-1.55390021025738,0.0811172353033317,
14.4515574724266));
#269468=CARTESIAN_POINT('Ctrl Pts',(-1.55547444188554,0.0410586581403037,
14.4543130783304));
#269469=CARTESIAN_POINT('Ctrl Pts',(-1.55558242940234,-0.130350922880776,
14.4659067034203));
#269470=CARTESIAN_POINT('Ctrl Pts',(-1.53903344529269,-0.261167877420479,
14.4743024819735));
#269471=CARTESIAN_POINT('Ctrl Pts',(-1.50026039181661,-0.411549096672414,
14.4847494019014));
#269472=CARTESIAN_POINT('Ctrl Pts',(-1.49374598462802,-0.434599529382573,
14.4863721093593));
#269473=CARTESIAN_POINT('Ctrl Pts',(-1.48505329777108,-0.462848124196335,
14.4883928726107));
#269474=CARTESIAN_POINT('Ctrl Pts',(-1.48337541042363,-0.468197686673823,
14.4887769860116));
#269475=CARTESIAN_POINT('Ctrl Pts',(-1.48031806823913,-0.477763905217369,
14.4894665281685));
#269476=CARTESIAN_POINT('Ctrl Pts',(-1.47894941925461,-0.481983969584611,
14.4897716462491));
#269477=CARTESIAN_POINT('Ctrl Pts',(-1.46989365726946,-0.509504556147677,
14.4917676833024));
#269478=CARTESIAN_POINT('Ctrl Pts',(-1.46167459625255,-0.532625117546181,
14.4934739866947));
#269479=CARTESIAN_POINT('Ctrl Pts',(-1.44962939782763,-0.564127083508641,
14.4958443460546));
#269480=CARTESIAN_POINT('Ctrl Pts',(-1.44627024113819,-0.572684154233286,
14.4964929005276));
#269481=CARTESIAN_POINT('Ctrl Pts',(-1.44078469007477,-0.586301843356348,
14.4975327403878));
#269482=CARTESIAN_POINT('Ctrl Pts',(-1.43870697567624,-0.591381950529767,
14.4979223867085));
#269483=CARTESIAN_POINT('Ctrl Pts',(-1.43437281002033,-0.601821155173974,
14.4987267096439));
#269484=CARTESIAN_POINT('Ctrl Pts',(-1.432113110824,-0.607178801556033,
14.4991414908342));
#269485=CARTESIAN_POINT('Ctrl Pts',(-1.42678831983815,-0.619608545011971,
14.5001084770268));
#269486=CARTESIAN_POINT('Ctrl Pts',(-1.42370061995286,-0.626670726508734,
14.5006614428106));
#269487=CARTESIAN_POINT('Ctrl Pts',(-1.4136344050101,-0.649235746098329,
14.5024399033955));
#269488=CARTESIAN_POINT('Ctrl Pts',(-1.40645438714995,-0.664646747761118,
14.5036722448325));
#269489=CARTESIAN_POINT('Ctrl Pts',(-1.36840372830881,-0.742939016893913,
14.5100267867545));
#269490=CARTESIAN_POINT('Ctrl Pts',(-1.33356790150155,-0.803791727598661,
14.5152850630738));
#269491=CARTESIAN_POINT('Ctrl Pts',(-1.23851960288269,-0.946544050852793,
14.5284073457598));
#269492=CARTESIAN_POINT('Ctrl Pts',(-1.17415745957458,-1.0252947383269,
14.536361339362));
#269493=CARTESIAN_POINT('Ctrl Pts',(-1.09485814420198,-1.10498233822317,
14.544962019682));
#269494=CARTESIAN_POINT('Ctrl Pts',(-1.08704672058147,-1.11266785748559,
14.5457976340851));
#269495=CARTESIAN_POINT('Ctrl Pts',(-1.05433096190226,-1.14418289378781,
14.5492476559074));
#269496=CARTESIAN_POINT('Ctrl Pts',(-1.02871693580132,-1.1672661190051,
14.5518315425071));
#269497=CARTESIAN_POINT('Ctrl Pts',(-0.997427498539236,-1.1936331729162,
14.5548324502846));
#269498=CARTESIAN_POINT('Ctrl Pts',(-0.992474468967387,-1.19775464875928,
14.5553030330538));
#269499=CARTESIAN_POINT('Ctrl Pts',(-0.984354670153629,-1.20442627908317,
14.5560670665393));
#269500=CARTESIAN_POINT('Ctrl Pts',(-0.981203326836895,-1.20699495062057,
14.5563617904985));
#269501=CARTESIAN_POINT('Ctrl Pts',(-0.975539574888806,-1.21157465453732,
14.5568882099897));
#269502=CARTESIAN_POINT('Ctrl Pts',(-0.973030974179026,-1.21359026431431,
14.5571202282162));
#269503=CARTESIAN_POINT('Ctrl Pts',(-0.967547555823956,-1.21796814661827,
14.5576248908952));
#269504=CARTESIAN_POINT('Ctrl Pts',(-0.96457033851482,-1.22032730931075,
14.5578973147137));
#269505=CARTESIAN_POINT('Ctrl Pts',(-0.956106922599905,-1.22698344069285,
14.558667366611));
#269506=CARTESIAN_POINT('Ctrl Pts',(-0.9506003554593,-1.23125455541696,
14.5591632079469));
#269507=CARTESIAN_POINT('Ctrl Pts',(-0.915002416928547,-1.2584845677591,
14.5623368753823));
#269508=CARTESIAN_POINT('Ctrl Pts',(-0.884107216886533,-1.2803780111328,
14.5649464116578));
#269509=CARTESIAN_POINT('Ctrl Pts',(-0.7618847624684,-1.36045291495877,
14.5748557419773));
#269510=CARTESIAN_POINT('Ctrl Pts',(-0.665376606737659,-1.41016953035004,
14.5818423690219));
#269511=CARTESIAN_POINT('Ctrl Pts',(-0.492474356317959,-1.4775048468549,
14.5941585880479));
#269512=CARTESIAN_POINT('Ctrl Pts',(-0.41848837780569,-1.50013880604874,
14.5993683872779));
#269513=CARTESIAN_POINT('Ctrl Pts',(-0.33162037720998,-1.51978535423363,
14.6055897154412));
#269514=CARTESIAN_POINT('Ctrl Pts',(-0.320077636616072,-1.52225815504397,
14.6064182853689));
#269515=CARTESIAN_POINT('Ctrl Pts',(-0.301278406107025,-1.5260622468872,
14.607771375509));
#269516=CARTESIAN_POINT('Ctrl Pts',(-0.294038468768413,-1.52747374277408,
14.6082933450789));
#269517=CARTESIAN_POINT('Ctrl Pts',(-0.281118076337098,-1.52989743667297,
14.609226526818));
#269518=CARTESIAN_POINT('Ctrl Pts',(-0.275441471715819,-1.53092963051871,
14.6096370964701));
#269519=CARTESIAN_POINT('Ctrl Pts',(-0.263449222806274,-1.53304135921232,
14.6105057308185));
#269520=CARTESIAN_POINT('Ctrl Pts',(-0.257132403957094,-1.53411349861104,
14.6109640214866));
#269521=CARTESIAN_POINT('Ctrl Pts',(-0.24033961603682,-1.53685707128588,
14.6121844284579));
#269522=CARTESIAN_POINT('Ctrl Pts',(-0.229853027484549,-1.53846038752966,
14.6129486782045));
#269523=CARTESIAN_POINT('Ctrl Pts',(-0.1795144870316,-1.54563060021993,
14.6166282252176));
#269524=CARTESIAN_POINT('Ctrl Pts',(-0.139476420704787,-1.54975649087051,
14.6195882101971));
#269525=CARTESIAN_POINT('Ctrl Pts',(0.049628203695662,-1.56185648608417,
14.6337392620499));
#269526=CARTESIAN_POINT('Ctrl Pts',(0.199172829396593,-1.54989517817302,
14.6455283080303));
#269527=CARTESIAN_POINT('Ctrl Pts',(0.381606903810736,-1.50843981305747,
14.6597751057999));
#269528=CARTESIAN_POINT('Ctrl Pts',(0.418222052045253,-1.49870123723444,
14.6626209922974));
#269529=CARTESIAN_POINT('Ctrl Pts',(0.460775739576232,-1.48570176561497,
14.665885632442));
#269530=CARTESIAN_POINT('Ctrl Pts',(0.46709063242107,-1.48372853439972,
14.6663689680884));
#269531=CARTESIAN_POINT('Ctrl Pts',(0.477315224547363,-1.48046188113127,
14.6671494978251));
#269532=CARTESIAN_POINT('Ctrl Pts',(0.481232627321724,-1.47919314645751,
14.6674480558005));
#269533=CARTESIAN_POINT('Ctrl Pts',(0.488206099426863,-1.47690400314015,
14.6679785945315));
#269534=CARTESIAN_POINT('Ctrl Pts',(0.491264073349703,-1.47588964389191,
14.6682109200075));
#269535=CARTESIAN_POINT('Ctrl Pts',(0.49788370355583,-1.47367099535311,
14.668713127481));
#269536=CARTESIAN_POINT('Ctrl Pts',(0.501444148246857,-1.47246329387548,
14.6689828061441));
#269537=CARTESIAN_POINT('Ctrl Pts',(0.511420793187353,-1.46903883639715,
14.6697373262768));
#269538=CARTESIAN_POINT('Ctrl Pts',(0.517827017720188,-1.46679293520486,
14.6702204933922));
#269539=CARTESIAN_POINT('Ctrl Pts',(0.556505600512279,-1.45294796594852,
14.6731308331912));
#269540=CARTESIAN_POINT('Ctrl Pts',(0.588404848215433,-1.4403251237996,
14.6755021300159));
#269541=CARTESIAN_POINT('Ctrl Pts',(0.695198042385484,-1.3939248848908,
14.6834267708379));
#269542=CARTESIAN_POINT('Ctrl Pts',(0.767827976580619,-1.35527465416929,
14.6887973520171));
#269543=CARTESIAN_POINT('Ctrl Pts',(0.927342274078477,-1.25343026065,14.7012603782791));
#269544=CARTESIAN_POINT('Ctrl Pts',(1.01140602005964,-1.18663557705038,
14.7083614280825));
#269545=CARTESIAN_POINT('Ctrl Pts',(1.09644066819439,-1.10342179916349,
14.7166712186744));
#269546=CARTESIAN_POINT('Ctrl Pts',(1.10484821117991,-1.09500329780913,
14.7175062382373));
#269547=CARTESIAN_POINT('Ctrl Pts',(1.1183298878144,-1.08119070234061,14.7188677815361));
#269548=CARTESIAN_POINT('Ctrl Pts',(1.12346363989359,-1.07585525012657,
14.719391701076));
#269549=CARTESIAN_POINT('Ctrl Pts',(1.13253197711948,-1.06629493978487,
14.7203270621179));
#269550=CARTESIAN_POINT('Ctrl Pts',(1.13648153107041,-1.0620844155251,14.7207378498221));
#269551=CARTESIAN_POINT('Ctrl Pts',(1.14475445392842,-1.05316586846507,
14.7216055933696));
#269552=CARTESIAN_POINT('Ctrl Pts',(1.14907241419645,-1.04845299893241,
14.7220627681592));
#269553=CARTESIAN_POINT('Ctrl Pts',(1.16043265078725,-1.03589931173692,
14.7232770350641));
#269554=CARTESIAN_POINT('Ctrl Pts',(1.16742438936073,-1.02801342697538,
14.7240362226237));
#269555=CARTESIAN_POINT('Ctrl Pts',(1.20019323418368,-0.990288475774633,
14.7276519056707));
#269556=CARTESIAN_POINT('Ctrl Pts',(1.22490753008888,-0.959549940723327,
14.73055122582));
#269557=CARTESIAN_POINT('Ctrl Pts',(1.3377594085566,-0.807716854184142,
14.7446695056808));
#269558=CARTESIAN_POINT('Ctrl Pts',(1.40926154753768,-0.675258831606486,
14.7564961230062));
#269559=CARTESIAN_POINT('Ctrl Pts',(1.47387977250682,-0.49872264221895,
14.7708163227759));
#269560=CARTESIAN_POINT('Ctrl Pts',(1.48570861944867,-0.462294665066724,
14.7736939763001));
#269561=CARTESIAN_POINT('Ctrl Pts',(1.49799705850008,-0.41908124900415,
14.7769904466823));
#269562=CARTESIAN_POINT('Ctrl Pts',(1.49977121346047,-0.41268703881596,
14.7774752447048));
#269563=CARTESIAN_POINT('Ctrl Pts',(1.50258148288639,-0.402301058156212,
14.7782576638021));
#269564=CARTESIAN_POINT('Ctrl Pts',(1.50364271259795,-0.398316266326904,
14.7785566593244));
#269565=CARTESIAN_POINT('Ctrl Pts',(1.50550496739803,-0.391210207308202,
14.7790876722839));
#269566=CARTESIAN_POINT('Ctrl Pts',(1.50631215039805,-0.388090633013378,
14.7793200369489));
#269567=CARTESIAN_POINT('Ctrl Pts',(1.50803907472301,-0.381329912391649,
14.7798219829311));
#269568=CARTESIAN_POINT('Ctrl Pts',(1.50895532511103,-0.3776879407694,14.7800913628154));
#269569=CARTESIAN_POINT('Ctrl Pts',(1.51148602956775,-0.367472513426196,
14.780844198789));
#269570=CARTESIAN_POINT('Ctrl Pts',(1.51307080689287,-0.360891678338084,
14.7813259925093));
#269571=CARTESIAN_POINT('Ctrl Pts',(1.52234218360128,-0.321257124619396,
14.7842097390996));
#269572=CARTESIAN_POINT('Ctrl Pts',(1.52898909699851,-0.287966395677746,
14.7865569967321));
#269573=CARTESIAN_POINT('Ctrl Pts',(1.56425065248389,-0.0753368845034653,
14.8012314348214));
#269574=CARTESIAN_POINT('Ctrl Pts',(1.56236500970744,0.107627522009729,
14.8126094172263));
#269575=CARTESIAN_POINT('Ctrl Pts',(1.52558848064339,0.30412905366778,14.8264773773804));
#269576=CARTESIAN_POINT('Ctrl Pts',(1.52190760050675,0.32204332017638,14.8277552236677));
#269577=CARTESIAN_POINT('Ctrl Pts',(1.51631020672089,0.347040828788507,
14.8295592702533));
#269578=CARTESIAN_POINT('Ctrl Pts',(1.51465801938965,0.354182242426665,
14.8300770675531));
#269579=CARTESIAN_POINT('Ctrl Pts',(1.5117004432393,0.366566790541964,14.8309793413134));
#269580=CARTESIAN_POINT('Ctrl Pts',(1.5104180852256,0.371815341937226,14.8313630756621));
#269581=CARTESIAN_POINT('Ctrl Pts',(1.50768574108579,0.382751097149428,
14.8321654947747));
#269582=CARTESIAN_POINT('Ctrl Pts',(1.50623086172509,0.388436977761936,
14.8325843313073));
#269583=CARTESIAN_POINT('Ctrl Pts',(1.50270745449472,0.401889480763949,
14.8335792191401));
#269584=CARTESIAN_POINT('Ctrl Pts',(1.50061085754058,0.409648505770617,
14.8341561676337));
#269585=CARTESIAN_POINT('Ctrl Pts',(1.49338844329536,0.43557734120893,14.8360949095229));
#269586=CARTESIAN_POINT('Ctrl Pts',(1.48799217319954,0.45366936966431,14.8374653984487));
#269587=CARTESIAN_POINT('Ctrl Pts',(1.47434382819559,0.49656169427142,14.8407584907405));
#269588=CARTESIAN_POINT('Ctrl Pts',(1.46579357257349,0.521260293856361,
14.8426903343373));
#269589=CARTESIAN_POINT('Ctrl Pts',(1.44962853802406,0.564406873256468,
14.8461292864136));
#269590=CARTESIAN_POINT('Ctrl Pts',(1.44227704762217,0.58293565034592,14.8476274724982));
#269591=CARTESIAN_POINT('Ctrl Pts',(1.43457662445954,0.601307041829941,
14.8491341039362));
#269592=CARTESIAN_POINT('Origin',(0.,0.,-1.29405622560371));
#269593=CARTESIAN_POINT('',(1.4345766974292,0.601306867741532,15.6881535475172));
#269594=CARTESIAN_POINT('',(1.43457668274383,0.601306902777371,15.5515012983457));
#269595=CARTESIAN_POINT('',(1.43457668357355,0.601306900797845,-1.29405622560371));
#269596=CARTESIAN_POINT('Ctrl Pts',(1.43457669742932,0.601306867741247,
15.6881535475172));
#269597=CARTESIAN_POINT('Ctrl Pts',(1.45874319013863,0.543651302572655,
15.6833052102356));
#269598=CARTESIAN_POINT('Ctrl Pts',(1.47944557503403,0.484511145403499,
15.6784494417411));
#269599=CARTESIAN_POINT('Ctrl Pts',(1.50559969200234,0.392241097227874,
15.6711766387542));
#269600=CARTESIAN_POINT('Ctrl Pts',(1.51363277875958,0.359999636504437,
15.6686905268506));
#269601=CARTESIAN_POINT('Ctrl Pts',(1.52203249339847,0.321001310937034,
15.6657678630902));
#269602=CARTESIAN_POINT('Ctrl Pts',(1.52339519752378,0.314470712569572,
15.6652812596447));
#269603=CARTESIAN_POINT('Ctrl Pts',(1.52544945226465,0.304299112998734,
15.664527951634));
#269604=CARTESIAN_POINT('Ctrl Pts',(1.52617005541673,0.300664171984863,
15.6642596576344));
#269605=CARTESIAN_POINT('Ctrl Pts',(1.52748518643701,0.293903686810627,
15.6637624004689));
#269606=CARTESIAN_POINT('Ctrl Pts',(1.52808311002675,0.290778921319678,
15.6635332547922));
#269607=CARTESIAN_POINT('Ctrl Pts',(1.52942423314351,0.28365178556088,15.6630121620093));
#269608=CARTESIAN_POINT('Ctrl Pts',(1.53016131116095,0.279648320617172,
15.6627205641679));
#269609=CARTESIAN_POINT('Ctrl Pts',(1.53204293262263,0.269198018218926,
15.6619621877474));
#269610=CARTESIAN_POINT('Ctrl Pts',(1.53316251837995,0.262746677708289,
15.6614967759841));
#269611=CARTESIAN_POINT('Ctrl Pts',(1.5403882809248,0.219490456809539,15.6583934791403));
#269612=CARTESIAN_POINT('Ctrl Pts',(1.54520998398117,0.182479554578232,
15.6558218672983));
#269613=CARTESIAN_POINT('Ctrl Pts',(1.55007179064466,0.13066923654386,15.6522928750845));
#269614=CARTESIAN_POINT('Ctrl Pts',(1.55123915758606,0.115991829365177,
15.6513010396435));
#269615=CARTESIAN_POINT('Ctrl Pts',(1.55446740582268,0.066525925349292,
15.6479784306287));
#269616=CARTESIAN_POINT('Ctrl Pts',(1.55556770599653,0.0316844245101462,
15.6456713653327));
#269617=CARTESIAN_POINT('Ctrl Pts',(1.55533385693495,-0.0832171977139087,
15.6380928381742));
#269618=CARTESIAN_POINT('Ctrl Pts',(1.54899173983458,-0.163133326739185,
15.6328632538657));
#269619=CARTESIAN_POINT('Ctrl Pts',(1.52743741979106,-0.299872221051706,
15.6235783621063));
#269620=CARTESIAN_POINT('Ctrl Pts',(1.51510906566858,-0.35697567083628,
15.6195976743679));
#269621=CARTESIAN_POINT('Ctrl Pts',(1.49648750822896,-0.424550190407996,
15.6146917783434));
#269622=CARTESIAN_POINT('Ctrl Pts',(1.49324491219919,-0.435818018605811,
15.6138671772992));
#269623=CARTESIAN_POINT('Ctrl Pts',(1.48797841216963,-0.453369671088375,
15.6125719290709));
#269624=CARTESIAN_POINT('Ctrl Pts',(1.48604131186894,-0.45967926941373,
15.6121041103411));
#269625=CARTESIAN_POINT('Ctrl Pts',(1.48253773367707,-0.470837637753408,
15.6112728021752));
#269626=CARTESIAN_POINT('Ctrl Pts',(1.48098746588687,-0.475691431133484,
15.6109098483265));
#269627=CARTESIAN_POINT('Ctrl Pts',(1.47736169311522,-0.486853967185574,
15.6100719995129));
#269628=CARTESIAN_POINT('Ctrl Pts',(1.47526958917049,-0.49315717006524,
15.6095965646843));
#269629=CARTESIAN_POINT('Ctrl Pts',(1.46941443471303,-0.510427173155055,
15.6082874275026));
#269630=CARTESIAN_POINT('Ctrl Pts',(1.4655690989699,-0.521365402229734,
15.6074510265751));
#269631=CARTESIAN_POINT('Ctrl Pts',(1.4445469761717,-0.579092852828204,
15.6029973999521));
#269632=CARTESIAN_POINT('Ctrl Pts',(1.4252528747187,-0.625074166119957,
15.5993104422468));
#269633=CARTESIAN_POINT('Ctrl Pts',(1.34071975863937,-0.802176257105888,
15.5845370711677));
#269634=CARTESIAN_POINT('Ctrl Pts',(1.25932694589711,-0.924717371307711,
15.5729452342796));
#269635=CARTESIAN_POINT('Ctrl Pts',(1.14170867403552,-1.05688925041815,
15.5595596940166));
#269636=CARTESIAN_POINT('Ctrl Pts',(1.12072945446215,-1.07911046959223,
15.5572775288031));
#269637=CARTESIAN_POINT('Ctrl Pts',(1.09449795302527,-1.10530399214629,
15.5545626498978));
#269638=CARTESIAN_POINT('Ctrl Pts',(1.08985943469471,-1.10987796665545,
15.5540876214665));
#269639=CARTESIAN_POINT('Ctrl Pts',(1.08256184439132,-1.11698414604593,
15.5533483121491));
#269640=CARTESIAN_POINT('Ctrl Pts',(1.0799223819164,-1.11953623400272,15.5530825335575));
#269641=CARTESIAN_POINT('Ctrl Pts',(1.07497553912838,-1.12428554713978,
15.5525874764719));
#269642=CARTESIAN_POINT('Ctrl Pts',(1.07267046762741,-1.12648500629478,
15.5523580308282));
#269643=CARTESIAN_POINT('Ctrl Pts',(1.06736838415157,-1.13151313072728,
15.5518330648835));
#269644=CARTESIAN_POINT('Ctrl Pts',(1.06436687829317,-1.13433697900724,
15.5515379143555));
#269645=CARTESIAN_POINT('Ctrl Pts',(1.05644484613809,-1.14173098127667,
15.5507641165993));
#269646=CARTESIAN_POINT('Ctrl Pts',(1.05150581517116,-1.14628132301999,
15.5502869285026));
#269647=CARTESIAN_POINT('Ctrl Pts',(1.01612399830472,-1.17845755209012,
15.5469042260504));
#269648=CARTESIAN_POINT('Ctrl Pts',(0.984622792796408,-1.20490201808363,
15.5440793453098));
#269649=CARTESIAN_POINT('Ctrl Pts',(0.937125174460898,-1.24166646384064,
15.5400205568663));
#269650=CARTESIAN_POINT('Ctrl Pts',(0.921931851616002,-1.25298878865298,
15.5387505126898));
#269651=CARTESIAN_POINT('Ctrl Pts',(0.84913468415556,-1.30519730260713,
15.5327778772585));
#269652=CARTESIAN_POINT('Ctrl Pts',(0.788995506759633,-1.34240693759025,
15.5281670272871));
#269653=CARTESIAN_POINT('Ctrl Pts',(0.644868598726049,-1.41853971744403,
15.5174026723607));
#269654=CARTESIAN_POINT('Ctrl Pts',(0.559536182516225,-1.45431283344704,
15.5112248625628));
#269655=CARTESIAN_POINT('Ctrl Pts',(0.459277692117528,-1.48620655328027,
15.5038732748825));
#269656=CARTESIAN_POINT('Ctrl Pts',(0.446964546459356,-1.48995590343311,
15.502969153361));
#269657=CARTESIAN_POINT('Ctrl Pts',(0.428034545496895,-1.49546431824363,
15.5015766122785));
#269658=CARTESIAN_POINT('Ctrl Pts',(0.421450027597146,-1.49733328648135,
15.5010917677439));
#269659=CARTESIAN_POINT('Ctrl Pts',(0.409448089354381,-1.5006545131494,
15.5002070608285));
#269660=CARTESIAN_POINT('Ctrl Pts',(0.404034710841987,-1.50212105259046,
15.4998076687979));
#269661=CARTESIAN_POINT('Ctrl Pts',(0.392223973644245,-1.50525223838375,
15.4989354612995));
#269662=CARTESIAN_POINT('Ctrl Pts',(0.385823722875915,-1.50690543798597,
15.4984622846564));
#269663=CARTESIAN_POINT('Ctrl Pts',(0.368300978655044,-1.51131265209707,
15.4971652633676));
#269664=CARTESIAN_POINT('Ctrl Pts',(0.357158480000599,-1.51398459383233,
15.4963388015963));
#269665=CARTESIAN_POINT('Ctrl Pts',(0.299308195396958,-1.52718278220831,
15.4920382400436));
#269666=CARTESIAN_POINT('Ctrl Pts',(0.25216701831684,-1.53567038326185,
15.4885000213669));
#269667=CARTESIAN_POINT('Ctrl Pts',(0.0589964587991515,-1.5613159558735,
15.4738516603627));
#269668=CARTESIAN_POINT('Ctrl Pts',(-0.0886988826687305,-1.55990710361526,
15.4622176580609));
#269669=CARTESIAN_POINT('Ctrl Pts',(-0.265642821647463,-1.53298382783339,
15.4486590115296));
#269670=CARTESIAN_POINT('Ctrl Pts',(-0.297145130524926,-1.52719045093759,
15.4462644710532));
#269671=CARTESIAN_POINT('Ctrl Pts',(-0.334902683999179,-1.51903391601913,
15.4434348722881));
#269672=CARTESIAN_POINT('Ctrl Pts',(-0.341347735255132,-1.51759862071411,
15.4429533101879));
#269673=CARTESIAN_POINT('Ctrl Pts',(-0.351380932425219,-1.51529710355211,
15.4422060965731));
#269674=CARTESIAN_POINT('Ctrl Pts',(-0.354975362517023,-1.51445909963988,
15.4419388958567));
#269675=CARTESIAN_POINT('Ctrl Pts',(-0.361664450821116,-1.51287448546476,
15.4414426048312));
#269676=CARTESIAN_POINT('Ctrl Pts',(-0.364759770699785,-1.5121311761055,
15.4412133386642));
#269677=CARTESIAN_POINT('Ctrl Pts',(-0.37182885646169,-1.51041063832276,
15.4406906072505));
#269678=CARTESIAN_POINT('Ctrl Pts',(-0.375801061018894,-1.50942722859638,
15.4403974999877));
#269679=CARTESIAN_POINT('Ctrl Pts',(-0.386187800823735,-1.50681221112393,
15.4396325832598));
#269680=CARTESIAN_POINT('Ctrl Pts',(-0.392595973949335,-1.5051552951318,
15.4391621794159));
#269681=CARTESIAN_POINT('Ctrl Pts',(-0.436585958248702,-1.49348105818434,
15.4359422059889));
#269682=CARTESIAN_POINT('Ctrl Pts',(-0.473795007339837,-1.4820971271957,
15.4332647348821));
#269683=CARTESIAN_POINT('Ctrl Pts',(-0.651630998362606,-1.42030517264415,
15.4205167036886));
#269684=CARTESIAN_POINT('Ctrl Pts',(-0.784926791220451,-1.35121643419585,
15.4110354358585));
#269685=CARTESIAN_POINT('Ctrl Pts',(-0.938398929554399,-1.24118668534751,
15.3981945814172));
#269686=CARTESIAN_POINT('Ctrl Pts',(-0.969575602328509,-1.21698793761691,
15.3954750300494));
#269687=CARTESIAN_POINT('Ctrl Pts',(-1.00780723286618,-1.18491103934747,
15.3919752602722));
#269688=CARTESIAN_POINT('Ctrl Pts',(-1.01574960983595,-1.17810963429126,
15.3912387983172));
#269689=CARTESIAN_POINT('Ctrl Pts',(-1.02838324571956,-1.16706817461973,
15.3900517563115));
#269690=CARTESIAN_POINT('Ctrl Pts',(-1.03311837379139,-1.16287860410109,
15.3896032684935));
#269691=CARTESIAN_POINT('Ctrl Pts',(-1.04207156308504,-1.15485911112617,
15.3887483413132));
#269692=CARTESIAN_POINT('Ctrl Pts',(-1.04629439177707,-1.15103464469578,
15.3883421352048));
#269693=CARTESIAN_POINT('Ctrl Pts',(-1.05587111589086,-1.14226509796828,
15.3874140450346));
#269694=CARTESIAN_POINT('Ctrl Pts',(-1.06121142277729,-1.13730544719794,
15.3868915473111));
#269695=CARTESIAN_POINT('Ctrl Pts',(-1.07501193334228,-1.12430680488447,
15.3855281694956));
#269696=CARTESIAN_POINT('Ctrl Pts',(-1.08341672904834,-1.11620993802489,
15.3846848125416));
#269697=CARTESIAN_POINT('Ctrl Pts',(-1.14571810467919,-1.05482451451753,
15.3783333393166));
#269698=CARTESIAN_POINT('Ctrl Pts',(-1.19573762981428,-0.99776391126455,
15.3726572283521));
#269699=CARTESIAN_POINT('Ctrl Pts',(-1.30770259268482,-0.84947259958713,
15.3584431895774));
#269700=CARTESIAN_POINT('Ctrl Pts',(-1.36450092300531,-0.754867889450489,
15.3497967750708));
#269701=CARTESIAN_POINT('Ctrl Pts',(-1.42685128866542,-0.620581257784346,
15.3385258350334));
#269702=CARTESIAN_POINT('Ctrl Pts',(-1.44159425794493,-0.585518821829499,
15.3356704585475));
#269703=CARTESIAN_POINT('Ctrl Pts',(-1.45748376826084,-0.543478742268391,
15.3323759735027));
#269704=CARTESIAN_POINT('Ctrl Pts',(-1.45988573846608,-0.536993215470201,
15.3318713032008));
#269705=CARTESIAN_POINT('Ctrl Pts',(-1.46352622396099,-0.526958601521506,
15.3310961887023));
#269706=CARTESIAN_POINT('Ctrl Pts',(-1.4647952240991,-0.523420794588629,
15.3308240073131));
#269707=CARTESIAN_POINT('Ctrl Pts',(-1.4671130372656,-0.516884586438547,
15.3303232031027));
#269708=CARTESIAN_POINT('Ctrl Pts',(-1.46816548251521,-0.513887590961846,
15.3300943743779));
#269709=CARTESIAN_POINT('Ctrl Pts',(-1.47052259306265,-0.50710901673015,
15.3295786041296));
#269710=CARTESIAN_POINT('Ctrl Pts',(-1.47182185447659,-0.503325621452828,
15.3292919830291));
#269711=CARTESIAN_POINT('Ctrl Pts',(-1.47561844614545,-0.492129690548404,
15.3284473791682));
#269712=CARTESIAN_POINT('Ctrl Pts',(-1.47807452733873,-0.484703135271742,
15.3278917479743));
#269713=CARTESIAN_POINT('Ctrl Pts',(-1.49720752986677,-0.425351770622989,
15.3234855812468));
#269714=CARTESIAN_POINT('Ctrl Pts',(-1.51120137157454,-0.372594262487917,
15.3197771830265));
#269715=CARTESIAN_POINT('Ctrl Pts',(-1.54432950799412,-0.214594635733381,
15.3089825340143));
#269716=CARTESIAN_POINT('Ctrl Pts',(-1.55542317921802,-0.108002426917552,
15.3020810023186));
#269717=CARTESIAN_POINT('Ctrl Pts',(-1.55554364612096,0.0604900793579502,
15.2908079468492));
#269718=CARTESIAN_POINT('Ctrl Pts',(-1.55192830998767,0.122033232736486,
15.2866182755));
#269719=CARTESIAN_POINT('Ctrl Pts',(-1.54335429864604,0.194328221685656,
15.2815282007728));
#269720=CARTESIAN_POINT('Ctrl Pts',(-1.54191358888956,0.20544688294018,
15.2807407189313));
#269721=CARTESIAN_POINT('Ctrl Pts',(-1.5393575461247,0.223628506224607,
15.2794449065531));
#269722=CARTESIAN_POINT('Ctrl Pts',(-1.53831346354665,0.230701210213163,
15.278938819604));
#269723=CARTESIAN_POINT('Ctrl Pts',(-1.53635209310862,0.243381974614483,
15.2780277165559));
#269724=CARTESIAN_POINT('Ctrl Pts',(-1.53545275543261,0.24899271842983,
15.2776232742252));
#269725=CARTESIAN_POINT('Ctrl Pts',(-1.53347446136182,0.260916351390305,
15.2767609151204));
#269726=CARTESIAN_POINT('Ctrl Pts',(-1.53238722239672,0.267227738903957,
15.2763027429033));
#269727=CARTESIAN_POINT('Ctrl Pts',(-1.52935693959747,0.284191573321525,
15.2750665532301));
#269728=CARTESIAN_POINT('Ctrl Pts',(-1.52734161963906,0.294830569878293,
15.2742862579238));
#269729=CARTESIAN_POINT('Ctrl Pts',(-1.516561721348,0.348658713670287,15.2703121351901));
#269730=CARTESIAN_POINT('Ctrl Pts',(-1.5060764796557,0.391478314807975,
15.2670641173678));
#269731=CARTESIAN_POINT('Ctrl Pts',(-1.46997649866109,0.515790941422989,
15.2573676720175));
#269732=CARTESIAN_POINT('Ctrl Pts',(-1.43945549096516,0.595680884742685,
15.2507820542005));
#269733=CARTESIAN_POINT('Ctrl Pts',(-1.3637243425151,0.75358673667765,15.2372012571951));
#269734=CARTESIAN_POINT('Ctrl Pts',(-1.31797239318387,0.831017008048588,
15.2302280801331));
#269735=CARTESIAN_POINT('Ctrl Pts',(-1.25864283021201,0.914084116088655,
15.2226674671));
#269736=CARTESIAN_POINT('Ctrl Pts',(-1.25137502440972,0.924008722347184,
15.2217629455501));
#269737=CARTESIAN_POINT('Ctrl Pts',(-1.24105881129791,0.937751094122978,
15.220509937278));
#269738=CARTESIAN_POINT('Ctrl Pts',(-1.23810924729513,0.941641960157849,
15.2201551131706));
#269739=CARTESIAN_POINT('Ctrl Pts',(-1.23332798399747,0.947887774778778,
15.2195855181641));
#269740=CARTESIAN_POINT('Ctrl Pts',(-1.2315077772983,0.950251411234026,
15.2193699602193));
#269741=CARTESIAN_POINT('Ctrl Pts',(-1.22766310470639,0.955214324486042,
15.218917373492));
#269742=CARTESIAN_POINT('Ctrl Pts',(-1.22563716274456,0.957812429464149,
15.2186804557609));
#269743=CARTESIAN_POINT('Ctrl Pts',(-1.22064377818878,0.964174251663145,
15.2181003081391));
#269744=CARTESIAN_POINT('Ctrl Pts',(-1.21766713184873,0.967930771519231,
15.2177577244571));
#269745=CARTESIAN_POINT('Ctrl Pts',(-1.20676503242662,0.981559306768895,
15.2165145200226));
#269746=CARTESIAN_POINT('Ctrl Pts',(-1.19873621960749,0.991348586182511,
15.2156209163984));
#269747=CARTESIAN_POINT('Ctrl Pts',(-1.14499794164625,1.05526234211818,
15.209774072517));
#269748=CARTESIAN_POINT('Ctrl Pts',(-1.09574989498326,1.10631541773307,
15.2050416775706));
#269749=CARTESIAN_POINT('Ctrl Pts',(-0.940501273564758,1.24667580500327,
15.1912054139043));
#269750=CARTESIAN_POINT('Ctrl Pts',(-0.825897460497674,1.3253801349975,
15.1822415339958));
#269751=CARTESIAN_POINT('Ctrl Pts',(-0.687346865705255,1.39549957638931,
15.1714467712168));
#269752=CARTESIAN_POINT('Ctrl Pts',(-0.672174104878261,1.40287088337617,
15.1702662195884));
#269753=CARTESIAN_POINT('Ctrl Pts',(-0.650046934092668,1.41317944399814,
15.1685453510928));
#269754=CARTESIAN_POINT('Ctrl Pts',(-0.643185918573314,1.41631529964121,
15.1680118689332));
#269755=CARTESIAN_POINT('Ctrl Pts',(-0.631054302493441,1.42175377466758,
15.1670686258953));
#269756=CARTESIAN_POINT('Ctrl Pts',(-0.6257931901356,1.42407731883909,15.1666595892612));
#269757=CARTESIAN_POINT('Ctrl Pts',(-0.614886628560528,1.4288220380778,
15.165811610362));
#269758=CARTESIAN_POINT('Ctrl Pts',(-0.609239490368795,1.43123905196035,
15.1653725350727));
#269759=CARTESIAN_POINT('Ctrl Pts',(-0.594694651887369,1.43736266409605,
15.1642415257729));
#269760=CARTESIAN_POINT('Ctrl Pts',(-0.585776663793272,1.44102007255408,
15.1635479439251));
#269761=CARTESIAN_POINT('Ctrl Pts',(-0.547976510140223,1.45611364630161,
15.1606071377234));
#269762=CARTESIAN_POINT('Ctrl Pts',(-0.518791056587234,1.46676541729477,
15.1583339879914));
#269763=CARTESIAN_POINT('Ctrl Pts',(-0.440390766161352,1.49274643600657,
15.1522157299155));
#269764=CARTESIAN_POINT('Ctrl Pts',(-0.390703055321786,1.50651454524288,
15.1483248642517));
#269765=CARTESIAN_POINT('Ctrl Pts',(-0.240313958295305,1.54024561565479,
15.1365307090132));
#269766=CARTESIAN_POINT('Ctrl Pts',(-0.138229735688819,1.55273902845089,
15.1284846707027));
#269767=CARTESIAN_POINT('Ctrl Pts',(-0.0175972229059484,1.55550541326658,
15.1192587878866));
#269768=CARTESIAN_POINT('Ctrl Pts',(0.000473968940785682,1.55560489128815,
15.1178847968187));
#269769=CARTESIAN_POINT('Ctrl Pts',(0.0457456455514533,1.55506515963206,
15.1144687695645));
#269770=CARTESIAN_POINT('Ctrl Pts',(0.072936920072047,1.55402727128559,
15.112440578103));
#269771=CARTESIAN_POINT('Ctrl Pts',(0.106591520627368,1.55185725999964,
15.1099702603373));
#269772=CARTESIAN_POINT('Ctrl Pts',(0.113091430064516,1.55139712522477,
15.1094950090082));
#269773=CARTESIAN_POINT('Ctrl Pts',(0.123288201764571,1.55061086000439,
15.1087525654169));
#269774=CARTESIAN_POINT('Ctrl Pts',(0.126987014839802,1.55031232940424,
15.1084838916767));
#269775=CARTESIAN_POINT('Ctrl Pts',(0.133854425822546,1.54973331924651,
15.1079862955285));
#269776=CARTESIAN_POINT('Ctrl Pts',(0.137023204588303,1.5494563594474,15.1077571883069));
#269777=CARTESIAN_POINT('Ctrl Pts',(0.144238087354764,1.54880345283545,
15.107236649318));
#269778=CARTESIAN_POINT('Ctrl Pts',(0.148283579395924,1.54842137109197,
15.1069455638534));
#269779=CARTESIAN_POINT('Ctrl Pts',(0.160686439678187,1.54720091294515,
15.1060554300551));
#269780=CARTESIAN_POINT('Ctrl Pts',(0.169038738122006,1.5463106771559,15.1054591895492));
#269781=CARTESIAN_POINT('Ctrl Pts',(0.188421523624302,1.54408581985507,
15.1040820738031));
#269782=CARTESIAN_POINT('Ctrl Pts',(0.199445880900395,1.54270056960888,
15.1033037498686));
#269783=CARTESIAN_POINT('Ctrl Pts',(0.350170938178949,1.52211863828171,
15.0927184195491));
#269784=CARTESIAN_POINT('Ctrl Pts',(0.486664105689321,1.48412785667841,
15.0837429924393));
#269785=CARTESIAN_POINT('Ctrl Pts',(0.680184039657533,1.4006386337053,15.0697040846656));
#269786=CARTESIAN_POINT('Ctrl Pts',(0.742249293970187,1.36875960454969,
15.0649845273215));
#269787=CARTESIAN_POINT('Ctrl Pts',(0.811814943939734,1.32690201440155,
15.0593106753447));
#269788=CARTESIAN_POINT('Ctrl Pts',(0.821600919005587,1.32086501068108,
15.0585033318073));
#269789=CARTESIAN_POINT('Ctrl Pts',(0.837435001934042,1.31085286410948,
15.057181441124));
#269790=CARTESIAN_POINT('Ctrl Pts',(0.843524006988558,1.30694294452568,
15.0566692947554));
#269791=CARTESIAN_POINT('Ctrl Pts',(0.854352904769364,1.29988220851742,
15.0557515138373));
#269792=CARTESIAN_POINT('Ctrl Pts',(0.859103237023871,1.29674757314841,
15.0553464876042));
#269793=CARTESIAN_POINT('Ctrl Pts',(0.869118521100297,1.29005953042814,
15.0544873522016));
#269794=CARTESIAN_POINT('Ctrl Pts',(0.874379110490841,1.28649981138507,
15.0540330108076));
#269795=CARTESIAN_POINT('Ctrl Pts',(0.888351451172761,1.27691976536659,
15.0528179277687));
#269796=CARTESIAN_POINT('Ctrl Pts',(0.897023639451311,1.27084262123153,
15.052055041082));
#269797=CARTESIAN_POINT('Ctrl Pts',(0.938998517390703,1.24078450014822,
15.0483190196218));
#269798=CARTESIAN_POINT('Ctrl Pts',(0.971402342309505,1.21558269846498,
15.0452992032494));
#269799=CARTESIAN_POINT('Ctrl Pts',(1.11623973692998,1.09344439369855,15.0311419453224));
#269800=CARTESIAN_POINT('Ctrl Pts',(1.21542313736418,0.982010693103723,
15.0194182120874));
#269801=CARTESIAN_POINT('Ctrl Pts',(1.31831441699774,0.826485654502356,
15.0052151198238));
#269802=CARTESIAN_POINT('Ctrl Pts',(1.33816130453385,0.793949845767243,
15.0023521594732));
#269803=CARTESIAN_POINT('Ctrl Pts',(1.36000973884674,0.754981434198667,
14.99907452962));
#269804=CARTESIAN_POINT('Ctrl Pts',(1.36318800909648,0.749227543326059,
14.9985943387916));
#269805=CARTESIAN_POINT('Ctrl Pts',(1.36827904239983,0.739871167942625,
14.9978197955366));
#269806=CARTESIAN_POINT('Ctrl Pts',(1.3702142346257,0.736281084425017,14.9975240894964));
#269807=CARTESIAN_POINT('Ctrl Pts',(1.37363417527809,0.729876378796892,
14.9969992517469));
#269808=CARTESIAN_POINT('Ctrl Pts',(1.37512442547233,0.727064777702217,
14.9967697781553));
#269809=CARTESIAN_POINT('Ctrl Pts',(1.37832891954686,0.720973876865821,
14.9962746643382));
#269810=CARTESIAN_POINT('Ctrl Pts',(1.38004009172385,0.717693031588492,
14.9960092174557));
#269811=CARTESIAN_POINT('Ctrl Pts',(1.38479199670207,0.708502326980686,
14.9952690000166));
#269812=CARTESIAN_POINT('Ctrl Pts',(1.38780663353652,0.70257894475651,14.9947958299672));
#269813=CARTESIAN_POINT('Ctrl Pts',(1.40546111689658,0.667333062475629,
14.9920022760485));
#269814=CARTESIAN_POINT('Ctrl Pts',(1.4192105620845,0.637570504649129,14.9897329765469));
#269815=CARTESIAN_POINT('Ctrl Pts',(1.43287024456846,0.605365972271906,
14.9873482618096));
#269816=CARTESIAN_POINT('Ctrl Pts',(1.43372565284231,0.603337259749617,
14.9871983329348));
#269817=CARTESIAN_POINT('Ctrl Pts',(1.4345766844093,0.601306898803946,14.987048570644));
#269818=CARTESIAN_POINT('',(-1.55549984403819,0.000696560963701701,15.1547003707517));
#269819=CARTESIAN_POINT('Ctrl Pts',(1.43457662445954,0.601307041829938,
14.8491341039362));
#269820=CARTESIAN_POINT('Ctrl Pts',(1.38448969431034,0.720802630912524,
14.8589338957143));
#269821=CARTESIAN_POINT('Ctrl Pts',(1.31964055215274,0.833634866082474,
14.8691504652631));
#269822=CARTESIAN_POINT('Ctrl Pts',(1.21848667811269,0.967641878853461,
14.8819394954867));
#269823=CARTESIAN_POINT('Ctrl Pts',(1.19434505119975,0.997286863375022,
14.8848118360002));
#269824=CARTESIAN_POINT('Ctrl Pts',(1.16475882936822,1.03100005139464,14.8881029831226));
#269825=CARTESIAN_POINT('Ctrl Pts',(1.16035223328545,1.03595701429165,14.8885875360038));
#269826=CARTESIAN_POINT('Ctrl Pts',(1.15315526016599,1.0439493243621,14.8893696384163));
#269827=CARTESIAN_POINT('Ctrl Pts',(1.15038434562817,1.04700196001743,14.8896685606221));
#269828=CARTESIAN_POINT('Ctrl Pts',(1.14542612551546,1.05242083959573,14.8901994940623));
#269829=CARTESIAN_POINT('Ctrl Pts',(1.14324357754077,1.05479133279857,14.8904318521045));
#269830=CARTESIAN_POINT('Ctrl Pts',(1.13850087716068,1.05991042592819,14.8909338416474));
#269831=CARTESIAN_POINT('Ctrl Pts',(1.1359381333817,1.06265653728012,14.8912032713976));
#269832=CARTESIAN_POINT('Ctrl Pts',(1.12872715883814,1.07032757169798,14.891956388374));
#269833=CARTESIAN_POINT('Ctrl Pts',(1.12405660107506,1.07523154338236,14.892438411234));
#269834=CARTESIAN_POINT('Ctrl Pts',(1.0957488184019,1.10456798008782,14.8953265704348));
#269835=CARTESIAN_POINT('Ctrl Pts',(1.07134569053159,1.12825296314354,14.8976778165618));
#269836=CARTESIAN_POINT('Ctrl Pts',(0.927480651971162,1.25900308988499,
14.9109128215768));
#269837=CARTESIAN_POINT('Ctrl Pts',(0.792802869301842,1.34788057355433,
14.9210388921652));
#269838=CARTESIAN_POINT('Ctrl Pts',(0.615733697305195,1.42885514108345,
14.9343289472299));
#269839=CARTESIAN_POINT('Ctrl Pts',(0.584103290076188,1.44207421660871,
14.9366971743447));
#269840=CARTESIAN_POINT('Ctrl Pts',(0.542289363653755,1.45794780756784,
14.93983381778));
#269841=CARTESIAN_POINT('Ctrl Pts',(0.532477746629139,1.46155978440423,
14.9405702227141));
#269842=CARTESIAN_POINT('Ctrl Pts',(0.51662774534732,1.46721390515693,14.9417608231288));
#269843=CARTESIAN_POINT('Ctrl Pts',(0.510611796395492,1.46931836643203,
14.9422129482956));
#269844=CARTESIAN_POINT('Ctrl Pts',(0.499118294731389,1.47325983954268,
14.9430772514466));
#269845=CARTESIAN_POINT('Ctrl Pts',(0.49364309527527,1.47510342680706,14.9434892042906));
#269846=CARTESIAN_POINT('Ctrl Pts',(0.481094645621458,1.47925100322241,
14.9444339211938));
#269847=CARTESIAN_POINT('Ctrl Pts',(0.474014931033483,1.48153482246555,
14.9449673370929));
#269848=CARTESIAN_POINT('Ctrl Pts',(0.452074583423186,1.48843911734937,
14.9466218710701));
#269849=CARTESIAN_POINT('Ctrl Pts',(0.437161201218259,1.4928872986568,14.9477485626628));
#269850=CARTESIAN_POINT('Ctrl Pts',(0.402548498640975,1.5026480536672,14.9503691628947));
#269851=CARTESIAN_POINT('Ctrl Pts',(0.382806774185083,1.50779818558583,
14.9518680474685));
#269852=CARTESIAN_POINT('Ctrl Pts',(0.313925902983509,1.52432760448762,
14.9571138143134));
#269853=CARTESIAN_POINT('Ctrl Pts',(0.264343080126861,1.53370333366798,
14.960919225385));
#269854=CARTESIAN_POINT('Ctrl Pts',(0.152232272556627,1.54930463864472,
14.9695743258279));
#269855=CARTESIAN_POINT('Ctrl Pts',(0.0896038512857674,1.55418464920886,
14.9744451851052));
#269856=CARTESIAN_POINT('Ctrl Pts',(-0.0208512102421502,1.55609192854191,
14.9830088027057));
#269857=CARTESIAN_POINT('Ctrl Pts',(-0.0685730245939707,1.55472024897298,
14.9866988749557));
#269858=CARTESIAN_POINT('Ctrl Pts',(-0.153498866993543,1.54836057822019,
14.9931821261876));
#269859=CARTESIAN_POINT('Ctrl Pts',(-0.19073015469002,1.54421661622696,
14.9959951332856));
#269860=CARTESIAN_POINT('Ctrl Pts',(-0.234303190953112,1.53776648477042,
14.9992268080692));
#269861=CARTESIAN_POINT('Ctrl Pts',(-0.240821267417033,1.53675920958705,
14.9997086234692));
#269862=CARTESIAN_POINT('Ctrl Pts',(-0.251392046586988,1.53505673935006,
15.0004871885796));
#269863=CARTESIAN_POINT('Ctrl Pts',(-0.255448655956028,1.53438689362732,
15.0007852912315));
#269864=CARTESIAN_POINT('Ctrl Pts',(-0.262678785810304,1.53316355366678,
15.0013153373323));
#269865=CARTESIAN_POINT('Ctrl Pts',(-0.265853279859228,1.53261627979498,
15.0015476228913));
#269866=CARTESIAN_POINT('Ctrl Pts',(-0.272733504773122,1.53140812772971,
15.0020501064023));
#269867=CARTESIAN_POINT('Ctrl Pts',(-0.27643853982599,1.53074366006012,
15.0023200990262));
#269868=CARTESIAN_POINT('Ctrl Pts',(-0.286838659520395,1.52883949233657,
15.0030763901819));
#269869=CARTESIAN_POINT('Ctrl Pts',(-0.293528179994305,1.52756925277144,
15.0035610017138));
#269870=CARTESIAN_POINT('Ctrl Pts',(-0.334232320751749,1.51956288351313,
15.006499692045));
#269871=CARTESIAN_POINT('Ctrl Pts',(-0.368025405070559,1.51173422558794,
15.0088966216291));
#269872=CARTESIAN_POINT('Ctrl Pts',(-0.48261977840887,1.48111549350689,
15.0169662237786));
#269873=CARTESIAN_POINT('Ctrl Pts',(-0.561828097148201,1.4529199965584,
15.0224485455255));
#269874=CARTESIAN_POINT('Ctrl Pts',(-0.733949938914209,1.37545679150609,
15.034881696169));
#269875=CARTESIAN_POINT('Ctrl Pts',(-0.824913647769721,1.32290459063556,
15.0418393207345));
#269876=CARTESIAN_POINT('Ctrl Pts',(-0.919583364846484,1.25462716070336,
15.049991123783));
#269877=CARTESIAN_POINT('Ctrl Pts',(-0.929188635688008,1.24753009689229,
15.0508292545906));
#269878=CARTESIAN_POINT('Ctrl Pts',(-0.944625733258137,1.23584687422173,
15.0521948741498));
#269879=CARTESIAN_POINT('Ctrl Pts',(-0.950508272640006,1.23132826356852,
15.0527197326911));
#269880=CARTESIAN_POINT('Ctrl Pts',(-0.960746214092261,1.22334701491011,
15.0536411845617));
#269881=CARTESIAN_POINT('Ctrl Pts',(-0.965115812586305,1.21990273120727,
15.0540370474519));
#269882=CARTESIAN_POINT('Ctrl Pts',(-0.974240211873082,1.21263082502837,
15.0548691684647));
#269883=CARTESIAN_POINT('Ctrl Pts',(-0.978991139004057,1.20879851755018,
15.055305609471));
#269884=CARTESIAN_POINT('Ctrl Pts',(-0.991250914205855,1.19878955956145,
15.0564401869939));
#269885=CARTESIAN_POINT('Ctrl Pts',(-0.998724523954861,1.19257037541106,
15.0571400328213));
#269886=CARTESIAN_POINT('Ctrl Pts',(-1.0149204122241,1.17883390937404,15.0586749524786));
#269887=CARTESIAN_POINT('Ctrl Pts',(-1.02361844768952,1.17128907164764,
15.0595111295317));
#269888=CARTESIAN_POINT('Ctrl Pts',(-1.04884775792436,1.1489090377648,15.0619719599693));
#269889=CARTESIAN_POINT('Ctrl Pts',(-1.06514537533249,1.13381604911318,
15.0636071132973));
#269890=CARTESIAN_POINT('Ctrl Pts',(-1.18729733638274,1.01573441430448,
15.0762212365456));
#269891=CARTESIAN_POINT('Ctrl Pts',(-1.27831057499782,0.898497496166772,
15.0878392077257));
#269892=CARTESIAN_POINT('Ctrl Pts',(-1.35603553146169,0.762125324186883,
15.0998637405688));
#269893=CARTESIAN_POINT('Ctrl Pts',(-1.36058439655371,0.753974454513514,
15.1005769159044));
#269894=CARTESIAN_POINT('Ctrl Pts',(-1.38331157793251,0.712375277228548,
15.1041872379123));
#269895=CARTESIAN_POINT('Ctrl Pts',(-1.40033284258663,0.678305226233278,
15.1070483184058));
#269896=CARTESIAN_POINT('Ctrl Pts',(-1.41882961088583,0.637610130828309,
15.1103281838581));
#269897=CARTESIAN_POINT('Ctrl Pts',(-1.42153253067859,0.631561091308568,
15.1108122184314));
#269898=CARTESIAN_POINT('Ctrl Pts',(-1.42585370940418,0.621722146847599,
15.1115936512264));
#269899=CARTESIAN_POINT('Ctrl Pts',(-1.42749566525312,0.6179428414073,15.111892418377));
#269900=CARTESIAN_POINT('Ctrl Pts',(-1.43039476312056,0.611196738492991,
15.1124231837184));
#269901=CARTESIAN_POINT('Ctrl Pts',(-1.4316577206618,0.608232523860307,
15.1126555278285));
#269902=CARTESIAN_POINT('Ctrl Pts',(-1.43437362509822,0.601802852413072,
15.1131576098349));
#269903=CARTESIAN_POINT('Ctrl Pts',(-1.43582322681121,0.598336052489105,
15.1134271453076));
#269904=CARTESIAN_POINT('Ctrl Pts',(-1.43985270173415,0.588600374451776,
15.1141808581556));
#269905=CARTESIAN_POINT('Ctrl Pts',(-1.44240422124614,0.582319732200108,
15.1146633669266));
#269906=CARTESIAN_POINT('Ctrl Pts',(-1.45755016023219,0.544327134834577,
15.1175609154676));
#269907=CARTESIAN_POINT('Ctrl Pts',(-1.46914057516394,0.512221549746112,
15.1199206489215));
#269908=CARTESIAN_POINT('Ctrl Pts',(-1.52983774872017,0.325019611299663,
15.1333167815798));
#269909=CARTESIAN_POINT('Ctrl Pts',(-1.55542699587216,0.163374799902079,
15.1435769870656));
#269910=CARTESIAN_POINT('Ctrl Pts',(-1.55549984403819,0.000696560963701701,
15.1547003707517));
#269911=CARTESIAN_POINT('Ctrl Pts',(-1.55549984481413,0.000694826046350984,
15.1547004893794));
#269912=CARTESIAN_POINT('Ctrl Pts',(-1.5555125263787,-0.0276952606902724,
15.1566417076067));
#269913=CARTESIAN_POINT('Ctrl Pts',(-1.55474797027491,-0.0560791253254835,
15.1586030095658));
#269914=CARTESIAN_POINT('Ctrl Pts',(-1.55272661854127,-0.0932668495106141,
15.1612072810071));
#269915=CARTESIAN_POINT('Ctrl Pts',(-1.55217054284928,-0.102104149637935,
15.1618287195237));
#269916=CARTESIAN_POINT('Ctrl Pts',(-1.55109545149386,-0.117140254106849,
15.1628906597484));
#269917=CARTESIAN_POINT('Ctrl Pts',(-1.55061464422912,-0.123341646914341,
15.1633299738422));
#269918=CARTESIAN_POINT('Ctrl Pts',(-1.54964882427644,-0.134898813301272,
15.1641512696402));
#269919=CARTESIAN_POINT('Ctrl Pts',(-1.54917320490023,-0.140255296904652,
15.1645329532254));
#269920=CARTESIAN_POINT('Ctrl Pts',(-1.5481508749264,-0.151128594537193,
15.1653098945114));
#269921=CARTESIAN_POINT('Ctrl Pts',(-1.54760242799074,-0.15664516282932,
15.1657052011876));
#269922=CARTESIAN_POINT('Ctrl Pts',(-1.54625519666379,-0.169498009803029,
15.1666288974961));
#269923=CARTESIAN_POINT('Ctrl Pts',(-1.54543367674206,-0.176831716199418,
15.167157992624));
#269924=CARTESIAN_POINT('Ctrl Pts',(-1.54316113496428,-0.195891733163291,
15.168538550544));
#269925=CARTESIAN_POINT('Ctrl Pts',(-1.54162865432939,-0.207607652601354,
15.1693925489004));
#269926=CARTESIAN_POINT('Ctrl Pts',(-1.53448962018521,-0.257738126566052,
15.1730705592355));
#269927=CARTESIAN_POINT('Ctrl Pts',(-1.52757997202731,-0.295949785225794,
15.1759348782609));
#269928=CARTESIAN_POINT('Ctrl Pts',(-1.50111487761445,-0.416380676512976,
15.1851631176065));
#269929=CARTESIAN_POINT('Ctrl Pts',(-1.47628969611336,-0.497276726124052,
15.1916730715154));
#269930=CARTESIAN_POINT('Ctrl Pts',(-1.40972685877153,-0.66433771623309,
15.2056158623732));
#269931=CARTESIAN_POINT('Ctrl Pts',(-1.36635336422968,-0.749504521562905,
15.2130316495414));
#269932=CARTESIAN_POINT('Ctrl Pts',(-1.31014347492284,-0.838572033497492,
15.2207985692926));
#269933=CARTESIAN_POINT('Ctrl Pts',(-1.30475989519401,-0.846924205501031,
15.2215268778759));
#269934=CARTESIAN_POINT('Ctrl Pts',(-1.29688681294401,-0.858885354798602,
15.2225692238688));
#269935=CARTESIAN_POINT('Ctrl Pts',(-1.29446165980958,-0.862536069290741,
15.2228872723498));
#269936=CARTESIAN_POINT('Ctrl Pts',(-1.29020977881723,-0.868878332722819,
15.2234395825227));
#269937=CARTESIAN_POINT('Ctrl Pts',(-1.28838999463197,-0.871574467851273,
15.2236742999759));
#269938=CARTESIAN_POINT('Ctrl Pts',(-1.28453639272768,-0.877245399413548,
15.2241678190269));
#269939=CARTESIAN_POINT('Ctrl Pts',(-1.28250068969525,-0.880218845902813,
15.2244264906434));
#269940=CARTESIAN_POINT('Ctrl Pts',(-1.27700388052335,-0.888188198847021,
15.2251195965164));
#269941=CARTESIAN_POINT('Ctrl Pts',(-1.2735237492052,-0.893171008775414,
15.2255527685777));
#269942=CARTESIAN_POINT('Ctrl Pts',(-1.25783899046606,-0.915350197077298,
15.2274806577308));
#269943=CARTESIAN_POINT('Ctrl Pts',(-1.2453139168844,-0.932318761945474,
15.2289550292966));
#269944=CARTESIAN_POINT('Ctrl Pts',(-1.13170546163315,-1.07985530960747,
15.2418208956206));
#269945=CARTESIAN_POINT('Ctrl Pts',(-1.01076733014357,-1.19382155551633,
15.2521922598749));
#269946=CARTESIAN_POINT('Ctrl Pts',(-0.85066970897933,-1.30259240762529,
15.26531550409));
#269947=CARTESIAN_POINT('Ctrl Pts',(-0.82676027028175,-1.31789727644882,
15.2672583379683));
#269948=CARTESIAN_POINT('Ctrl Pts',(-0.790710977032655,-1.33960593890161,
15.2701726471617));
#269949=CARTESIAN_POINT('Ctrl Pts',(-0.77888278058075,-1.34651755079651,
15.2711265250598));
#269950=CARTESIAN_POINT('Ctrl Pts',(-0.757194135280786,-1.35880956373169,
15.2728724540265));
#269951=CARTESIAN_POINT('Ctrl Pts',(-0.747363663911357,-1.36424115579042,
15.2736626513386));
#269952=CARTESIAN_POINT('Ctrl Pts',(-0.731770183702935,-1.37263783879527,
15.2749147297762));
#269953=CARTESIAN_POINT('Ctrl Pts',(-0.726045845280711,-1.37567425886233,
15.275374078512));
#269954=CARTESIAN_POINT('Ctrl Pts',(-0.720239872991005,-1.37870764863017,
15.275839736497));
#269955=CARTESIAN_POINT('Ctrl Pts',(-0.720176964191238,-1.37874051049707,
15.2758447819601));
#269956=CARTESIAN_POINT('Ctrl Pts',(-0.720044566835006,-1.37880965978515,
15.2758554005412));
#269957=CARTESIAN_POINT('Ctrl Pts',(-0.719975077788481,-1.37884594625683,
15.2758609736923));
#269958=CARTESIAN_POINT('Ctrl Pts',(-0.719828835990497,-1.3789222981636,
15.2758727024839));
#269959=CARTESIAN_POINT('Ctrl Pts',(-0.719752082636228,-1.37896236244396,
15.2758788581652));
#269960=CARTESIAN_POINT('Ctrl Pts',(-0.719590559099501,-1.37904665852802,
15.275891812395));
#269961=CARTESIAN_POINT('Ctrl Pts',(-0.719505788184481,-1.37909088892337,
15.2758986109929));
#269962=CARTESIAN_POINT('Ctrl Pts',(-0.719327401019969,-1.37918394396459,
15.2759129174733));
#269963=CARTESIAN_POINT('Ctrl Pts',(-0.719233783880984,-1.37923276689328,
15.2759204254159));
#269964=CARTESIAN_POINT('Ctrl Pts',(-0.719036792794181,-1.37933547558167,
15.2759362236498));
#269965=CARTESIAN_POINT('Ctrl Pts',(-0.71893341776129,-1.37938935925073,
15.2759445140145));
#269966=CARTESIAN_POINT('Ctrl Pts',(-0.718715918409621,-1.37950269850554,
15.2759619566442));
#269967=CARTESIAN_POINT('Ctrl Pts',(-0.718601789401949,-1.37956215330405,
15.2759711092687));
#269968=CARTESIAN_POINT('Ctrl Pts',(-0.718392146452066,-1.37967133242328,
15.2759879215053));
#269969=CARTESIAN_POINT('Ctrl Pts',(-0.718296636739827,-1.37972105994079,
15.2759955808057));
#269970=CARTESIAN_POINT('Ctrl Pts',(-0.718046176039664,-1.37985143025878,
15.2760156660685));
#269971=CARTESIAN_POINT('Ctrl Pts',(-0.717891219256346,-1.37993205551082,
15.2760280923907));
#269972=CARTESIAN_POINT('Ctrl Pts',(-0.712795492074503,-1.38258231245329,
15.2764367243206));
#269973=CARTESIAN_POINT('Ctrl Pts',(-0.707841029936725,-1.3851253874963,
15.2768338571734));
#269974=CARTESIAN_POINT('Ctrl Pts',(-0.696247099781216,-1.39099798482353,
15.2777628515641));
#269975=CARTESIAN_POINT('Ctrl Pts',(-0.689597277286889,-1.39430664107737,
15.2782954313772));
#269976=CARTESIAN_POINT('Ctrl Pts',(-0.67216463462957,-1.40282513638577,
15.2796910817107));
#269977=CARTESIAN_POINT('Ctrl Pts',(-0.661345081613867,-1.40795821224977,
15.2805567797875));
#269978=CARTESIAN_POINT('Ctrl Pts',(-0.556443296402479,-1.45625040579505,
15.2889471079586));
#269979=CARTESIAN_POINT('Ctrl Pts',(-0.458353207163089,-1.49003305843016,
15.2967954051994));
#269980=CARTESIAN_POINT('Ctrl Pts',(-0.274985716201144,-1.53335546002276,
15.3113583425522));
#269981=CARTESIAN_POINT('Ctrl Pts',(-0.190852682925785,-1.54608286829337,
15.3179933058857));
#269982=CARTESIAN_POINT('Ctrl Pts',(-0.0712949703106406,-1.55425682309582,
15.3270936693173));
#269983=CARTESIAN_POINT('Ctrl Pts',(-0.0364170491154879,-1.55546504859568,
15.3297080553145));
#269984=CARTESIAN_POINT('Ctrl Pts',(0.00529519210871108,-1.55550593812472,
15.3327649713313));
#269985=CARTESIAN_POINT('Ctrl Pts',(0.0121153435057373,-1.5554677706894,
15.3332625568429));
#269986=CARTESIAN_POINT('Ctrl Pts',(0.0227014169890424,-1.5553388962645,
15.3340312054375));
#269987=CARTESIAN_POINT('Ctrl Pts',(0.0264675192671187,-1.55527936648302,
15.3343039345515));
#269988=CARTESIAN_POINT('Ctrl Pts',(0.0334538907940433,-1.55514355045724,
15.3348084742616));
#269989=CARTESIAN_POINT('Ctrl Pts',(0.0366741134858062,-1.55507094214065,
15.3350404776992));
#269990=CARTESIAN_POINT('Ctrl Pts',(0.0440009473277864,-1.55488296769438,
15.3355671054639));
#269991=CARTESIAN_POINT('Ctrl Pts',(0.048107339048445,-1.55476133588665,
15.3358613780457));
#269992=CARTESIAN_POINT('Ctrl Pts',(0.0587936721339433,-1.5544024268926,
15.3366250036344));
#269993=CARTESIAN_POINT('Ctrl Pts',(0.0653727646067616,-1.55413963540062,
15.3370929824602));
#269994=CARTESIAN_POINT('Ctrl Pts',(0.109126931100659,-1.55211360405198,
15.340192151669));
#269995=CARTESIAN_POINT('Ctrl Pts',(0.146233800687356,-1.5490582827536,
15.3427575391598));
#269996=CARTESIAN_POINT('Ctrl Pts',(0.230623835750005,-1.53904959577818,
15.3485210706069));
#269997=CARTESIAN_POINT('Ctrl Pts',(0.277767677739557,-1.53124351483212,
15.3516899932918));
#269998=CARTESIAN_POINT('Ctrl Pts',(0.385565986350445,-1.50825075848853,
15.3589639980438));
#269999=CARTESIAN_POINT('Ctrl Pts',(0.445810583517784,-1.49155431539201,
15.3630516468424));
#270000=CARTESIAN_POINT('Ctrl Pts',(0.570453894172218,-1.44878147799923,
15.371805766872));
#270001=CARTESIAN_POINT('Ctrl Pts',(0.634434822829089,-1.4219268594508,
15.376477754972));
#270002=CARTESIAN_POINT('Ctrl Pts',(0.71152724343633,-1.38332757430809,
15.3824708352682));
#270003=CARTESIAN_POINT('Ctrl Pts',(0.726522788193741,-1.37551110325834,
15.3836542615365));
#270004=CARTESIAN_POINT('Ctrl Pts',(0.748148751208125,-1.36378621835699,
15.3853884098071));
#270005=CARTESIAN_POINT('Ctrl Pts',(0.754882680674469,-1.36007041652513,
15.3859323281794));
#270006=CARTESIAN_POINT('Ctrl Pts',(0.766656568833255,-1.35345917454319,
15.3868904214634));
#270007=CARTESIAN_POINT('Ctrl Pts',(0.771708415055184,-1.35058511473642,
15.38730382605));
#270008=CARTESIAN_POINT('Ctrl Pts',(0.781503614782134,-1.34493960074805,
15.3881099668274));
#270009=CARTESIAN_POINT('Ctrl Pts',(0.786248633459315,-1.34217119419752,
15.3885025884737));
#270010=CARTESIAN_POINT('Ctrl Pts',(0.798916838421896,-1.33468989773695,
15.3895565351928));
#270011=CARTESIAN_POINT('Ctrl Pts',(0.80681285082437,-1.3299316729776,15.3902194980925));
#270012=CARTESIAN_POINT('Ctrl Pts',(0.835726756589508,-1.3121555732434,
15.3926698929321));
#270013=CARTESIAN_POINT('Ctrl Pts',(0.856474693350269,-1.29870798471957,
15.3944729657176));
#270014=CARTESIAN_POINT('Ctrl Pts',(0.881379653929259,-1.28170966765153,
15.396694085811));
#270015=CARTESIAN_POINT('Ctrl Pts',(0.885850862663507,-1.27862348417631,
15.397095126387));
#270016=CARTESIAN_POINT('Ctrl Pts',(0.894739849751391,-1.27241899204902,
15.3978969935394));
#270017=CARTESIAN_POINT('Ctrl Pts',(0.899157719173715,-1.26930094335778,
15.3982978068634));
#270018=CARTESIAN_POINT('Ctrl Pts',(1.03517479679167,-1.1722362083094,15.4107088706492));
#270019=CARTESIAN_POINT('Ctrl Pts',(1.15130595135913,-1.05839497997946,
15.4235134913719));
#270020=CARTESIAN_POINT('Ctrl Pts',(1.26810612266311,-0.901466873722713,
15.4383581420086));
#270021=CARTESIAN_POINT('Ctrl Pts',(1.28750393421204,-0.873538621993595,
15.4409038897354));
#270022=CARTESIAN_POINT('Ctrl Pts',(1.30965124679445,-0.839309072424249,
15.4438913958631));
#270023=CARTESIAN_POINT('Ctrl Pts',(1.31329281778026,-0.833599476102055,
15.4443854221251));
#270024=CARTESIAN_POINT('Ctrl Pts',(1.31889611845211,-0.824686235311817,
15.4451497716214));
#270025=CARTESIAN_POINT('Ctrl Pts',(1.32088366779136,-0.821499053531846,
15.4454217318491));
#270026=CARTESIAN_POINT('Ctrl Pts',(1.32455481675404,-0.815564326289604,
15.4459255824182));
#270027=CARTESIAN_POINT('Ctrl Pts',(1.32624140965404,-0.812818772275222,
15.4461576608905));
#270028=CARTESIAN_POINT('Ctrl Pts',(1.33006649676801,-0.806548424171424,
15.4466853969884));
#270029=CARTESIAN_POINT('Ctrl Pts',(1.33219951637633,-0.803020358385821,
15.4469806968542));
#270030=CARTESIAN_POINT('Ctrl Pts',(1.3377274009304,-0.793794456961812,
15.4477487654474));
#270031=CARTESIAN_POINT('Ctrl Pts',(1.34109994250851,-0.788083236376625,
15.4482201336208));
#270032=CARTESIAN_POINT('Ctrl Pts',(1.36365813520844,-0.749317944644559,
15.4513932065983));
#270033=CARTESIAN_POINT('Ctrl Pts',(1.38165842701888,-0.715584715891151,
15.4540254786558));
#270034=CARTESIAN_POINT('Ctrl Pts',(1.46393663406337,-0.546684918543369,
15.4667550113932));
#270035=CARTESIAN_POINT('Ctrl Pts',(1.50971968806793,-0.403395233726827,
15.4762533022922));
#270036=CARTESIAN_POINT('Ctrl Pts',(1.5408337241483,-0.216741045405577,
15.4891191015357));
#270037=CARTESIAN_POINT('Ctrl Pts',(1.54584687883676,-0.177488650248184,
15.4918455413033));
#270038=CARTESIAN_POINT('Ctrl Pts',(1.55029494254361,-0.127581929092454,
15.4953588806552));
#270039=CARTESIAN_POINT('Ctrl Pts',(1.55112458913943,-0.117064327345026,
15.4961018856068));
#270040=CARTESIAN_POINT('Ctrl Pts',(1.55228512741467,-0.100159977558526,
15.4973005919637));
#270041=CARTESIAN_POINT('Ctrl Pts',(1.5526837436891,-0.0937780772025266,
15.4977541712973));
#270042=CARTESIAN_POINT('Ctrl Pts',(1.55336731394945,-0.0816306280322024,
15.4986195714066));
#270043=CARTESIAN_POINT('Ctrl Pts',(1.55365954550481,-0.0758655817320582,
15.499031157336));
#270044=CARTESIAN_POINT('Ctrl Pts',(1.55425314618952,-0.0627069589700235,
15.4999726625137));
#270045=CARTESIAN_POINT('Ctrl Pts',(1.55453385730008,-0.0553126400381016,
15.5005032177799));
#270046=CARTESIAN_POINT('Ctrl Pts',(1.55512783124167,-0.0360398672224341,
15.5018900934238));
#270047=CARTESIAN_POINT('Ctrl Pts',(1.55535775502189,-0.0241595294448888,
15.5027489876862));
#270048=CARTESIAN_POINT('Ctrl Pts',(1.55629621137896,0.0947295848169169,
15.5113857622986));
#270049=CARTESIAN_POINT('Ctrl Pts',(1.54609636708754,0.201515767774227,
15.5195113411043));
#270050=CARTESIAN_POINT('Ctrl Pts',(1.50882657284367,0.387023167389231,
15.5341474368718));
#270051=CARTESIAN_POINT('Ctrl Pts',(1.48625653958619,0.466247815391386,
15.5405661445793));
#270052=CARTESIAN_POINT('Ctrl Pts',(1.45026520959079,0.562799534624391,
15.5483874352204));
#270053=CARTESIAN_POINT('Ctrl Pts',(1.44261352366488,0.582132892741886,
15.5499529745773));
#270054=CARTESIAN_POINT('Ctrl Pts',(1.43457668274383,0.601306902777371,
15.5515012983457));
#270055=CARTESIAN_POINT('Origin',(0.,0.,-1.29405622560371));
#270056=CARTESIAN_POINT('',(1.43457668357428,0.601306900796103,16.3897484311226));
#270057=CARTESIAN_POINT('',(1.43457653793677,0.601307248252799,16.2500928067243));
#270058=CARTESIAN_POINT('',(1.43457668357355,0.601306900797845,-1.29405622560371));
#270059=CARTESIAN_POINT('',(-1.555499922686,-0.000490432305788335,15.9926617964138));
#270060=CARTESIAN_POINT('Ctrl Pts',(1.43457668357428,0.601306900796103,
16.3897484311226));
#270061=CARTESIAN_POINT('Ctrl Pts',(1.43622124916671,0.597383354516543,
16.3894460676227));
#270062=CARTESIAN_POINT('Ctrl Pts',(1.43784969886007,0.593453108296744,
16.3891431618272));
#270063=CARTESIAN_POINT('Ctrl Pts',(1.44185258584415,0.583678986602261,
16.3883897712346));
#270064=CARTESIAN_POINT('Ctrl Pts',(1.44420761711323,0.577827305700601,
16.3879386389247));
#270065=CARTESIAN_POINT('Ctrl Pts',(1.4503473683068,0.562299486109962,16.3867412122664));
#270066=CARTESIAN_POINT('Ctrl Pts',(1.45407078622349,0.552599619749088,
16.3859928814586));
#270067=CARTESIAN_POINT('Ctrl Pts',(1.47119863463307,0.506607924974705,
16.3824425147161));
#270068=CARTESIAN_POINT('Ctrl Pts',(1.48334209387819,0.469864612056201,
16.3795992326525));
#270069=CARTESIAN_POINT('Ctrl Pts',(1.53579686969054,0.28874363162374,16.3655365191552));
#270070=CARTESIAN_POINT('Ctrl Pts',(1.55645950951083,0.139514110338311,
16.3537026292281));
#270071=CARTESIAN_POINT('Ctrl Pts',(1.55520547888475,-0.0495653299290125,
16.3392885804976));
#270072=CARTESIAN_POINT('Ctrl Pts',(1.55345967028794,-0.0887947076208234,
16.3363363303646));
#270073=CARTESIAN_POINT('Ctrl Pts',(1.54968469411606,-0.134542785712773,
16.3329680120167));
#270074=CARTESIAN_POINT('Ctrl Pts',(1.54909573938789,-0.141162341969934,
16.3324824692211));
#270075=CARTESIAN_POINT('Ctrl Pts',(1.54807484319533,-0.151859607825807,
16.3317010162551));
#270076=CARTESIAN_POINT('Ctrl Pts',(1.54766917921796,-0.155939646554834,
16.3314037137795));
#270077=CARTESIAN_POINT('Ctrl Pts',(1.54691983009985,-0.163185254925248,
16.3308771347085));
#270078=CARTESIAN_POINT('Ctrl Pts',(1.54658255368569,-0.16635141574489,
16.3306475072039));
#270079=CARTESIAN_POINT('Ctrl Pts',(1.54583392657445,-0.173179972737344,
16.3301532974776));
#270080=CARTESIAN_POINT('Ctrl Pts',(1.54541928246134,-0.176841945440848,
16.3298889019365));
#270081=CARTESIAN_POINT('Ctrl Pts',(1.54422833614253,-0.187035723799553,
16.3291545920577));
#270082=CARTESIAN_POINT('Ctrl Pts',(1.54342359950181,-0.193564234129192,
16.3286862372278));
#270083=CARTESIAN_POINT('Ctrl Pts',(1.53851317896824,-0.231421173267933,
16.3259805360574));
#270084=CARTESIAN_POINT('Ctrl Pts',(1.53349477728767,-0.262626524767828,
16.3237906006973));
#270085=CARTESIAN_POINT('Ctrl Pts',(1.49999444498925,-0.436884888645756,
16.3116784456318));
#270086=CARTESIAN_POINT('Ctrl Pts',(1.45245317451607,-0.575534479184962,
16.3024225177903));
#270087=CARTESIAN_POINT('Ctrl Pts',(1.36393426180833,-0.749461223127075,
16.2892596207072));
#270088=CARTESIAN_POINT('Ctrl Pts',(1.33950949241042,-0.79228927050142,
16.2858845049917));
#270089=CARTESIAN_POINT('Ctrl Pts',(1.30690068846105,-0.843637583639098,
16.2816269434337));
#270090=CARTESIAN_POINT('Ctrl Pts',(1.30059752645406,-0.853322824885235,
16.2808142771389));
#270091=CARTESIAN_POINT('Ctrl Pts',(1.29050769501656,-0.868455024471865,
16.2795288497129));
#270092=CARTESIAN_POINT('Ctrl Pts',(1.28679299744938,-0.873949666554983,
16.2790587851867));
#270093=CARTESIAN_POINT('Ctrl Pts',(1.27987300396394,-0.884045693874743,
16.2781888385319));
#270094=CARTESIAN_POINT('Ctrl Pts',(1.27667773322361,-0.888653846620655,
16.2777893409963));
#270095=CARTESIAN_POINT('Ctrl Pts',(1.26954167458808,-0.898827396873072,
16.2769019019813));
#270096=CARTESIAN_POINT('Ctrl Pts',(1.26558908437035,-0.904384331834199,
16.2764135147403));
#270097=CARTESIAN_POINT('Ctrl Pts',(1.25414152922805,-0.92025640440821,
16.2750078858892));
#270098=CARTESIAN_POINT('Ctrl Pts',(1.24655626077617,-0.930505398104111,
16.2740871759472));
#270099=CARTESIAN_POINT('Ctrl Pts',(1.18640577760831,-1.00972340706203,
16.2668660946348));
#270100=CARTESIAN_POINT('Ctrl Pts',(1.12829217320694,-1.07426801437701,
16.2603434412624));
#270101=CARTESIAN_POINT('Ctrl Pts',(1.00108949750904,-1.19378314426523,
16.2469295933528));
#270102=CARTESIAN_POINT('Ctrl Pts',(0.932084566585866,-1.24840548094538,
16.2400591007981));
#270103=CARTESIAN_POINT('Ctrl Pts',(0.848937209399679,-1.30346726204182,
16.2324127972949));
#270104=CARTESIAN_POINT('Ctrl Pts',(0.838960542287971,-1.30991087834649,
16.2315051394349));
#270105=CARTESIAN_POINT('Ctrl Pts',(0.797454687077481,-1.33604947061021,
16.2277718414017));
#270106=CARTESIAN_POINT('Ctrl Pts',(0.765295191208394,-1.35472727669639,
16.2249798438761));
#270107=CARTESIAN_POINT('Ctrl Pts',(0.726734595774218,-1.37531076566749,
16.2217733536623));
#270108=CARTESIAN_POINT('Ctrl Pts',(0.720955586806194,-1.37834898364336,
16.2212964412069));
#270109=CARTESIAN_POINT('Ctrl Pts',(0.711547574183233,-1.38321973093594,
16.2205261336903));
#270110=CARTESIAN_POINT('Ctrl Pts',(0.707930294861838,-1.38507453698824,
16.2202314084864));
#270111=CARTESIAN_POINT('Ctrl Pts',(0.70146949582348,-1.38835547145709,
16.2197076353591));
#270112=CARTESIAN_POINT('Ctrl Pts',(0.698628840221144,-1.38978707469345,
16.2194782511067));
#270113=CARTESIAN_POINT('Ctrl Pts',(0.69246590248059,-1.3928693353179,16.2189825580635));
#270114=CARTESIAN_POINT('Ctrl Pts',(0.689142105309287,-1.39451682343256,
16.2187164467997));
#270115=CARTESIAN_POINT('Ctrl Pts',(0.67980815278537,-1.39910181017468,
16.2179724888132));
#270116=CARTESIAN_POINT('Ctrl Pts',(0.673784798076448,-1.40201249995334,
16.2174962688064));
#270117=CARTESIAN_POINT('Ctrl Pts',(0.637442093168647,-1.41928621852338,
16.214644996229));
#270118=CARTESIAN_POINT('Ctrl Pts',(0.606680555216482,-1.43270545586184,
16.2123235206432));
#270119=CARTESIAN_POINT('Ctrl Pts',(0.414697011581696,-1.50916117926978,
16.1982478450922));
#270120=CARTESIAN_POINT('Ctrl Pts',(0.244324212070338,-1.54591657966354,
16.1873755292736));
#270121=CARTESIAN_POINT('Ctrl Pts',(0.0464991820170724,-1.5550043521393,
16.1737368210692));
#270122=CARTESIAN_POINT('Ctrl Pts',(0.0215938335854684,-1.55554951540799,
16.1720049393561));
#270123=CARTESIAN_POINT('Ctrl Pts',(-0.0124914097454679,-1.55547692482545,
16.1696094418835));
#270124=CARTESIAN_POINT('Ctrl Pts',(-0.0216695802801524,-1.55537613515637,
16.168961907389));
#270125=CARTESIAN_POINT('Ctrl Pts',(-0.0362840079143223,-1.55508626857893,
16.1679266279421));
#270126=CARTESIAN_POINT('Ctrl Pts',(-0.0417212009102184,-1.55494989371981,
16.1675405319428));
#270127=CARTESIAN_POINT('Ctrl Pts',(-0.0528862023635586,-1.5546112529404,
16.1667457420892));
#270128=CARTESIAN_POINT('Ctrl Pts',(-0.0586138245277649,-1.55440584022524,
16.1663369559689));
#270129=CARTESIAN_POINT('Ctrl Pts',(-0.0718781794081574,-1.55385671707094,
16.1653877418562));
#270130=CARTESIAN_POINT('Ctrl Pts',(-0.0794137522707384,-1.55348982040239,
16.1648465978156));
#270131=CARTESIAN_POINT('Ctrl Pts',(-0.103342343882475,-1.55215021337,16.1631220543335));
#270132=CARTESIAN_POINT('Ctrl Pts',(-0.119722277857939,-1.55097274722946,
16.1619323031679));
#270133=CARTESIAN_POINT('Ctrl Pts',(-0.20195809291009,-1.54375081592702,
16.1559103961131));
#270134=CARTESIAN_POINT('Ctrl Pts',(-0.267390634171013,-1.53377105005858,
16.1509572296355));
#270135=CARTESIAN_POINT('Ctrl Pts',(-0.395241876496527,-1.50584093383744,
16.1409670568313));
#270136=CARTESIAN_POINT('Ctrl Pts',(-0.457573954285048,-1.48808542459818,
16.1359437441298));
#270137=CARTESIAN_POINT('Ctrl Pts',(-0.599424521885813,-1.43792123016951,
16.1242776453891));
#270138=CARTESIAN_POINT('Ctrl Pts',(-0.6777453710834,-1.40270892192832,
16.1176534644634));
#270139=CARTESIAN_POINT('Ctrl Pts',(-0.759654392830792,-1.35741197616246,
16.1107768516612));
#270140=CARTESIAN_POINT('Ctrl Pts',(-0.766506144926125,-1.35355472971061,
16.1102020962037));
#270141=CARTESIAN_POINT('Ctrl Pts',(-0.776806897008622,-1.34765253902365,
16.1093390788116));
#270142=CARTESIAN_POINT('Ctrl Pts',(-0.780277584656725,-1.34564602070483,
16.1090484803062));
#270143=CARTESIAN_POINT('Ctrl Pts',(-0.786384154429284,-1.34208404292978,
16.1085375554856));
#270144=CARTESIAN_POINT('Ctrl Pts',(-0.789023229894871,-1.34053420691248,
16.1083168761084));
#270145=CARTESIAN_POINT('Ctrl Pts',(-0.794773538276345,-1.3371343890138,
16.1078363187212));
#270146=CARTESIAN_POINT('Ctrl Pts',(-0.797882889462375,-1.33528133621917,
16.1075766434577));
#270147=CARTESIAN_POINT('Ctrl Pts',(-0.804324903347557,-1.33141160909593,
16.1070389462636));
#270148=CARTESIAN_POINT('Ctrl Pts',(-0.80765652127111,-1.32939323283044,
16.106761034654));
#270149=CARTESIAN_POINT('Ctrl Pts',(-0.816127845920436,-1.32421749481746,
16.1060547249551));
#270150=CARTESIAN_POINT('Ctrl Pts',(-0.821256893698819,-1.32104267609436,
16.105627401268));
#270151=CARTESIAN_POINT('Ctrl Pts',(-0.836070685458236,-1.31175349563657,
16.1043937247262));
#270152=CARTESIAN_POINT('Ctrl Pts',(-0.845706772380946,-1.3055617558416,
16.1035918981216));
#270153=CARTESIAN_POINT('Ctrl Pts',(-0.976461631052707,-1.21948900371196,
16.0927078148246));
#270154=CARTESIAN_POINT('Ctrl Pts',(-1.08590940391926,-1.12314059161889,
16.0834962595416));
#270155=CARTESIAN_POINT('Ctrl Pts',(-1.22293597596988,-0.963467028996656,
16.0694479952498));
#270156=CARTESIAN_POINT('Ctrl Pts',(-1.26228043043216,-0.911310868972647,
16.0650174533412));
#270157=CARTESIAN_POINT('Ctrl Pts',(-1.30447885558593,-0.847374686860039,
16.0596624793527));
#270158=CARTESIAN_POINT('Ctrl Pts',(-1.3106239526464,-0.837838759763592,
16.0588657945625));
#270159=CARTESIAN_POINT('Ctrl Pts',(-1.32049227288281,-0.822150898163259,
16.0575578941453));
#270160=CARTESIAN_POINT('Ctrl Pts',(-1.32427819042192,-0.816038732739042,
16.0570489943488));
#270161=CARTESIAN_POINT('Ctrl Pts',(-1.3309822859232,-0.805045799915239,
16.0561348019584));
#270162=CARTESIAN_POINT('Ctrl Pts',(-1.33391634949332,-0.80017482863684,
16.0557300991647));
#270163=CARTESIAN_POINT('Ctrl Pts',(-1.34008524180136,-0.789805350546408,
16.054869287775));
#270164=CARTESIAN_POINT('Ctrl Pts',(-1.3433130759484,-0.784302827223577,
16.0544129346997));
#270165=CARTESIAN_POINT('Ctrl Pts',(-1.351871410928,-0.769505519530362,
16.0531867731405));
#270166=CARTESIAN_POINT('Ctrl Pts',(-1.35713978827913,-0.760175401246038,
16.0524147503176));
#270167=CARTESIAN_POINT('Ctrl Pts',(-1.38287156433815,-0.713485111054437,
16.0485560946431));
#270168=CARTESIAN_POINT('Ctrl Pts',(-1.40188874034638,-0.675353296657955,
16.0454189887703));
#270169=CARTESIAN_POINT('Ctrl Pts',(-1.48483081101455,-0.490400613932409,
16.0302534114448));
#270170=CARTESIAN_POINT('Ctrl Pts',(-1.52738494115264,-0.33510522985144,
16.0175353988927));
#270171=CARTESIAN_POINT('Ctrl Pts',(-1.54848231151036,-0.149918712130985,
16.0034886715258));
#270172=CARTESIAN_POINT('Ctrl Pts',(-1.55079768980039,-0.123692497960716,
16.001528261944));
#270173=CARTESIAN_POINT('Ctrl Pts',(-1.55283995640408,-0.0911471365309453,
15.9991409602467));
#270174=CARTESIAN_POINT('Ctrl Pts',(-1.55319548055527,-0.0848736325823962,
15.9986828695023));
#270175=CARTESIAN_POINT('Ctrl Pts',(-1.55369778872703,-0.0749453617730281,
15.9979613907529));
#270176=CARTESIAN_POINT('Ctrl Pts',(-1.55386970929931,-0.0712920277401801,
15.997696651721));
#270177=CARTESIAN_POINT('Ctrl Pts',(-1.55416497753361,-0.0645080476316434,
15.9972064757795));
#270178=CARTESIAN_POINT('Ctrl Pts',(-1.55429175119681,-0.0613776672525384,
15.9969808586445));
#270179=CARTESIAN_POINT('Ctrl Pts',(-1.55452553951862,-0.0551386554779275,
15.9965323038761));
#270180=CARTESIAN_POINT('Ctrl Pts',(-1.55463268773893,-0.0520300971929322,
15.9963093609128));
#270181=CARTESIAN_POINT('Ctrl Pts',(-1.55485755933656,-0.0448836101606422,
15.9957980359545));
#270182=CARTESIAN_POINT('Ctrl Pts',(-1.55496887945015,-0.0408454794407842,
15.995510002288));
#270183=CARTESIAN_POINT('Ctrl Pts',(-1.55535093414078,-0.0247039502565554,
15.9943620471943));
#270184=CARTESIAN_POINT('Ctrl Pts',(-1.55549610541594,-0.0125976349117609,
15.9935086974294));
#270185=CARTESIAN_POINT('Ctrl Pts',(-1.555499922686,-0.000490432305788335,
15.9926617964138));
#270186=CARTESIAN_POINT('Ctrl Pts',(-1.5554999222446,-0.000491830301829164,
15.9926618942039));
#270187=CARTESIAN_POINT('Ctrl Pts',(-1.55554030562071,0.127227706631577,
15.9837278841703));
#270188=CARTESIAN_POINT('Ctrl Pts',(-1.5398505335658,0.254495564010868,
15.9755208537055));
#270189=CARTESIAN_POINT('Ctrl Pts',(-1.48952695169905,0.455128082193538,
15.9618391493048));
#270190=CARTESIAN_POINT('Ctrl Pts',(-1.46447355021139,0.530232798088373,
15.9565425441433));
#270191=CARTESIAN_POINT('Ctrl Pts',(-1.42684502869873,0.619691391172787,
15.9498050035162));
#270192=CARTESIAN_POINT('Ctrl Pts',(-1.41957991519656,0.636157978547014,
15.948546584934));
#270193=CARTESIAN_POINT('Ctrl Pts',(-1.40874790931139,0.659598995112758,
15.9467269703452));
#270194=CARTESIAN_POINT('Ctrl Pts',(-1.40541130331365,0.666678761345963,
15.9461736595929));
#270195=CARTESIAN_POINT('Ctrl Pts',(-1.39951968555009,0.678939071313797,
15.9452087912896));
#270196=CARTESIAN_POINT('Ctrl Pts',(-1.39698895894683,0.684131171438668,
15.9447980803877));
#270197=CARTESIAN_POINT('Ctrl Pts',(-1.39205422289453,0.694113836870691,
15.944004300602));
#270198=CARTESIAN_POINT('Ctrl Pts',(-1.38965425108613,0.698906316415611,
15.943621377177));
#270199=CARTESIAN_POINT('Ctrl Pts',(-1.3839105396724,0.710229326492192,
15.9427122219029));
#270200=CARTESIAN_POINT('Ctrl Pts',(-1.38054529681994,0.716748741213035,
15.9421852414407));
#270201=CARTESIAN_POINT('Ctrl Pts',(-1.3684995150176,0.739685201061264,
15.9403185794652));
#270202=CARTESIAN_POINT('Ctrl Pts',(-1.35957154558131,0.755969758789627,
15.9389702124151));
#270203=CARTESIAN_POINT('Ctrl Pts',(-1.29519000225675,0.868570511218385,
15.929480064824));
#270204=CARTESIAN_POINT('Ctrl Pts',(-1.2298553969229,0.958842089365959,
15.9209731408593));
#270205=CARTESIAN_POINT('Ctrl Pts',(-1.09333104534222,1.11032665730706,
15.9051649285799));
#270206=CARTESIAN_POINT('Ctrl Pts',(-1.02512803857659,1.17359015713718,
15.8979363380555));
#270207=CARTESIAN_POINT('Ctrl Pts',(-0.944018339322086,1.23632663234336,
15.8903209042197));
#270208=CARTESIAN_POINT('Ctrl Pts',(-0.93629723493177,1.24218423213741,
15.8896050853797));
#270209=CARTESIAN_POINT('Ctrl Pts',(-0.924217891554731,1.25117157686216,
15.8884999080377));
#270210=CARTESIAN_POINT('Ctrl Pts',(-0.919897516201082,1.2543514609951,
15.8881075003065));
#270211=CARTESIAN_POINT('Ctrl Pts',(-0.911793773768553,1.26025159221254,
15.8873769453647));
#270212=CARTESIAN_POINT('Ctrl Pts',(-0.908014481900579,1.26297730135247,
15.8870384474337));
#270213=CARTESIAN_POINT('Ctrl Pts',(-0.901600430749328,1.26755958478693,
15.8864677617847));
#270214=CARTESIAN_POINT('Ctrl Pts',(-0.898972069865703,1.26942500999133,
15.8862349761029));
#270215=CARTESIAN_POINT('Ctrl Pts',(-0.893903015961476,1.27299902743729,
15.8857881109913));
#270216=CARTESIAN_POINT('Ctrl Pts',(-0.891463190891873,1.27470879242905,
15.8855739490452));
#270217=CARTESIAN_POINT('Ctrl Pts',(-0.885029707953356,1.27918970216261,
15.8850116115073));
#270218=CARTESIAN_POINT('Ctrl Pts',(-0.881027902956447,1.28194918541921,
15.8846642226194));
#270219=CARTESIAN_POINT('Ctrl Pts',(-0.867036088347509,1.29150091098132,
15.8834577085358));
#270220=CARTESIAN_POINT('Ctrl Pts',(-0.856979609319309,1.29819573045059,
15.8826048244042));
#270221=CARTESIAN_POINT('Ctrl Pts',(-0.765874142598457,1.35732653583144,
15.8749956956541));
#270222=CARTESIAN_POINT('Ctrl Pts',(-0.680172933462574,1.40223719870668,
15.8686579403287));
#270223=CARTESIAN_POINT('Ctrl Pts',(-0.481580870613016,1.48378322846103,
15.8545291965505));
#270224=CARTESIAN_POINT('Ctrl Pts',(-0.367575910434226,1.51605252721111,
15.8467542408138));
#270225=CARTESIAN_POINT('Ctrl Pts',(-0.237554502424209,1.53731403682826,
15.8375580332332));
#270226=CARTESIAN_POINT('Ctrl Pts',(-0.224054784418524,1.53933947594232,
15.8365998990486));
#270227=CARTESIAN_POINT('Ctrl Pts',(-0.203589011586023,1.54213515884334,
15.8351415475675));
#270228=CARTESIAN_POINT('Ctrl Pts',(-0.19664127367615,1.5430364676057,15.8346454578352));
#270229=CARTESIAN_POINT('Ctrl Pts',(-0.184059758045968,1.5445822763151,
15.8337451680965));
#270230=CARTESIAN_POINT('Ctrl Pts',(-0.178428060747985,1.54524296743774,
15.8333414848725));
#270231=CARTESIAN_POINT('Ctrl Pts',(-0.166331305626079,1.54659510577575,
15.8324728220715));
#270232=CARTESIAN_POINT('Ctrl Pts',(-0.159865293933973,1.54727683685333,
15.8320075451354));
#270233=CARTESIAN_POINT('Ctrl Pts',(-0.142463626944474,1.54900130398847,
15.8307526948474));
#270234=CARTESIAN_POINT('Ctrl Pts',(-0.131521065255699,1.54996874892331,
15.8299607792273));
#270235=CARTESIAN_POINT('Ctrl Pts',(-0.0791205196508659,1.554042660268,
15.8261542349543));
#270236=CARTESIAN_POINT('Ctrl Pts',(-0.037563078176485,1.55560183088846,
15.823091915796));
#270237=CARTESIAN_POINT('Ctrl Pts',(0.147616518815006,1.55512522061724,
15.8092397272847));
#270238=CARTESIAN_POINT('Ctrl Pts',(0.290479054988182,1.53486643416447,
15.7979142255212));
#270239=CARTESIAN_POINT('Ctrl Pts',(0.468613472780923,1.4838204924963,15.7837699061838));
#270240=CARTESIAN_POINT('Ctrl Pts',(0.508256883953022,1.4707132774537,15.7806276780636));
#270241=CARTESIAN_POINT('Ctrl Pts',(0.553953404949826,1.4535356749029,15.7770477936374));
#270242=CARTESIAN_POINT('Ctrl Pts',(0.560560874023978,1.45100029107967,
15.7765312228227));
#270243=CARTESIAN_POINT('Ctrl Pts',(0.570682756067301,1.44703691309852,
15.7757417753155));
#270244=CARTESIAN_POINT('Ctrl Pts',(0.574209517190068,1.44564105750517,
15.775467061043));
#270245=CARTESIAN_POINT('Ctrl Pts',(0.580678461139734,1.44305330850844,
15.7749638618381));
#270246=CARTESIAN_POINT('Ctrl Pts',(0.583622088372616,1.4418653143792,15.7747351559546));
#270247=CARTESIAN_POINT('Ctrl Pts',(0.590228337269242,1.4391756073858,15.7742224761117));
#270248=CARTESIAN_POINT('Ctrl Pts',(0.593888869289395,1.43766892255628,
15.7739388053781));
#270249=CARTESIAN_POINT('Ctrl Pts',(0.604585858185119,1.43321818572596,
15.773110924296));
#270250=CARTESIAN_POINT('Ctrl Pts',(0.611606595866989,1.43023627628909,
15.7725689290351));
#270251=CARTESIAN_POINT('Ctrl Pts',(0.662621819692862,1.40812428991122,
15.7686385510335));
#270252=CARTESIAN_POINT('Ctrl Pts',(0.705737631372396,1.38701737455483,
15.7653598328581));
#270253=CARTESIAN_POINT('Ctrl Pts',(0.830884781060122,1.31840281325852,
15.7557708201339));
#270254=CARTESIAN_POINT('Ctrl Pts',(0.909624761125001,1.26536163017004,
15.7496301680889));
#270255=CARTESIAN_POINT('Ctrl Pts',(1.04118128410883,1.15807940032096,15.7383734959797));
#270256=CARTESIAN_POINT('Ctrl Pts',(1.09579828535327,1.10653972841146,15.7333275347108));
#270257=CARTESIAN_POINT('Ctrl Pts',(1.1572552109425,1.03951661073784,15.7269989430662));
#270258=CARTESIAN_POINT('Ctrl Pts',(1.1678479961554,1.02760178680621,15.725882299104));
#270259=CARTESIAN_POINT('Ctrl Pts',(1.18312271699436,1.00987943227182,15.7242322736868));
#270260=CARTESIAN_POINT('Ctrl Pts',(1.1879492446031,1.00419740088748,15.723704857187));
#270261=CARTESIAN_POINT('Ctrl Pts',(1.19640548705963,0.994096003161028,
15.722769912651));
#270262=CARTESIAN_POINT('Ctrl Pts',(1.20005205446257,0.989690869892641,
15.7223630803908));
#270263=CARTESIAN_POINT('Ctrl Pts',(1.20713797849269,0.981034176317199,
15.7215652709919));
#270264=CARTESIAN_POINT('Ctrl Pts',(1.2105793729228,0.976784384941612,15.7211743841208));
#270265=CARTESIAN_POINT('Ctrl Pts',(1.21983230208397,0.965233898349809,
15.7201140267467));
#270266=CARTESIAN_POINT('Ctrl Pts',(1.225600586333,0.957899013185116,15.7194428458201));
#270267=CARTESIAN_POINT('Ctrl Pts',(1.24716338059975,0.929966385597103,
15.7168946474326));
#270268=CARTESIAN_POINT('Ctrl Pts',(1.26250664122506,0.909027395911184,
15.7150001798617));
#270269=CARTESIAN_POINT('Ctrl Pts',(1.28071860612345,0.882822522779436,
15.7126466390402));
#270270=CARTESIAN_POINT('Ctrl Pts',(1.28409095564,0.877910115374345,15.7122061771278));
#270271=CARTESIAN_POINT('Ctrl Pts',(1.34546691838573,0.78739521878424,15.7041036790209));
#270272=CARTESIAN_POINT('Ctrl Pts',(1.39473129640741,0.696368618857575,
15.6961474234014));
#270273=CARTESIAN_POINT('Ctrl Pts',(1.43457669742932,0.601306867741246,
15.6881535475172));
#270274=CARTESIAN_POINT('Ctrl Pts',(1.43457668274383,0.601306902777371,
15.5515012983457));
#270275=CARTESIAN_POINT('Ctrl Pts',(1.42934844806766,0.613780239643622,
15.5525085349074));
#270276=CARTESIAN_POINT('Ctrl Pts',(1.42395721819853,0.626186141922541,
15.5535084794065));
#270277=CARTESIAN_POINT('Ctrl Pts',(1.41561724659483,0.644712461489998,
15.5549973208906));
#270278=CARTESIAN_POINT('Ctrl Pts',(1.41278964660618,0.650885370738069,
15.5554926512506));
#270279=CARTESIAN_POINT('Ctrl Pts',(1.40833348086355,0.660447721965127,
15.55625857616));
#270280=CARTESIAN_POINT('Ctrl Pts',(1.40673293767129,0.663850005388352,
15.556530818317));
#270281=CARTESIAN_POINT('Ctrl Pts',(1.40373802512826,0.670156837512861,
15.5570349207783));
#270282=CARTESIAN_POINT('Ctrl Pts',(1.40234698007989,0.673062833517404,
15.5572669709428));
#270283=CARTESIAN_POINT('Ctrl Pts',(1.39915764745773,0.679672773936283,
15.5577942970538));
#270284=CARTESIAN_POINT('Ctrl Pts',(1.39735367740164,0.683373911833856,
15.5580892174614));
#270285=CARTESIAN_POINT('Ctrl Pts',(1.3926133340234,0.693002239854106,15.5588556440012));
#270286=CARTESIAN_POINT('Ctrl Pts',(1.38965377158621,0.698918022213251,
15.5593257593537));
#270287=CARTESIAN_POINT('Ctrl Pts',(1.36962984442554,0.738313201347103,
15.5624523506666));
#270288=CARTESIAN_POINT('Ctrl Pts',(1.3513931545769,0.771187014485425,15.5650417529206));
#270289=CARTESIAN_POINT('Ctrl Pts',(1.25506506696459,0.930898075588822,
15.5776864907652));
#270290=CARTESIAN_POINT('Ctrl Pts',(1.16023235582736,1.04672200712425,15.5871399182306));
#270291=CARTESIAN_POINT('Ctrl Pts',(1.03052492131856,1.16547098614687,15.5990848128733));
#270292=CARTESIAN_POINT('Ctrl Pts',(1.0102118927016,1.1831213073835,15.6009292642349));
#270293=CARTESIAN_POINT('Ctrl Pts',(0.974554263842389,1.21251681484336,
15.604132582659));
#270294=CARTESIAN_POINT('Ctrl Pts',(0.959429485372816,1.22451951576753,
15.6054811898572));
#270295=CARTESIAN_POINT('Ctrl Pts',(0.937640810738469,1.24115902391904,
15.6074120797511));
#270296=CARTESIAN_POINT('Ctrl Pts',(0.931157555623165,1.246030342628,15.6079851562898));
#270297=CARTESIAN_POINT('Ctrl Pts',(0.919906685743735,1.25434705585255,
15.6089773184488));
#270298=CARTESIAN_POINT('Ctrl Pts',(0.915157022637549,1.25781654830282,
15.6093954596554));
#270299=CARTESIAN_POINT('Ctrl Pts',(0.906019661718658,1.26441197601966,
15.6101985862839));
#270300=CARTESIAN_POINT('Ctrl Pts',(0.901635169418222,1.26754222511353,
15.6105833979205));
#270301=CARTESIAN_POINT('Ctrl Pts',(0.891298315762892,1.2748413123673,15.6114893657844));
#270302=CARTESIAN_POINT('Ctrl Pts',(0.885332870111243,1.27899130770212,
15.6120112303675));
#270303=CARTESIAN_POINT('Ctrl Pts',(0.864615643544258,1.29318931902059,
15.6138204236947));
#270304=CARTESIAN_POINT('Ctrl Pts',(0.849720648974535,1.30302478692408,
15.615115677387));
#270305=CARTESIAN_POINT('Ctrl Pts',(0.728275641506958,1.3802495425295,15.6256369559465));
#270306=CARTESIAN_POINT('Ctrl Pts',(0.61408279200549,1.43469969242128,15.6353461738357));
#270307=CARTESIAN_POINT('Ctrl Pts',(0.444520143592107,1.49156719770015,
15.6492135003694));
#270308=CARTESIAN_POINT('Ctrl Pts',(0.393609754801732,1.50580304159952,
15.6533033741496));
#270309=CARTESIAN_POINT('Ctrl Pts',(0.306242534213506,1.52549818145962,
15.6601144994287));
#270310=CARTESIAN_POINT('Ctrl Pts',(0.270135121165863,1.53230439260416,
15.6628705570639));
#270311=CARTESIAN_POINT('Ctrl Pts',(0.226981413298368,1.53886565228877,
15.6660701444033));
#270312=CARTESIAN_POINT('Ctrl Pts',(0.220138631157557,1.53985942398576,
15.6665746924036));
#270313=CARTESIAN_POINT('Ctrl Pts',(0.209538179049052,1.54132681216738,
15.6673517447645));
#270314=CARTESIAN_POINT('Ctrl Pts',(0.205785139586706,1.54183237335995,
15.6676259725834));
#270315=CARTESIAN_POINT('Ctrl Pts',(0.198838445709416,1.54274232613377,
15.6681318746976));
#270316=CARTESIAN_POINT('Ctrl Pts',(0.195645404825771,1.54315050733253,
15.6683637509709));
#270317=CARTESIAN_POINT('Ctrl Pts',(0.188401678718804,1.54405366148103,
15.6688883046321));
#270318=CARTESIAN_POINT('Ctrl Pts',(0.184350302424393,1.54454260837944,
15.6691806416247));
#270319=CARTESIAN_POINT('Ctrl Pts',(0.172289696565317,1.54595003162697,
15.670047929346));
#270320=CARTESIAN_POINT('Ctrl Pts',(0.164275035421767,1.54682221343174,
15.6706203700988));
#270321=CARTESIAN_POINT('Ctrl Pts',(0.0878890321656346,1.55453438098304,
15.6760422108649));
#270322=CARTESIAN_POINT('Ctrl Pts',(0.0191314642421557,1.5569002588872,
15.6806650907233));
#270323=CARTESIAN_POINT('Ctrl Pts',(-0.123717841429334,1.5523460265859,
15.6901466418542));
#270324=CARTESIAN_POINT('Ctrl Pts',(-0.197605372077892,1.54468010560252,
15.6949846986021));
#270325=CARTESIAN_POINT('Ctrl Pts',(-0.341552558709919,1.51924459721154,
15.7046827646893));
#270326=CARTESIAN_POINT('Ctrl Pts',(-0.411477035943539,1.5018145355335,
15.7095263283126));
#270327=CARTESIAN_POINT('Ctrl Pts',(-0.496337524567553,1.47428849324218,
15.715725298707));
#270328=CARTESIAN_POINT('Ctrl Pts',(-0.512647105714802,1.46869683845198,
15.7169315538374));
#270329=CARTESIAN_POINT('Ctrl Pts',(-0.536149195959212,1.46020011284151,
15.7186930244006));
#270330=CARTESIAN_POINT('Ctrl Pts',(-0.543418644266888,1.45751037835709,
15.7192411255614));
#270331=CARTESIAN_POINT('Ctrl Pts',(-0.556111993204555,1.45270561019864,
15.7202040481441));
#270332=CARTESIAN_POINT('Ctrl Pts',(-0.561544736460079,1.45061423064821,
15.720618074617));
#270333=CARTESIAN_POINT('Ctrl Pts',(-0.572064696659957,1.44649653224233,
15.7214235453037));
#270334=CARTESIAN_POINT('Ctrl Pts',(-0.577153212239487,1.44447374608946,
15.7218148659096));
#270335=CARTESIAN_POINT('Ctrl Pts',(-0.589291257647919,1.43957425460287,
15.7227524766097));
#270336=CARTESIAN_POINT('Ctrl Pts',(-0.596330495111955,1.43667259931803,
15.7232996007539));
#270337=CARTESIAN_POINT('Ctrl Pts',(-0.621749120791783,1.42597575204317,
15.7252877228035));
#270338=CARTESIAN_POINT('Ctrl Pts',(-0.639998589627072,1.41787889153704,
15.7267388683028));
#270339=CARTESIAN_POINT('Ctrl Pts',(-0.820527571616443,1.33358709687311,
15.7413401328465));
#270340=CARTESIAN_POINT('Ctrl Pts',(-0.968618873358817,1.23022956974228,
15.7555528068988));
#270341=CARTESIAN_POINT('Ctrl Pts',(-1.11981784811301,1.08015464159224,
15.771716709502));
#270342=CARTESIAN_POINT('Ctrl Pts',(-1.14306003135819,1.05552842900918,
15.774251600495));
#270343=CARTESIAN_POINT('Ctrl Pts',(-1.16996165699715,1.025093031421,15.7772281100735));
#270344=CARTESIAN_POINT('Ctrl Pts',(-1.17440826799998,1.01999569923434,
15.7777215616844));
#270345=CARTESIAN_POINT('Ctrl Pts',(-1.18127109364515,1.01202418380928,
15.778485216888));
#270346=CARTESIAN_POINT('Ctrl Pts',(-1.18371031895236,1.00917006837892,
15.7787570528064));
#270347=CARTESIAN_POINT('Ctrl Pts',(-1.18822393676091,1.00384984449521,
15.7792607926071));
#270348=CARTESIAN_POINT('Ctrl Pts',(-1.19030098197612,1.00138614271979,
15.7794928838574));
#270349=CARTESIAN_POINT('Ctrl Pts',(-1.19501945585576,0.995753868258473,
15.7800208020681));
#270350=CARTESIAN_POINT('Ctrl Pts',(-1.19765594509,0.992581233086318,15.7803162702837));
#270351=CARTESIAN_POINT('Ctrl Pts',(-1.20450351664006,0.98427416034673,
15.7810850677255));
#270352=CARTESIAN_POINT('Ctrl Pts',(-1.20869445583477,0.97912310815566,
15.7815569920491));
#270353=CARTESIAN_POINT('Ctrl Pts',(-1.23688489886833,0.944017597118781,
15.7847421845554));
#270354=CARTESIAN_POINT('Ctrl Pts',(-1.25980400446532,0.913207510243438,
15.787385415763));
#270355=CARTESIAN_POINT('Ctrl Pts',(-1.36649169966915,0.758114147660761,
15.8001380528514));
#270356=CARTESIAN_POINT('Ctrl Pts',(-1.43313778581445,0.623024121988957,
15.8096491627439));
#270357=CARTESIAN_POINT('Ctrl Pts',(-1.49155088772275,0.443165068054534,
15.8225100803645));
#270358=CARTESIAN_POINT('Ctrl Pts',(-1.50225208250412,0.405410368434929,
15.8252143780538));
#270359=CARTESIAN_POINT('Ctrl Pts',(-1.51399866275157,0.357070026138771,
15.8287028112708));
#270360=CARTESIAN_POINT('Ctrl Pts',(-1.51637923511729,0.346821221994342,
15.8294438262542));
#270361=CARTESIAN_POINT('Ctrl Pts',(-1.520037726189,0.330312531122009,15.8306400884911));
#270362=CARTESIAN_POINT('Ctrl Pts',(-1.5213813999129,0.324067417434184,
15.8310932293327));
#270363=CARTESIAN_POINT('Ctrl Pts',(-1.52386624949489,0.312162203669072,
15.8319582958353));
#270364=CARTESIAN_POINT('Ctrl Pts',(-1.5250144553291,0.306503665778198,
15.8323699895656));
#270365=CARTESIAN_POINT('Ctrl Pts',(-1.52756450164253,0.293567491085846,
15.8333124494089));
#270366=CARTESIAN_POINT('Ctrl Pts',(-1.52894587651818,0.286286013732919,
15.8338438562475));
#270367=CARTESIAN_POINT('Ctrl Pts',(-1.53241339035425,0.267266858826115,
15.8352344206141));
#270368=CARTESIAN_POINT('Ctrl Pts',(-1.53441668264626,0.255514778583605,
15.836096174526));
#270369=CARTESIAN_POINT('Ctrl Pts',(-1.54914924951,0.162656358876138,15.8429265024275));
#270370=CARTESIAN_POINT('Ctrl Pts',(-1.55557208489254,0.0806950259623673,
15.8490932619655));
#270371=CARTESIAN_POINT('Ctrl Pts',(-1.5554120703512,-0.0999616197188796,
15.8629544420336));
#270372=CARTESIAN_POINT('Ctrl Pts',(-1.54595327256803,-0.198309895053453,
15.870680526702));
#270373=CARTESIAN_POINT('Ctrl Pts',(-1.5193725451513,-0.335874966079489,
15.8813781973874));
#270374=CARTESIAN_POINT('Ctrl Pts',(-1.50986320948355,-0.376322676413595,
15.8845068123646));
#270375=CARTESIAN_POINT('Ctrl Pts',(-1.49692813352857,-0.422885912252754,
15.8880540353352));
#270376=CARTESIAN_POINT('Ctrl Pts',(-1.4950683214219,-0.429414776749792,
15.888550136866));
#270377=CARTESIAN_POINT('Ctrl Pts',(-1.49199730164097,-0.439933728839646,
15.8893471438969));
#270378=CARTESIAN_POINT('Ctrl Pts',(-1.49081271558257,-0.443931393381345,
15.8896495066573));
#270379=CARTESIAN_POINT('Ctrl Pts',(-1.48868296448025,-0.451014069723026,
15.8901841951944));
#270380=CARTESIAN_POINT('Ctrl Pts',(-1.48774426167838,-0.454100949576394,
15.8904168874582));
#270381=CARTESIAN_POINT('Ctrl Pts',(-1.4857013661754,-0.460744581512379,
15.890916939358));
#270382=CARTESIAN_POINT('Ctrl Pts',(-1.48459400439268,-0.464300292653457,
15.891184111735));
#270383=CARTESIAN_POINT('Ctrl Pts',(-1.48148127871369,-0.474170180518937,
15.8919245397757));
#270384=CARTESIAN_POINT('Ctrl Pts',(-1.4794482989959,-0.480475674788657,
15.8923962201653));
#270385=CARTESIAN_POINT('Ctrl Pts',(-1.4675348760013,-0.516633739557499,
15.8950942856192));
#270386=CARTESIAN_POINT('Ctrl Pts',(-1.45679045193464,-0.546196822495111,
15.8972738476213));
#270387=CARTESIAN_POINT('Ctrl Pts',(-1.41785960741151,-0.643971496555455,
15.9044581095223));
#270388=CARTESIAN_POINT('Ctrl Pts',(-1.38571700242618,-0.710503683917368,
15.9093094563308));
#270389=CARTESIAN_POINT('Ctrl Pts',(-1.29437567048341,-0.869594070895327,
15.9213839861234));
#270390=CARTESIAN_POINT('Ctrl Pts',(-1.22988950761889,-0.958629108956368,
15.9285993075028));
#270391=CARTESIAN_POINT('Ctrl Pts',(-1.14410059163391,-1.05402212292164,
15.9374948780266));
#270392=CARTESIAN_POINT('Ctrl Pts',(-1.13136816714337,-1.06767730036343,
15.9387989510139));
#270393=CARTESIAN_POINT('Ctrl Pts',(-1.11324609141095,-1.08642452184601,
15.9406349142027));
#270394=CARTESIAN_POINT('Ctrl Pts',(-1.10806077413058,-1.09171260830882,
15.9411580139155));
#270395=CARTESIAN_POINT('Ctrl Pts',(-1.09901415828145,-1.10080767166477,
15.9420669427638));
#270396=CARTESIAN_POINT('Ctrl Pts',(-1.09517031658875,-1.10463189633755,
15.942452002397));
#270397=CARTESIAN_POINT('Ctrl Pts',(-1.08713454834094,-1.11254348322454,
15.9432546932393));
#270398=CARTESIAN_POINT('Ctrl Pts',(-1.08293938958395,-1.11662742444639,
15.9436724648996));
#270399=CARTESIAN_POINT('Ctrl Pts',(-1.07299021366747,-1.12620403516568,
15.9446603115157));
#270400=CARTESIAN_POINT('Ctrl Pts',(-1.0672169687623,-1.13167639574182,
15.9452312491333));
#270401=CARTESIAN_POINT('Ctrl Pts',(-1.04795443279522,-1.14965653971391,
15.9471289039081));
#270402=CARTESIAN_POINT('Ctrl Pts',(-1.03428571218525,-1.16196887400984,
15.9484638206013));
#270403=CARTESIAN_POINT('Ctrl Pts',(-1.00132795128539,-1.19061381683405,
15.9516567169589));
#270404=CARTESIAN_POINT('Ctrl Pts',(-0.981853395783587,-1.20672395402667,
15.9535232064232));
#270405=CARTESIAN_POINT('Ctrl Pts',(-0.843711303932902,-1.31544237099492,
15.966629289372));
#270406=CARTESIAN_POINT('Ctrl Pts',(-0.712545280346618,-1.39086371500204,
15.9785143108742));
#270407=CARTESIAN_POINT('Ctrl Pts',(-0.53650775481938,-1.46056489265463,
15.9929430332127));
#270408=CARTESIAN_POINT('Ctrl Pts',(-0.499849217277457,-1.47351340759649,
15.9958652416534));
#270409=CARTESIAN_POINT('Ctrl Pts',(-0.456377607788493,-1.48705889158308,
15.9992064405419));
#270410=CARTESIAN_POINT('Ctrl Pts',(-0.450001837833795,-1.4890006776742,
15.9996933928782));
#270411=CARTESIAN_POINT('Ctrl Pts',(-0.439652887823633,-1.49207997929655,
16.0004785944465));
#270412=CARTESIAN_POINT('Ctrl Pts',(-0.435687399434212,-1.49324271886152,
16.0007782337497));
#270413=CARTESIAN_POINT('Ctrl Pts',(-0.428620852744101,-1.4952841878815,
16.0013099459183));
#270414=CARTESIAN_POINT('Ctrl Pts',(-0.425521657526806,-1.49616909392795,
16.0015423696985));
#270415=CARTESIAN_POINT('Ctrl Pts',(-0.418811303747745,-1.49806254829275,
16.0020439375468));
#270416=CARTESIAN_POINT('Ctrl Pts',(-0.415199246348476,-1.4990676747164,
16.0023128829537));
#270417=CARTESIAN_POINT('Ctrl Pts',(-0.40508342294535,-1.50184323509203,
16.0030632719579));
#270418=CARTESIAN_POINT('Ctrl Pts',(-0.39857162590491,-1.50358449904523,
16.0035430705299));
#270419=CARTESIAN_POINT('Ctrl Pts',(-0.359703204987075,-1.51370771449768,
16.0063887985263));
#270420=CARTESIAN_POINT('Ctrl Pts',(-0.327091621469221,-1.52108807554105,
16.008701697389));
#270421=CARTESIAN_POINT('Ctrl Pts',(-0.128081056059097,-1.55942857772257,
16.0225077268172));
#270422=CARTESIAN_POINT('Ctrl Pts',(0.0422172938819871,-1.56411338524212,
16.0331544213128));
#270423=CARTESIAN_POINT('Ctrl Pts',(0.214032242580014,-1.54071006648652,
16.045062626977));
#270424=CARTESIAN_POINT('Ctrl Pts',(0.218122538668752,-1.54013631456753,
16.0453467197997));
#270425=CARTESIAN_POINT('Ctrl Pts',(0.246516970173361,-1.53603800322895,
16.0473231770209));
#270426=CARTESIAN_POINT('Ctrl Pts',(0.270735733481293,-1.531954767939,16.0490310229766));
#270427=CARTESIAN_POINT('Ctrl Pts',(0.303875700185424,-1.5255570694587,
16.0514031683096));
#270428=CARTESIAN_POINT('Ctrl Pts',(0.312889008325581,-1.5237339909968,
16.0520519346301));
#270429=CARTESIAN_POINT('Ctrl Pts',(0.32725581576149,-1.52069523972461,
16.0530920280967));
#270430=CARTESIAN_POINT('Ctrl Pts',(0.332620066055354,-1.51953093792877,
16.0534817146912));
#270431=CARTESIAN_POINT('Ctrl Pts',(0.343653491025345,-1.51707492748415,
16.054286055969));
#270432=CARTESIAN_POINT('Ctrl Pts',(0.349321802615655,-1.51577977754852,
16.0547008149319));
#270433=CARTESIAN_POINT('Ctrl Pts',(0.362485064934866,-1.51269435326561,
16.0556676381989));
#270434=CARTESIAN_POINT('Ctrl Pts',(0.369974181756807,-1.51088011753997,
16.05622046249));
#270435=CARTESIAN_POINT('Ctrl Pts',(0.393931925753363,-1.50488755703987,
16.0579980054344));
#270436=CARTESIAN_POINT('Ctrl Pts',(0.410345176873168,-1.50049515652697,
16.0592295607999));
#270437=CARTESIAN_POINT('Ctrl Pts',(0.493962508726928,-1.47664355403327,
16.0655769830527));
#270438=CARTESIAN_POINT('Ctrl Pts',(0.559860743095888,-1.4529378671706,
16.07082858045));
#270439=CARTESIAN_POINT('Ctrl Pts',(0.717574364942324,-1.38387771829978,
16.0840015443296));
#270440=CARTESIAN_POINT('Ctrl Pts',(0.806940907251016,-1.33374490097917,
16.0920163453326));
#270441=CARTESIAN_POINT('Ctrl Pts',(0.902666854512966,-1.26687979351112,
16.1009460085624));
#270442=CARTESIAN_POINT('Ctrl Pts',(0.914475397680684,-1.25838254646261,
16.102053628093));
#270443=CARTESIAN_POINT('Ctrl Pts',(0.950787795580712,-1.23147156331882,
16.1054749978316));
#270444=CARTESIAN_POINT('Ctrl Pts',(0.974869746746093,-1.21249699033323,
16.1077662230733));
#270445=CARTESIAN_POINT('Ctrl Pts',(1.00360837571268,-1.18844310502144,
16.110513249889));
#270446=CARTESIAN_POINT('Ctrl Pts',(1.00881081194145,-1.18403020906588,
16.111011057188));
#270447=CARTESIAN_POINT('Ctrl Pts',(1.01687233312155,-1.17710042620274,
16.1117830414109));
#270448=CARTESIAN_POINT('Ctrl Pts',(1.01975140515304,-1.17460709506081,
16.1120588663488));
#270449=CARTESIAN_POINT('Ctrl Pts',(1.02504562078543,-1.1699880666837,16.1125662466186));
#270450=CARTESIAN_POINT('Ctrl Pts',(1.02746331299255,-1.16786546388028,
16.1127980136026));
#270451=CARTESIAN_POINT('Ctrl Pts',(1.03291174020139,-1.16305202460563,
16.1133204753159));
#270452=CARTESIAN_POINT('Ctrl Pts',(1.03593855155773,-1.16035683881633,
16.1136108412362));
#270453=CARTESIAN_POINT('Ctrl Pts',(1.04505212702312,-1.15217768719108,
16.1144856035957));
#270454=CARTESIAN_POINT('Ctrl Pts',(1.05110626241287,-1.14665731757139,
16.1150673656332));
#270455=CARTESIAN_POINT('Ctrl Pts',(1.12538028097479,-1.07784911003095,
16.1222170814118));
#270456=CARTESIAN_POINT('Ctrl Pts',(1.18784364608688,-1.00859946737058,
16.1283670068836));
#270457=CARTESIAN_POINT('Ctrl Pts',(1.31571249277058,-0.838355549884314,
16.1423918693914));
#270458=CARTESIAN_POINT('Ctrl Pts',(1.37635565566783,-0.734561096730959,
16.1502323200143));
#270459=CARTESIAN_POINT('Ctrl Pts',(1.43183283736425,-0.60808692592948,
16.159812664107));
#270460=CARTESIAN_POINT('Ctrl Pts',(1.43888574261177,-0.591204494469641,
16.1610910562212));
#270461=CARTESIAN_POINT('Ctrl Pts',(1.44834531423227,-0.567388623149606,
16.1628957474056));
#270462=CARTESIAN_POINT('Ctrl Pts',(1.4510033914926,-0.56055611094073,16.1634136353778));
#270463=CARTESIAN_POINT('Ctrl Pts',(1.45553641666728,-0.548655798566441,
16.1643160227701));
#270464=CARTESIAN_POINT('Ctrl Pts',(1.45743345924851,-0.543596501153376,
16.1646997796119));
#270465=CARTESIAN_POINT('Ctrl Pts',(1.46133592356034,-0.533021586576347,
16.1655022024487));
#270466=CARTESIAN_POINT('Ctrl Pts',(1.46333656278031,-0.527504308549459,
16.1659210200159));
#270467=CARTESIAN_POINT('Ctrl Pts',(1.46800248658415,-0.514405991977171,
16.1669157838157));
#270468=CARTESIAN_POINT('Ctrl Pts',(1.47064031787978,-0.506815426101302,
16.1674926266324));
#270469=CARTESIAN_POINT('Ctrl Pts',(1.47927520391315,-0.481332743861357,
16.1694306406548));
#270470=CARTESIAN_POINT('Ctrl Pts',(1.48500525660034,-0.463352639903636,
16.1708004984707));
#270471=CARTESIAN_POINT('Ctrl Pts',(1.49788326072202,-0.42024775313346,
16.1740918068332));
#270472=CARTESIAN_POINT('Ctrl Pts',(1.50472800136901,-0.395039150347152,
16.1760224843062));
#270473=CARTESIAN_POINT('Ctrl Pts',(1.54650760837292,-0.224276054029034,
16.189143502219));
#270474=CARTESIAN_POINT('Ctrl Pts',(1.56090331708873,-0.0745135463966356,
16.2009647394349));
#270475=CARTESIAN_POINT('Ctrl Pts',(1.55185140635719,0.113131397764378,
16.2152746077481));
#270476=CARTESIAN_POINT('Ctrl Pts',(1.54860247285123,0.151236506442244,
16.2181478669469));
#270477=CARTESIAN_POINT('Ctrl Pts',(1.54314555494617,0.195770376752052,
16.2214399345214));
#270478=CARTESIAN_POINT('Ctrl Pts',(1.54229672266842,0.202348875941217,
16.2219245297602));
#270479=CARTESIAN_POINT('Ctrl Pts',(1.54085207858474,0.21300732200163,16.2227066868933));
#270480=CARTESIAN_POINT('Ctrl Pts',(1.54028209219645,0.217090591289451,
16.2230056217683));
#270481=CARTESIAN_POINT('Ctrl Pts',(1.53923771138108,0.224361094183342,
16.2235365689481));
#270482=CARTESIAN_POINT('Ctrl Pts',(1.53876964281009,0.227549159070106,
16.2237689281331));
#270483=CARTESIAN_POINT('Ctrl Pts',(1.53773451178213,0.234450269018181,
16.2242709101417));
#270484=CARTESIAN_POINT('Ctrl Pts',(1.53716390735117,0.238162717723234,
16.2245403312696));
#270485=CARTESIAN_POINT('Ctrl Pts',(1.53552692771861,0.248562178244353,
16.2252933996548));
#270486=CARTESIAN_POINT('Ctrl Pts',(1.53443030930661,0.255244456456546,
16.2257753828915));
#270487=CARTESIAN_POINT('Ctrl Pts',(1.5275676521542,0.295418796690088,16.2286627783639));
#270488=CARTESIAN_POINT('Ctrl Pts',(1.52074838454615,0.328724793222004,
16.2310133341582));
#270489=CARTESIAN_POINT('Ctrl Pts',(1.49324451285637,0.443735601225883,
16.2390641417353));
#270490=CARTESIAN_POINT('Ctrl Pts',(1.46705034582479,0.523832441439846,
16.2445596914745));
#270491=CARTESIAN_POINT('Ctrl Pts',(1.43457653793677,0.601307248252799,
16.2500928067243));
#270492=CARTESIAN_POINT('Origin',(0.,0.,-1.29405622560371));
#270493=CARTESIAN_POINT('',(1.43457668369174,0.601306900515888,17.0878643847065));
#270494=CARTESIAN_POINT('',(1.4345766824505,0.601306903477194,16.9487204703706));
#270495=CARTESIAN_POINT('',(1.43457668357355,0.601306900797845,-1.29405622560371));
#270496=CARTESIAN_POINT('Ctrl Pts',(1.43457668369174,0.601306900515888,
17.0878643847065));
#270497=CARTESIAN_POINT('Ctrl Pts',(1.46485147221303,0.529078383465645,
17.0827019053849));
#270498=CARTESIAN_POINT('Ctrl Pts',(1.48962766213377,0.454668124152851,
17.0775806645933));
#270499=CARTESIAN_POINT('Ctrl Pts',(1.51793983480686,0.341878389690674,
17.0697763105215));
#270500=CARTESIAN_POINT('Ctrl Pts',(1.52583248471291,0.304724565586252,
17.067200233606));
#270501=CARTESIAN_POINT('Ctrl Pts',(1.535236909699,0.250815869464161,17.0634298083927));
#270502=CARTESIAN_POINT('Ctrl Pts',(1.53784933366876,0.234265575817172,
17.0622679549121));
#270503=CARTESIAN_POINT('Ctrl Pts',(1.54205269612597,0.204524271440075,
17.060170295671));
#270504=CARTESIAN_POINT('Ctrl Pts',(1.54374295426395,0.191348810213299,
17.0592376115309));
#270505=CARTESIAN_POINT('Ctrl Pts',(1.5460579799202,0.171268806576169,17.0578102390323));
#270506=CARTESIAN_POINT('Ctrl Pts',(1.5468057028868,0.164378818842778,17.0573194132758));
#270507=CARTESIAN_POINT('Ctrl Pts',(1.54808095594149,0.151847632093962,
17.0564246979273));
#270508=CARTESIAN_POINT('Ctrl Pts',(1.54862375870161,0.146208077577833,
17.0560212950401));
#270509=CARTESIAN_POINT('Ctrl Pts',(1.54972849489882,0.134033089691732,
17.0551487397923));
#270510=CARTESIAN_POINT('Ctrl Pts',(1.55027992016421,0.127496838124804,
17.054679265863));
#270511=CARTESIAN_POINT('Ctrl Pts',(1.55166370731226,0.109755356467329,
17.0534020490485));
#270512=CARTESIAN_POINT('Ctrl Pts',(1.55241601186724,0.0985444703630529,
17.0525918197777));
#270513=CARTESIAN_POINT('Ctrl Pts',(1.55556657379776,0.0425138312444026,
17.0485258351188));
#270514=CARTESIAN_POINT('Ctrl Pts',(1.55614535237466,-0.00238242058257087,
17.0452140644875));
#270515=CARTESIAN_POINT('Ctrl Pts',(1.55022249010626,-0.197330826533279,
17.0305862958485));
#270516=CARTESIAN_POINT('Ctrl Pts',(1.52395590129271,-0.345941650565378,
17.0186976790508));
#270517=CARTESIAN_POINT('Ctrl Pts',(1.46668625166107,-0.519087295236012,
17.0048794168187));
#270518=CARTESIAN_POINT('Ctrl Pts',(1.45560886776008,-0.549384554985741,
17.0024674184821));
#270519=CARTESIAN_POINT('Ctrl Pts',(1.44113246698195,-0.585458140215961,
16.9996200489091));
#270520=CARTESIAN_POINT('Ctrl Pts',(1.43862925210175,-0.591582539082508,
16.9991375067435));
#270521=CARTESIAN_POINT('Ctrl Pts',(1.43466771577604,-0.601101021765354,
16.9983891080523));
#270522=CARTESIAN_POINT('Ctrl Pts',(1.43323629207973,-0.604506099965401,
16.9981216945372));
#270523=CARTESIAN_POINT('Ctrl Pts',(1.43054879111752,-0.610835933435642,
16.9976252166475));
#270524=CARTESIAN_POINT('Ctrl Pts',(1.42929587756749,-0.613761904999399,
16.9973959751171));
#270525=CARTESIAN_POINT('Ctrl Pts',(1.42641331820236,-0.620436947642356,
16.9968735679961));
#270526=CARTESIAN_POINT('Ctrl Pts',(1.42477787000566,-0.624183452615307,
16.996580758669));
#270527=CARTESIAN_POINT('Ctrl Pts',(1.42046149163215,-0.633966104729296,
16.99581713422));
#270528=CARTESIAN_POINT('Ctrl Pts',(1.41775681636755,-0.639991785030695,
16.995347717012));
#270529=CARTESIAN_POINT('Ctrl Pts',(1.39894172088783,-0.681204805565765,
16.9921423413064));
#270530=CARTESIAN_POINT('Ctrl Pts',(1.38155974331485,-0.715801107936104,
16.9894777671423));
#270531=CARTESIAN_POINT('Ctrl Pts',(1.29103514846456,-0.880365057652797,
16.976757524794));
#270532=CARTESIAN_POINT('Ctrl Pts',(1.20075460499769,-1.00000449689836,
16.9672919631132));
#270533=CARTESIAN_POINT('Ctrl Pts',(1.07612343688604,-1.12349058272458,
16.9553656978949));
#270534=CARTESIAN_POINT('Ctrl Pts',(1.05696402724497,-1.14153390531805,
16.9535606220944));
#270535=CARTESIAN_POINT('Ctrl Pts',(1.0232478454372,-1.17170927270085,16.950422798444));
#270536=CARTESIAN_POINT('Ctrl Pts',(1.00890981438683,-1.18407757555334,
16.9490998309626));
#270537=CARTESIAN_POINT('Ctrl Pts',(0.988208376135252,-1.20128607833971,
16.9472035492496));
#270538=CARTESIAN_POINT('Ctrl Pts',(0.982027507472763,-1.20634406657612,
16.9466390822869));
#270539=CARTESIAN_POINT('Ctrl Pts',(0.971288221787149,-1.21499511349565,
16.9456610902617));
#270540=CARTESIAN_POINT('Ctrl Pts',(0.966748093993297,-1.21861070760625,
16.9452484782359));
#270541=CARTESIAN_POINT('Ctrl Pts',(0.958005463364686,-1.2254934175481,
16.9444554847823));
#270542=CARTESIAN_POINT('Ctrl Pts',(0.953806207871142,-1.22876454246446,
16.9440752703585));
#270543=CARTESIAN_POINT('Ctrl Pts',(0.94389513623882,-1.23640362556131,
16.9431794188314));
#270544=CARTESIAN_POINT('Ctrl Pts',(0.93816970111598,-1.24075362671324,
16.9426630849868));
#270545=CARTESIAN_POINT('Ctrl Pts',(0.918240942793458,-1.25567805275695,
16.9408697642755));
#270546=CARTESIAN_POINT('Ctrl Pts',(0.903887842906313,-1.26604917775412,
16.9395849603637));
#270547=CARTESIAN_POINT('Ctrl Pts',(0.78496497359218,-1.34892621341377,
16.9289901837927));
#270548=CARTESIAN_POINT('Ctrl Pts',(0.672056801019739,-1.40858009442183,
16.9191860684388));
#270549=CARTESIAN_POINT('Ctrl Pts',(0.504199142671074,-1.47245028350452,
16.9052594361015));
#270550=CARTESIAN_POINT('Ctrl Pts',(0.454306101138838,-1.48860107349504,
16.9012028041132));
#270551=CARTESIAN_POINT('Ctrl Pts',(0.368472821598813,-1.51166725673301,
16.8944448835673));
#270552=CARTESIAN_POINT('Ctrl Pts',(0.332929393732065,-1.51989100569227,
16.8917090163716));
#270553=CARTESIAN_POINT('Ctrl Pts',(0.290410768648681,-1.5281651227565,
16.888534291323));
#270554=CARTESIAN_POINT('Ctrl Pts',(0.283686466091494,-1.52942768726112,
16.8880351005877));
#270555=CARTESIAN_POINT('Ctrl Pts',(0.273271190817226,-1.53131221915521,
16.887266594048));
#270556=CARTESIAN_POINT('Ctrl Pts',(0.269586049045342,-1.53196528003321,
16.8869955864562));
#270557=CARTESIAN_POINT('Ctrl Pts',(0.262767579194244,-1.53314824699708,
16.8864958706089));
#270558=CARTESIAN_POINT('Ctrl Pts',(0.259635006466371,-1.53368184827483,
16.8862669634726));
#270559=CARTESIAN_POINT('Ctrl Pts',(0.252535145957948,-1.5348688593619,
16.8857496641785));
#270560=CARTESIAN_POINT('Ctrl Pts',(0.248566950899842,-1.5355164887707,
16.8854616008202));
#270561=CARTESIAN_POINT('Ctrl Pts',(0.238293718029,-1.53715226398202,16.884718473888));
#270562=CARTESIAN_POINT('Ctrl Pts',(0.231984947042247,-1.53811701985817,
16.8842646886189));
#270563=CARTESIAN_POINT('Ctrl Pts',(0.191740365933215,-1.54401809343218,
16.8813852305919));
#270564=CARTESIAN_POINT('Ctrl Pts',(0.15765191133053,-1.5478703322816,16.8790154595782));
#270565=CARTESIAN_POINT('Ctrl Pts',(0.103435768649945,-1.55218711416128,
16.8753158601897));
#270566=CARTESIAN_POINT('Ctrl Pts',(0.08338094353823,-1.55339353450533,
16.8739623380437));
#270567=CARTESIAN_POINT('Ctrl Pts',(-0.0197240895592042,-1.5575933109998,
16.8670553858614));
#270568=CARTESIAN_POINT('Ctrl Pts',(-0.102896028625891,-1.55431639394722,
16.861649172063));
#270569=CARTESIAN_POINT('Ctrl Pts',(-0.271201494249236,-1.53411086464129,
16.8504338057363));
#270570=CARTESIAN_POINT('Ctrl Pts',(-0.355972126701788,-1.51668284563349,
16.8446342439596));
#270571=CARTESIAN_POINT('Ctrl Pts',(-0.451075661100523,-1.48871534853524,
16.8377061688898));
#270572=CARTESIAN_POINT('Ctrl Pts',(-0.463256287901399,-1.48497011273172,
16.836810916571));
#270573=CARTESIAN_POINT('Ctrl Pts',(-0.481880793068728,-1.47899210053651,
16.8354292044706));
#270574=CARTESIAN_POINT('Ctrl Pts',(-0.488358509778034,-1.47686583528251,
16.8349462325171));
#270575=CARTESIAN_POINT('Ctrl Pts',(-0.50013819919708,-1.4729132616241,
16.8340634590291));
#270576=CARTESIAN_POINT('Ctrl Pts',(-0.505444702032444,-1.47110072606917,
16.8336641171281));
#270577=CARTESIAN_POINT('Ctrl Pts',(-0.517007306063693,-1.46708135555474,
16.8327902559369));
#270578=CARTESIAN_POINT('Ctrl Pts',(-0.52325929717968,-1.46486312115931,
16.8323153657752));
#270579=CARTESIAN_POINT('Ctrl Pts',(-0.540367899222976,-1.45866941171774,
16.8310091537131));
#270580=CARTESIAN_POINT('Ctrl Pts',(-0.551194482331632,-1.45461285172834,
16.830175153005));
#270581=CARTESIAN_POINT('Ctrl Pts',(-0.608004639160203,-1.43260163452344,
16.8257587722325));
#270582=CARTESIAN_POINT('Ctrl Pts',(-0.653154387550186,-1.41258820270241,
16.8221080483415));
#270583=CARTESIAN_POINT('Ctrl Pts',(-0.82774098791286,-1.32503877398737,
16.807410148088));
#270584=CARTESIAN_POINT('Ctrl Pts',(-0.948328741761421,-1.24159000017251,
16.7958582314524));
#270585=CARTESIAN_POINT('Ctrl Pts',(-1.07861014055851,-1.12123555442892,
16.782428785693));
#270586=CARTESIAN_POINT('Ctrl Pts',(-1.10105712124808,-1.09920088172291,
16.7800782784836));
#270587=CARTESIAN_POINT('Ctrl Pts',(-1.12736840889186,-1.07175737356725,
16.7772935629172));
#270588=CARTESIAN_POINT('Ctrl Pts',(-1.13188433666563,-1.06698699603247,
16.7768145139129));
#270589=CARTESIAN_POINT('Ctrl Pts',(-1.13888521816745,-1.05949718112267,
16.7760703398128));
#270590=CARTESIAN_POINT('Ctrl Pts',(-1.14139088962725,-1.05679735749544,
16.775803685409));
#270591=CARTESIAN_POINT('Ctrl Pts',(-1.14604487670847,-1.05174689481779,
16.7753078715292));
#270592=CARTESIAN_POINT('Ctrl Pts',(-1.14819554348618,-1.04939858224281,
16.7750785395331));
#270593=CARTESIAN_POINT('Ctrl Pts',(-1.15310087881565,-1.0440093141107,
16.7745549638485));
#270594=CARTESIAN_POINT('Ctrl Pts',(-1.15585073639902,-1.04096405359845,
16.7742610826111));
#270595=CARTESIAN_POINT('Ctrl Pts',(-1.16302928511924,-1.03295083356297,
16.7734928055837));
#270596=CARTESIAN_POINT('Ctrl Pts',(-1.1674382613916,-1.02796520010947,
16.7730198355505));
#270597=CARTESIAN_POINT('Ctrl Pts',(-1.19792797539884,-0.993038502859575,
16.769740032826));
#270598=CARTESIAN_POINT('Ctrl Pts',(-1.22288862889438,-0.962133552808118,
16.7670083772452));
#270599=CARTESIAN_POINT('Ctrl Pts',(-1.33664116407618,-0.809700973999434,
16.7541392857221));
#270600=CARTESIAN_POINT('Ctrl Pts',(-1.40866637824048,-0.676675914152685,
16.7445884700309));
#270601=CARTESIAN_POINT('Ctrl Pts',(-1.47345893538007,-0.499924124621506,
16.7317693357119));
#270602=CARTESIAN_POINT('Ctrl Pts',(-1.48515627741034,-0.464021334520767,
16.7291646076415));
#270603=CARTESIAN_POINT('Ctrl Pts',(-1.49836959416402,-0.417821773003317,
16.7257940241061));
#270604=CARTESIAN_POINT('Ctrl Pts',(-1.50110506510699,-0.407884847873317,
16.7250679959893));
#270605=CARTESIAN_POINT('Ctrl Pts',(-1.50535046715196,-0.391841521636461,
16.7238937687649));
#270606=CARTESIAN_POINT('Ctrl Pts',(-1.50692249265256,-0.385751741484423,
16.7234475809426));
#270607=CARTESIAN_POINT('Ctrl Pts',(-1.50984989893882,-0.374120404957784,
16.7225943955109));
#270608=CARTESIAN_POINT('Ctrl Pts',(-1.51121181353593,-0.368580585173296,
16.7221876160121));
#270609=CARTESIAN_POINT('Ctrl Pts',(-1.5142585999138,-0.3558864495967,16.7212544800439));
#270610=CARTESIAN_POINT('Ctrl Pts',(-1.51592328743781,-0.348727480400935,
16.7207274853312));
#270611=CARTESIAN_POINT('Ctrl Pts',(-1.52014502174021,-0.329970327526181,
16.7193446260913));
#270612=CARTESIAN_POINT('Ctrl Pts',(-1.5226200371931,-0.318354381078791,
16.7184861669611));
#270613=CARTESIAN_POINT('Ctrl Pts',(-1.54536881320966,-0.205248058170481,
16.710105289614));
#270614=CARTESIAN_POINT('Ctrl Pts',(-1.55559463716222,-0.102022711011283,
16.7022588051956));
#270615=CARTESIAN_POINT('Ctrl Pts',(-1.55539500295535,0.114702355763758,
16.6855071832301));
#270616=CARTESIAN_POINT('Ctrl Pts',(-1.54291906605899,0.227629022166531,
16.6766211945832));
#270617=CARTESIAN_POINT('Ctrl Pts',(-1.51586821381248,0.349066783705029,
16.6674237523592));
#270618=CARTESIAN_POINT('Ctrl Pts',(-1.51333234485893,0.359901784005148,
16.6666066131679));
#270619=CARTESIAN_POINT('Ctrl Pts',(-1.50967322038962,0.374813120533336,
16.6654877136615));
#270620=CARTESIAN_POINT('Ctrl Pts',(-1.50864937693395,0.378913138187209,
16.6651806549299));
#270621=CARTESIAN_POINT('Ctrl Pts',(-1.50686564642258,0.385934299246099,
16.6646559031947));
#270622=CARTESIAN_POINT('Ctrl Pts',(-1.50611395011581,0.388857466683658,
16.6644377506967));
#270623=CARTESIAN_POINT('Ctrl Pts',(-1.50453193483721,0.394936138309345,
16.663984801268));
#270624=CARTESIAN_POINT('Ctrl Pts',(-1.50370019119181,0.39809123523306,
16.6637500945618));
#270625=CARTESIAN_POINT('Ctrl Pts',(-1.50166427583753,0.405716757071498,
16.663183738763));
#270626=CARTESIAN_POINT('Ctrl Pts',(-1.50045004779117,0.41018451928302,
16.662852665635));
#270627=CARTESIAN_POINT('Ctrl Pts',(-1.49612362863004,0.425827314932196,
16.6616959145881));
#270628=CARTESIAN_POINT('Ctrl Pts',(-1.49290629471815,0.436973260888894,
16.6608760381759));
#270629=CARTESIAN_POINT('Ctrl Pts',(-1.47250438771779,0.504795476639918,
16.6559077510363));
#270630=CARTESIAN_POINT('Ctrl Pts',(-1.45221710042606,0.560495240825511,
16.6519149120071));
#270631=CARTESIAN_POINT('Ctrl Pts',(-1.40607871372675,0.667702278374972,
16.6441561599367));
#270632=CARTESIAN_POINT('Ctrl Pts',(-1.38044884964969,0.719197440059563,
16.6403926960556));
#270633=CARTESIAN_POINT('Ctrl Pts',(-1.34613548323605,0.779513621113158,
16.6358182669723));
#270634=CARTESIAN_POINT('Ctrl Pts',(-1.34012488293191,0.789802202578729,
16.6350319409928));
#270635=CARTESIAN_POINT('Ctrl Pts',(-1.2889156826116,0.875191130038503,
16.6284486981176));
#270636=CARTESIAN_POINT('Ctrl Pts',(-1.23756866300656,0.946405567453251,
16.6225729910319));
#270637=CARTESIAN_POINT('Ctrl Pts',(-1.17275402907612,1.02194416898097,
16.6156213096609));
#270638=CARTESIAN_POINT('Ctrl Pts',(-1.1649007450776,1.03088706342611,16.614786034343));
#270639=CARTESIAN_POINT('Ctrl Pts',(-1.15202788055219,1.04521105261589,
16.6134275341423));
#270640=CARTESIAN_POINT('Ctrl Pts',(-1.14707127330378,1.05064831065563,
16.6129069391673));
#270641=CARTESIAN_POINT('Ctrl Pts',(-1.13820265226072,1.0602393728886,16.6119797157614));
#270642=CARTESIAN_POINT('Ctrl Pts',(-1.13430597700229,1.06440723146045,
16.611573743941));
#270643=CARTESIAN_POINT('Ctrl Pts',(-1.1260686182145,1.07312125388745,16.6107184652592));
#270644=CARTESIAN_POINT('Ctrl Pts',(-1.12172314282997,1.07766272421838,
16.6102689562537));
#270645=CARTESIAN_POINT('Ctrl Pts',(-1.11019213510238,1.08956850966515,
16.6090804571449));
#270646=CARTESIAN_POINT('Ctrl Pts',(-1.1029609595622,1.09688797346021,16.6083394846244));
#270647=CARTESIAN_POINT('Ctrl Pts',(-1.06899859592078,1.13058958667524,
16.6048787703327));
#270648=CARTESIAN_POINT('Ctrl Pts',(-1.04139229346829,1.15606766786562,
16.6021202771157));
#270649=CARTESIAN_POINT('Ctrl Pts',(-0.898566181413095,1.27861333074479,
16.5880986431829));
#270650=CARTESIAN_POINT('Ctrl Pts',(-0.770600720303237,1.35957076732516,
16.5762068811241));
#270651=CARTESIAN_POINT('Ctrl Pts',(-0.596693210522621,1.43705293595673,
16.5616879313495));
#270652=CARTESIAN_POINT('Ctrl Pts',(-0.559730291076118,1.45184937140861,
16.5586935816575));
#270653=CARTESIAN_POINT('Ctrl Pts',(-0.515964199725549,1.46744864940867,
16.5552841035713));
#270654=CARTESIAN_POINT('Ctrl Pts',(-0.5096771450536,1.46964410865359,16.5547975507935));
#270655=CARTESIAN_POINT('Ctrl Pts',(-0.4994927147271,1.47312732718678,16.5540147946011));
#270656=CARTESIAN_POINT('Ctrl Pts',(-0.49560409132311,1.47444012421066,
16.5537171915272));
#270657=CARTESIAN_POINT('Ctrl Pts',(-0.488689114795489,1.4767441686675,
16.5531902834324));
#270658=CARTESIAN_POINT('Ctrl Pts',(-0.485664872710304,1.47774152771564,
16.5529606258042));
#270659=CARTESIAN_POINT('Ctrl Pts',(-0.47913668864465,1.4798722393654,16.5524665811086));
#270660=CARTESIAN_POINT('Ctrl Pts',(-0.475631782245464,1.48100243744932,
16.5522023794871));
#270661=CARTESIAN_POINT('Ctrl Pts',(-0.465867457944091,1.48411281985807,
16.5514691577558));
#270662=CARTESIAN_POINT('Ctrl Pts',(-0.45959936930184,1.48606587144153,
16.5510016896542));
#270663=CARTESIAN_POINT('Ctrl Pts',(-0.423296203274179,1.49712577940899,
16.5483117503545));
#270664=CARTESIAN_POINT('Ctrl Pts',(-0.393000756460136,1.50536242681236,
16.5461360464508));
#270665=CARTESIAN_POINT('Ctrl Pts',(-0.220541367577036,1.54668787780174,
16.5340284524399));
#270666=CARTESIAN_POINT('Ctrl Pts',(-0.0745197199249979,1.56055669520138,
16.5247666406067));
#270667=CARTESIAN_POINT('Ctrl Pts',(0.120650740593084,1.55160033741761,
16.5115900508908));
#270668=CARTESIAN_POINT('Ctrl Pts',(0.169854034310815,1.54698706618201,
16.5082072384773));
#270669=CARTESIAN_POINT('Ctrl Pts',(0.230199618560858,1.53841545335448,
16.5039410627464));
#270670=CARTESIAN_POINT('Ctrl Pts',(0.241629728667893,1.53666165207661,
16.5031278275039));
#270671=CARTESIAN_POINT('Ctrl Pts',(0.25958497877861,1.53370137379655,16.5018416961694));
#270672=CARTESIAN_POINT('Ctrl Pts',(0.266123937588478,1.53258027932054,
16.5013715016191));
#270673=CARTESIAN_POINT('Ctrl Pts',(0.278176142391241,1.53043448998946,
16.5005014308093));
#270674=CARTESIAN_POINT('Ctrl Pts',(0.283691428426807,1.52942174244735,
16.5001019399123));
#270675=CARTESIAN_POINT('Ctrl Pts',(0.295899394574699,1.52711174199839,
16.4992146594712));
#270676=CARTESIAN_POINT('Ctrl Pts',(0.302589231843184,1.52580027470608,
16.4987264250012));
#270677=CARTESIAN_POINT('Ctrl Pts',(0.321756296771107,1.52191177681647,
16.4973216715952));
#270678=CARTESIAN_POINT('Ctrl Pts',(0.334210508786813,1.51922542394985,
16.4964016910652));
#270679=CARTESIAN_POINT('Ctrl Pts',(0.430754504023246,1.4971564831268,16.4892120874183));
#270680=CARTESIAN_POINT('Ctrl Pts',(0.513117067217718,1.47096325188963,
16.4827224524802));
#270681=CARTESIAN_POINT('Ctrl Pts',(0.667557380823319,1.40729297229781,
16.4698865239128));
#270682=CARTESIAN_POINT('Ctrl Pts',(0.739728905204007,1.3707322643646,16.4635786113087));
#270683=CARTESIAN_POINT('Ctrl Pts',(0.856058764237086,1.29992809980425,
16.4530988785788));
#270684=CARTESIAN_POINT('Ctrl Pts',(0.901817872054727,1.26861173610823,
16.4488881690252));
#270685=CARTESIAN_POINT('Ctrl Pts',(0.952044217633804,1.23014375657088,
16.4442403209255));
#270686=CARTESIAN_POINT('Ctrl Pts',(0.958239394602735,1.2253240892562,16.4436665799035));
#270687=CARTESIAN_POINT('Ctrl Pts',(0.967541105962813,1.21797393486456,
16.4428047823928));
#270688=CARTESIAN_POINT('Ctrl Pts',(0.970674657794897,1.21547809829273,
16.442514398903));
#270689=CARTESIAN_POINT('Ctrl Pts',(0.976275803966315,1.21098137740805,
16.4419952867025));
#270690=CARTESIAN_POINT('Ctrl Pts',(0.978746931192432,1.20898502354244,
16.4417662463225));
#270691=CARTESIAN_POINT('Ctrl Pts',(0.984124807308284,1.20461309361595,
16.4412677552552));
#270692=CARTESIAN_POINT('Ctrl Pts',(0.987029074315152,1.20223456485563,
16.4409985215179));
#270693=CARTESIAN_POINT('Ctrl Pts',(0.995242888944374,1.19545781046219,
16.4402369015307));
#270694=CARTESIAN_POINT('Ctrl Pts',(1.00053193537072,1.19103469118462,16.4397462683783));
#270695=CARTESIAN_POINT('Ctrl Pts',(1.03444744237669,1.16228649729511,16.4365974357485));
#270696=CARTESIAN_POINT('Ctrl Pts',(1.06221705469526,1.13696390578309,16.4340066660361));
#270697=CARTESIAN_POINT('Ctrl Pts',(1.16537743360218,1.03581098158832,16.4242054798981));
#270698=CARTESIAN_POINT('Ctrl Pts',(1.23379573212081,0.953289370161784,
16.4173027414172));
#270699=CARTESIAN_POINT('Ctrl Pts',(1.337243725789,0.798522168580856,16.4049566985637));
#270700=CARTESIAN_POINT('Ctrl Pts',(1.37617118222644,0.729389158769463,
16.3996201717271));
#270701=CARTESIAN_POINT('Ctrl Pts',(1.41463274000653,0.646941084534134,
16.3932646970309));
#270702=CARTESIAN_POINT('Ctrl Pts',(1.41948336477519,0.636227569154962,
16.392439198595));
#270703=CARTESIAN_POINT('Ctrl Pts',(1.42715333419177,0.618762573683803,
16.3910935038768));
#270704=CARTESIAN_POINT('Ctrl Pts',(1.43004740958704,0.612044250784941,
16.3905758562236));
#270705=CARTESIAN_POINT('Ctrl Pts',(1.43345671918452,0.603973654829153,
16.3899539384062));
#270706=CARTESIAN_POINT('Ctrl Pts',(1.434017632541,0.602640664929218,16.3898512160938));
#270707=CARTESIAN_POINT('Ctrl Pts',(1.43457668357428,0.601306900796103,
16.3897484311226));
#270708=CARTESIAN_POINT('',(-1.55550041526741,0.000134513367580657,16.5574036059057));
#270709=CARTESIAN_POINT('Ctrl Pts',(1.43457653793677,0.601307248252799,
16.2500928067243));
#270710=CARTESIAN_POINT('Ctrl Pts',(1.40375589294166,0.674838000330927,
16.2553442444805));
#270711=CARTESIAN_POINT('Ctrl Pts',(1.3672790165716,0.746006945298649,16.2606305819942));
#270712=CARTESIAN_POINT('Ctrl Pts',(1.32228285271093,0.819258241307971,
16.2665149389514));
#270713=CARTESIAN_POINT('Ctrl Pts',(1.31912362583802,0.824335409140046,
16.2669251564596));
#270714=CARTESIAN_POINT('Ctrl Pts',(1.31502854246759,0.830832759401978,
16.2674532434056));
#270715=CARTESIAN_POINT('Ctrl Pts',(1.31411949431617,0.83226984579663,16.2675702432442));
#270716=CARTESIAN_POINT('Ctrl Pts',(1.29971672369564,0.854956317759878,
16.2694203970959));
#270717=CARTESIAN_POINT('Ctrl Pts',(1.28571221442915,0.875875473284353,
16.271170144239));
#270718=CARTESIAN_POINT('Ctrl Pts',(1.2658554292215,0.90403346813135,16.2735913319866));
#270719=CARTESIAN_POINT('Ctrl Pts',(1.2604361248971,0.911574049415152,16.2742463743444));
#270720=CARTESIAN_POINT('Ctrl Pts',(1.25169623176006,0.923508048038257,
16.2752939852326));
#270721=CARTESIAN_POINT('Ctrl Pts',(1.24841920170457,0.927933223238932,
16.27568486899));
#270722=CARTESIAN_POINT('Ctrl Pts',(1.24163876797836,0.936988329373549,
16.2764897828329));
#270723=CARTESIAN_POINT('Ctrl Pts',(1.23813280443094,0.941616225668033,
16.2769039085194));
#270724=CARTESIAN_POINT('Ctrl Pts',(1.22994782061302,0.952295711886498,
16.2778660258924));
#270725=CARTESIAN_POINT('Ctrl Pts',(1.22524994015833,0.958332585576827,
16.2784147546055));
#270726=CARTESIAN_POINT('Ctrl Pts',(1.21016541601565,0.977424280486823,
16.2801658708772));
#270727=CARTESIAN_POINT('Ctrl Pts',(1.19961351132416,0.99034637445705,16.2813748125574));
#270728=CARTESIAN_POINT('Ctrl Pts',(1.14531153710402,1.05470437279876,16.2875194427389));
#270729=CARTESIAN_POINT('Ctrl Pts',(1.09845911430131,1.10341515587118,16.2925812292881));
#270730=CARTESIAN_POINT('Ctrl Pts',(0.975081264765485,1.21601944539658,
16.3053435603302));
#270731=CARTESIAN_POINT('Ctrl Pts',(0.895300707009709,1.27590033556052,
16.313138458457));
#270732=CARTESIAN_POINT('Ctrl Pts',(0.795860468760591,1.33659062846146,
16.322075392268));
#270733=CARTESIAN_POINT('Ctrl Pts',(0.781226830362618,1.34519629397978,
16.3233718038171));
#270734=CARTESIAN_POINT('Ctrl Pts',(0.737317315515137,1.37006008694333,
16.327201053015));
#270735=CARTESIAN_POINT('Ctrl Pts',(0.707651817970889,1.38561567217687,
16.3297094558764));
#270736=CARTESIAN_POINT('Ctrl Pts',(0.671753476962848,1.40298550796603,
16.3326338633877));
#270737=CARTESIAN_POINT('Ctrl Pts',(0.665985111905587,1.40573287072954,
16.3331004309786));
#270738=CARTESIAN_POINT('Ctrl Pts',(0.656533633349744,1.41016319365411,
16.3338592634462));
#270739=CARTESIAN_POINT('Ctrl Pts',(0.652860662763911,1.41186741604147,
16.3341527735727));
#270740=CARTESIAN_POINT('Ctrl Pts',(0.646257550609289,1.41489991786983,
16.3346779033301));
#270741=CARTESIAN_POINT('Ctrl Pts',(0.643329919531836,1.41623346048127,
16.3349098386584));
#270742=CARTESIAN_POINT('Ctrl Pts',(0.636924512140874,1.41912717681864,
16.3354153437078));
#270743=CARTESIAN_POINT('Ctrl Pts',(0.633445136290934,1.42068365173367,
16.3356886870629));
#270744=CARTESIAN_POINT('Ctrl Pts',(0.623532948312553,1.42507414682746,
16.3364639661754));
#270745=CARTESIAN_POINT('Ctrl Pts',(0.617086487388842,1.42787742248762,
16.336964076607));
#270746=CARTESIAN_POINT('Ctrl Pts',(0.574601452153752,1.44601078457249,
16.3402346133114));
#270747=CARTESIAN_POINT('Ctrl Pts',(0.538010166588153,1.46002045463908,
16.3429318510077));
#270748=CARTESIAN_POINT('Ctrl Pts',(0.389271906533926,1.51061462838705,
16.3535731808969));
#270749=CARTESIAN_POINT('Ctrl Pts',(0.273655694459271,1.53577529529139,
16.3611522460564));
#270750=CARTESIAN_POINT('Ctrl Pts',(0.0898508929878587,1.55433829059288,
16.3734765024534));
#270751=CARTESIAN_POINT('Ctrl Pts',(0.0230473944813672,1.55676192536714,
16.3780054870758));
#270752=CARTESIAN_POINT('Ctrl Pts',(-0.0551838605018441,1.55456328063912,
16.3834750801024));
#270753=CARTESIAN_POINT('Ctrl Pts',(-0.0666643294699243,1.55411328631946,
16.3842818128188));
#270754=CARTESIAN_POINT('Ctrl Pts',(-0.0854103796816846,1.55317041277752,
16.3856062523885));
#270755=CARTESIAN_POINT('Ctrl Pts',(-0.0926794929868463,1.55275360969185,
16.3861215861844));
#270756=CARTESIAN_POINT('Ctrl Pts',(-0.105692655121872,1.55191574566971,
16.3870474109874));
#270757=CARTESIAN_POINT('Ctrl Pts',(-0.111437837002576,1.55151378526135,
16.3874572978031));
#270758=CARTESIAN_POINT('Ctrl Pts',(-0.123624618541308,1.55059310145363,
16.3883292511753));
#270759=CARTESIAN_POINT('Ctrl Pts',(-0.130065465214612,1.55006612278847,
16.3887915686556));
#270760=CARTESIAN_POINT('Ctrl Pts',(-0.147319935784709,1.54854609426637,
16.3900341510085));
#270761=CARTESIAN_POINT('Ctrl Pts',(-0.158126581764484,1.54747993285136,
16.3908166888547));
#270762=CARTESIAN_POINT('Ctrl Pts',(-0.211983531035931,1.54159649394849,
16.3947388239744));
#270763=CARTESIAN_POINT('Ctrl Pts',(-0.254826497700319,1.53509593843784,
16.3979305804161));
#270764=CARTESIAN_POINT('Ctrl Pts',(-0.463972099294807,1.49436604351247,
16.4138826266288));
#270765=CARTESIAN_POINT('Ctrl Pts',(-0.624130871568306,1.4348673470839,
16.4274299238938));
#270766=CARTESIAN_POINT('Ctrl Pts',(-0.786332168583866,1.34221969835758,
16.4413616221168));
#270767=CARTESIAN_POINT('Ctrl Pts',(-0.801024131977854,1.33350380681095,
16.4426240225975));
#270768=CARTESIAN_POINT('Ctrl Pts',(-0.820256344781417,1.32166185643422,
16.444274295303));
#270769=CARTESIAN_POINT('Ctrl Pts',(-0.824927107367844,1.31875160811054,
16.4446749039408));
#270770=CARTESIAN_POINT('Ctrl Pts',(-0.832505625629978,1.31397358232262,
16.4453244940857));
#270771=CARTESIAN_POINT('Ctrl Pts',(-0.835422720002956,1.31212082952986,
16.4455744309721));
#270772=CARTESIAN_POINT('Ctrl Pts',(-0.84103537413148,1.30852972334829,
16.4460550923816));
#270773=CARTESIAN_POINT('Ctrl Pts',(-0.843731742235814,1.30679274744793,
16.4462858982283));
#270774=CARTESIAN_POINT('Ctrl Pts',(-0.849143965876476,1.30328250782357,
16.4467489946652));
#270775=CARTESIAN_POINT('Ctrl Pts',(-0.851859693212711,1.30150906012126,
16.4469812733594));
#270776=CARTESIAN_POINT('Ctrl Pts',(-0.861273974911252,1.29531917488499,
16.4477862390695));
#270777=CARTESIAN_POINT('Ctrl Pts',(-0.867944048445492,1.29085931098709,
16.4483561267084));
#270778=CARTESIAN_POINT('Ctrl Pts',(-0.946266740737118,1.23760822646027,
16.4550466516388));
#270779=CARTESIAN_POINT('Ctrl Pts',(-1.01376677756615,1.18295257977444,
16.4608037035514));
#270780=CARTESIAN_POINT('Ctrl Pts',(-1.16823942158121,1.03488728743512,
16.474914989481));
#270781=CARTESIAN_POINT('Ctrl Pts',(-1.2489451727583,0.935898778966701,
16.4832070053746));
#270782=CARTESIAN_POINT('Ctrl Pts',(-1.32614104473809,0.813169809459138,
16.4932710172997));
#270783=CARTESIAN_POINT('Ctrl Pts',(-1.33533196633021,0.797987283337744,
16.4945116056877));
#270784=CARTESIAN_POINT('Ctrl Pts',(-1.34790840246709,0.776386336854409,
16.4962722362941));
#270785=CARTESIAN_POINT('Ctrl Pts',(-1.35151210513657,0.770095988803044,
16.4967844230542));
#270786=CARTESIAN_POINT('Ctrl Pts',(-1.3577147769389,0.759091437493524,
16.4976796780455));
#270787=CARTESIAN_POINT('Ctrl Pts',(-1.3603335127657,0.754388466715651,
16.4980620328953));
#270788=CARTESIAN_POINT('Ctrl Pts',(-1.36576433631322,0.744515055892219,
16.4988642878019));
#270789=CARTESIAN_POINT('Ctrl Pts',(-1.36857158905733,0.739342068780553,
16.4992843519822));
#270790=CARTESIAN_POINT('Ctrl Pts',(-1.37518653562031,0.726985790614702,
16.5002871749432));
#270791=CARTESIAN_POINT('Ctrl Pts',(-1.37896736907099,0.719788397998064,
16.5008708699764));
#270792=CARTESIAN_POINT('Ctrl Pts',(-1.39159306338327,0.695288852579852,
16.5028564974421));
#270793=CARTESIAN_POINT('Ctrl Pts',(-1.40016974301459,0.677851362622899,
16.5042677101531));
#270794=CARTESIAN_POINT('Ctrl Pts',(-1.41993378502312,0.635692092658565,
16.5076763978822));
#270795=CARTESIAN_POINT('Ctrl Pts',(-1.43080497558965,0.61083004732621,
16.5096839985814));
#270796=CARTESIAN_POINT('Ctrl Pts',(-1.49703028996313,0.447892783368919,
16.522828012903));
#270797=CARTESIAN_POINT('Ctrl Pts',(-1.53297886410841,0.302770674755422,
16.5345787089787));
#270798=CARTESIAN_POINT('Ctrl Pts',(-1.54793564095542,0.153225353892046,
16.5460196773578));
#270799=CARTESIAN_POINT('Ctrl Pts',(-1.54809082728922,0.151649425026329,
16.5461401588464));
#270800=CARTESIAN_POINT('Ctrl Pts',(-1.54980250097743,0.133990796826681,
16.5474892108777));
#270801=CARTESIAN_POINT('Ctrl Pts',(-1.5511107748881,0.117884391851123,
16.5487106811146));
#270802=CARTESIAN_POINT('Ctrl Pts',(-1.55359029641752,0.0800636724071525,
16.5515538065943));
#270803=CARTESIAN_POINT('Ctrl Pts',(-1.55455773496866,0.0583384735902952,
16.553167623083));
#270804=CARTESIAN_POINT('Ctrl Pts',(-1.5552111032702,0.0305770339096044,
16.5551994321998));
#270805=CARTESIAN_POINT('Ctrl Pts',(-1.55531784954197,0.0245544462477771,
16.5556383875253));
#270806=CARTESIAN_POINT('Ctrl Pts',(-1.55543223145612,0.014953995409549,
16.5563350456703));
#270807=CARTESIAN_POINT('Ctrl Pts',(-1.55546251112997,0.0113765461869869,
16.5565939646384));
#270808=CARTESIAN_POINT('Ctrl Pts',(-1.55549071071321,0.00575223046998475,
16.5569999255921));
#270809=CARTESIAN_POINT('Ctrl Pts',(-1.55549693308948,0.00370547598347781,
16.5571474292398));
#270810=CARTESIAN_POINT('Ctrl Pts',(-1.555499657428,0.00115060015537671,
16.5573312652292));
#270811=CARTESIAN_POINT('Ctrl Pts',(-1.55549995027406,0.000642525155756949,
16.5573678096748));
#270812=CARTESIAN_POINT('Ctrl Pts',(-1.55549999418946,0.000134449200880738,
16.5574043402006));
#270813=CARTESIAN_POINT('Ctrl Pts',(-1.5554999941794,0.000134565524924873,
16.557404331837));
#270814=CARTESIAN_POINT('Ctrl Pts',(-1.55550005631452,-0.000583680669580982,
16.5574559735501));
#270815=CARTESIAN_POINT('Ctrl Pts',(-1.55549962097871,-0.00130192819956115,
16.5575075874042));
#270816=CARTESIAN_POINT('Ctrl Pts',(-1.55549439591342,-0.00532513151133239,
16.5577965427963));
#270817=CARTESIAN_POINT('Ctrl Pts',(-1.55547957060547,-0.00863010535305416,
16.5580333263913));
#270818=CARTESIAN_POINT('Ctrl Pts',(-1.55539859988764,-0.0191827435514825,
16.5587875644079));
#270819=CARTESIAN_POINT('Ctrl Pts',(-1.55529233098782,-0.0264301491038218,
16.559302850863));
#270820=CARTESIAN_POINT('Ctrl Pts',(-1.55430327163282,-0.0721032610949992,
16.5625345873586));
#270821=CARTESIAN_POINT('Ctrl Pts',(-1.55204708527963,-0.11048980600777,
16.565181236402));
#270822=CARTESIAN_POINT('Ctrl Pts',(-1.53402892344551,-0.298035761655428,
16.5779439561759));
#270823=CARTESIAN_POINT('Ctrl Pts',(-1.49817646609508,-0.444458831348207,
16.587461995549));
#270824=CARTESIAN_POINT('Ctrl Pts',(-1.4272635103738,-0.619697063958071,
16.6003204069466));
#270825=CARTESIAN_POINT('Ctrl Pts',(-1.41125605076399,-0.655333122806546,
16.603012879769));
#270826=CARTESIAN_POINT('Ctrl Pts',(-1.38926318635584,-0.699741687877563,
16.6064880075852));
#270827=CARTESIAN_POINT('Ctrl Pts',(-1.38450539084191,-0.709108908298952,
16.607227952405));
#270828=CARTESIAN_POINT('Ctrl Pts',(-1.37670433675246,-0.724089899864763,
16.6084229002773));
#270829=CARTESIAN_POINT('Ctrl Pts',(-1.37372070382062,-0.729734499394515,
16.6088758053203));
#270830=CARTESIAN_POINT('Ctrl Pts',(-1.36797248394207,-0.740449106850769,
16.6097406934233));
#270831=CARTESIAN_POINT('Ctrl Pts',(-1.36521424190891,-0.745522413275524,
16.6101524461245));
#270832=CARTESIAN_POINT('Ctrl Pts',(-1.35884855105654,-0.757077200767418,
16.6110954242065));
#270833=CARTESIAN_POINT('Ctrl Pts',(-1.35522288469019,-0.763548428007948,
16.6116272928666));
#270834=CARTESIAN_POINT('Ctrl Pts',(-1.34563932637681,-0.780370220919685,
16.613019858976));
#270835=CARTESIAN_POINT('Ctrl Pts',(-1.33960837148295,-0.790678363595692,
16.613883165057));
#270836=CARTESIAN_POINT('Ctrl Pts',(-1.28085517119875,-0.888497652019422,
16.6221730921203));
#270837=CARTESIAN_POINT('Ctrl Pts',(-1.21976152713595,-0.970665722630313,
16.6299145302193));
#270838=CARTESIAN_POINT('Ctrl Pts',(-1.10228510645782,-1.09991301332591,
16.6434092977767));
#270839=CARTESIAN_POINT('Ctrl Pts',(-1.04980530641377,-1.1501087559358,
16.6490656360401));
#270840=CARTESIAN_POINT('Ctrl Pts',(-0.969187023403972,-1.21708610632094,
16.6570963760611));
#270841=CARTESIAN_POINT('Ctrl Pts',(-0.943722108275766,-1.23693611598278,
16.6595472649625));
#270842=CARTESIAN_POINT('Ctrl Pts',(-0.907554751915153,-1.26336104618176,
16.662893468804));
#270843=CARTESIAN_POINT('Ctrl Pts',(-0.897364204209617,-1.27061964019404,
16.6638220292012));
#270844=CARTESIAN_POINT('Ctrl Pts',(-0.879498454045766,-1.28302301490749,
16.6654238787073));
#270845=CARTESIAN_POINT('Ctrl Pts',(-0.871863075041391,-1.28822372938218,
16.6661003608773));
#270846=CARTESIAN_POINT('Ctrl Pts',(-0.86137966774159,-1.29522842525874,
16.6670176914443));
#270847=CARTESIAN_POINT('Ctrl Pts',(-0.858571652746082,-1.29709148608409,
16.6672622886862));
#270848=CARTESIAN_POINT('Ctrl Pts',(-0.853245960579193,-1.30060010259783,
16.6677240583768));
#270849=CARTESIAN_POINT('Ctrl Pts',(-0.850729527833492,-1.30224750605124,
16.6679413518457));
#270850=CARTESIAN_POINT('Ctrl Pts',(-0.845528973077091,-1.30563058420997,
16.6683885473436));
#270851=CARTESIAN_POINT('Ctrl Pts',(-0.842844250581885,-1.30736530335068,
16.6686183826911));
#270852=CARTESIAN_POINT('Ctrl Pts',(-0.836231292345833,-1.31160939429937,
16.6691820470341));
#270853=CARTESIAN_POINT('Ctrl Pts',(-0.832297047013893,-1.31410943400867,
16.6695152624206));
#270854=CARTESIAN_POINT('Ctrl Pts',(-0.818824551861958,-1.32258583676254,
16.6706493115965));
#270855=CARTESIAN_POINT('Ctrl Pts',(-0.8092324042918,-1.3284765250317,16.671444780997));
#270856=CARTESIAN_POINT('Ctrl Pts',(-0.704420550919519,-1.39128658470135,
16.6800176144275));
#270857=CARTESIAN_POINT('Ctrl Pts',(-0.603420639387468,-1.43797721376659,
16.6872345086983));
#270858=CARTESIAN_POINT('Ctrl Pts',(-0.401632461431591,-1.50621520461431,
16.7012649782695));
#270859=CARTESIAN_POINT('Ctrl Pts',(-0.302000648323582,-1.5293083800525,
16.7080346195901));
#270860=CARTESIAN_POINT('Ctrl Pts',(-0.185652149056219,-1.54445715874957,
16.7162067707985));
#270861=CARTESIAN_POINT('Ctrl Pts',(-0.170442768572791,-1.54620951657286,
16.7172796966736));
#270862=CARTESIAN_POINT('Ctrl Pts',(-0.147857038815427,-1.54847446304233,
16.7188809667008));
#270863=CARTESIAN_POINT('Ctrl Pts',(-0.14049857011486,-1.54915945435491,
16.7194039147117));
#270864=CARTESIAN_POINT('Ctrl Pts',(-0.127385429832946,-1.55028594487522,
16.7203381890206));
#270865=CARTESIAN_POINT('Ctrl Pts',(-0.121632614303835,-1.55074790475653,
16.7207488671424));
#270866=CARTESIAN_POINT('Ctrl Pts',(-0.109495750635575,-1.5516545632689,
16.7216170499274));
#270867=CARTESIAN_POINT('Ctrl Pts',(-0.103111278205868,-1.55209189971729,
16.7220747770206));
#270868=CARTESIAN_POINT('Ctrl Pts',(-0.0861714662690325,-1.55314729648499,
16.7232920827909));
#270869=CARTESIAN_POINT('Ctrl Pts',(-0.0756123759146554,-1.5536971405432,
16.7240537756847));
#270870=CARTESIAN_POINT('Ctrl Pts',(-0.0522965277171016,-1.55467302895351,
16.7257424232621));
#270871=CARTESIAN_POINT('Ctrl Pts',(-0.0395385943510725,-1.55504978548417,
16.7266708588757));
#270872=CARTESIAN_POINT('Ctrl Pts',(0.0964432028722504,-1.55739104874265,
16.7366159310021));
#270873=CARTESIAN_POINT('Ctrl Pts',(0.219454959696569,-1.54486089523714,
16.7460964634013));
#270874=CARTESIAN_POINT('Ctrl Pts',(0.392965155545203,-1.50603491758828,
16.7598840688127));
#270875=CARTESIAN_POINT('Ctrl Pts',(0.445597437267887,-1.49131026441339,
16.7641155303527));
#270876=CARTESIAN_POINT('Ctrl Pts',(0.532776837083353,-1.4618916493064,
16.7711165372224));
#270877=CARTESIAN_POINT('Ctrl Pts',(0.567766425841591,-1.44866152311005,
16.7739236689726));
#270878=CARTESIAN_POINT('Ctrl Pts',(0.608653300959912,-1.43149211163754,
16.7771745023783));
#270879=CARTESIAN_POINT('Ctrl Pts',(0.615040266671612,-1.42875959548013,
16.7776814405567));
#270880=CARTESIAN_POINT('Ctrl Pts',(0.62488682302739,-1.4244687085434,16.7784613760123));
#270881=CARTESIAN_POINT('Ctrl Pts',(0.628359269315785,-1.42294036161469,
16.7787361166533));
#270882=CARTESIAN_POINT('Ctrl Pts',(0.634767120984724,-1.42009200776305,
16.7792424905287));
#270883=CARTESIAN_POINT('Ctrl Pts',(0.637704001739351,-1.41877560415379,
16.779474328854));
#270884=CARTESIAN_POINT('Ctrl Pts',(0.644347103606848,-1.4157731590593,
16.7799981979163));
#270885=CARTESIAN_POINT('Ctrl Pts',(0.648050799832014,-1.41408167716587,
16.7802898920336));
#270886=CARTESIAN_POINT('Ctrl Pts',(0.659028760119822,-1.40901584199773,
16.7811534969775));
#270887=CARTESIAN_POINT('Ctrl Pts',(0.666283769100503,-1.40559969265221,
16.7817229292086));
#270888=CARTESIAN_POINT('Ctrl Pts',(0.730371797147227,-1.37481499476078,
16.7867444012345));
#270889=CARTESIAN_POINT('Ctrl Pts',(0.785525727972356,-1.34406503529633,
16.7910059989779));
#270890=CARTESIAN_POINT('Ctrl Pts',(0.912255095560012,-1.26293530584869,
16.8010163641911));
#270891=CARTESIAN_POINT('Ctrl Pts',(0.981743908824223,-1.20970835957524,
16.8066944160147));
#270892=CARTESIAN_POINT('Ctrl Pts',(1.09500324685008,-1.10673558929196,
16.8168825926789));
#270893=CARTESIAN_POINT('Ctrl Pts',(1.14075585346209,-1.05951413465942,
16.8213203466108));
#270894=CARTESIAN_POINT('Ctrl Pts',(1.1940578583454,-0.997033896665379,
16.8270324458937));
#270895=CARTESIAN_POINT('Ctrl Pts',(1.20453287609112,-0.984353226540621,
16.8281839410511));
#270896=CARTESIAN_POINT('Ctrl Pts',(1.21955493493162,-0.965569190443507,
16.8298797995177));
#270897=CARTESIAN_POINT('Ctrl Pts',(1.22426164324301,-0.959594459150302,
16.8304177822563));
#270898=CARTESIAN_POINT('Ctrl Pts',(1.2324797119608,-0.949003501514645,
16.8313690631042));
#270899=CARTESIAN_POINT('Ctrl Pts',(1.23600945557266,-0.944401667910239,
16.8317816256643));
#270900=CARTESIAN_POINT('Ctrl Pts',(1.24284862292754,-0.935381219693552,
16.8325888812655));
#270901=CARTESIAN_POINT('Ctrl Pts',(1.24616042553597,-0.930964509553055,
16.8329834730188));
#270902=CARTESIAN_POINT('Ctrl Pts',(1.25502295768887,-0.919013169942722,
16.834049488398));
#270903=CARTESIAN_POINT('Ctrl Pts',(1.26052923912267,-0.911446027511432,
16.8347226185924));
#270904=CARTESIAN_POINT('Ctrl Pts',(1.28087932618228,-0.882942282508785,
16.837251727528));
#270905=CARTESIAN_POINT('Ctrl Pts',(1.29527175601318,-0.861690115472988,
16.8391246756498));
#270906=CARTESIAN_POINT('Ctrl Pts',(1.31238370166954,-0.835024274253569,
16.8414608468509));
#270907=CARTESIAN_POINT('Ctrl Pts',(1.31560675529061,-0.829936975084977,
16.8419059259617));
#270908=CARTESIAN_POINT('Ctrl Pts',(1.40686814550163,-0.684021614678269,
16.8546544950382));
#270909=CARTESIAN_POINT('Ctrl Pts',(1.47180837690826,-0.530020496406353,
16.8678184023214));
#270910=CARTESIAN_POINT('Ctrl Pts',(1.51904880942607,-0.336418749923332,
16.8829314001696));
#270911=CARTESIAN_POINT('Ctrl Pts',(1.52589659067416,-0.303853372962476,
16.8854214974098));
#270912=CARTESIAN_POINT('Ctrl Pts',(1.53286834057281,-0.264462119343719,
16.8883525840522));
#270913=CARTESIAN_POINT('Ctrl Pts',(1.53399847463748,-0.257826000118732,
16.8888436300476));
#270914=CARTESIAN_POINT('Ctrl Pts',(1.53569063447191,-0.247484479117746,
16.8896043782268));
#270915=CARTESIAN_POINT('Ctrl Pts',(1.53628239178288,-0.243784137531892,
16.8898756932562));
#270916=CARTESIAN_POINT('Ctrl Pts',(1.53735827748471,-0.236896953102605,
16.890378970915));
#270917=CARTESIAN_POINT('Ctrl Pts',(1.53784586841758,-0.233710772246146,
16.8906111177098));
#270918=CARTESIAN_POINT('Ctrl Pts',(1.53893638871303,-0.22643352418955,
16.8911398080761));
#270919=CARTESIAN_POINT('Ctrl Pts',(1.53953291078763,-0.22234155493375,
16.8914359887352));
#270920=CARTESIAN_POINT('Ctrl Pts',(1.54104951580669,-0.211639271602126,
16.8922078729318));
#270921=CARTESIAN_POINT('Ctrl Pts',(1.54194339974385,-0.205025236647381,
16.8926821530798));
#270922=CARTESIAN_POINT('Ctrl Pts',(1.54777078982401,-0.159711640484578,
16.8959140059561));
#270923=CARTESIAN_POINT('Ctrl Pts',(1.55128995472198,-0.120840139787276,
16.8985992083349));
#270924=CARTESIAN_POINT('Ctrl Pts',(1.56091952725396,0.0618566635447943,
16.9109856866003));
#270925=CARTESIAN_POINT('Ctrl Pts',(1.54851151526834,0.205946077313584,
16.920141896236));
#270926=CARTESIAN_POINT('Ctrl Pts',(1.506730076061,0.388918033882374,16.9328600800483));
#270927=CARTESIAN_POINT('Ctrl Pts',(1.49520169161464,0.431119545182808,
16.9358666928964));
#270928=CARTESIAN_POINT('Ctrl Pts',(1.47860161689127,0.483152280035275,
16.9396943425542));
#270929=CARTESIAN_POINT('Ctrl Pts',(1.47518257109654,0.493492896011304,
16.9404610441578));
#270930=CARTESIAN_POINT('Ctrl Pts',(1.4695599631504,0.509917266403414,16.9416888582295));
#270931=CARTESIAN_POINT('Ctrl Pts',(1.46742649515984,0.516024789016074,
16.9421476585144));
#270932=CARTESIAN_POINT('Ctrl Pts',(1.46332226468621,0.527542751909619,
16.9430172029556));
#270933=CARTESIAN_POINT('Ctrl Pts',(1.46135943255118,0.53295592001184,16.9434276782068));
#270934=CARTESIAN_POINT('Ctrl Pts',(1.45685063793552,0.545178241116116,
16.9443586550454));
#270935=CARTESIAN_POINT('Ctrl Pts',(1.45428692194885,0.551980652892509,
16.9448797404049));
#270936=CARTESIAN_POINT('Ctrl Pts',(1.44756221276699,0.569451505920662,
16.9462257969949));
#270937=CARTESIAN_POINT('Ctrl Pts',(1.44333098934203,0.580092250937445,
16.9470530992632));
#270938=CARTESIAN_POINT('Ctrl Pts',(1.43752707603031,0.594231310765164,
16.9481626327223));
#270939=CARTESIAN_POINT('Ctrl Pts',(1.43605836754101,0.597771951742406,
16.9484413407064));
#270940=CARTESIAN_POINT('Ctrl Pts',(1.4345766824505,0.601306903477194,16.9487204703706));
#270941=CARTESIAN_POINT('Origin',(0.,0.,-1.29405622560371));
#270942=CARTESIAN_POINT('',(1.43457675882331,0.601306721269597,17.7872340762022));
#270943=CARTESIAN_POINT('',(1.43457667260785,0.601306926959429,17.650811911463));
#270944=CARTESIAN_POINT('',(1.43457668357355,0.601306900797845,-1.29405622560371));
#270945=CARTESIAN_POINT('',(-1.5554999603012,-0.000351429880857887,17.395456864983));
#270946=CARTESIAN_POINT('Ctrl Pts',(1.43457675882332,0.601306721269597,
17.7872340762022));
#270947=CARTESIAN_POINT('Ctrl Pts',(1.44690679487224,0.57189014812056,17.7848031153696));
#270948=CARTESIAN_POINT('Ctrl Pts',(1.45833584107452,0.542085259084417,
17.7823974315995));
#270949=CARTESIAN_POINT('Ctrl Pts',(1.47275577373232,0.500711392614961,
17.7791544208958));
#270950=CARTESIAN_POINT('Ctrl Pts',(1.47653821205348,0.489444990848641,
17.7782809671412));
#270951=CARTESIAN_POINT('Ctrl Pts',(1.4816705060036,0.473556669248412,17.7770637326209));
#270952=CARTESIAN_POINT('Ctrl Pts',(1.48312847097578,0.468970518901122,
17.7767140701249));
#270953=CARTESIAN_POINT('Ctrl Pts',(1.48545190330485,0.461542755981358,
17.7761505671935));
#270954=CARTESIAN_POINT('Ctrl Pts',(1.4863305400394,0.458705350725448,17.7759359707686));
#270955=CARTESIAN_POINT('Ctrl Pts',(1.48817082176006,0.452701673250632,
17.775483328293));
#270956=CARTESIAN_POINT('Ctrl Pts',(1.48913050113314,0.449534815929342,
17.7752454017436));
#270957=CARTESIAN_POINT('Ctrl Pts',(1.49147575321705,0.44170576507869,17.7746592111106));
#270958=CARTESIAN_POINT('Ctrl Pts',(1.49284959472888,0.437040037713588,
17.7743116244073));
#270959=CARTESIAN_POINT('Ctrl Pts',(1.49785472595556,0.41974301921536,17.7730292501083));
#270960=CARTESIAN_POINT('Ctrl Pts',(1.50134790722727,0.407071829227247,
17.7721020710032));
#270961=CARTESIAN_POINT('Ctrl Pts',(1.50972741120255,0.375099623352245,
17.7697896832));
#270962=CARTESIAN_POINT('Ctrl Pts',(1.51440471423828,0.355745739213263,
17.7684145389477));
#270963=CARTESIAN_POINT('Ctrl Pts',(1.55043747873432,0.193027148764359,
17.7570169255336));
#270964=CARTESIAN_POINT('Ctrl Pts',(1.56173358295706,0.0459693221400361,
17.7477094026532));
#270965=CARTESIAN_POINT('Ctrl Pts',(1.54900674702494,-0.150590046290445,
17.7344327353212));
#270966=CARTESIAN_POINT('Ctrl Pts',(1.54334205350967,-0.20048366796201,
17.7309971157239));
#270967=CARTESIAN_POINT('Ctrl Pts',(1.53340914686726,-0.261479683018524,
17.7266719271998));
#270968=CARTESIAN_POINT('Ctrl Pts',(1.53141337830653,-0.272925425943734,
17.725854904451));
#270969=CARTESIAN_POINT('Ctrl Pts',(1.52807458283947,-0.290882277453159,
17.724564087975));
#270970=CARTESIAN_POINT('Ctrl Pts',(1.52681768155549,-0.297409137147886,
17.7240930287585));
#270971=CARTESIAN_POINT('Ctrl Pts',(1.52452345518529,-0.308924660432629,
17.7232585099452));
#270972=CARTESIAN_POINT('Ctrl Pts',(1.52350337030061,-0.313916694017427,
17.7228956045271));
#270973=CARTESIAN_POINT('Ctrl Pts',(1.52110672131121,-0.325358395022645,
17.7220611678649));
#270974=CARTESIAN_POINT('Ctrl Pts',(1.51971363750734,-0.331804460980519,
17.7215891151783));
#270975=CARTESIAN_POINT('Ctrl Pts',(1.51573542085201,-0.349661664745591,
17.7202758974049));
#270976=CARTESIAN_POINT('Ctrl Pts',(1.51306251269409,-0.361052578698618,
17.7194319411809));
#270977=CARTESIAN_POINT('Ctrl Pts',(1.49639841718896,-0.428631342342926,
17.714386524882));
#270978=CARTESIAN_POINT('Ctrl Pts',(1.47940900194819,-0.484025270831817,
17.7100893632637));
#270979=CARTESIAN_POINT('Ctrl Pts',(1.43175498639562,-0.613210113420364,
17.6996710425956));
#270980=CARTESIAN_POINT('Ctrl Pts',(1.39841703382149,-0.685840068163576,
17.6934861479448));
#270981=CARTESIAN_POINT('Ctrl Pts',(1.32085659472172,-0.825408402874694,
17.6811050806827));
#270982=CARTESIAN_POINT('Ctrl Pts',(1.27672902221003,-0.892147458294287,
17.6749280062949));
#270983=CARTESIAN_POINT('Ctrl Pts',(1.22010249534743,-0.964925794909212,
17.6680979772779));
#270984=CARTESIAN_POINT('Ctrl Pts',(1.21242510087692,-0.974554918432606,
17.6671924145254));
#270985=CARTESIAN_POINT('Ctrl Pts',(1.20154346927468,-0.987875195851234,
17.6659382034851));
#270986=CARTESIAN_POINT('Ctrl Pts',(1.1984352340874,-0.991643636884611,
17.6655832022986));
#270987=CARTESIAN_POINT('Ctrl Pts',(1.19339992479924,-0.997690218357838,
17.6650133985101));
#270988=CARTESIAN_POINT('Ctrl Pts',(1.1914839927223,-0.999977523655699,
17.6647978077846));
#270989=CARTESIAN_POINT('Ctrl Pts',(1.18743896637812,-1.00477848418966,
17.6643452224476));
#270990=CARTESIAN_POINT('Ctrl Pts',(1.18530844978136,-1.00729091151195,
17.6641083386001));
#270991=CARTESIAN_POINT('Ctrl Pts',(1.18006011939083,-1.01344033502069,
17.6635283936405));
#270992=CARTESIAN_POINT('Ctrl Pts',(1.17693341921679,-1.0170697745923,17.6631859777038));
#270993=CARTESIAN_POINT('Ctrl Pts',(1.16549340833,-1.03022581461333,17.6619440652548));
#270994=CARTESIAN_POINT('Ctrl Pts',(1.15708049465765,-1.03966574920664,
17.6610515668366));
#270995=CARTESIAN_POINT('Ctrl Pts',(1.10090314421147,-1.10117434486033,
17.655218655124));
#270996=CARTESIAN_POINT('Ctrl Pts',(1.04974697676919,-1.15004638052301,
17.6504979634673));
#270997=CARTESIAN_POINT('Ctrl Pts',(0.888867301873258,-1.28402865935836,
17.6366559401494));
#270998=CARTESIAN_POINT('Ctrl Pts',(0.770920378940911,-1.35812089762546,
17.6276766423771));
#270999=CARTESIAN_POINT('Ctrl Pts',(0.629398982446087,-1.42257532779914,
17.6168658550513));
#271000=CARTESIAN_POINT('Ctrl Pts',(0.613967085195139,-1.42930333452608,
17.6156876356169));
#271001=CARTESIAN_POINT('Ctrl Pts',(0.591472048558315,-1.43867921435167,
17.6139695534218));
#271002=CARTESIAN_POINT('Ctrl Pts',(0.584493675976079,-1.4415284267653,
17.6134364939884));
#271003=CARTESIAN_POINT('Ctrl Pts',(0.572155581096667,-1.44646165104697,
17.612493744104));
#271004=CARTESIAN_POINT('Ctrl Pts',(0.566804451279021,-1.44856688810552,
17.6120847754956));
#271005=CARTESIAN_POINT('Ctrl Pts',(0.555710975706681,-1.45286039378464,
17.6112366882273));
#271006=CARTESIAN_POINT('Ctrl Pts',(0.549967098930028,-1.45504439810024,
17.6107974352973));
#271007=CARTESIAN_POINT('Ctrl Pts',(0.535170371209446,-1.46057045238012,
17.609665440056));
#271008=CARTESIAN_POINT('Ctrl Pts',(0.526099207623039,-1.4638623529982,
17.6089710443485));
#271009=CARTESIAN_POINT('Ctrl Pts',(0.487604731311496,-1.47742788181399,
17.6060220445099));
#271010=CARTESIAN_POINT('Ctrl Pts',(0.457908732017132,-1.48689974570038,
17.6037413341823));
#271011=CARTESIAN_POINT('Ctrl Pts',(0.378171027456508,-1.5097177915959,
17.5975969243279));
#271012=CARTESIAN_POINT('Ctrl Pts',(0.327716807777019,-1.52146699633172,
17.5936869752201));
#271013=CARTESIAN_POINT('Ctrl Pts',(0.180535503645951,-1.54808014006072,
17.5822395797291));
#271014=CARTESIAN_POINT('Ctrl Pts',(0.082874869517439,-1.55636614997997,
17.5745794231732));
#271015=CARTESIAN_POINT('Ctrl Pts',(-0.0250205497408982,-1.55533159461845,
17.5663084949911));
#271016=CARTESIAN_POINT('Ctrl Pts',(-0.0351258713253945,-1.55513619263152,
17.5655359054609));
#271017=CARTESIAN_POINT('Ctrl Pts',(-0.0835731852144278,-1.55372691060975,
17.5618436516246));
#271018=CARTESIAN_POINT('Ctrl Pts',(-0.121867350590717,-1.55119332944801,
17.5589601508508));
#271019=CARTESIAN_POINT('Ctrl Pts',(-0.166583549676007,-1.54656831366107,
17.5556619228482));
#271020=CARTESIAN_POINT('Ctrl Pts',(-0.173130572719318,-1.54584909895374,
17.5551807649105));
#271021=CARTESIAN_POINT('Ctrl Pts',(-0.183727945077796,-1.54461676711698,
17.5544049728898));
#271022=CARTESIAN_POINT('Ctrl Pts',(-0.187781097753289,-1.54412926124093,
17.5541089782319));
#271023=CARTESIAN_POINT('Ctrl Pts',(-0.194990500014386,-1.54323332094478,
17.5535838265887));
#271024=CARTESIAN_POINT('Ctrl Pts',(-0.198147454703101,-1.54283115241295,
17.5533543260882));
#271025=CARTESIAN_POINT('Ctrl Pts',(-0.204969632960233,-1.54194078061221,
17.5528593795015));
#271026=CARTESIAN_POINT('Ctrl Pts',(-0.208634352565216,-1.54144919768787,
17.5525941255405));
#271027=CARTESIAN_POINT('Ctrl Pts',(-0.218868836227695,-1.54003918353441,
17.5518549939548));
#271028=CARTESIAN_POINT('Ctrl Pts',(-0.225434634864877,-1.53909177241289,
17.5513827092611));
#271029=CARTESIAN_POINT('Ctrl Pts',(-0.264183175652776,-1.53324727083779,
17.5486056083556));
#271030=CARTESIAN_POINT('Ctrl Pts',(-0.296214714029169,-1.52738246035465,
17.5463511774142));
#271031=CARTESIAN_POINT('Ctrl Pts',(-0.47921709607514,-1.48790088970543,
17.5335857949565));
#271032=CARTESIAN_POINT('Ctrl Pts',(-0.624691046510996,-1.43292301553589,
17.5238059666347));
#271033=CARTESIAN_POINT('Ctrl Pts',(-0.795181463123512,-1.33750606586419,
17.5105419518066));
#271034=CARTESIAN_POINT('Ctrl Pts',(-0.829893632763427,-1.31624925673716,
17.5077411410696));
#271035=CARTESIAN_POINT('Ctrl Pts',(-0.872892158193993,-1.28754063568279,
17.5041186230854));
#271036=CARTESIAN_POINT('Ctrl Pts',(-0.881988573871251,-1.28132655980388,
17.503343252725));
#271037=CARTESIAN_POINT('Ctrl Pts',(-0.896301460054811,-1.27132430559928,
17.5021084189028));
#271038=CARTESIAN_POINT('Ctrl Pts',(-0.901561831072859,-1.26759932935658,
17.5016513610177));
#271039=CARTESIAN_POINT('Ctrl Pts',(-0.911235620088362,-1.26065844449219,
17.5008047695889));
#271040=CARTESIAN_POINT('Ctrl Pts',(-0.91565556631832,-1.25745176903959,
17.5004155956519));
#271041=CARTESIAN_POINT('Ctrl Pts',(-0.920127347815195,-1.25417140818013,
17.5000194188615));
#271042=CARTESIAN_POINT('Ctrl Pts',(-0.920196206647987,-1.25412088674282,
17.5000133177343));
#271043=CARTESIAN_POINT('Ctrl Pts',(-0.920331683582465,-1.25402147071847,
17.5000013128558));
#271044=CARTESIAN_POINT('Ctrl Pts',(-0.92039830195099,-1.25397257649216,
17.4999954091186));
#271045=CARTESIAN_POINT('Ctrl Pts',(-0.926044458638076,-1.24982791502793,
17.4994949984296));
#271046=CARTESIAN_POINT('Ctrl Pts',(-0.931596516533388,-1.24569502048958,
17.4989990523982));
#271047=CARTESIAN_POINT('Ctrl Pts',(-0.943112681260327,-1.23700245748673,
17.4979621404227));
#271048=CARTESIAN_POINT('Ctrl Pts',(-0.949071717140402,-1.23243640056207,
17.4974209320286));
#271049=CARTESIAN_POINT('Ctrl Pts',(-0.964507341940575,-1.22043065742354,
17.4960067155646));
#271050=CARTESIAN_POINT('Ctrl Pts',(-0.973930799545166,-1.21292381655863,
17.4951310719277));
#271051=CARTESIAN_POINT('Ctrl Pts',(-1.00169890515288,-1.19027116684355,
17.4925135380778));
#271052=CARTESIAN_POINT('Ctrl Pts',(-1.01978359084261,-1.17481379879,17.490759424453));
#271053=CARTESIAN_POINT('Ctrl Pts',(-1.13845847377506,-1.06857449830548,
17.4789082507005));
#271054=CARTESIAN_POINT('Ctrl Pts',(-1.22715853292402,-0.965406078891215,
17.468293690062));
#271055=CARTESIAN_POINT('Ctrl Pts',(-1.33194779482776,-0.805365730683185,
17.4535700699966));
#271056=CARTESIAN_POINT('Ctrl Pts',(-1.36000478742733,-0.757025386093227,
17.4493246277061));
#271057=CARTESIAN_POINT('Ctrl Pts',(-1.38897448861438,-0.700279803433184,
17.4446438484717));
#271058=CARTESIAN_POINT('Ctrl Pts',(-1.392492655234,-0.693257632608618,
17.4440697354421));
#271059=CARTESIAN_POINT('Ctrl Pts',(-1.39772528710097,-0.682612868450967,
17.4432074901694));
#271060=CARTESIAN_POINT('Ctrl Pts',(-1.39947911843154,-0.679009944278098,
17.4429170274254));
#271061=CARTESIAN_POINT('Ctrl Pts',(-1.40259842032801,-0.672538484829419,
17.4423978306542));
#271062=CARTESIAN_POINT('Ctrl Pts',(-1.40396903753513,-0.669672520383105,
17.4421687845073));
#271063=CARTESIAN_POINT('Ctrl Pts',(-1.40693974057702,-0.663411562876161,
17.4416703472381));
#271064=CARTESIAN_POINT('Ctrl Pts',(-1.40853632080669,-0.660014976456627,
17.441401172699));
#271065=CARTESIAN_POINT('Ctrl Pts',(-1.41302930741365,-0.650365979357112,
17.4406398890738));
#271066=CARTESIAN_POINT('Ctrl Pts',(-1.4158965325938,-0.644099949082936,
17.4401495306365));
#271067=CARTESIAN_POINT('Ctrl Pts',(-1.43409150073586,-0.603628014989925,
17.4370067962985));
#271068=CARTESIAN_POINT('Ctrl Pts',(-1.4482217931586,-0.56889316116657,
17.4344215493099));
#271069=CARTESIAN_POINT('Ctrl Pts',(-1.48807801336718,-0.459776275902577,
17.4265402540847));
#271070=CARTESIAN_POINT('Ctrl Pts',(-1.50942778119496,-0.383927164863786,
17.4213940892309));
#271071=CARTESIAN_POINT('Ctrl Pts',(-1.54524553084811,-0.205885544366946,
17.4094361640154));
#271072=CARTESIAN_POINT('Ctrl Pts',(-1.55547671460093,-0.103241615985641,
17.4026172025359));
#271073=CARTESIAN_POINT('Ctrl Pts',(-1.5554999603012,-0.000351429880857887,
17.395456864983));
#271074=CARTESIAN_POINT('Ctrl Pts',(-1.55549996055179,-0.000350318978951627,
17.3954567876731));
#271075=CARTESIAN_POINT('Ctrl Pts',(-1.5555020360747,0.00886549862816396,
17.394815439967));
#271076=CARTESIAN_POINT('Ctrl Pts',(-1.55542221061676,0.0180810189639046,
17.394171699026));
#271077=CARTESIAN_POINT('Ctrl Pts',(-1.55511197823933,0.035757859119276,
17.3929319368728));
#271078=CARTESIAN_POINT('Ctrl Pts',(-1.55489438855453,0.0442190544186781,
17.3923363295072));
#271079=CARTESIAN_POINT('Ctrl Pts',(-1.55441798831586,0.0582783737622305,
17.3913428268625));
#271080=CARTESIAN_POINT('Ctrl Pts',(-1.55419795658096,0.063877707554238,
17.3909461401424));
#271081=CARTESIAN_POINT('Ctrl Pts',(-1.55370512290485,0.0749008154391519,
17.390163154582));
#271082=CARTESIAN_POINT('Ctrl Pts',(-1.55343416312172,0.0803245950657222,
17.38977691865));
#271083=CARTESIAN_POINT('Ctrl Pts',(-1.55279782395194,0.0918506312577073,
17.3889539969631));
#271084=CARTESIAN_POINT('Ctrl Pts',(-1.55242486257448,0.0979523589495593,
17.3885170804876));
#271085=CARTESIAN_POINT('Ctrl Pts',(-1.55138024292207,0.113533720313811,
17.3873980333919));
#271086=CARTESIAN_POINT('Ctrl Pts',(-1.55065766795671,0.123009565221441,
17.3867143217273));
#271087=CARTESIAN_POINT('Ctrl Pts',(-1.54752617426158,0.15964463058344,
17.3840583411605));
#271088=CARTESIAN_POINT('Ctrl Pts',(-1.54449028669734,0.186743803352096,
17.3820666525217));
#271089=CARTESIAN_POINT('Ctrl Pts',(-1.5205575959555,0.359256320838537,
17.369205188255));
#271090=CARTESIAN_POINT('Ctrl Pts',(-1.47986110201174,0.501152983121043,
17.3576922870742));
#271091=CARTESIAN_POINT('Ctrl Pts',(-1.40454160001679,0.669520086941398,
17.3435043038259));
#271092=CARTESIAN_POINT('Ctrl Pts',(-1.38794532269747,0.703279787160669,
17.3406366122605));
#271093=CARTESIAN_POINT('Ctrl Pts',(-1.36359833980893,0.748579172761733,
17.3367853698398));
#271094=CARTESIAN_POINT('Ctrl Pts',(-1.35689401465341,0.760664101502796,
17.3357576404983));
#271095=CARTESIAN_POINT('Ctrl Pts',(-1.34508406620527,0.781299057773077,
17.3340042454211));
#271096=CARTESIAN_POINT('Ctrl Pts',(-1.34005586931038,0.789892172249686,
17.3332745118182));
#271097=CARTESIAN_POINT('Ctrl Pts',(-1.33271061932318,0.802173054509789,
17.3322328826455));
#271098=CARTESIAN_POINT('Ctrl Pts',(-1.33046018325886,0.805900059713476,
17.3319169391457));
#271099=CARTESIAN_POINT('Ctrl Pts',(-1.32652038913346,0.812363371652627,
17.3313693973018));
#271100=CARTESIAN_POINT('Ctrl Pts',(-1.32483815312171,0.815103956097704,
17.3311373431652));
#271101=CARTESIAN_POINT('Ctrl Pts',(-1.32128451516139,0.820853235135281,
17.330650797765));
#271102=CARTESIAN_POINT('Ctrl Pts',(-1.31941132680581,0.823860761911189,
17.330396426292));
#271103=CARTESIAN_POINT('Ctrl Pts',(-1.31437412876736,0.831887070408513,
17.3297178942402));
#271104=CARTESIAN_POINT('Ctrl Pts',(-1.3111916124328,0.836894262626329,
17.3292949292892));
#271105=CARTESIAN_POINT('Ctrl Pts',(-1.29706636013733,0.858839769150748,
17.3274420626684));
#271106=CARTESIAN_POINT('Ctrl Pts',(-1.28582286786256,0.875583546451696,
17.3260307564443));
#271107=CARTESIAN_POINT('Ctrl Pts',(-1.27208265307508,0.895209661101148,
17.3243732442507));
#271108=CARTESIAN_POINT('Ctrl Pts',(-1.26989770293045,0.898306427817408,
17.3241116105747));
#271109=CARTESIAN_POINT('Ctrl Pts',(-1.18257179152736,1.02111957571539,
17.3137303524027));
#271110=CARTESIAN_POINT('Ctrl Pts',(-1.08090336990349,1.12819340188835,
17.3044171457754));
#271111=CARTESIAN_POINT('Ctrl Pts',(-0.936139129157414,1.2428380922563,
17.2920211506613));
#271112=CARTESIAN_POINT('Ctrl Pts',(-0.90572941557981,1.26517069249233,
17.2894616971732));
#271113=CARTESIAN_POINT('Ctrl Pts',(-0.860748393691952,1.29575096702797,
17.2857136295249));
#271114=CARTESIAN_POINT('Ctrl Pts',(-0.846807500938753,1.30490435911294,
17.2845570613963));
#271115=CARTESIAN_POINT('Ctrl Pts',(-0.824802832481698,1.3188511881578,
17.2827375503216));
#271116=CARTESIAN_POINT('Ctrl Pts',(-0.816838021323161,1.3237990063342,
17.2820801748405));
#271117=CARTESIAN_POINT('Ctrl Pts',(-0.803362652134913,1.33200212273425,
17.2809697267821));
#271118=CARTESIAN_POINT('Ctrl Pts',(-0.797875780186113,1.33529601325457,
17.2805180568162));
#271119=CARTESIAN_POINT('Ctrl Pts',(-0.787097128068209,1.34167652206558,
17.2796316157982));
#271120=CARTESIAN_POINT('Ctrl Pts',(-0.781807125893892,1.34476592566285,
17.2791969552695));
#271121=CARTESIAN_POINT('Ctrl Pts',(-0.771696678839268,1.3505906869611,
17.2783668845521));
#271122=CARTESIAN_POINT('Ctrl Pts',(-0.766879582402399,1.35333169344035,
17.277971685855));
#271123=CARTESIAN_POINT('Ctrl Pts',(-0.755677478716684,1.3596268598496,
17.2770532567584));
#271124=CARTESIAN_POINT('Ctrl Pts',(-0.749281914841805,1.36316186074075,
17.2765293514285));
#271125=CARTESIAN_POINT('Ctrl Pts',(-0.732551637641446,1.37225582690031,
17.2751598847431));
#271126=CARTESIAN_POINT('Ctrl Pts',(-0.722178678292795,1.37774304529251,
17.2743118100013));
#271127=CARTESIAN_POINT('Ctrl Pts',(-0.642088156542963,1.41895735732056,
17.267770104671));
#271128=CARTESIAN_POINT('Ctrl Pts',(-0.56983531290357,1.44948305707374,
17.2618964892526));
#271129=CARTESIAN_POINT('Ctrl Pts',(-0.393482747641707,1.5087604785845,
17.2476466391434));
#271130=CARTESIAN_POINT('Ctrl Pts',(-0.288079069319143,1.53238252900044,
17.239185215477));
#271131=CARTESIAN_POINT('Ctrl Pts',(-0.143652882207271,1.54931092245702,
17.2281181003721));
#271132=CARTESIAN_POINT('Ctrl Pts',(-0.1060720383946,1.55233688085673,17.2252883913725));
#271133=CARTESIAN_POINT('Ctrl Pts',(-0.0615212249774581,1.55429823452016,
17.2220195834915));
#271134=CARTESIAN_POINT('Ctrl Pts',(-0.0546255714621406,1.55455585768492,
17.2215160625967));
#271135=CARTESIAN_POINT('Ctrl Pts',(-0.0439749222149352,1.55488281135439,
17.2207423338028));
#271136=CARTESIAN_POINT('Ctrl Pts',(-0.0402211242258011,1.55498444133869,
17.2204703982776));
#271137=CARTESIAN_POINT('Ctrl Pts',(-0.0332911163985541,1.55514695221371,
17.2199698232113));
#271138=CARTESIAN_POINT('Ctrl Pts',(-0.0301151084918541,1.55521169685317,
17.219740979235));
#271139=CARTESIAN_POINT('Ctrl Pts',(-0.0229350133192406,1.55533606352476,
17.2192248940198));
#271140=CARTESIAN_POINT('Ctrl Pts',(-0.0189308857210311,1.55538995363686,
17.218937974936));
#271141=CARTESIAN_POINT('Ctrl Pts',(-0.00682550035110079,1.55550612192181,
17.2180731110734));
#271142=CARTESIAN_POINT('Ctrl Pts',(0.00127624944527889,1.55552057572554,
17.2174977475247));
#271143=CARTESIAN_POINT('Ctrl Pts',(0.0796879713836924,1.55504782971908,
17.2119594379467));
#271144=CARTESIAN_POINT('Ctrl Pts',(0.149899444054184,1.54985711091355,
17.2072343336937));
#271145=CARTESIAN_POINT('Ctrl Pts',(0.284973747043006,1.53060132227121,
17.1981896154152));
#271146=CARTESIAN_POINT('Ctrl Pts',(0.349758562626398,1.51710895594546,
17.1938712486912));
#271147=CARTESIAN_POINT('Ctrl Pts',(0.488520571526831,1.47884607062597,
17.1843459079556));
#271148=CARTESIAN_POINT('Ctrl Pts',(0.561883860438447,1.45255710583265,
17.1791280738521));
#271149=CARTESIAN_POINT('Ctrl Pts',(0.649275351134604,1.41362673401151,
17.1724852028277));
#271150=CARTESIAN_POINT('Ctrl Pts',(0.665457651816556,1.40608146723739,
17.171236647396));
#271151=CARTESIAN_POINT('Ctrl Pts',(0.688518990003329,1.3948414666327,17.1694287767374));
#271152=CARTESIAN_POINT('Ctrl Pts',(0.695506115592836,1.39137067520223,
17.1688772046197));
#271153=CARTESIAN_POINT('Ctrl Pts',(0.707616486990826,1.38524094354631,
17.1679143706662));
#271154=CARTESIAN_POINT('Ctrl Pts',(0.712751638764899,1.38260575151938,
17.1675039452158));
#271155=CARTESIAN_POINT('Ctrl Pts',(0.722632385487544,1.37746560036033,
17.166709997566));
#271156=CARTESIAN_POINT('Ctrl Pts',(0.727379925897033,1.37496454019816,
17.1663266173624));
#271157=CARTESIAN_POINT('Ctrl Pts',(0.738609140058618,1.36897442394996,
17.1654152447034));
#271158=CARTESIAN_POINT('Ctrl Pts',(0.745079124051548,1.36546385182905,
17.1648864949309));
#271159=CARTESIAN_POINT('Ctrl Pts',(0.767910039065515,1.35286536296374,
17.1630075452129));
#271160=CARTESIAN_POINT('Ctrl Pts',(0.784131011321175,1.34352857009894,
17.1616485097875));
#271161=CARTESIAN_POINT('Ctrl Pts',(0.916605468070933,1.26405999604718,
17.1503437468259));
#271162=CARTESIAN_POINT('Ctrl Pts',(1.02336450301627,1.17928887908859,17.1398304470286));
#271163=CARTESIAN_POINT('Ctrl Pts',(1.16665034876433,1.03123845142085,17.1238719145491));
#271164=CARTESIAN_POINT('Ctrl Pts',(1.21208015275551,0.977440421709085,
17.1184588642416));
#271165=CARTESIAN_POINT('Ctrl Pts',(1.26118415251025,0.910578894214684,
17.1123139481622));
#271166=CARTESIAN_POINT('Ctrl Pts',(1.26852772644086,0.900320400611983,
17.1113863331313));
#271167=CARTESIAN_POINT('Ctrl Pts',(1.27848436177573,0.886047907182715,
17.1101177638395));
#271168=CARTESIAN_POINT('Ctrl Pts',(1.28120465031244,0.882109858683324,
17.109770018682));
#271169=CARTESIAN_POINT('Ctrl Pts',(1.28576596562492,0.875441018587189,
17.1091850494671));
#271170=CARTESIAN_POINT('Ctrl Pts',(1.28761655759249,0.872716847974279,
17.1089471887841));
#271171=CARTESIAN_POINT('Ctrl Pts',(1.29112774842616,0.867512705720129,
17.1084949024555));
#271172=CARTESIAN_POINT('Ctrl Pts',(1.29278987578452,0.865033811375427,
17.1082803708945));
#271173=CARTESIAN_POINT('Ctrl Pts',(1.29715604002407,0.858481428153496,
17.1077156491046));
#271174=CARTESIAN_POINT('Ctrl Pts',(1.29984805371944,0.854399902640539,
17.1073662583828));
#271175=CARTESIAN_POINT('Ctrl Pts',(1.30926623911597,0.839972876048405,
17.1061393582122));
#271176=CARTESIAN_POINT('Ctrl Pts',(1.31588873938611,0.82955974362176,17.1052683954196));
#271177=CARTESIAN_POINT('Ctrl Pts',(1.36481324392354,0.750571081033337,
17.0987618315329));
#271178=CARTESIAN_POINT('Ctrl Pts',(1.40185983736245,0.678870315930969,
17.0934147810645));
#271179=CARTESIAN_POINT('Ctrl Pts',(1.43365138259542,0.603510887816935,
17.0880219605327));
#271180=CARTESIAN_POINT('Ctrl Pts',(1.43411467340915,0.602409148267333,
17.0879431670415));
#271181=CARTESIAN_POINT('Ctrl Pts',(1.43457668369174,0.601306900515888,
17.0878643847065));
#271182=CARTESIAN_POINT('Ctrl Pts',(1.4345766824505,0.601306903477194,16.9487204703706));
#271183=CARTESIAN_POINT('Ctrl Pts',(1.41065121726306,0.658387429704644,
16.9532277081806));
#271184=CARTESIAN_POINT('Ctrl Pts',(1.38334239509286,0.71398433722006,16.9578483572576));
#271185=CARTESIAN_POINT('Ctrl Pts',(1.30587879174838,0.850467794813364,
16.9697880774579));
#271186=CARTESIAN_POINT('Ctrl Pts',(1.25148488824473,0.928653887924648,
16.9772109967927));
#271187=CARTESIAN_POINT('Ctrl Pts',(1.1539314621347,1.04461207454308,16.9888998715124));
#271188=CARTESIAN_POINT('Ctrl Pts',(1.11522752055849,1.08583665850537,16.9932128911011));
#271189=CARTESIAN_POINT('Ctrl Pts',(1.06612735060895,1.13273226376113,16.998232468779));
#271190=CARTESIAN_POINT('Ctrl Pts',(1.05780649673004,1.1405066176505,16.9990685990261));
#271191=CARTESIAN_POINT('Ctrl Pts',(1.0459830347572,1.15131280648582,17.0002355480977));
#271192=CARTESIAN_POINT('Ctrl Pts',(1.04255138244816,1.1544211986196,17.0005717842922));
#271193=CARTESIAN_POINT('Ctrl Pts',(1.0366549692451,1.15971443563753,17.0011452493219));
#271194=CARTESIAN_POINT('Ctrl Pts',(1.03419707232768,1.16190684391341,17.0013830377421));
#271195=CARTESIAN_POINT('Ctrl Pts',(1.0294325236598,1.16612965479541,17.0018415296063));
#271196=CARTESIAN_POINT('Ctrl Pts',(1.0271268104418,1.16816103696411,17.0020623102749));
#271197=CARTESIAN_POINT('Ctrl Pts',(1.02154979698476,1.1730452257836,17.0025937325973));
#271198=CARTESIAN_POINT('Ctrl Pts',(1.01827252123555,1.17589122080303,17.002903875017));
#271199=CARTESIAN_POINT('Ctrl Pts',(1.00610862330614,1.18636539347976,17.0040472911871));
#271200=CARTESIAN_POINT('Ctrl Pts',(0.997147549874596,1.19390711290743,
17.0048745272426));
#271201=CARTESIAN_POINT('Ctrl Pts',(0.905928195060317,1.2689345560661,17.0131546221594));
#271202=CARTESIAN_POINT('Ctrl Pts',(0.817022862169967,1.32792389058456,
17.0200957731965));
#271203=CARTESIAN_POINT('Ctrl Pts',(0.62700283298634,1.4276366287111,17.034224400446));
#271204=CARTESIAN_POINT('Ctrl Pts',(0.52626293681144,1.46776063342804,17.0413851160088));
#271205=CARTESIAN_POINT('Ctrl Pts',(0.408769510776668,1.50089373899557,
17.0499029942113));
#271206=CARTESIAN_POINT('Ctrl Pts',(0.395304485573703,1.50449621809098,
17.0508810629107));
#271207=CARTESIAN_POINT('Ctrl Pts',(0.374892880614281,1.50966428237514,
17.0523674197553));
#271208=CARTESIAN_POINT('Ctrl Pts',(0.367980713570848,1.51136398951791,
17.052871393978));
#271209=CARTESIAN_POINT('Ctrl Pts',(0.355469431700181,1.51434960779717,
17.05378486863));
#271210=CARTESIAN_POINT('Ctrl Pts',(0.349874362541732,1.51565206440121,
17.0541938303977));
#271211=CARTESIAN_POINT('Ctrl Pts',(0.337865366384993,1.51837755746418,
17.0550726439349));
#271212=CARTESIAN_POINT('Ctrl Pts',(0.33144940221459,1.51979100673046,17.0555427936852));
#271213=CARTESIAN_POINT('Ctrl Pts',(0.314208083979798,1.52347493322075,
17.0568080067576));
#271214=CARTESIAN_POINT('Ctrl Pts',(0.303367324910997,1.525670621931,17.0576054329312));
#271215=CARTESIAN_POINT('Ctrl Pts',(0.251809559381007,1.53554191302735,
17.0614076889888));
#271216=CARTESIAN_POINT('Ctrl Pts',(0.21082363738004,1.54170354353255,17.0644597575803));
#271217=CARTESIAN_POINT('Ctrl Pts',(0.152765132844512,1.54807344495159,
17.0688286024449));
#271218=CARTESIAN_POINT('Ctrl Pts',(0.135857591844307,1.54964875220432,
17.0701061697115));
#271219=CARTESIAN_POINT('Ctrl Pts',(-0.00857402935856209,1.56072391446616,
17.0810630422577));
#271220=CARTESIAN_POINT('Ctrl Pts',(-0.136776883644167,1.55474078191262,
17.0911333588831));
#271221=CARTESIAN_POINT('Ctrl Pts',(-0.302537509833343,1.52632806506721,
17.1039577965584));
#271222=CARTESIAN_POINT('Ctrl Pts',(-0.34200676025461,1.51797179791216,
17.10699125915));
#271223=CARTESIAN_POINT('Ctrl Pts',(-0.387975284496668,1.5063550589897,
17.110468052147));
#271224=CARTESIAN_POINT('Ctrl Pts',(-0.394828341840151,1.5045733517298,
17.1109848813355));
#271225=CARTESIAN_POINT('Ctrl Pts',(-0.405362076225008,1.50175778641549,
17.1117767371911));
#271226=CARTESIAN_POINT('Ctrl Pts',(-0.409051388150394,1.50075708381014,
17.1120535906333));
#271227=CARTESIAN_POINT('Ctrl Pts',(-0.415838059003677,1.49888935662649,
17.1125619363595));
#271228=CARTESIAN_POINT('Ctrl Pts',(-0.41893640170209,1.49802633036415,
17.1127936464935));
#271229=CARTESIAN_POINT('Ctrl Pts',(-0.425916234884315,1.49605878755416,
17.1133148219938));
#271230=CARTESIAN_POINT('Ctrl Pts',(-0.42979611204794,1.49494877437938,
17.1136039657528));
#271231=CARTESIAN_POINT('Ctrl Pts',(-0.439764656422691,1.49205480800695,
17.1143455205239));
#271232=CARTESIAN_POINT('Ctrl Pts',(-0.445846887197351,1.49024865709088,
17.1147966849212));
#271233=CARTESIAN_POINT('Ctrl Pts',(-0.483091837997484,1.4789401345226,
17.1175524811405));
#271234=CARTESIAN_POINT('Ctrl Pts',(-0.51396349263689,1.46849704245836,
17.1198068679091));
#271235=CARTESIAN_POINT('Ctrl Pts',(-0.556369258735124,1.45265081832783,
17.122891631052));
#271236=CARTESIAN_POINT('Ctrl Pts',(-0.56819702318692,1.44806536843342,
17.1237507116978));
#271237=CARTESIAN_POINT('Ctrl Pts',(-0.593487451078253,1.43790305407977,
17.1255874441537));
#271238=CARTESIAN_POINT('Ctrl Pts',(-0.606930548159199,1.43228065560838,
17.1265636503821));
#271239=CARTESIAN_POINT('Ctrl Pts',(-0.731178810506834,1.37825195711156,
17.1356023516139));
#271240=CARTESIAN_POINT('Ctrl Pts',(-0.836061665654816,1.31727086162147,
17.1433872438295));
#271241=CARTESIAN_POINT('Ctrl Pts',(-0.969733356535987,1.21709686757906,
17.1546861510329));
#271242=CARTESIAN_POINT('Ctrl Pts',(-1.00539032086086,1.18781192853032,
17.1578527409197));
#271243=CARTESIAN_POINT('Ctrl Pts',(-1.04792466465391,1.1495897878392,17.1618592656355));
#271244=CARTESIAN_POINT('Ctrl Pts',(-1.05607878154922,1.1421034887585,17.162638357859));
#271245=CARTESIAN_POINT('Ctrl Pts',(-1.06889932089553,1.13007825144332,
17.1638813911792));
#271246=CARTESIAN_POINT('Ctrl Pts',(-1.07361846144058,1.12559584643604,
17.1643429180008));
#271247=CARTESIAN_POINT('Ctrl Pts',(-1.08245495395808,1.11709650863134,
17.1652147407189));
#271248=CARTESIAN_POINT('Ctrl Pts',(-1.08657843861664,1.11308608474222,
17.1656247503448));
#271249=CARTESIAN_POINT('Ctrl Pts',(-1.09581847478791,1.10399912589227,
17.1665507822077));
#271250=CARTESIAN_POINT('Ctrl Pts',(-1.10092214563348,1.09890974409878,
17.1670673634063));
#271251=CARTESIAN_POINT('Ctrl Pts',(-1.11389916599741,1.08578791933433,
17.1683941292419));
#271252=CARTESIAN_POINT('Ctrl Pts',(-1.12172097738593,1.07770533742928,
17.1692065340253));
#271253=CARTESIAN_POINT('Ctrl Pts',(-1.1708443051417,1.02583012727984,17.1743912778714));
#271254=CARTESIAN_POINT('Ctrl Pts',(-1.20965656967211,0.979761730200339,
17.1788674967194));
#271255=CARTESIAN_POINT('Ctrl Pts',(-1.32008634431358,0.832094091443326,
17.1928491228821));
#271256=CARTESIAN_POINT('Ctrl Pts',(-1.38228342693806,0.724083098582645,
17.2026270303946));
#271257=CARTESIAN_POINT('Ctrl Pts',(-1.44662201997292,0.573112824702904,
17.2151374687387));
#271258=CARTESIAN_POINT('Ctrl Pts',(-1.46085374442986,0.535799023713378,
17.2181394134452));
#271259=CARTESIAN_POINT('Ctrl Pts',(-1.47589636177564,0.491284096185955,
17.2215848475293));
#271260=CARTESIAN_POINT('Ctrl Pts',(-1.47811191100088,0.484577462867704,
17.2221003645994));
#271261=CARTESIAN_POINT('Ctrl Pts',(-1.48145489454376,0.474221707980983,
17.222890640125));
#271262=CARTESIAN_POINT('Ctrl Pts',(-1.48261466186322,0.470583253172999,
17.2231672141938));
#271263=CARTESIAN_POINT('Ctrl Pts',(-1.48472660558073,0.463872291670716,
17.22367529662));
#271264=CARTESIAN_POINT('Ctrl Pts',(-1.48568264617349,0.460801119318555,
17.2239070211465));
#271265=CARTESIAN_POINT('Ctrl Pts',(-1.48781804113083,0.45386567286715,
17.2244285413521));
#271266=CARTESIAN_POINT('Ctrl Pts',(-1.48899186972508,0.449999761568095,
17.2247180134872));
#271267=CARTESIAN_POINT('Ctrl Pts',(-1.49240815865066,0.438588752321901,
17.2255689477027));
#271268=CARTESIAN_POINT('Ctrl Pts',(-1.49460847194814,0.431031006024629,
17.2261280376584));
#271269=CARTESIAN_POINT('Ctrl Pts',(-1.51144754253984,0.371511570518042,
17.2304981492817));
#271270=CARTESIAN_POINT('Ctrl Pts',(-1.52343154515495,0.318829667591794,
17.2341702780645));
#271271=CARTESIAN_POINT('Ctrl Pts',(-1.54778284418114,0.178322931254887,
17.243709188987));
#271272=CARTESIAN_POINT('Ctrl Pts',(-1.55542678203105,0.0898856949061964,
17.2494634277349));
#271273=CARTESIAN_POINT('Ctrl Pts',(-1.5555643000369,-0.0777392159181324,
17.2605816601617));
#271274=CARTESIAN_POINT('Ctrl Pts',(-1.54960862271705,-0.15663349341355,
17.2659036460172));
#271275=CARTESIAN_POINT('Ctrl Pts',(-1.53589951286607,-0.246441400897236,
17.2722493047636));
#271276=CARTESIAN_POINT('Ctrl Pts',(-1.53397753675704,-0.258134811300338,
17.2730810360388));
#271277=CARTESIAN_POINT('Ctrl Pts',(-1.53064038076691,-0.277082815583653,
17.2744382700025));
#271278=CARTESIAN_POINT('Ctrl Pts',(-1.5293067428239,-0.284351446066126,
17.2749611958606));
#271279=CARTESIAN_POINT('Ctrl Pts',(-1.52683942996924,-0.297279184021857,
17.275895445311));
#271280=CARTESIAN_POINT('Ctrl Pts',(-1.52572594961302,-0.302942045937434,
17.2763061208544));
#271281=CARTESIAN_POINT('Ctrl Pts',(-1.52331135952387,-0.31487093745215,
17.2771743134407));
#271282=CARTESIAN_POINT('Ctrl Pts',(-1.5220030453951,-0.321135380883416,
17.2776320529928));
#271283=CARTESIAN_POINT('Ctrl Pts',(-1.51843055118434,-0.33772877269013,
17.2788494276892));
#271284=CARTESIAN_POINT('Ctrl Pts',(-1.51609967535642,-0.348042851960356,
17.2796111774784));
#271285=CARTESIAN_POINT('Ctrl Pts',(-1.5044867037265,-0.397098278603461,
17.2832590184124));
#271286=CARTESIAN_POINT('Ctrl Pts',(-1.49382453463064,-0.435493983656121,
17.286188866976));
#271287=CARTESIAN_POINT('Ctrl Pts',(-1.43619853328125,-0.615845046848618,
17.3003234502519));
#271288=CARTESIAN_POINT('Ctrl Pts',(-1.37040185280259,-0.750943510157263,
17.3121309454437));
#271289=CARTESIAN_POINT('Ctrl Pts',(-1.26496539288794,-0.90603131375259,
17.3264141750078));
#271290=CARTESIAN_POINT('Ctrl Pts',(-1.24240560334809,-0.936727866878998,
17.3292759945909));
#271291=CARTESIAN_POINT('Ctrl Pts',(-1.21462243135818,-0.971759486173735,
17.3325566004207));
#271292=CARTESIAN_POINT('Ctrl Pts',(-1.21047208769491,-0.976924500056415,
17.3330406688579));
#271293=CARTESIAN_POINT('Ctrl Pts',(-1.20368721237451,-0.985258506381139,
17.3338221453396));
#271294=CARTESIAN_POINT('Ctrl Pts',(-1.20107292650043,-0.988443754554928,
17.3341209225585));
#271295=CARTESIAN_POINT('Ctrl Pts',(-1.19639194625467,-0.994101072580532,
17.3346516986926));
#271296=CARTESIAN_POINT('Ctrl Pts',(-1.19433020394037,-0.996577140129893,
17.3348840435856));
#271297=CARTESIAN_POINT('Ctrl Pts',(-1.18984740224431,-1.00192690759184,
17.3353861191417));
#271298=CARTESIAN_POINT('Ctrl Pts',(-1.18742362230327,-1.00479824382265,
17.335655647426));
#271299=CARTESIAN_POINT('Ctrl Pts',(-1.18059831963597,-1.01282466641958,
17.3364093203394));
#271300=CARTESIAN_POINT('Ctrl Pts',(-1.17617339823225,-1.01795989066736,
17.3368917966454));
#271301=CARTESIAN_POINT('Ctrl Pts',(-1.14927871464012,-1.04876230029075,
17.3397887209236));
#271302=CARTESIAN_POINT('Ctrl Pts',(-1.12600108223504,-1.0737159471893,
17.3421478902356));
#271303=CARTESIAN_POINT('Ctrl Pts',(-1.01257864251097,-1.18755506920908,
17.3530869096874));
#271304=CARTESIAN_POINT('Ctrl Pts',(-0.912621221041073,-1.26599002033087,
17.361191472381));
#271305=CARTESIAN_POINT('Ctrl Pts',(-0.749595222740299,-1.36446512563377,
17.3739176921002));
#271306=CARTESIAN_POINT('Ctrl Pts',(-0.692960729870463,-1.39408101267082,
17.378255078321));
#271307=CARTESIAN_POINT('Ctrl Pts',(-0.624280775254326,-1.42477482558215,
17.3835134132907));
#271308=CARTESIAN_POINT('Ctrl Pts',(-0.613839299660503,-1.42930440846725,
17.3843126891726));
#271309=CARTESIAN_POINT('Ctrl Pts',(-0.596668376026993,-1.43653041680071,
17.3856273349851));
#271310=CARTESIAN_POINT('Ctrl Pts',(-0.589967989060717,-1.43929516014522,
17.3861403911803));
#271311=CARTESIAN_POINT('Ctrl Pts',(-0.577912598806179,-1.44417118423408,
17.3870637134475));
#271312=CARTESIAN_POINT('Ctrl Pts',(-0.572564701082553,-1.44629977621355,
17.387473388467));
#271313=CARTESIAN_POINT('Ctrl Pts',(-0.561168972070333,-1.45076244032229,
17.3883465905612));
#271314=CARTESIAN_POINT('Ctrl Pts',(-0.555118134554774,-1.45308847900039,
17.3888103775251));
#271315=CARTESIAN_POINT('Ctrl Pts',(-0.538807193992186,-1.45924191802844,
17.3900610630777));
#271316=CARTESIAN_POINT('Ctrl Pts',(-0.5285210885085,-1.46299884321139,
17.3908502865333));
#271317=CARTESIAN_POINT('Ctrl Pts',(-0.476225403894931,-1.48147598227702,
17.394866136168));
#271318=CARTESIAN_POINT('Ctrl Pts',(-0.433641533703983,-1.49449523301362,
17.3981479766127));
#271319=CARTESIAN_POINT('Ctrl Pts',(-0.306706351760254,-1.52742146809097,
17.4079748907209));
#271320=CARTESIAN_POINT('Ctrl Pts',(-0.221190032584251,-1.54212730821209,
17.4146610622803));
#271321=CARTESIAN_POINT('Ctrl Pts',(-0.0476035777568375,-1.55723908488537,
17.428172722137));
#271322=CARTESIAN_POINT('Ctrl Pts',(0.0401942170759024,-1.55744900950112,
17.4349737173638));
#271323=CARTESIAN_POINT('Ctrl Pts',(0.139870214339904,-1.54924800501987,
17.4423820589408));
#271324=CARTESIAN_POINT('Ctrl Pts',(0.152178138610366,-1.54808749679548,
17.4432911709351));
#271325=CARTESIAN_POINT('Ctrl Pts',(0.169371344039356,-1.54625931798855,
17.444552022568));
#271326=CARTESIAN_POINT('Ctrl Pts',(0.174268848550884,-1.54571501282018,
17.4449101416354));
#271327=CARTESIAN_POINT('Ctrl Pts',(0.182161693362209,-1.54479981739838,
17.4454855292806));
#271328=CARTESIAN_POINT('Ctrl Pts',(0.185158630688581,-1.5444434726692,
17.4457035963151));
#271329=CARTESIAN_POINT('Ctrl Pts',(0.191471477455945,-1.54367421715733,
17.4461620503212));
#271330=CARTESIAN_POINT('Ctrl Pts',(0.194787125711285,-1.54325934031195,
17.4464023208941));
#271331=CARTESIAN_POINT('Ctrl Pts',(0.202940182094938,-1.54221247949117,
17.4469919150714));
#271332=CARTESIAN_POINT('Ctrl Pts',(0.207776058966439,-1.54156840926714,
17.4473405658007));
#271333=CARTESIAN_POINT('Ctrl Pts',(0.225478575423955,-1.53912586990373,
17.4486132439202));
#271334=CARTESIAN_POINT('Ctrl Pts',(0.238326048206005,-1.53718891341575,
17.4495298786573));
#271335=CARTESIAN_POINT('Ctrl Pts',(0.324254962320279,-1.52313052945659,
17.4556229183146));
#271336=CARTESIAN_POINT('Ctrl Pts',(0.396424431272561,-1.50596101982678,
17.4605590621444));
#271337=CARTESIAN_POINT('Ctrl Pts',(0.594575958919266,-1.44357866735489,
17.47427807543));
#271338=CARTESIAN_POINT('Ctrl Pts',(0.716329082674257,-1.38719439360538,
17.4829551333107));
#271339=CARTESIAN_POINT('Ctrl Pts',(0.844160802090589,-1.30662858782822,
17.4934514732183));
#271340=CARTESIAN_POINT('Ctrl Pts',(0.858788368133264,-1.29706137945197,
17.4946740659064));
#271341=CARTESIAN_POINT('Ctrl Pts',(0.879056386197448,-1.28331186013718,
17.4964001889486));
#271342=CARTESIAN_POINT('Ctrl Pts',(0.884834852460365,-1.27933449162295,
17.496896040153));
#271343=CARTESIAN_POINT('Ctrl Pts',(0.895390292746814,-1.27196336767508,
17.4978087951101));
#271344=CARTESIAN_POINT('Ctrl Pts',(0.900175396133304,-1.26858142802688,
17.4982252450285));
#271345=CARTESIAN_POINT('Ctrl Pts',(0.909855076808487,-1.26165783341647,
17.4990731844213));
#271346=CARTESIAN_POINT('Ctrl Pts',(0.914748352841473,-1.25811454108599,
17.4995047318337));
#271347=CARTESIAN_POINT('Ctrl Pts',(0.926817386233817,-1.24926754642543,
17.500576408885));
#271348=CARTESIAN_POINT('Ctrl Pts',(0.93396830432656,-1.2439304925656,17.5012178238799));
#271349=CARTESIAN_POINT('Ctrl Pts',(0.960721416522171,-1.22360270198446,
17.5036422559697));
#271350=CARTESIAN_POINT('Ctrl Pts',(0.98001089325329,-1.20820848037454,
17.5054410171653));
#271351=CARTESIAN_POINT('Ctrl Pts',(1.02747424977924,-1.1684451312156,17.5099995636182));
#271352=CARTESIAN_POINT('Ctrl Pts',(1.05515294055462,-1.14351179353789,
17.512780905484));
#271353=CARTESIAN_POINT('Ctrl Pts',(1.19069544862219,-1.01229926667695,
17.527041030381));
#271354=CARTESIAN_POINT('Ctrl Pts',(1.28350849502977,-0.891685862471345,
17.5390689531139));
#271355=CARTESIAN_POINT('Ctrl Pts',(1.36718971042241,-0.74214001425734,
17.5518969241535));
#271356=CARTESIAN_POINT('Ctrl Pts',(1.37661069057193,-0.724515432997913,
17.5533777007348));
#271357=CARTESIAN_POINT('Ctrl Pts',(1.38839684147589,-0.701405700235204,
17.555274906769));
#271358=CARTESIAN_POINT('Ctrl Pts',(1.39107321793935,-0.696082646801564,
17.5557088932698));
#271359=CARTESIAN_POINT('Ctrl Pts',(1.39530736332402,-0.687539384901019,
17.5564004617379));
#271360=CARTESIAN_POINT('Ctrl Pts',(1.39688468770652,-0.684329024586538,
17.5566592232629));
#271361=CARTESIAN_POINT('Ctrl Pts',(1.39987904725894,-0.678181052562585,
17.5571525961916));
#271362=CARTESIAN_POINT('Ctrl Pts',(1.40129790137036,-0.675244458583352,
17.5573873116029));
#271363=CARTESIAN_POINT('Ctrl Pts',(1.40462650090365,-0.668299599985734,
17.5579402098999));
#271364=CARTESIAN_POINT('Ctrl Pts',(1.40652833724146,-0.66428758849565,
17.5582579041266));
#271365=CARTESIAN_POINT('Ctrl Pts',(1.41276789502226,-0.650978020280832,
17.5593063566281));
#271366=CARTESIAN_POINT('Ctrl Pts',(1.4170309323208,-0.6416454315532,17.5600327118311));
#271367=CARTESIAN_POINT('Ctrl Pts',(1.4270234861773,-0.619184442842082,
17.5617614557874));
#271368=CARTESIAN_POINT('Ctrl Pts',(1.43266472277255,-0.606017517396869,
17.5627591650315));
#271369=CARTESIAN_POINT('Ctrl Pts',(1.45318464212921,-0.556234330639917,
17.5664796694373));
#271370=CARTESIAN_POINT('Ctrl Pts',(1.46684894186761,-0.519130922979059,
17.5691485122344));
#271371=CARTESIAN_POINT('Ctrl Pts',(1.52248940548107,-0.348228695388594,
17.5811458693348));
#271372=CARTESIAN_POINT('Ctrl Pts',(1.54766876886642,-0.209664333579345,
17.5901294631626));
#271373=CARTESIAN_POINT('Ctrl Pts',(1.55420874426898,-0.0636469458925181,
17.6001448968772));
#271374=CARTESIAN_POINT('Ctrl Pts',(1.55444114672544,-0.0576929314050126,
17.6005540967318));
#271375=CARTESIAN_POINT('Ctrl Pts',(1.55548393915306,-0.0263586577107222,
17.6027121701981));
#271376=CARTESIAN_POINT('Ctrl Pts',(1.55570691560009,-0.000963988855314317,
17.6044770347516));
#271377=CARTESIAN_POINT('Ctrl Pts',(1.55516192950211,0.0337410831718555,
17.6069159347291));
#271378=CARTESIAN_POINT('Ctrl Pts',(1.55493189003653,0.043056918905161,
17.6075732541421));
#271379=CARTESIAN_POINT('Ctrl Pts',(1.5544325627692,0.0578796041006588,
17.6086235937809));
#271380=CARTESIAN_POINT('Ctrl Pts',(1.55421767434555,0.0633881700060483,
17.6090149130737));
#271381=CARTESIAN_POINT('Ctrl Pts',(1.55371648378194,0.0746927957007798,
17.6098200463262));
#271382=CARTESIAN_POINT('Ctrl Pts',(1.55342701982006,0.0804886210664853,
17.6102339527805));
#271383=CARTESIAN_POINT('Ctrl Pts',(1.55268192440377,0.093900493853736,
17.6111944152708));
#271384=CARTESIAN_POINT('Ctrl Pts',(1.55220267921316,0.101515023115226,
17.6117417002655));
#271385=CARTESIAN_POINT('Ctrl Pts',(1.55050463073375,0.125659739615937,
17.6134835666887));
#271386=CARTESIAN_POINT('Ctrl Pts',(1.54907766158329,0.142173622688831,
17.6146846048149));
#271387=CARTESIAN_POINT('Ctrl Pts',(1.54058531952777,0.224997650445406,
17.6207592771234));
#271388=CARTESIAN_POINT('Ctrl Pts',(1.52952584874133,0.290818553216241,
17.6257557775075));
#271389=CARTESIAN_POINT('Ctrl Pts',(1.49455995587657,0.439666811062609,
17.6374320639716));
#271390=CARTESIAN_POINT('Ctrl Pts',(1.46789682906557,0.521812883171184,
17.6441592130327));
#271391=CARTESIAN_POINT('Ctrl Pts',(1.43457667260785,0.601306926959429,
17.650811911463));
#271392=CARTESIAN_POINT('Origin',(0.,0.,-1.29405622560371));
#271393=CARTESIAN_POINT('',(1.4345766894261,0.601306886835045,18.4895593986216));
#271394=CARTESIAN_POINT('',(1.43457668357356,0.601306900797837,18.3502241513278));
#271395=CARTESIAN_POINT('',(1.43457668357355,0.601306900797845,-1.29405622560371));
#271396=CARTESIAN_POINT('Ctrl Pts',(1.4345766894261,0.601306886835045,18.4895593986216));
#271397=CARTESIAN_POINT('Ctrl Pts',(1.44099262732833,0.585999969257908,
18.4883253124721));
#271398=CARTESIAN_POINT('Ctrl Pts',(1.44716375031046,0.570589955881822,
18.4870836263227));
#271399=CARTESIAN_POINT('Ctrl Pts',(1.50521501525075,0.418624171181762,
18.47484644818));
#271400=CARTESIAN_POINT('Ctrl Pts',(1.53785299730756,0.275529789507252,
18.4632869760968));
#271401=CARTESIAN_POINT('Ctrl Pts',(1.55271006181731,0.0983794845858045,
18.4498238883417));
#271402=CARTESIAN_POINT('Ctrl Pts',(1.55439400902584,0.0666835145531882,
18.4474515840324));
#271403=CARTESIAN_POINT('Ctrl Pts',(1.55525525106296,0.028368393556693,
18.4446443741028));
#271404=CARTESIAN_POINT('Ctrl Pts',(1.55536146467843,0.0217802678371933,
18.4441638484235));
#271405=CARTESIAN_POINT('Ctrl Pts',(1.55546184680569,0.0115023590345889,
18.4434177712575));
#271406=CARTESIAN_POINT('Ctrl Pts',(1.55548475348198,0.00781303948000507,
18.4431506805459));
#271407=CARTESIAN_POINT('Ctrl Pts',(1.55550297799219,0.000938469125552495,
18.4426543727589));
#271408=CARTESIAN_POINT('Ctrl Pts',(1.55550163873953,-0.00224665648035469,
18.4424249810905));
#271409=CARTESIAN_POINT('Ctrl Pts',(1.55547620170596,-0.00953092583499308,
18.4419016242649));
#271410=CARTESIAN_POINT('Ctrl Pts',(1.5554456843582,-0.0136299916416392,
18.4416080194258));
#271411=CARTESIAN_POINT('Ctrl Pts',(1.55532327272769,-0.0243694262571884,
18.4408410355608));
#271412=CARTESIAN_POINT('Ctrl Pts',(1.55520505607159,-0.0310095043566609,
18.4403690738874));
#271413=CARTESIAN_POINT('Ctrl Pts',(1.55409443362784,-0.0768826299381814,
18.4371228343138));
#271414=CARTESIAN_POINT('Ctrl Pts',(1.55165997838199,-0.116070700703275,
18.4344219490485));
#271415=CARTESIAN_POINT('Ctrl Pts',(1.53278910478316,-0.304348693341901,
18.4216134252618));
#271416=CARTESIAN_POINT('Ctrl Pts',(1.49633371708744,-0.450624091519519,
18.4120945941951));
#271417=CARTESIAN_POINT('Ctrl Pts',(1.42487850704468,-0.6251320705219,18.3992626610119));
#271418=CARTESIAN_POINT('Ctrl Pts',(1.40893616252026,-0.660278223834177,
18.3966018427199));
#271419=CARTESIAN_POINT('Ctrl Pts',(1.38706817648677,-0.704080880216519,
18.3931681062349));
#271420=CARTESIAN_POINT('Ctrl Pts',(1.38233861890689,-0.713321768556348,
18.3924369064952));
#271421=CARTESIAN_POINT('Ctrl Pts',(1.37458797847935,-0.72809882861183,
18.3912563192389));
#271422=CARTESIAN_POINT('Ctrl Pts',(1.37162504272376,-0.733665288023133,
18.3908089828107));
#271423=CARTESIAN_POINT('Ctrl Pts',(1.36591905692746,-0.744229724501757,
18.389954920219));
#271424=CARTESIAN_POINT('Ctrl Pts',(1.36318220897893,-0.749230950002752,
18.3895484196763));
#271425=CARTESIAN_POINT('Ctrl Pts',(1.35686907877674,-0.760618251300391,
18.3886177862348));
#271426=CARTESIAN_POINT('Ctrl Pts',(1.35327511571427,-0.766994314807492,
18.3880930273882));
#271427=CARTESIAN_POINT('Ctrl Pts',(1.34378293520718,-0.783560009482311,
18.3867198940818));
#271428=CARTESIAN_POINT('Ctrl Pts',(1.33781389059965,-0.79370828731514,
18.3858689842551));
#271429=CARTESIAN_POINT('Ctrl Pts',(1.29051723935601,-0.87207026867969,
18.379221095764));
#271430=CARTESIAN_POINT('Ctrl Pts',(1.24412093999459,-0.937070127111359,
18.373237264182));
#271431=CARTESIAN_POINT('Ctrl Pts',(1.12461686025537,-1.0798875346337,18.3589644413066));
#271432=CARTESIAN_POINT('Ctrl Pts',(1.04807677573844,-1.15431986270894,
18.3506025653542));
#271433=CARTESIAN_POINT('Ctrl Pts',(0.935112393364499,-1.24360426880536,
18.3396454061971));
#271434=CARTESIAN_POINT('Ctrl Pts',(0.904854885140763,-1.26579025872893,
18.336829731358));
#271435=CARTESIAN_POINT('Ctrl Pts',(0.868120824893188,-1.29073388894021,
18.3335750105203));
#271436=CARTESIAN_POINT('Ctrl Pts',(0.862393938066913,-1.29456727867069,
18.3330721523315));
#271437=CARTESIAN_POINT('Ctrl Pts',(0.853509059394139,-1.30042939840533,
18.3322992375892));
#271438=CARTESIAN_POINT('Ctrl Pts',(0.850368981347824,-1.30248490627538,
18.3320274586255));
#271439=CARTESIAN_POINT('Ctrl Pts',(0.844557515507106,-1.30625914072608,
18.3315270591057));
#271440=CARTESIAN_POINT('Ctrl Pts',(0.841888319921899,-1.30798103842754,
18.3312982348637));
#271441=CARTESIAN_POINT('Ctrl Pts',(0.835840795634892,-1.31185611356475,
18.3307820535295));
#271442=CARTESIAN_POINT('Ctrl Pts',(0.8324594165039,-1.31400442129854,18.3304950194327));
#271443=CARTESIAN_POINT('Ctrl Pts',(0.822427045266144,-1.32032406610473,
18.3296479518456));
#271444=CARTESIAN_POINT('Ctrl Pts',(0.815752597956168,-1.3244582251277,
18.3290902910988));
#271445=CARTESIAN_POINT('Ctrl Pts',(0.761437172958825,-1.35753488813396,
18.3245971366684));
#271446=CARTESIAN_POINT('Ctrl Pts',(0.71229676877724,-1.38395176898821,
18.3208102353864));
#271447=CARTESIAN_POINT('Ctrl Pts',(0.539473415545995,-1.46520700576085,
18.3080508928008));
#271448=CARTESIAN_POINT('Ctrl Pts',(0.410135161450797,-1.50653686145066,
18.2993841477549));
#271449=CARTESIAN_POINT('Ctrl Pts',(0.241384635176272,-1.53708477167178,
18.2876917611887));
#271450=CARTESIAN_POINT('Ctrl Pts',(0.205477170021583,-1.54229533969842,
18.2851866318275));
#271451=CARTESIAN_POINT('Ctrl Pts',(0.159313589844035,-1.54735349898748,
18.281928418628));
#271452=CARTESIAN_POINT('Ctrl Pts',(0.149194093412839,-1.54836196817265,
18.2812119192598));
#271453=CARTESIAN_POINT('Ctrl Pts',(0.132832027352404,-1.54983065965365,
18.2800494334376));
#271454=CARTESIAN_POINT('Ctrl Pts',(0.126595172320891,-1.55035256679105,
18.2796053859526));
#271455=CARTESIAN_POINT('Ctrl Pts',(0.114660944160205,-1.55127874356464,
18.2787538357524));
#271456=CARTESIAN_POINT('Ctrl Pts',(0.108964148856134,-1.55168930041261,
18.2783465372102));
#271457=CARTESIAN_POINT('Ctrl Pts',(0.0959960805833042,-1.55255211759448,
18.2774174598443));
#271458=CARTESIAN_POINT('Ctrl Pts',(0.0887236790606858,-1.55298468465123,
18.2768950734314));
#271459=CARTESIAN_POINT('Ctrl Pts',(0.0695389104639085,-1.55399061164669,
18.2755132662739));
#271460=CARTESIAN_POINT('Ctrl Pts',(0.057622730851717,-1.55447807553019,
18.274651186594));
#271461=CARTESIAN_POINT('Ctrl Pts',(-0.0464485217667476,-1.55753713248777,
18.2670873490543));
#271462=CARTESIAN_POINT('Ctrl Pts',(-0.138639676173716,-1.55204783098059,
18.2601321836644));
#271463=CARTESIAN_POINT('Ctrl Pts',(-0.32250845557302,-1.52458440797311,
18.2458108166579));
#271464=CARTESIAN_POINT('Ctrl Pts',(-0.413787248841978,-1.50238134171011,
18.2384695942592));
#271465=CARTESIAN_POINT('Ctrl Pts',(-0.537984195734153,-1.45998567522091,
18.2284832640889));
#271466=CARTESIAN_POINT('Ctrl Pts',(-0.57301114219307,-1.4465973777693,
18.2256692454341));
#271467=CARTESIAN_POINT('Ctrl Pts',(-0.613866109633851,-1.42926418844628,
18.2224162056396));
#271468=CARTESIAN_POINT('Ctrl Pts',(-0.620191007168949,-1.42653105129318,
18.2219134445991));
#271469=CARTESIAN_POINT('Ctrl Pts',(-0.629932434868032,-1.42224451458921,
18.2211406559713));
#271470=CARTESIAN_POINT('Ctrl Pts',(-0.633361747014747,-1.42072067275909,
18.2208689067071));
#271471=CARTESIAN_POINT('Ctrl Pts',(-0.639683885475553,-1.4178839403086,
18.2203685175538));
#271472=CARTESIAN_POINT('Ctrl Pts',(-0.642578185280274,-1.41657460717597,
18.2201396742988));
#271473=CARTESIAN_POINT('Ctrl Pts',(-0.649114309721366,-1.41359361886664,
18.2196234032342));
#271474=CARTESIAN_POINT('Ctrl Pts',(-0.652753694096921,-1.41191675469987,
18.2193362987182));
#271475=CARTESIAN_POINT('Ctrl Pts',(-0.663506702440633,-1.4069117898032,
18.2184889630306));
#271476=CARTESIAN_POINT('Ctrl Pts',(-0.670601789610282,-1.4035437916603,
18.2179311059489));
#271477=CARTESIAN_POINT('Ctrl Pts',(-0.727913745657558,-1.37580430717528,
18.2134324804981));
#271478=CARTESIAN_POINT('Ctrl Pts',(-0.776817761694269,-1.34879639978296,
18.2096406754315));
#271479=CARTESIAN_POINT('Ctrl Pts',(-0.939025099630886,-1.24745851724816,
18.1968625482307));
#271480=CARTESIAN_POINT('Ctrl Pts',(-1.04401443246632,-1.16101497075151,
18.1881821369283));
#271481=CARTESIAN_POINT('Ctrl Pts',(-1.16108416153649,-1.03574219593744,
18.1764894060544));
#271482=CARTESIAN_POINT('Ctrl Pts',(-1.18476015245662,-1.00857392364514,
18.1740008957899));
#271483=CARTESIAN_POINT('Ctrl Pts',(-1.21386745043356,-0.972732768074702,
18.170761357718));
#271484=CARTESIAN_POINT('Ctrl Pts',(-1.22018731831987,-0.964793306792589,
18.1700463785509));
#271485=CARTESIAN_POINT('Ctrl Pts',(-1.23027621267952,-0.951861235651385,
18.1688856971323));
#271486=CARTESIAN_POINT('Ctrl Pts',(-1.23409367329407,-0.946906634720758,
18.1684419216164));
#271487=CARTESIAN_POINT('Ctrl Pts',(-1.24134136563078,-0.937381734916853,
18.1675904464395));
#271488=CARTESIAN_POINT('Ctrl Pts',(-1.24477650538448,-0.932815283441667,
18.1671829484996));
#271489=CARTESIAN_POINT('Ctrl Pts',(-1.25254099298447,-0.922374415461869,
18.166252797018));
#271490=CARTESIAN_POINT('Ctrl Pts',(-1.25685429177768,-0.916488290859181,
18.1657295316527));
#271491=CARTESIAN_POINT('Ctrl Pts',(-1.26812975415566,-0.900871979136829,
18.1643440601856));
#271492=CARTESIAN_POINT('Ctrl Pts',(-1.27502122562983,-0.891091608917545,
18.1634791736943));
#271493=CARTESIAN_POINT('Ctrl Pts',(-1.33583058462001,-0.802641244987016,
18.1556808901109));
#271494=CARTESIAN_POINT('Ctrl Pts',(-1.38250890604917,-0.719262747387282,
18.1484753071038));
#271495=CARTESIAN_POINT('Ctrl Pts',(-1.45859351186842,-0.548203239973813,
18.1340376678064));
#271496=CARTESIAN_POINT('Ctrl Pts',(-1.48842150298396,-0.46111144524232,
18.1268469235825));
#271497=CARTESIAN_POINT('Ctrl Pts',(-1.51903955266582,-0.33676149716116,
18.1171117755219));
#271498=CARTESIAN_POINT('Ctrl Pts',(-1.52646272842221,-0.301332924161396,
18.1143977850868));
#271499=CARTESIAN_POINT('Ctrl Pts',(-1.53381012171295,-0.258946677652709,
18.1112449967756));
#271500=CARTESIAN_POINT('Ctrl Pts',(-1.53493203790112,-0.252211250704046,
18.1107468094738));
#271501=CARTESIAN_POINT('Ctrl Pts',(-1.53659976130025,-0.241775535931313,
18.1099794957395));
#271502=CARTESIAN_POINT('Ctrl Pts',(-1.53717661765396,-0.238080413183043,
18.1097086860612));
#271503=CARTESIAN_POINT('Ctrl Pts',(-1.53821903976589,-0.231241295104207,
18.1092091366221));
#271504=CARTESIAN_POINT('Ctrl Pts',(-1.53868829352599,-0.228097975855216,
18.108980199246));
#271505=CARTESIAN_POINT('Ctrl Pts',(-1.53972997980427,-0.220970672634736,
18.1084625742004));
#271506=CARTESIAN_POINT('Ctrl Pts',(-1.54029658535265,-0.216985895878232,
18.1081742169543));
#271507=CARTESIAN_POINT('Ctrl Pts',(-1.54193456342525,-0.205136657505268,
18.1073197168071));
#271508=CARTESIAN_POINT('Ctrl Pts',(-1.54296123858723,-0.197265986512507,
18.1067560080165));
#271509=CARTESIAN_POINT('Ctrl Pts',(-1.55158387649242,-0.126972417229791,
18.101753254382));
#271510=CARTESIAN_POINT('Ctrl Pts',(-1.55544934855044,-0.0641411672581848,
18.0975039681037));
#271511=CARTESIAN_POINT('Ctrl Pts',(-1.55557649265697,0.0953077447216411,
18.086895551804));
#271512=CARTESIAN_POINT('Ctrl Pts',(-1.54666464037744,0.191652626258326,
18.080636899838));
#271513=CARTESIAN_POINT('Ctrl Pts',(-1.51722265917634,0.348739012408554,
18.0699541997557));
#271514=CARTESIAN_POINT('Ctrl Pts',(-1.5017850109423,0.410150797896472,
18.0656549407979));
#271515=CARTESIAN_POINT('Ctrl Pts',(-1.47924411408363,0.481190341075226,
18.0604445189198));
#271516=CARTESIAN_POINT('Ctrl Pts',(-1.47571860479897,0.491896209664127,
18.0596528927329));
#271517=CARTESIAN_POINT('Ctrl Pts',(-1.46976139478114,0.509345723631646,
18.0583516364342));
#271518=CARTESIAN_POINT('Ctrl Pts',(-1.46739882868512,0.516112679786625,
18.0578442823139));
#271519=CARTESIAN_POINT('Ctrl Pts',(-1.46307895049382,0.528216380201834,
18.056931790686));
#271520=CARTESIAN_POINT('Ctrl Pts',(-1.46113898069707,0.533559216215017,
18.0565272341718));
#271521=CARTESIAN_POINT('Ctrl Pts',(-1.45695499241949,0.544888309948024,
18.0556655862453));
#271522=CARTESIAN_POINT('Ctrl Pts',(-1.45470327195844,0.550871589894027,
18.0552082443756));
#271523=CARTESIAN_POINT('Ctrl Pts',(-1.44855700065793,0.566902987328941,
18.0539766305722));
#271524=CARTESIAN_POINT('Ctrl Pts',(-1.44459486962785,0.576924633703933,
18.0532001098454));
#271525=CARTESIAN_POINT('Ctrl Pts',(-1.42415751167201,0.627087187710649,
18.0492792102401));
#271526=CARTESIAN_POINT('Ctrl Pts',(-1.40611350201907,0.666563643426204,
18.0460823718672));
#271527=CARTESIAN_POINT('Ctrl Pts',(-1.30859408566014,0.858281378753664,
18.0299791444942));
#271528=CARTESIAN_POINT('Ctrl Pts',(-1.20596047058541,0.9973504821537,18.0162626550089));
#271529=CARTESIAN_POINT('Ctrl Pts',(-1.07140623721043,1.12779282998613,
18.0023113678841));
#271530=CARTESIAN_POINT('Ctrl Pts',(-1.0599389199155,1.13857697586493,18.0011496421168));
#271531=CARTESIAN_POINT('Ctrl Pts',(-1.04432374498317,1.15282143830702,
17.9996061082658));
#271532=CARTESIAN_POINT('Ctrl Pts',(-1.04031922357721,1.15643645235584,
17.9992135808113));
#271533=CARTESIAN_POINT('Ctrl Pts',(-1.03399674381684,1.16208454444556,
17.9985991382254));
#271534=CARTESIAN_POINT('Ctrl Pts',(-1.0316914626088,1.16413164251117,17.998376197177));
#271535=CARTESIAN_POINT('Ctrl Pts',(-1.02696427770189,1.16830432923321,
17.9979212975794));
#271536=CARTESIAN_POINT('Ctrl Pts',(-1.02454188864819,1.17042921699715,
17.9976893990028));
#271537=CARTESIAN_POINT('Ctrl Pts',(-1.01879854225242,1.17543571148285,
17.9971423927193));
#271538=CARTESIAN_POINT('Ctrl Pts',(-1.01547194286804,1.17831078924332,
17.9968277672999));
#271539=CARTESIAN_POINT('Ctrl Pts',(-1.00438672081637,1.18780959450976,
17.9957864605753));
#271540=CARTESIAN_POINT('Ctrl Pts',(-0.996574914238254,1.19437128764136,
17.995064147019));
#271541=CARTESIAN_POINT('Ctrl Pts',(-0.977688205756535,1.20992125257977,
17.993343548437));
#271542=CARTESIAN_POINT('Ctrl Pts',(-0.96655293761215,1.2188351481963,17.992349926939));
#271543=CARTESIAN_POINT('Ctrl Pts',(-0.924167320144902,1.25181900548173,
17.9886384379965));
#271544=CARTESIAN_POINT('Ctrl Pts',(-0.892125765467794,1.27485221686184,
17.9859745206246));
#271545=CARTESIAN_POINT('Ctrl Pts',(-0.74230372613235,1.3741340559806,17.9739763288162));
#271546=CARTESIAN_POINT('Ctrl Pts',(-0.615428649756594,1.43544676418496,
17.9649902542972));
#271547=CARTESIAN_POINT('Ctrl Pts',(-0.476515378732291,1.48072524226858,
17.9549813409096));
#271548=CARTESIAN_POINT('Ctrl Pts',(-0.470969682316836,1.48249846751525,
17.9545816218799));
#271549=CARTESIAN_POINT('Ctrl Pts',(-0.440813428220075,1.49195458292039,
17.952406962847));
#271550=CARTESIAN_POINT('Ctrl Pts',(-0.416025975249983,1.49905543951122,
17.9506154867378));
#271551=CARTESIAN_POINT('Ctrl Pts',(-0.38206743833399,1.50787642984636,
17.9481502600115));
#271552=CARTESIAN_POINT('Ctrl Pts',(-0.373039533313863,1.51013521082684,
17.9474938497226));
#271553=CARTESIAN_POINT('Ctrl Pts',(-0.358680243632234,1.5135912866127,
17.9464479295517));
#271554=CARTESIAN_POINT('Ctrl Pts',(-0.353361774722541,1.5148417590165,
17.9460601312896));
#271555=CARTESIAN_POINT('Ctrl Pts',(-0.34246141974605,1.51734411063948,
17.9452644434042));
#271556=CARTESIAN_POINT('Ctrl Pts',(-0.336879001227993,1.5185932671491,
17.9448564733315));
#271557=CARTESIAN_POINT('Ctrl Pts',(-0.32399197203918,1.52140239328206,
17.9439135178281));
#271558=CARTESIAN_POINT('Ctrl Pts',(-0.316682813591592,1.52294058721888,
17.9433778464958));
#271559=CARTESIAN_POINT('Ctrl Pts',(-0.29366551257478,1.527611657187,17.9416881050753));
#271560=CARTESIAN_POINT('Ctrl Pts',(-0.277920348728082,1.53055449185459,
17.9405280402885));
#271561=CARTESIAN_POINT('Ctrl Pts',(-0.19999858621564,1.54387640563394,
17.9347643142724));
#271562=CARTESIAN_POINT('Ctrl Pts',(-0.137284555786867,1.55071104944769,
17.9300510861638));
#271563=CARTESIAN_POINT('Ctrl Pts',(0.0361201960514034,1.55900742080409,
17.9168239847331));
#271564=CARTESIAN_POINT('Ctrl Pts',(0.146815121103837,1.55249844714107,
17.9081425744055));
#271565=CARTESIAN_POINT('Ctrl Pts',(0.269268730094863,1.53207664963422,
17.8986468272466));
#271566=CARTESIAN_POINT('Ctrl Pts',(0.282628592492905,1.52966846341167,
17.8976127506854));
#271567=CARTESIAN_POINT('Ctrl Pts',(0.327151869831379,1.52103966651652,
17.8941762651607));
#271568=CARTESIAN_POINT('Ctrl Pts',(0.358158504806672,1.51403859420429,
17.8917988869589));
#271569=CARTESIAN_POINT('Ctrl Pts',(0.394973212107597,1.50453160422406,
17.8890116289492));
#271570=CARTESIAN_POINT('Ctrl Pts',(0.401005607914505,1.50293502598157,
17.88855606867));
#271571=CARTESIAN_POINT('Ctrl Pts',(0.410867149888422,1.50026139541515,
17.8878134090439));
#271572=CARTESIAN_POINT('Ctrl Pts',(0.414701984828125,1.49920590119147,
17.88752512811));
#271573=CARTESIAN_POINT('Ctrl Pts',(0.421590857204795,1.49728136327028,
17.8870082415381));
#271574=CARTESIAN_POINT('Ctrl Pts',(0.424646302092774,1.49641767244223,
17.886779336226));
#271575=CARTESIAN_POINT('Ctrl Pts',(0.431330511419027,1.49450610738197,
17.8862793453093));
#271576=CARTESIAN_POINT('Ctrl Pts',(0.434958105813315,1.49345437228297,
17.8860084866318));
#271577=CARTESIAN_POINT('Ctrl Pts',(0.445299775302416,1.49041517296627,
17.885237622148));
#271578=CARTESIAN_POINT('Ctrl Pts',(0.452004426932,1.48839553904711,17.8847394373079));
#271579=CARTESIAN_POINT('Ctrl Pts',(0.496860322581334,1.47455259494447,
17.8814155974756));
#271580=CARTESIAN_POINT('Ctrl Pts',(0.534561657787864,1.4613076527429,17.8786663079853));
#271581=CARTESIAN_POINT('Ctrl Pts',(0.688105264841811,1.40062625548094,
17.8674914553822));
#271582=CARTESIAN_POINT('Ctrl Pts',(0.798524167917304,1.34074840299653,
17.8594733432572));
#271583=CARTESIAN_POINT('Ctrl Pts',(0.922297338057383,1.25285966460046,
17.8493050660907));
#271584=CARTESIAN_POINT('Ctrl Pts',(0.943614365476525,1.23688380156222,
17.8475078655875));
#271585=CARTESIAN_POINT('Ctrl Pts',(0.99292362052183,1.19791258758639,17.8432249904034));
#271586=CARTESIAN_POINT('Ctrl Pts',(1.02054225539802,1.17447223755887,17.8407254398259));
#271587=CARTESIAN_POINT('Ctrl Pts',(1.05514124593311,1.14296509702396,17.8374444712517));
#271588=CARTESIAN_POINT('Ctrl Pts',(1.06289331718636,1.13575967894952,17.8366991783033));
#271589=CARTESIAN_POINT('Ctrl Pts',(1.07517826454215,1.12410510146682,17.8355012855254));
#271590=CARTESIAN_POINT('Ctrl Pts',(1.07975856652805,1.11970621839984,17.8350508474147));
#271591=CARTESIAN_POINT('Ctrl Pts',(1.08798451491493,1.11170867816885,17.8342348713813));
#271592=CARTESIAN_POINT('Ctrl Pts',(1.09163958553006,1.10811980577965,17.8338697634288));
#271593=CARTESIAN_POINT('Ctrl Pts',(1.10021689213668,1.09961422434851,17.8330068972699));
#271594=CARTESIAN_POINT('Ctrl Pts',(1.10512396492404,1.09468245229901,17.8325084785688));
#271595=CARTESIAN_POINT('Ctrl Pts',(1.11939387742573,1.08014697590798,17.8310448570047));
#271596=CARTESIAN_POINT('Ctrl Pts',(1.12866557302372,1.07045511147971,17.8300757255545));
#271597=CARTESIAN_POINT('Ctrl Pts',(1.21529253635949,0.977525729089931,
17.8208441503756));
#271598=CARTESIAN_POINT('Ctrl Pts',(1.28341652657203,0.886185021926734,
17.8121871100004));
#271599=CARTESIAN_POINT('Ctrl Pts',(1.37635065837062,0.728087679216828,
17.7979817476697));
#271600=CARTESIAN_POINT('Ctrl Pts',(1.4076174574621,0.66562528914666,17.7925493084874));
#271601=CARTESIAN_POINT('Ctrl Pts',(1.43457675882332,0.601306721269597,
17.7872340762022));
#271602=CARTESIAN_POINT('',(-1.55549978108786,-0.000825248823992286,17.9559437744364));
#271603=CARTESIAN_POINT('Ctrl Pts',(1.43457667260785,0.601306926959429,
17.650811911463));
#271604=CARTESIAN_POINT('Ctrl Pts',(1.43113399608224,0.609520342128201,
17.651499275844));
#271605=CARTESIAN_POINT('Ctrl Pts',(1.42762025295567,0.617705455986721,
17.6521857231963));
#271606=CARTESIAN_POINT('Ctrl Pts',(1.4021602503384,0.675635147384968,17.6570526399232));
#271607=CARTESIAN_POINT('Ctrl Pts',(1.37768732429456,0.724234300833138,
17.6611822828632));
#271608=CARTESIAN_POINT('Ctrl Pts',(1.34680672295463,0.778302022177472,
17.6657568881588));
#271609=CARTESIAN_POINT('Ctrl Pts',(1.34284518487173,0.785117318104389,
17.6663331255922));
#271610=CARTESIAN_POINT('Ctrl Pts',(1.33677383223619,0.795381866662972,
17.6672000637687));
#271611=CARTESIAN_POINT('Ctrl Pts',(1.33470217901971,0.798853357438681,
17.6674931005432));
#271612=CARTESIAN_POINT('Ctrl Pts',(1.33095784951244,0.805072543159744,
17.6680177285659));
#271613=CARTESIAN_POINT('Ctrl Pts',(1.32929017148378,0.807823147454503,
17.6682496327848));
#271614=CARTESIAN_POINT('Ctrl Pts',(1.32562502644105,0.813826214088698,
17.6687554725779));
#271615=CARTESIAN_POINT('Ctrl Pts',(1.32362412003024,0.817076500203668,
17.6690291795223));
#271616=CARTESIAN_POINT('Ctrl Pts',(1.31789148072096,0.826312317648029,
17.6698065323808));
#271617=CARTESIAN_POINT('Ctrl Pts',(1.31413090669652,0.832279980745032,
17.6703083375393));
#271618=CARTESIAN_POINT('Ctrl Pts',(1.28893439363693,0.871667805203456,
17.6736186503033));
#271619=CARTESIAN_POINT('Ctrl Pts',(1.26626397475577,0.904285825314207,
17.6763519054269));
#271620=CARTESIAN_POINT('Ctrl Pts',(1.16873821955681,1.03373279638744,17.6873240216271));
#271621=CARTESIAN_POINT('Ctrl Pts',(1.08383150223828,1.12243752577813,17.6951732857353));
#271622=CARTESIAN_POINT('Ctrl Pts',(0.941467757430883,1.23978923026179,
17.7075132449342));
#271623=CARTESIAN_POINT('Ctrl Pts',(0.89121749146488,1.27638894317095,17.7117364742955));
#271624=CARTESIAN_POINT('Ctrl Pts',(0.829388377278725,1.31598755565156,
17.7168692343652));
#271625=CARTESIAN_POINT('Ctrl Pts',(0.819792158598439,1.32198681226502,
17.7176640451095));
#271626=CARTESIAN_POINT('Ctrl Pts',(0.803960559703583,1.33164556993064,
17.7189728238172));
#271627=CARTESIAN_POINT('Ctrl Pts',(0.797763494663612,1.33536733106362,
17.7194845132424));
#271628=CARTESIAN_POINT('Ctrl Pts',(0.786587428259023,1.34197376172988,
17.7204063394339));
#271629=CARTESIAN_POINT('Ctrl Pts',(0.781617903023633,1.34487427349591,
17.7208158930284));
#271630=CARTESIAN_POINT('Ctrl Pts',(0.771004975045411,1.35098991959559,
17.7216898723472));
#271631=CARTESIAN_POINT('Ctrl Pts',(0.765357315606547,1.35419740491497,
17.7221545634451));
#271632=CARTESIAN_POINT('Ctrl Pts',(0.750084715597447,1.36274514349672,
17.7234102393004));
#271633=CARTESIAN_POINT('Ctrl Pts',(0.740423065030309,1.36801866942586,
17.7242035811303));
#271634=CARTESIAN_POINT('Ctrl Pts',(0.690742500299907,1.39445487636839,
17.7282786178758));
#271635=CARTESIAN_POINT('Ctrl Pts',(0.64987342773491,1.41396370334272,17.7316175054669));
#271636=CARTESIAN_POINT('Ctrl Pts',(0.526052398128402,1.46656684796264,
17.7417048207064));
#271637=CARTESIAN_POINT('Ctrl Pts',(0.441046210272524,1.49433061930852,
17.7486041154104));
#271638=CARTESIAN_POINT('Ctrl Pts',(0.312158981485861,1.52446574335081,
17.7588683380363));
#271639=CARTESIAN_POINT('Ctrl Pts',(0.269786358485031,1.5325320825178,17.7622098542381));
#271640=CARTESIAN_POINT('Ctrl Pts',(0.217100737758217,1.54030852184419,
17.7662925857506));
#271641=CARTESIAN_POINT('Ctrl Pts',(0.20705484337072,1.54169107540618,17.7670678256692));
#271642=CARTESIAN_POINT('Ctrl Pts',(0.158748951216467,1.54785842372358,
17.7707781516433));
#271643=CARTESIAN_POINT('Ctrl Pts',(0.120329485984408,1.55131826431919,
17.773676970177));
#271644=CARTESIAN_POINT('Ctrl Pts',(0.0751777223401169,1.55369648523671,
17.776994655763));
#271645=CARTESIAN_POINT('Ctrl Pts',(0.0685356704071852,1.55400364358276,
17.7774804427378));
#271646=CARTESIAN_POINT('Ctrl Pts',(0.057767335211512,1.55443244379102,
17.7782641396524));
#271647=CARTESIAN_POINT('Ctrl Pts',(0.0536422719712951,1.55458026330299,
17.7785634311973));
#271648=CARTESIAN_POINT('Ctrl Pts',(0.0462955853778806,1.55481425072788,
17.7790947671676));
#271649=CARTESIAN_POINT('Ctrl Pts',(0.0430742423888775,1.55490682867004,
17.7793271605005));
#271650=CARTESIAN_POINT('Ctrl Pts',(0.0361011483696269,1.55508554081373,
17.7798289384273));
#271651=CARTESIAN_POINT('Ctrl Pts',(0.0323493702975275,1.55516811027254,
17.7800981228477));
#271652=CARTESIAN_POINT('Ctrl Pts',(0.0218426313284958,1.55536130532916,
17.780849845549));
#271653=CARTESIAN_POINT('Ctrl Pts',(0.0150870844119887,1.55544150484054,
17.7813307294216));
#271654=CARTESIAN_POINT('Ctrl Pts',(-0.025368272809293,1.55565818184316,
17.7841969575686));
#271655=CARTESIAN_POINT('Ctrl Pts',(-0.059067829802532,1.55474350001894,
17.7865283783039));
#271656=CARTESIAN_POINT('Ctrl Pts',(-0.267821558628838,1.54227876786996,
17.8007700496928));
#271657=CARTESIAN_POINT('Ctrl Pts',(-0.439902145632824,1.50228153164371,
17.8117827128674));
#271658=CARTESIAN_POINT('Ctrl Pts',(-0.62275574276581,1.4255795557092,17.825468268183));
#271659=CARTESIAN_POINT('Ctrl Pts',(-0.643617041614602,1.41628344441866,
17.8270583972346));
#271660=CARTESIAN_POINT('Ctrl Pts',(-0.672336860873234,1.40271988573675,
17.829291769397));
#271661=CARTESIAN_POINT('Ctrl Pts',(-0.680375361178384,1.39883855190258,
17.8299217786094));
#271662=CARTESIAN_POINT('Ctrl Pts',(-0.693256533989951,1.39248167024186,
17.8309394626847));
#271663=CARTESIAN_POINT('Ctrl Pts',(-0.698120494706753,1.39004949458005,
17.8313256266196));
#271664=CARTESIAN_POINT('Ctrl Pts',(-0.708080530036251,1.3850036151129,
17.8321203162579));
#271665=CARTESIAN_POINT('Ctrl Pts',(-0.713175116901813,1.38238717511097,
17.8325289329897));
#271666=CARTESIAN_POINT('Ctrl Pts',(-0.725032372407305,1.37621462278791,
17.8334850103942));
#271667=CARTESIAN_POINT('Ctrl Pts',(-0.731783467495394,1.37263672610601,
17.8340332316358));
#271668=CARTESIAN_POINT('Ctrl Pts',(-0.745991264066383,1.36497237430686,
17.8351952957927));
#271669=CARTESIAN_POINT('Ctrl Pts',(-0.753441341533812,1.36087423673705,
17.8358095404717));
#271670=CARTESIAN_POINT('Ctrl Pts',(-0.773418794734829,1.34967071355989,
17.8374700792865));
#271671=CARTESIAN_POINT('Ctrl Pts',(-0.78588143304076,1.34245223919781,
17.8385203643568));
#271672=CARTESIAN_POINT('Ctrl Pts',(-0.824391243673544,1.31942698949943,
17.8418116476528));
#271673=CARTESIAN_POINT('Ctrl Pts',(-0.850074070661018,1.3030281449115,
17.8440732757223));
#271674=CARTESIAN_POINT('Ctrl Pts',(-0.976087522835685,1.21725527815718,
17.8555111960299));
#271675=CARTESIAN_POINT('Ctrl Pts',(-1.06848669106969,1.13700741940009,
17.8650590748476));
#271676=CARTESIAN_POINT('Ctrl Pts',(-1.15155213513869,1.04571035665813,
17.8745639570488));
#271677=CARTESIAN_POINT('Ctrl Pts',(-1.15255325501982,1.04460684677261,
17.8746786575593));
#271678=CARTESIAN_POINT('Ctrl Pts',(-1.19086295786352,1.00225688587125,
17.8790734425361));
#271679=CARTESIAN_POINT('Ctrl Pts',(-1.22593911208545,0.959035083441107,
17.8833010737216));
#271680=CARTESIAN_POINT('Ctrl Pts',(-1.26327927075591,0.90761687570065,
17.8879701280684));
#271681=CARTESIAN_POINT('Ctrl Pts',(-1.26788178564335,0.901176283363509,
17.888548811554));
#271682=CARTESIAN_POINT('Ctrl Pts',(-1.27476436756329,0.891387938531102,
17.8894186941819));
#271683=CARTESIAN_POINT('Ctrl Pts',(-1.27708076411719,0.888066085771792,
17.8897122524698));
#271684=CARTESIAN_POINT('Ctrl Pts',(-1.2812139900587,0.882089174140487,
17.8902374322009));
#271685=CARTESIAN_POINT('Ctrl Pts',(-1.28303557102551,0.879437504082222,
17.8904693696341));
#271686=CARTESIAN_POINT('Ctrl Pts',(-1.28699709807433,0.873632212847786,
17.8909748359383));
#271687=CARTESIAN_POINT('Ctrl Pts',(-1.28913368283199,0.870476376708512,
17.8912481386878));
#271688=CARTESIAN_POINT('Ctrl Pts',(-1.29517669275266,0.861479518671514,
17.8920232002549));
#271689=CARTESIAN_POINT('Ctrl Pts',(-1.29905523447166,0.855619734056771,
17.8925231352883));
#271690=CARTESIAN_POINT('Ctrl Pts',(-1.32425891917043,0.816975003872333,
17.8957897358448));
#271691=CARTESIAN_POINT('Ctrl Pts',(-1.34438303107358,0.783418633132571,
17.8984834134827));
#271692=CARTESIAN_POINT('Ctrl Pts',(-1.43199947549411,0.623980637876081,
17.9108063631384));
#271693=CARTESIAN_POINT('Ctrl Pts',(-1.48321658409031,0.489947597489042,
17.9198939126238));
#271694=CARTESIAN_POINT('Ctrl Pts',(-1.52412099448071,0.313243439519537,
17.9321711032087));
#271695=CARTESIAN_POINT('Ctrl Pts',(-1.53141486931275,0.275380383841871,
17.9348134062791));
#271696=CARTESIAN_POINT('Ctrl Pts',(-1.53956781459652,0.222560673256452,
17.9385378446545));
#271697=CARTESIAN_POINT('Ctrl Pts',(-1.54162920738253,0.207801994766207,
17.9395825620292));
#271698=CARTESIAN_POINT('Ctrl Pts',(-1.54438533709497,0.185762283358565,
17.9411497354098));
#271699=CARTESIAN_POINT('Ctrl Pts',(-1.5452413216916,0.178501960203745,
17.9416671290568));
#271700=CARTESIAN_POINT('Ctrl Pts',(-1.54665236575565,0.165762002719634,
17.9425771300317));
#271701=CARTESIAN_POINT('Ctrl Pts',(-1.54722956586231,0.160284906143858,
17.9429690356483));
#271702=CARTESIAN_POINT('Ctrl Pts',(-1.54831303645293,0.149452100981205,
17.9437455629745));
#271703=CARTESIAN_POINT('Ctrl Pts',(-1.54882063450804,0.144096599955775,
17.944130137285));
#271704=CARTESIAN_POINT('Ctrl Pts',(-1.54985769130544,0.13251574111988,
17.9449632594407));
#271705=CARTESIAN_POINT('Ctrl Pts',(-1.55037744169917,0.126289631802385,
17.9454121050563));
#271706=CARTESIAN_POINT('Ctrl Pts',(-1.55154844155662,0.111163472316023,
17.9465049253662));
#271707=CARTESIAN_POINT('Ctrl Pts',(-1.55216063089044,0.102260714930382,
17.9471501078678));
#271708=CARTESIAN_POINT('Ctrl Pts',(-1.55458343907947,0.0619634477458824,
17.9500797668325));
#271709=CARTESIAN_POINT('Ctrl Pts',(-1.55551823661414,0.0305261394203842,
17.9523910747632));
#271710=CARTESIAN_POINT('Ctrl Pts',(-1.55549973056384,-0.000915541269661115,
17.9547299826528));
#271711=CARTESIAN_POINT('Ctrl Pts',(-1.55549978108786,-0.000825248823992286,
17.9559437744364));
#271712=CARTESIAN_POINT('Ctrl Pts',(-1.55546570367139,-0.0650572868587075,
17.9605236044809));
#271713=CARTESIAN_POINT('Ctrl Pts',(-1.55144892983626,-0.12914984215493,
17.9651034345255));
#271714=CARTESIAN_POINT('Ctrl Pts',(-1.54352576552891,-0.192635565637285,
17.9696832645701));
#271715=CARTESIAN_POINT('Ctrl Pts',(-1.53557083843072,-0.256375793971246,
17.9742814544742));
#271716=CARTESIAN_POINT('Ctrl Pts',(-1.52367828485016,-0.319504020046929,
17.9788796443784));
#271717=CARTESIAN_POINT('Ctrl Pts',(-1.5079750791896,-0.381564425154021,
17.9834778342825));
#271718=CARTESIAN_POINT('Ctrl Pts',(-1.492194322415,-0.443931318863357,
17.9880987325913));
#271719=CARTESIAN_POINT('Ctrl Pts',(-1.47256533691098,-0.505219534397231,
17.9927196309002));
#271720=CARTESIAN_POINT('Ctrl Pts',(-1.44926486241833,-0.56498814904349,
17.997340529209));
#271721=CARTESIAN_POINT('Ctrl Pts',(-1.44470837165074,-0.576676114492983,
17.9982441623299));
#271722=CARTESIAN_POINT('Ctrl Pts',(-1.44001162060527,-0.588306042235484,
17.9991477954507));
#271723=CARTESIAN_POINT('Ctrl Pts',(-1.43517613547869,-0.599874745386444,
18.0000514285715));
#271724=CARTESIAN_POINT('Ctrl Pts',(-1.4129793509677,-0.652979657136013,
18.0041994611131));
#271725=CARTESIAN_POINT('Ctrl Pts',(-1.38778447851346,-0.704962388747883,
18.0083474936548));
#271726=CARTESIAN_POINT('Ctrl Pts',(-1.35972678115222,-0.755462329052493,
18.0124955261964));
#271727=CARTESIAN_POINT('Ctrl Pts',(-1.33171897319288,-0.805872475394861,
18.0166361831199));
#271728=CARTESIAN_POINT('Ctrl Pts',(-1.30085869485994,-0.854804612100729,
18.0207768400434));
#271729=CARTESIAN_POINT('Ctrl Pts',(-1.26732882366757,-0.901919011165288,
18.0249174969668));
#271730=CARTESIAN_POINT('Ctrl Pts',(-1.23383230732935,-0.948986541755466,
18.0290540348465));
#271731=CARTESIAN_POINT('Ctrl Pts',(-1.19767176020619,-0.99423949518981,
18.0331905727262));
#271732=CARTESIAN_POINT('Ctrl Pts',(-1.15907453297798,-1.03736516087725,
18.0373271106059));
#271733=CARTESIAN_POINT('Ctrl Pts',(-1.12050086338133,-1.08046450502254,
18.0414611237696));
#271734=CARTESIAN_POINT('Ctrl Pts',(-1.07949380837069,-1.12143874788174,
18.0455951369333));
#271735=CARTESIAN_POINT('Ctrl Pts',(-1.03632097951966,-1.1600082229913,
18.049729150097));
#271736=CARTESIAN_POINT('Ctrl Pts',(-0.993157904702015,-1.19856898410276,
18.0538622292635));
#271737=CARTESIAN_POINT('Ctrl Pts',(-0.947830415658562,-1.2347257092607,
18.05799530843));
#271738=CARTESIAN_POINT('Ctrl Pts',(-0.900641343215095,-1.26823713117528,
18.0621283875965));
#271739=CARTESIAN_POINT('Ctrl Pts',(-0.853409621944049,-1.30177884024707,
18.0662652021825));
#271740=CARTESIAN_POINT('Ctrl Pts',(-0.804313379998956,-1.33267016508006,
18.0704020167685));
#271741=CARTESIAN_POINT('Ctrl Pts',(-0.753685657002759,-1.3607123797586,
18.0745388313545));
#271742=CARTESIAN_POINT('Ctrl Pts',(-0.703037019623535,-1.38876617871517,
18.0786773548643));
#271743=CARTESIAN_POINT('Ctrl Pts',(-0.650856109387414,-1.41396829298555,
18.0828158783742));
#271744=CARTESIAN_POINT('Ctrl Pts',(-0.597498983686705,-1.43616684772117,
18.086954401884));
#271745=CARTESIAN_POINT('Ctrl Pts',(-0.544037834057248,-1.45840868029167,
18.0911009937722));
#271746=CARTESIAN_POINT('Ctrl Pts',(-0.489396379134149,-1.47763507686832,
18.0952475856603));
#271747=CARTESIAN_POINT('Ctrl Pts',(-0.433948124184827,-1.49374337672723,
18.0993941775485));
#271748=CARTESIAN_POINT('Ctrl Pts',(-0.381491169641016,-1.50898267243183,
18.1033170707466));
#271749=CARTESIAN_POINT('Ctrl Pts',(-0.328312606387049,-1.52143158288161,
18.1072399639447));
#271750=CARTESIAN_POINT('Ctrl Pts',(-0.274735110446107,-1.53104567831537,
18.1111628571429));
#271751=CARTESIAN_POINT('Ctrl Pts',(-0.21808230386972,-1.54121161607431,
18.1153109216552));
#271752=CARTESIAN_POINT('Ctrl Pts',(-0.160745571050524,-1.54825018790437,
18.1194589861676));
#271753=CARTESIAN_POINT('Ctrl Pts',(-0.103101228021132,-1.55207937515468,
18.1236070506799));
#271754=CARTESIAN_POINT('Ctrl Pts',(-0.0455593729887791,-1.55590175435217,
18.1277477401958));
#271755=CARTESIAN_POINT('Ctrl Pts',(0.0122884913517671,-1.55652604048254,
18.1318884297118));
#271756=CARTESIAN_POINT('Ctrl Pts',(0.070057759223516,-1.55392154254086,
18.1360291192277));
#271757=CARTESIAN_POINT('Ctrl Pts',(0.127769564769916,-1.55131963525878,
18.1401656900546));
#271758=CARTESIAN_POINT('Ctrl Pts',(0.185402411102989,-1.54549533040801,
18.1443022608815));
#271759=CARTESIAN_POINT('Ctrl Pts',(0.242570259876582,-1.53646995383034,
18.1484388317085));
#271760=CARTESIAN_POINT('Ctrl Pts',(0.299703220892861,-1.52745008515885,
18.1525728781151));
#271761=CARTESIAN_POINT('Ctrl Pts',(0.356371233489937,-1.51523309821701,
18.1567069245217));
#271762=CARTESIAN_POINT('Ctrl Pts',(0.412194174568351,-1.49989206693412,
18.1608409709283));
#271763=CARTESIAN_POINT('Ctrl Pts',(0.468004506875572,-1.48455450074192,
18.1649740835746));
#271764=CARTESIAN_POINT('Ctrl Pts',(0.522969644665716,-1.46609442900677,
18.1691071962209));
#271765=CARTESIAN_POINT('Ctrl Pts',(0.576722613642818,-1.44463534392351,
18.1732403088673));
#271766=CARTESIAN_POINT('Ctrl Pts',(0.630524164682245,-1.42315686406767,
18.1773771570307));
#271767=CARTESIAN_POINT('Ctrl Pts',(0.683110872245827,-1.39867414664148,
18.1815140051942));
#271768=CARTESIAN_POINT('Ctrl Pts',(0.734135108671954,-1.37135914049355,
18.1856508533576));
#271769=CARTESIAN_POINT('Ctrl Pts',(0.785180424456432,-1.34403284984941,
18.1897894105541));
#271770=CARTESIAN_POINT('Ctrl Pts',(0.834661535923235,-1.31387220838579,
18.1939279677506));
#271771=CARTESIAN_POINT('Ctrl Pts',(0.882257683604024,-1.28109391916505,
18.198066524947));
#271772=CARTESIAN_POINT('Ctrl Pts',(0.929946619950204,-1.24825172868635,
18.2022131502586));
#271773=CARTESIAN_POINT('Ctrl Pts',(0.975742835023639,-1.21278201166987,
18.2063597755702));
#271774=CARTESIAN_POINT('Ctrl Pts',(1.01935744443746,-1.17494282859632,
18.2105064008818));
#271775=CARTESIAN_POINT('Ctrl Pts',(1.06061603120207,-1.13914768474603,
18.2144290291593));
#271776=CARTESIAN_POINT('Ctrl Pts',(1.09992237905076,-1.10123275944642,
18.2183516574368));
#271777=CARTESIAN_POINT('Ctrl Pts',(1.13706414369385,-1.06144495058659,
18.2222742857143));
#271778=CARTESIAN_POINT('Ctrl Pts',(1.17633885422906,-1.01937224104206,
18.2264221793757));
#271779=CARTESIAN_POINT('Ctrl Pts',(1.21335778128719,-0.975028418356394,
18.2305700730371));
#271780=CARTESIAN_POINT('Ctrl Pts',(1.24784786515699,-0.928685067944537,
18.2347179666985));
#271781=CARTESIAN_POINT('Ctrl Pts',(1.28227662322299,-0.882424119281116,
18.2388584851121));
#271782=CARTESIAN_POINT('Ctrl Pts',(1.31418515450624,-0.83417111400729,
18.2429990035258));
#271783=CARTESIAN_POINT('Ctrl Pts',(1.34333901653407,-0.784232450653037,
18.2471395219395));
#271784=CARTESIAN_POINT('Ctrl Pts',(1.37246387812037,-0.734343463162846,
18.251275921624));
#271785=CARTESIAN_POINT('Ctrl Pts',(1.39883923824252,-0.682772587311995,
18.2554123213084));
#271786=CARTESIAN_POINT('Ctrl Pts',(1.42227357161143,-0.629855648141438,
18.2595487209929));
#271787=CARTESIAN_POINT('Ctrl Pts',(1.44569360453453,-0.576971000728829,
18.2636825965024));
#271788=CARTESIAN_POINT('Ctrl Pts',(1.46617595784719,-0.522742393527044,
18.2678164720118));
#271789=CARTESIAN_POINT('Ctrl Pts',(1.48357578473478,-0.467528759488206,
18.2719503475212));
#271790=CARTESIAN_POINT('Ctrl Pts',(1.50097168358037,-0.412327590025899,
18.2760832898009));
#271791=CARTESIAN_POINT('Ctrl Pts',(1.5152862810371,-0.35614233171361,18.2802162320805));
#271792=CARTESIAN_POINT('Ctrl Pts',(1.52642421658827,-0.299348227008068,
18.2843491743602));
#271793=CARTESIAN_POINT('Ctrl Pts',(1.53757222495343,-0.242502759422096,
18.2884858543486));
#271794=CARTESIAN_POINT('Ctrl Pts',(1.54553772862851,-0.185047857209864,
18.2926225343369));
#271795=CARTESIAN_POINT('Ctrl Pts',(1.5502765683613,-0.127368801477861,
18.2967592143253));
#271796=CARTESIAN_POINT('Ctrl Pts',(1.55501736695423,-0.0696659033688531,
18.3008976042634));
#271797=CARTESIAN_POINT('Ctrl Pts',(1.55652882773326,-0.011739188796491,
18.3050359942014));
#271798=CARTESIAN_POINT('Ctrl Pts',(1.55481896346577,0.0460243505900421,
18.3091743841395));
#271799=CARTESIAN_POINT('Ctrl Pts',(1.55310576413567,0.103900556826267,
18.3133208459402));
#271800=CARTESIAN_POINT('Ctrl Pts',(1.5481587271621,0.161612430901385,18.317467307741));
#271801=CARTESIAN_POINT('Ctrl Pts',(1.54003790034462,0.218777319441797,
18.3216137695417));
#271802=CARTESIAN_POINT('Ctrl Pts',(1.53235280003774,0.272875000914189,
18.3255377511231));
#271803=CARTESIAN_POINT('Ctrl Pts',(1.52182588147778,0.326482519924142,
18.3294617327044));
#271804=CARTESIAN_POINT('Ctrl Pts',(1.50854945504498,0.379287215291371,
18.3333857142858));
#271805=CARTESIAN_POINT('Ctrl Pts',(1.49451645174172,0.435101064618002,
18.3375333097831));
#271806=CARTESIAN_POINT('Ctrl Pts',(1.4773522856722,0.490252203646958,18.3416809052804));
#271807=CARTESIAN_POINT('Ctrl Pts',(1.45713693966284,0.544364022571303,
18.3458285007778));
#271808=CARTESIAN_POINT('Ctrl Pts',(1.44999548490416,0.563480049899223,
18.3472937176278));
#271809=CARTESIAN_POINT('Ctrl Pts',(1.44247371498061,0.582466443269449,
18.3487589344778));
#271810=CARTESIAN_POINT('Ctrl Pts',(1.43457668357356,0.601306900797837,
18.3502241513278));
#271811=CARTESIAN_POINT('Origin',(0.,0.,-1.29405622560371));
#271812=CARTESIAN_POINT('',(1.43457668357355,0.601306900797844,19.188224604057));
#271813=CARTESIAN_POINT('',(1.43457668357356,0.601306900797836,19.0501843444911));
#271814=CARTESIAN_POINT('',(1.43457668357355,0.601306900797845,-1.29405622560371));
#271815=CARTESIAN_POINT('',(-1.55549954655085,0.00118772054205428,18.7940562256531));
#271816=CARTESIAN_POINT('Ctrl Pts',(-1.55549954655085,0.00118772054205428,
18.7940562256531));
#271817=CARTESIAN_POINT('Ctrl Pts',(-1.55554293531709,-0.0556364260569684,
18.7981393593524));
#271818=CARTESIAN_POINT('Ctrl Pts',(-1.55246831755618,-0.112576373261054,
18.8022224930517));
#271819=CARTESIAN_POINT('Ctrl Pts',(-1.54626410196496,-0.169255951075549,
18.8063056267509));
#271820=CARTESIAN_POINT('Ctrl Pts',(-1.54006667370066,-0.225873522207911,
18.8103842935578));
#271821=CARTESIAN_POINT('Ctrl Pts',(-1.53074648102143,-0.282230757233944,
18.8144629603647));
#271822=CARTESIAN_POINT('Ctrl Pts',(-1.51834394447829,-0.33795253552255,
18.8185416271716));
#271823=CARTESIAN_POINT('Ctrl Pts',(-1.50594988631056,-0.393636222397049,
18.8226175058014));
#271824=CARTESIAN_POINT('Ctrl Pts',(-1.49047777290168,-0.44868478979142,
18.8266933844312));
#271825=CARTESIAN_POINT('Ctrl Pts',(-1.47201938618257,-0.502731714438912,
18.830769263061));
#271826=CARTESIAN_POINT('Ctrl Pts',(-1.45356604480038,-0.556763866129879,
18.8348440276075));
#271827=CARTESIAN_POINT('Ctrl Pts',(-1.43212822258919,-0.60979441012812,
18.838918792154));
#271828=CARTESIAN_POINT('Ctrl Pts',(-1.40784729205727,-0.661472790254456,
18.8429935567004));
#271829=CARTESIAN_POINT('Ctrl Pts',(-1.38354594597962,-0.713194621859364,
18.8470717473323));
#271830=CARTESIAN_POINT('Ctrl Pts',(-1.35639694404575,-0.763561530749342,
18.8511499379642));
#271831=CARTESIAN_POINT('Ctrl Pts',(-1.32658881136516,-0.81224526810612,
18.8552281285961));
#271832=CARTESIAN_POINT('Ctrl Pts',(-1.29676823386543,-0.860949330798692,
18.8593080218621));
#271833=CARTESIAN_POINT('Ctrl Pts',(-1.2642866209274,-0.907968380249418,
18.8633879151282));
#271834=CARTESIAN_POINT('Ctrl Pts',(-1.22937539611821,-0.953003874818558,
18.8674678083942));
#271835=CARTESIAN_POINT('Ctrl Pts',(-1.19439986236409,-0.9981223279535,
18.8715552171121));
#271836=CARTESIAN_POINT('Ctrl Pts',(-1.15698613404714,-1.04124952517296,
18.8756426258301));
#271837=CARTESIAN_POINT('Ctrl Pts',(-1.11740452834311,-1.08212169834928,
18.879730034548));
#271838=CARTESIAN_POINT('Ctrl Pts',(-1.08838209309471,-1.11209041685809,
18.8827270467395));
#271839=CARTESIAN_POINT('Ctrl Pts',(-1.05819496421084,-1.14084751914303,
18.8857240589309));
#271840=CARTESIAN_POINT('Ctrl Pts',(-1.02696061094917,-1.16830310859764,
18.8887210711223));
#271841=CARTESIAN_POINT('Ctrl Pts',(-0.983795291387467,-1.20624624392158,
18.8928628885593));
#271842=CARTESIAN_POINT('Ctrl Pts',(-0.938431985387361,-1.24187503920902,
18.8970047059963));
#271843=CARTESIAN_POINT('Ctrl Pts',(-0.89114917915262,-1.27492485680357,
18.9011465234333));
#271844=CARTESIAN_POINT('Ctrl Pts',(-0.843950718407869,-1.30791571844181,
18.9052809524843));
#271845=CARTESIAN_POINT('Ctrl Pts',(-0.79483997769596,-1.33833643592707,
18.9094153815354));
#271846=CARTESIAN_POINT('Ctrl Pts',(-0.744129160547715,-1.36596194764809,
18.9135498105864));
#271847=CARTESIAN_POINT('Ctrl Pts',(-0.693468916016077,-1.39355990914429,
18.9176801164758));
#271848=CARTESIAN_POINT('Ctrl Pts',(-0.641212212707886,-1.41836793849242,
18.9218104223653));
#271849=CARTESIAN_POINT('Ctrl Pts',(-0.587699447516429,-1.44020471093136,
18.9259407282547));
#271850=CARTESIAN_POINT('Ctrl Pts',(-0.534219314459006,-1.46202816728614,
18.9300685154797));
#271851=CARTESIAN_POINT('Ctrl Pts',(-0.479485120448245,-1.48088376089469,
18.9341963027048));
#271852=CARTESIAN_POINT('Ctrl Pts',(-0.423859012247329,-1.49663749376284,
18.9383240899298));
#271853=CARTESIAN_POINT('Ctrl Pts',(-0.36824527219923,-1.51238772387695,
18.9424509593646));
#271854=CARTESIAN_POINT('Ctrl Pts',(-0.311740514143425,-1.52503731999041,
18.9465778287993));
#271855=CARTESIAN_POINT('Ctrl Pts',(-0.254721736165568,-1.53450222780053,
18.950704698234));
#271856=CARTESIAN_POINT('Ctrl Pts',(-0.197650249626981,-1.54397588503823,
18.954835382576));
#271857=CARTESIAN_POINT('Ctrl Pts',(-0.140064310195615,-1.55025888399788,
18.958966066918));
#271858=CARTESIAN_POINT('Ctrl Pts',(-0.0823494398928511,-1.55331864720325,
18.9630967512599));
#271859=CARTESIAN_POINT('Ctrl Pts',(-0.0246102727265254,-1.55637969851078,
18.9672291745415));
#271860=CARTESIAN_POINT('Ctrl Pts',(0.0332574098223974,-1.55621480986918,
18.9713615978231));
#271861=CARTESIAN_POINT('Ctrl Pts',(0.0908679535572635,-1.55284360610343,
18.9754940211046));
#271862=CARTESIAN_POINT('Ctrl Pts',(0.148592996712049,-1.54946570216007,
18.9796346574673));
#271863=CARTESIAN_POINT('Ctrl Pts',(0.206059358632892,-1.54286880761442,
18.98377529383));
#271864=CARTESIAN_POINT('Ctrl Pts',(0.262887291216128,-1.53312443138744,
18.9879159301927));
#271865=CARTESIAN_POINT('Ctrl Pts',(0.317606314807269,-1.52374167314853,
18.9919029057611));
#271866=CARTESIAN_POINT('Ctrl Pts',(0.371733071489943,-1.51144114537106,
18.9958898813295));
#271867=CARTESIAN_POINT('Ctrl Pts',(0.424942317006753,-1.4963302700998,
18.9998768568979));
#271868=CARTESIAN_POINT('Ctrl Pts',(0.48040560926309,-1.48057926887287,
19.0040327284766));
#271869=CARTESIAN_POINT('Ctrl Pts',(0.535106637496891,-1.46170783515026,
19.0081886000553));
#271870=CARTESIAN_POINT('Ctrl Pts',(0.588670275789439,-1.43980816652844,
19.0123444716341));
#271871=CARTESIAN_POINT('Ctrl Pts',(0.642137947017385,-1.41794773435471,
19.0164928973632));
#271872=CARTESIAN_POINT('Ctrl Pts',(0.694471797372421,-1.3930700323487,
19.0206413230923));
#271873=CARTESIAN_POINT('Ctrl Pts',(0.745311852489109,-1.36531699342653,
19.0247897488214));
#271874=CARTESIAN_POINT('Ctrl Pts',(0.796100836951593,-1.33759183342484,
19.0289340073084));
#271875=CARTESIAN_POINT('Ctrl Pts',(0.845398546695094,-1.30699730735699,
19.0330782657954));
#271876=CARTESIAN_POINT('Ctrl Pts',(0.892866584321714,-1.27372269847156,
19.0372225242825));
#271877=CARTESIAN_POINT('Ctrl Pts',(0.940305006694703,-1.24046884957603,
19.0413641971715));
#271878=CARTESIAN_POINT('Ctrl Pts',(0.985915596241511,-1.20453853002213,
19.0455058700604));
#271879=CARTESIAN_POINT('Ctrl Pts',(1.02938799067036,-1.1661649174382,19.0496475429494));
#271880=CARTESIAN_POINT('Ctrl Pts',(1.07284980880515,-1.12780064067798,
19.0537882082208));
#271881=CARTESIAN_POINT('Ctrl Pts',(1.11417407590801,-1.08699459410041,
19.0579288734921));
#271882=CARTESIAN_POINT('Ctrl Pts',(1.15308435880024,-1.04401949765809,
19.0620695387635));
#271883=CARTESIAN_POINT('Ctrl Pts',(1.19202813818442,-1.00100740546901,
19.0662137685877));
#271884=CARTESIAN_POINT('Ctrl Pts',(1.22855343011921,-0.955822916064633,
19.070357998412));
#271885=CARTESIAN_POINT('Ctrl Pts',(1.26242243533336,-0.908773813865138,
19.0745022282362));
#271886=CARTESIAN_POINT('Ctrl Pts',(1.29630471826431,-0.861706266935699,
19.0786480827291));
#271887=CARTESIAN_POINT('Ctrl Pts',(1.32752835665271,-0.812773086740959,
19.0827939372219));
#271888=CARTESIAN_POINT('Ctrl Pts',(1.35589929068108,-0.762310542712448,
19.0869397917148));
#271889=CARTESIAN_POINT('Ctrl Pts',(1.38432390192683,-0.711752524599698,
19.0910934900782));
#271890=CARTESIAN_POINT('Ctrl Pts',(1.40988479167735,-0.659659826671731,
19.0952471884416));
#271891=CARTESIAN_POINT('Ctrl Pts',(1.43243465760223,-0.606391953854926,
19.0994008868049));
#271892=CARTESIAN_POINT('Ctrl Pts',(1.45348373341846,-0.556669286002903,
19.1032781387611));
#271893=CARTESIAN_POINT('Ctrl Pts',(1.47190961747841,-0.505923193972485,
19.1071553907173));
#271894=CARTESIAN_POINT('Ctrl Pts',(1.48763200304815,-0.454457119547008,
19.1110326426734));
#271895=CARTESIAN_POINT('Ctrl Pts',(1.50447220800571,-0.399331945454153,
19.1151855568304));
#271896=CARTESIAN_POINT('Ctrl Pts',(1.51827854514202,-0.343157182743916,
19.1193384709874));
#271897=CARTESIAN_POINT('Ctrl Pts',(1.52892569376488,-0.286297874504137,
19.1234913851443));
#271898=CARTESIAN_POINT('Ctrl Pts',(1.5395574624503,-0.229520700236023,
19.1276383003656));
#271899=CARTESIAN_POINT('Ctrl Pts',(1.5470389930162,-0.172061446218813,
19.1317852155869));
#271900=CARTESIAN_POINT('Ctrl Pts',(1.5512948910046,-0.1142996550433,19.1359321308082));
#271901=CARTESIAN_POINT('Ctrl Pts',(1.55576711955347,-0.0536017876994527,
19.1402898369122));
#271902=CARTESIAN_POINT('Ctrl Pts',(1.55667684533764,0.00742962794439894,
19.1446475430163));
#271903=CARTESIAN_POINT('Ctrl Pts',(1.55399785510563,0.0683441023578467,
19.1490052491204));
#271904=CARTESIAN_POINT('Ctrl Pts',(1.55145262355544,0.12621719210948,19.1531453803273));
#271905=CARTESIAN_POINT('Ctrl Pts',(1.54566854178028,0.183984161633242,
19.1572855115342));
#271906=CARTESIAN_POINT('Ctrl Pts',(1.53667653344422,0.241258122271234,
19.1614256427411));
#271907=CARTESIAN_POINT('Ctrl Pts',(1.52768705099214,0.298515994470013,
19.1655646109719));
#271908=CARTESIAN_POINT('Ctrl Pts',(1.51549151678963,0.355280621099329,
19.1697035792027));
#271909=CARTESIAN_POINT('Ctrl Pts',(1.5001723928256,0.411172763937408,19.1738425474335));
#271910=CARTESIAN_POINT('Ctrl Pts',(1.48484781488213,0.467084805733029,
19.1779829892373));
#271911=CARTESIAN_POINT('Ctrl Pts',(1.4663975721555,0.522123245313919,19.1821234310411));
#271912=CARTESIAN_POINT('Ctrl Pts',(1.44495416056346,0.575923366317395,
19.1862638728448));
#271913=CARTESIAN_POINT('Ctrl Pts',(1.44156927489217,0.584415823682041,
19.1869174499156));
#271914=CARTESIAN_POINT('Ctrl Pts',(1.43810990577921,0.59287746453593,19.1875710269863));
#271915=CARTESIAN_POINT('Ctrl Pts',(1.43457668357355,0.601306900797844,
19.188224604057));
#271916=CARTESIAN_POINT('Ctrl Pts',(-1.55549958889311,0.00113090820362872,
18.7933196395821));
#271917=CARTESIAN_POINT('Ctrl Pts',(-1.55545428746057,0.063440439139176,
18.7885137489814));
#271918=CARTESIAN_POINT('Ctrl Pts',(-1.55166503816927,0.125700707766695,
18.7837601818246));
#271919=CARTESIAN_POINT('Ctrl Pts',(-1.54346157201289,0.193233343957606,
18.7787617229099));
#271920=CARTESIAN_POINT('Ctrl Pts',(-1.54274300200048,0.198888868159507,
18.7783443600553));
#271921=CARTESIAN_POINT('Ctrl Pts',(-1.54149823805131,0.208272918818632,
18.7776540288749));
#271922=CARTESIAN_POINT('Ctrl Pts',(-1.54098957760577,0.212003653569252,
18.7773801549248));
#271923=CARTESIAN_POINT('Ctrl Pts',(-1.54004607427961,0.218740866127462,
18.776886657891));
#271924=CARTESIAN_POINT('Ctrl Pts',(-1.53961596361043,0.221747970547353,
18.7766667795202));
#271925=CARTESIAN_POINT('Ctrl Pts',(-1.53871697917945,0.227904467166324,
18.7762174447576));
#271926=CARTESIAN_POINT('Ctrl Pts',(-1.53824724718087,0.231053663042422,
18.7759880469244));
#271927=CARTESIAN_POINT('Ctrl Pts',(-1.53717053254376,0.238123375196727,
18.7754740648235));
#271928=CARTESIAN_POINT('Ctrl Pts',(-1.53655822097506,0.242043017735181,
18.775189783164));
#271929=CARTESIAN_POINT('Ctrl Pts',(-1.53495114962413,0.252078581312601,
18.7744635825857));
#271930=CARTESIAN_POINT('Ctrl Pts',(-1.53393481770518,0.258191055855722,
18.7740228424643));
#271931=CARTESIAN_POINT('Ctrl Pts',(-1.52762155742059,0.294806935424441,
18.7713912110674));
#271932=CARTESIAN_POINT('Ctrl Pts',(-1.52145098600253,0.325155329425654,
18.7692456656695));
#271933=CARTESIAN_POINT('Ctrl Pts',(-1.50885764965102,0.378831015110621,
18.7654817713843));
#271934=CARTESIAN_POINT('Ctrl Pts',(-1.50278939559762,0.402229391684932,
18.7638516212343));
#271935=CARTESIAN_POINT('Ctrl Pts',(-1.48360231947615,0.469700075827315,
18.75915720477));
#271936=CARTESIAN_POINT('Ctrl Pts',(-1.46907165424801,0.513344718846042,
18.7561278793318));
#271937=CARTESIAN_POINT('Ctrl Pts',(-1.43787516749469,0.594808476515452,
18.7503850315676));
#271938=CARTESIAN_POINT('Ctrl Pts',(-1.42159527624399,0.632731304633764,
18.7476734337654));
#271939=CARTESIAN_POINT('Ctrl Pts',(-1.36862436450953,0.743725771684251,
18.7395218517367));
#271940=CARTESIAN_POINT('Ctrl Pts',(-1.32766740394668,0.814590050468797,
18.7340215262471));
#271941=CARTESIAN_POINT('Ctrl Pts',(-1.27412831319303,0.892378285496051,
18.7274212817382));
#271942=CARTESIAN_POINT('Ctrl Pts',(-1.26679052298963,0.902764485826335,
18.7265278421246));
#271943=CARTESIAN_POINT('Ctrl Pts',(-1.2553265552259,0.918576030052865,
18.7251481951955));
#271944=CARTESIAN_POINT('Ctrl Pts',(-1.25129055835476,0.924066349966369,
18.7246654547836));
#271945=CARTESIAN_POINT('Ctrl Pts',(-1.24386621855829,0.934028133105149,
18.7237827167207));
#271946=CARTESIAN_POINT('Ctrl Pts',(-1.24048949255047,0.938508146188682,
18.72338317615));
#271947=CARTESIAN_POINT('Ctrl Pts',(-1.23306131330517,0.94825322686272,
18.7225084160979));
#271948=CARTESIAN_POINT('Ctrl Pts',(-1.22900023325334,0.95351078061902,
18.7220328229874));
#271949=CARTESIAN_POINT('Ctrl Pts',(-1.21775923065159,0.967872482167281,
18.7207234875946));
#271950=CARTESIAN_POINT('Ctrl Pts',(-1.21051112748825,0.976922454580197,
18.7198870483512));
#271951=CARTESIAN_POINT('Ctrl Pts',(-1.17161032374428,1.02439629118279,
18.7154376524296));
#271952=CARTESIAN_POINT('Ctrl Pts',(-1.13823128300075,1.06136093455897,
18.7117551572179));
#271953=CARTESIAN_POINT('Ctrl Pts',(-1.0004780880754,1.19992842391073,18.697046120097));
#271954=CARTESIAN_POINT('Ctrl Pts',(-0.88384303124947,1.28825327817098,
18.6855202920137));
#271955=CARTESIAN_POINT('Ctrl Pts',(-0.738245916070925,1.36931245208684,
18.6729008077676));
#271956=CARTESIAN_POINT('Ctrl Pts',(-0.719641346799062,1.37918093686114,
18.6713197796696));
#271957=CARTESIAN_POINT('Ctrl Pts',(-0.692556218430453,1.39285040720813,
18.6690686115381));
#271958=CARTESIAN_POINT('Ctrl Pts',(-0.684233811270484,1.39695757794949,
18.6683836446252));
#271959=CARTESIAN_POINT('Ctrl Pts',(-0.669385714753562,1.4041206944867,
18.6671741451085));
#271960=CARTESIAN_POINT('Ctrl Pts',(-0.662874693880398,1.40720620571879,
18.6666480110027));
#271961=CARTESIAN_POINT('Ctrl Pts',(-0.652888222664744,1.41185400577409,
18.6658477589511));
#271962=CARTESIAN_POINT('Ctrl Pts',(-0.649428199112855,1.41344889541703,
18.6655717200872));
#271963=CARTESIAN_POINT('Ctrl Pts',(-0.645953593567903,1.41503505435319,
18.66529576954));
#271964=CARTESIAN_POINT('Ctrl Pts',(-0.645944886371479,1.41503902909501,
18.6652950780289));
#271965=CARTESIAN_POINT('Ctrl Pts',(-0.645927441107565,1.4150469924764,
18.6652936925708));
#271966=CARTESIAN_POINT('Ctrl Pts',(-0.645918703058556,1.41505098110684,
18.6652929986252));
#271967=CARTESIAN_POINT('Ctrl Pts',(-0.645901195925661,1.41505897233816,
18.6652916082853));
#271968=CARTESIAN_POINT('Ctrl Pts',(-0.645892426791781,1.41506297496117,
18.6652909118871));
#271969=CARTESIAN_POINT('Ctrl Pts',(-0.645874857233824,1.41507099429208,
18.6652895166216));
#271970=CARTESIAN_POINT('Ctrl Pts',(-0.64586605689437,1.41507501096066,
18.6652888177612));
#271971=CARTESIAN_POINT('Ctrl Pts',(-0.645848424741837,1.41508305846432,
18.6652874175571));
#271972=CARTESIAN_POINT('Ctrl Pts',(-0.645839592936646,1.4150870892951,
18.6652867162141));
#271973=CARTESIAN_POINT('Ctrl Pts',(-0.645821897664302,1.41509516520699,
18.66528531103));
#271974=CARTESIAN_POINT('Ctrl Pts',(-0.645813034239644,1.415099210268,18.6652846071923));
#271975=CARTESIAN_POINT('Ctrl Pts',(-0.645795275620331,1.4151073146875,
18.6652831970104));
#271976=CARTESIAN_POINT('Ctrl Pts',(-0.645786380324565,1.41511137409142,
18.6652824906583));
#271977=CARTESIAN_POINT('Ctrl Pts',(-0.645768557719544,1.4151195073057,
18.6652810754283));
#271978=CARTESIAN_POINT('Ctrl Pts',(-0.645759630456149,1.4151235810944,
18.6652803665542));
#271979=CARTESIAN_POINT('Ctrl Pts',(-0.645741743715666,1.41513174316741,
18.6652789462647));
#271980=CARTESIAN_POINT('Ctrl Pts',(-0.645732784219057,1.4151358314599,
18.6652782348477));
#271981=CARTESIAN_POINT('Ctrl Pts',(-0.645714832802365,1.41514402263399,
18.6652768094559));
#271982=CARTESIAN_POINT('Ctrl Pts',(-0.645705840916108,1.41514812549942,
18.6652760954838));
#271983=CARTESIAN_POINT('Ctrl Pts',(-0.645687824520127,1.41515634590842,
18.6652746649661));
#271984=CARTESIAN_POINT('Ctrl Pts',(-0.645678800021557,1.41516046344615,
18.6652739484215));
#271985=CARTESIAN_POINT('Ctrl Pts',(-0.645660718250003,1.41516871326637,
18.6652725127468));
#271986=CARTESIAN_POINT('Ctrl Pts',(-0.645651660928029,1.41517284557046,
18.6652717936129));
#271987=CARTESIAN_POINT('Ctrl Pts',(-0.64563351330241,1.41518112501567,
18.6652703527436));
#271988=CARTESIAN_POINT('Ctrl Pts',(-0.645624422990814,1.41518527215966,
18.6652696310076));
#271989=CARTESIAN_POINT('Ctrl Pts',(-0.645606209148752,1.4151935813906,
18.6652681849152));
#271990=CARTESIAN_POINT('Ctrl Pts',(-0.645597085643688,1.41519774346518,
18.665267460561));
#271991=CARTESIAN_POINT('Ctrl Pts',(-0.645578805209261,1.4152060826487,
18.6652660092161));
#271992=CARTESIAN_POINT('Ctrl Pts',(-0.645569648292943,1.41521025975091,
18.6652652822266));
#271993=CARTESIAN_POINT('Ctrl Pts',(-0.645551300862317,1.41521862906655,
18.6652638255976));
#271994=CARTESIAN_POINT('Ctrl Pts',(-0.645542110321833,1.41522282129115,
18.6652630959561));
#271995=CARTESIAN_POINT('Ctrl Pts',(-0.645523695448889,1.4152312209377,
18.6652616340079));
#271996=CARTESIAN_POINT('Ctrl Pts',(-0.64551447109297,1.41523542836955,
18.6652609016994));
#271997=CARTESIAN_POINT('Ctrl Pts',(-0.645495988347904,1.41524385853828,
18.6652594343982));
#271998=CARTESIAN_POINT('Ctrl Pts',(-0.645486729985911,1.41524808126196,
18.6652586994078));
#271999=CARTESIAN_POINT('Ctrl Pts',(-0.64546817901382,1.41525654210991,
18.6652572267259));
#272000=CARTESIAN_POINT('Ctrl Pts',(-0.645458886415928,1.41526078022781,
18.6652564890355));
#272001=CARTESIAN_POINT('Ctrl Pts',(-0.64544026675778,1.41526927195949,
18.6652550109368));
#272002=CARTESIAN_POINT('Ctrl Pts',(-0.645430939724615,1.41527352556009,
18.6652542705308));
#272003=CARTESIAN_POINT('Ctrl Pts',(-0.645412251023805,1.41528204833321,
18.6652527869875));
#272004=CARTESIAN_POINT('Ctrl Pts',(-0.645402889317873,1.41528631752236,
18.6652520438472));
#272005=CARTESIAN_POINT('Ctrl Pts',(-0.645384131052972,1.41529487156976,
18.6652505548182));
#272006=CARTESIAN_POINT('Ctrl Pts',(-0.645374734498175,1.41529915642526,
18.6652498089299));
#272007=CARTESIAN_POINT('Ctrl Pts',(-0.645355906318788,1.41530774190171,
18.6652483143878));
#272008=CARTESIAN_POINT('Ctrl Pts',(-0.645346474682014,1.41531204252735,
18.6652475657332));
#272009=CARTESIAN_POINT('Ctrl Pts',(-0.645327576142191,1.41532065963113,
18.6652460656431));
#272010=CARTESIAN_POINT('Ctrl Pts',(-0.645318109207583,1.4153249761228,
18.6652453142052));
#272011=CARTESIAN_POINT('Ctrl Pts',(-0.645299139822707,1.41533362506977,
18.665243808529));
#272012=CARTESIAN_POINT('Ctrl Pts',(-0.645289637400272,1.41533795751152,
18.6652430542929));
#272013=CARTESIAN_POINT('Ctrl Pts',(-0.645270596835231,1.41534663844932,
18.6652415430044));
#272014=CARTESIAN_POINT('Ctrl Pts',(-0.645261058670962,1.41535098695437,
18.6652407859503));
#272015=CARTESIAN_POINT('Ctrl Pts',(-0.645241946389719,1.41535970012217,
18.6652392690074));
#272016=CARTESIAN_POINT('Ctrl Pts',(-0.645232372296066,1.41536406477341,
18.6652385091205));
#272017=CARTESIAN_POINT('Ctrl Pts',(-0.645213187967082,1.41537281031709,
18.6652369864973));
#272018=CARTESIAN_POINT('Ctrl Pts',(-0.645203577685199,1.41537719122988,
18.6652362237574));
#272019=CARTESIAN_POINT('Ctrl Pts',(-0.645184320694549,1.415385969424,18.6652346954056));
#272020=CARTESIAN_POINT('Ctrl Pts',(-0.645174674069118,1.41539036666645,
18.6652339298005));
#272021=CARTESIAN_POINT('Ctrl Pts',(-0.645155060872781,1.41539930675065,
18.6652323732173));
#272022=CARTESIAN_POINT('Ctrl Pts',(-0.645145094260424,1.41540384960324,
18.6652315822367));
#272023=CARTESIAN_POINT('Ctrl Pts',(-0.645124990212183,1.41541301291455,
18.6652299867392));
#272024=CARTESIAN_POINT('Ctrl Pts',(-0.645114852758563,1.41541763337695,
18.6652291822212));
#272025=CARTESIAN_POINT('Ctrl Pts',(-0.64509440382662,1.41542695335365,
18.6652275593961));
#272026=CARTESIAN_POINT('Ctrl Pts',(-0.645084092352085,1.41543165286166,
18.6652267410896));
#272027=CARTESIAN_POINT('Ctrl Pts',(-0.645063292137594,1.41544113239282,
18.6652250904313));
#272028=CARTESIAN_POINT('Ctrl Pts',(-0.645052803384069,1.41544591241743,
18.6652242580788));
#272029=CARTESIAN_POINT('Ctrl Pts',(-0.645031645273522,1.4154555544888,
18.6652225790647));
#272030=CARTESIAN_POINT('Ctrl Pts',(-0.645020975950331,1.41546041651526,
18.6652217324062));
#272031=CARTESIAN_POINT('Ctrl Pts',(-0.644999453313102,1.4154702241192,
18.6652200245126));
#272032=CARTESIAN_POINT('Ctrl Pts',(-0.644988600018616,1.4154751696827,
18.6652191632795));
#272033=CARTESIAN_POINT('Ctrl Pts',(-0.644966706038322,1.41548514589496,
18.6652174259679));
#272034=CARTESIAN_POINT('Ctrl Pts',(-0.64495566530293,1.41549017656106,
18.665216549886));
#272035=CARTESIAN_POINT('Ctrl Pts',(-0.644933392913297,1.41550032456997,
18.6652147825984));
#272036=CARTESIAN_POINT('Ctrl Pts',(-0.644922161250578,1.4155054419112,
18.6652138913924));
#272037=CARTESIAN_POINT('Ctrl Pts',(-0.644899503383262,1.41551576490468,
18.6652120935704));
#272038=CARTESIAN_POINT('Ctrl Pts',(-0.644888077189239,1.41552097054647,
18.6652111869557));
#272039=CARTESIAN_POINT('Ctrl Pts',(-0.644865026554577,1.41553147181189,
18.6652093580237));
#272040=CARTESIAN_POINT('Ctrl Pts',(-0.644853402164402,1.41553676740668,
18.6652084357109));
#272041=CARTESIAN_POINT('Ctrl Pts',(-0.644829951437513,1.41554745024601,
18.6652065750905));
#272042=CARTESIAN_POINT('Ctrl Pts',(-0.644818125058231,1.41555283750388,
18.6652056367801));
#272043=CARTESIAN_POINT('Ctrl Pts',(-0.644794266521604,1.41556370539643,
18.6652037438621));
#272044=CARTESIAN_POINT('Ctrl Pts',(-0.644782234374757,1.41556918602006,
18.6652027892559));
#272045=CARTESIAN_POINT('Ctrl Pts',(-0.644757960379225,1.41558024241248,
18.6652008634363));
#272046=CARTESIAN_POINT('Ctrl Pts',(-0.644745718539001,1.4155858181709,
18.6651998922243));
#272047=CARTESIAN_POINT('Ctrl Pts',(-0.641838847815903,1.41690975732146,
18.6649692779887));
#272048=CARTESIAN_POINT('Ctrl Pts',(-0.638940222190832,1.41821922133179,
18.6647401934099));
#272049=CARTESIAN_POINT('Ctrl Pts',(-0.632310924005199,1.42118957951864,
18.6642182422463));
#272050=CARTESIAN_POINT('Ctrl Pts',(-0.628577716537844,1.42284467910259,
18.6639257311539));
#272051=CARTESIAN_POINT('Ctrl Pts',(-0.618796535415627,1.42713510902408,
18.6631629317355));
#272052=CARTESIAN_POINT('Ctrl Pts',(-0.612738154290542,1.42974673632314,
18.6626940396309));
#272053=CARTESIAN_POINT('Ctrl Pts',(-0.571081476420635,1.44739054284323,
18.6594932335859));
#272054=CARTESIAN_POINT('Ctrl Pts',(-0.534946735748217,1.46113177000206,
18.656832577638));
#272055=CARTESIAN_POINT('Ctrl Pts',(-0.489602866938786,1.47646680798279,
18.6535907030145));
#272056=CARTESIAN_POINT('Ctrl Pts',(-0.48084548258812,1.47934202605214,
18.652968986519));
#272057=CARTESIAN_POINT('Ctrl Pts',(-0.369158319168309,1.51491450453478,
18.645089650469));
#272058=CARTESIAN_POINT('Ctrl Pts',(-0.263117194499882,1.53688497405591,
18.6381235289083));
#272059=CARTESIAN_POINT('Ctrl Pts',(-0.0897978240626272,1.55431563052022,
18.6265095832142));
#272060=CARTESIAN_POINT('Ctrl Pts',(-0.0235973980838778,1.55672801854881,
18.622025469096));
#272061=CARTESIAN_POINT('Ctrl Pts',(0.0561733953246495,1.55454512464419,
18.6164553414199));
#272062=CARTESIAN_POINT('Ctrl Pts',(0.0697912386742956,1.55399329379031,
18.6154987509854));
#272063=CARTESIAN_POINT('Ctrl Pts',(0.0903868226196514,1.55288745017551,
18.6140425859668));
#272064=CARTESIAN_POINT('Ctrl Pts',(0.0973712280972347,1.55246515312185,
18.613547128563));
#272065=CARTESIAN_POINT('Ctrl Pts',(0.110004004127844,1.55161575578494,
18.6126479096249));
#272066=CARTESIAN_POINT('Ctrl Pts',(0.115653376373959,1.55120489604063,
18.6122446636767));
#272067=CARTESIAN_POINT('Ctrl Pts',(0.127776636086444,1.55025661768673,
18.6113768607707));
#272068=CARTESIAN_POINT('Ctrl Pts',(0.134249632152219,1.54970948351902,
18.6109120063419));
#272069=CARTESIAN_POINT('Ctrl Pts',(0.151651893589408,1.54812869922284,
18.6096581134512));
#272070=CARTESIAN_POINT('Ctrl Pts',(0.162573777559015,1.54701988401345,
18.6088667328782));
#272071=CARTESIAN_POINT('Ctrl Pts',(0.21479461266815,1.5411592033393,18.6050609760018));
#272072=CARTESIAN_POINT('Ctrl Pts',(0.255900017248029,1.53486904679568,
18.601998861258));
#272073=CARTESIAN_POINT('Ctrl Pts',(0.44768543244785,1.49760310761251,18.5873839826503));
#272074=CARTESIAN_POINT('Ctrl Pts',(0.593449121149683,1.44604338696173,
18.5752010628627));
#272075=CARTESIAN_POINT('Ctrl Pts',(0.757969857199383,1.35871923474111,
18.5610844278182));
#272076=CARTESIAN_POINT('Ctrl Pts',(0.786191786473468,1.34258673130148,
18.5586533335845));
#272077=CARTESIAN_POINT('Ctrl Pts',(0.819535986366454,1.32211380430319,
18.5557869729577));
#272078=CARTESIAN_POINT('Ctrl Pts',(0.825159919884402,1.31861110845188,
18.5553037393027));
#272079=CARTESIAN_POINT('Ctrl Pts',(0.833883730356905,1.3131000774609,18.5545546917192));
#272080=CARTESIAN_POINT('Ctrl Pts',(0.836999034648797,1.31111651120397,
18.5542873126004));
#272081=CARTESIAN_POINT('Ctrl Pts',(0.842784809381132,1.30740358596413,
18.5537909786182));
#272082=CARTESIAN_POINT('Ctrl Pts',(0.845457012337971,1.30567714696205,
18.553561846256));
#272083=CARTESIAN_POINT('Ctrl Pts',(0.85154647669686,1.30171637349602,18.5530399076791));
#272084=CARTESIAN_POINT('Ctrl Pts',(0.854960249953708,1.29947677587154,
18.5527474561279));
#272085=CARTESIAN_POINT('Ctrl Pts',(0.863858386379808,1.29358893197377,
18.5519854476243));
#272086=CARTESIAN_POINT('Ctrl Pts',(0.869328540350324,1.28991919500765,
18.5515172785256));
#272087=CARTESIAN_POINT('Ctrl Pts',(0.906496109011111,1.26464093326206,
18.5483369267465));
#272088=CARTESIAN_POINT('Ctrl Pts',(0.937411287606931,1.24189877760512,
18.5456948677055));
#272089=CARTESIAN_POINT('Ctrl Pts',(1.04309024184874,1.15796040031711,18.5365516675918));
#272090=CARTESIAN_POINT('Ctrl Pts',(1.11296910070648,1.09096842337835,18.5302878316224));
#272091=CARTESIAN_POINT('Ctrl Pts',(1.23412181179439,0.950979269136698,
18.5180474601914));
#272092=CARTESIAN_POINT('Ctrl Pts',(1.28622808701608,0.879222361561054,
18.5121123890196));
#272093=CARTESIAN_POINT('Ctrl Pts',(1.33855487551464,0.792473872806984,
18.5050325516305));
#272094=CARTESIAN_POINT('Ctrl Pts',(1.34502862181958,0.781435847087287,
18.5041336176649));
#272095=CARTESIAN_POINT('Ctrl Pts',(1.35474805469087,0.764385124250459,
18.5027472769333));
#272096=CARTESIAN_POINT('Ctrl Pts',(1.35809164917245,0.758428625262346,
18.5022633919723));
#272097=CARTESIAN_POINT('Ctrl Pts',(1.36410983615106,0.747540020506673,
18.501379498948));
#272098=CARTESIAN_POINT('Ctrl Pts',(1.36679719827266,0.742615071638851,
18.5009799547102));
#272099=CARTESIAN_POINT('Ctrl Pts',(1.37260117237279,0.731840286449427,
18.5001063013854));
#272100=CARTESIAN_POINT('Ctrl Pts',(1.3757071423129,0.725984875424026,18.4996318248346));
#272101=CARTESIAN_POINT('Ctrl Pts',(1.3841127159513,0.70989094334789,18.4983284014019));
#272102=CARTESIAN_POINT('Ctrl Pts',(1.38933597134251,0.69961325554501,18.4974967973479));
#272103=CARTESIAN_POINT('Ctrl Pts',(1.40873301588408,0.660372090505318,
18.4943238944194));
#272104=CARTESIAN_POINT('Ctrl Pts',(1.42211652744284,0.631033900310215,
18.4919560728974));
#272105=CARTESIAN_POINT('Ctrl Pts',(1.4345766894261,0.601306886835045,18.4895593986216));
#272106=CARTESIAN_POINT('',(-1.5554997549337,-0.000873155876330299,18.655943774337));
#272107=CARTESIAN_POINT('Ctrl Pts',(1.43457668357356,0.601306900797837,
18.3502241513278));
#272108=CARTESIAN_POINT('Ctrl Pts',(1.41226823356769,0.654529609838117,
18.3543632657824));
#272109=CARTESIAN_POINT('Ctrl Pts',(1.38696156950888,0.706586430174956,
18.3585023802371));
#272110=CARTESIAN_POINT('Ctrl Pts',(1.35880418892424,0.757120483253445,
18.3626414946918));
#272111=CARTESIAN_POINT('Ctrl Pts',(1.33067099704232,0.807611124865335,
18.3667770534248));
#272112=CARTESIAN_POINT('Ctrl Pts',(1.29969219388313,0.856581138214668,
18.3709126121577));
#272113=CARTESIAN_POINT('Ctrl Pts',(1.26606223462692,0.903696114881263,
18.3750481708907));
#272114=CARTESIAN_POINT('Ctrl Pts',(1.23244823856831,0.950788727391055,
18.3791817665901));
#272115=CARTESIAN_POINT('Ctrl Pts',(1.19618588385133,0.996027625870422,
18.3833153622894));
#272116=CARTESIAN_POINT('Ctrl Pts',(1.15751298206812,1.03910728336576,18.3874489579887));
#272117=CARTESIAN_POINT('Ctrl Pts',(1.11884357276049,1.08218305041986,18.391582180391));
#272118=CARTESIAN_POINT('Ctrl Pts',(1.07776439773428,1.12309957741441,18.3957154027932));
#272119=CARTESIAN_POINT('Ctrl Pts',(1.03455213303515,1.16158604245765,18.3998486251955));
#272120=CARTESIAN_POINT('Ctrl Pts',(0.991296757475191,1.20011090365184,
18.4039859711209));
#272121=CARTESIAN_POINT('Ctrl Pts',(0.945904433359631,1.23620051571814,
18.4081233170463));
#272122=CARTESIAN_POINT('Ctrl Pts',(0.898686080166107,1.26962340058605,
18.4122606629718));
#272123=CARTESIAN_POINT('Ctrl Pts',(0.851442481341058,1.3030641552393,18.4164002209589));
#272124=CARTESIAN_POINT('Ctrl Pts',(0.802371351123281,1.33383506677874,
18.4205397789461));
#272125=CARTESIAN_POINT('Ctrl Pts',(0.751811143945473,1.3617489687308,18.4246793369332));
#272126=CARTESIAN_POINT('Ctrl Pts',(0.701158309541624,1.38971400946274,
18.4288264786664));
#272127=CARTESIAN_POINT('Ctrl Pts',(0.64901142148413,1.41481136490602,18.4329736203997));
#272128=CARTESIAN_POINT('Ctrl Pts',(0.595730896403694,1.43690116190017,
18.4371207621329));
#272129=CARTESIAN_POINT('Ctrl Pts',(0.564141473819204,1.44999795347646,
18.4395795557077));
#272130=CARTESIAN_POINT('Ctrl Pts',(0.532153905931037,1.46203847331314,
18.4420383492824));
#272131=CARTESIAN_POINT('Ctrl Pts',(0.499845551780331,1.47300192612414,
18.4444971428572));
#272132=CARTESIAN_POINT('Ctrl Pts',(0.445337743066455,1.49149849781201,
18.4486454027536));
#272133=CARTESIAN_POINT('Ctrl Pts',(0.389687539204677,1.5070042221029,18.4527936626499));
#272134=CARTESIAN_POINT('Ctrl Pts',(0.333254870821266,1.51938192732239,
18.4569419225463));
#272135=CARTESIAN_POINT('Ctrl Pts',(0.276922497358692,1.53173763427384,
18.4610828099507));
#272136=CARTESIAN_POINT('Ctrl Pts',(0.219810924045607,1.54097624588835,
18.465223697355));
#272137=CARTESIAN_POINT('Ctrl Pts',(0.162295924297699,1.54701011081258,
18.4693645847593));
#272138=CARTESIAN_POINT('Ctrl Pts',(0.104838111984474,1.55303797623655,
18.4735013548598));
#272139=CARTESIAN_POINT('Ctrl Pts',(0.0469781832756797,1.55586735430706,
18.4776381249604));
#272140=CARTESIAN_POINT('Ctrl Pts',(-0.0108989230934016,1.55546181678478,
18.4817748950609));
#272141=CARTESIAN_POINT('Ctrl Pts',(-0.0687407250667601,1.55505652663591,
18.4859091417773));
#272142=CARTESIAN_POINT('Ctrl Pts',(-0.126599164262136,1.55142023610591,
18.4900433884938));
#272143=CARTESIAN_POINT('Ctrl Pts',(-0.184087441730226,1.54456856882342,
18.4941776352102));
#272144=CARTESIAN_POINT('Ctrl Pts',(-0.241562744488456,1.53771844791523,
18.4983109488555));
#272145=CARTESIAN_POINT('Ctrl Pts',(-0.298667534541657,1.5276544525376,
18.5024442625009));
#272146=CARTESIAN_POINT('Ctrl Pts',(-0.355020502908433,1.51444402092472,
18.5065775761462));
#272147=CARTESIAN_POINT('Ctrl Pts',(-0.411424393247191,1.50122165203067,
18.5107146247586));
#272148=CARTESIAN_POINT('Ctrl Pts',(-0.46707459575755,1.48484728305153,
18.514851673371));
#272149=CARTESIAN_POINT('Ctrl Pts',(-0.521601711801954,1.46543915064573,
18.5189887219834));
#272150=CARTESIAN_POINT('Ctrl Pts',(-0.57615135366955,1.44602300050139,
18.5231274796615));
#272151=CARTESIAN_POINT('Ctrl Pts',(-0.629576502509719,1.42357078941286,
18.5272662373396));
#272152=CARTESIAN_POINT('Ctrl Pts',(-0.681527658364044,1.39824901247411,
18.5314049950178));
#272153=CARTESIAN_POINT('Ctrl Pts',(-0.733580055445961,1.37287788903401,
18.5355518182125));
#272154=CARTESIAN_POINT('Ctrl Pts',(-0.784152262372308,1.34462627839229,
18.5396986414072));
#272155=CARTESIAN_POINT('Ctrl Pts',(-0.832920134865223,1.31370632141895,
18.5438454646019));
#272156=CARTESIAN_POINT('Ctrl Pts',(-0.87903267828431,1.28446990437703,
18.5477665002108));
#272157=CARTESIAN_POINT('Ctrl Pts',(-0.923531971664942,1.25284841053402,
18.5516875358197));
#272158=CARTESIAN_POINT('Ctrl Pts',(-0.966171551974055,1.21905405218803,
18.5556085714287));
#272159=CARTESIAN_POINT('Ctrl Pts',(-1.01163414749869,1.18302228936671,
18.5597892048832));
#272160=CARTESIAN_POINT('Ctrl Pts',(-1.05518758759132,1.14435700776817,
18.5639698383377));
#272161=CARTESIAN_POINT('Ctrl Pts',(-1.09650642551172,1.10329230433803,
18.5681504717922));
#272162=CARTESIAN_POINT('Ctrl Pts',(-1.13691930318326,1.06312798898295,
18.5722394403327));
#272163=CARTESIAN_POINT('Ctrl Pts',(-1.1751941580597,1.02066878544996,18.5763284088732));
#272164=CARTESIAN_POINT('Ctrl Pts',(-1.21105782752621,0.97617579789068,
18.5804173774137));
#272165=CARTESIAN_POINT('Ctrl Pts',(-1.24688668618988,0.931725997117362,
18.5845023770275));
#272166=CARTESIAN_POINT('Ctrl Pts',(-1.28030865878357,0.885246734994203,
18.5885873766412));
#272167=CARTESIAN_POINT('Ctrl Pts',(-1.31108850350603,0.83703475792486,
18.592672376255));
#272168=CARTESIAN_POINT('Ctrl Pts',(-1.34185101365334,0.788849932848869,
18.596755075281));
#272169=CARTESIAN_POINT('Ctrl Pts',(-1.36997405671991,0.738934776415113,
18.600837774307));
#272170=CARTESIAN_POINT('Ctrl Pts',(-1.39526510124146,0.687615842791343,
18.604920473333));
#272171=CARTESIAN_POINT('Ctrl Pts',(-1.42160455154756,0.63416955271055,
18.6091724150834));
#272172=CARTESIAN_POINT('Ctrl Pts',(-1.44487170883023,0.579201061646552,
18.6134243568337));
#272173=CARTESIAN_POINT('Ctrl Pts',(-1.4649027724697,0.523106219816391,
18.617676298584));
#272174=CARTESIAN_POINT('Ctrl Pts',(-1.48414973309998,0.469207174229017,
18.6217618008291));
#272175=CARTESIAN_POINT('Ctrl Pts',(-1.50040916787234,0.414268887386565,
18.6258473030742));
#272176=CARTESIAN_POINT('Ctrl Pts',(-1.51358652346675,0.358658731916363,
18.6299328053194));
#272177=CARTESIAN_POINT('Ctrl Pts',(-1.52677097037022,0.303018650199013,
18.6340205061512));
#272178=CARTESIAN_POINT('Ctrl Pts',(-1.53686994623477,0.246706507368367,
18.638108206983));
#272179=CARTESIAN_POINT('Ctrl Pts',(-1.54384031258021,0.190098235794666,
18.6421959078149));
#272180=CARTESIAN_POINT('Ctrl Pts',(-1.55082123451994,0.133404239322336,
18.6462897988682));
#272181=CARTESIAN_POINT('Ctrl Pts',(-1.5546640712529,0.0764137526860417,
18.6503836899215));
#272182=CARTESIAN_POINT('Ctrl Pts',(-1.55537771270569,0.0195043794678024,
18.6544775809749));
#272183=CARTESIAN_POINT('Ctrl Pts',(-1.55546290764187,0.012710505036345,
18.6549663120956));
#272184=CARTESIAN_POINT('Ctrl Pts',(-1.55550356692172,0.00591778098874543,
18.6554550432163));
#272185=CARTESIAN_POINT('Ctrl Pts',(-1.55549975493371,-0.000873155876329073,
18.655943774337));
#272186=CARTESIAN_POINT('Ctrl Pts',(-1.55549975493324,-0.0008731566999196,
18.6559437743963));
#272187=CARTESIAN_POINT('Ctrl Pts',(-1.55547173756343,-0.0507851734952812,
18.6595358495975));
#272188=CARTESIAN_POINT('Ctrl Pts',(-1.55304159676454,-0.100629236248426,
18.6631279247988));
#272189=CARTESIAN_POINT('Ctrl Pts',(-1.54822763866007,-0.150237907630056,
18.66672));
#272190=CARTESIAN_POINT('Ctrl Pts',(-1.54266732521047,-0.207537900009354,
18.6708689900037));
#272191=CARTESIAN_POINT('Ctrl Pts',(-1.53391005274538,-0.264648874929275,
18.6750179800073));
#272192=CARTESIAN_POINT('Ctrl Pts',(-1.52197885983842,-0.32118623912761,
18.679166970011));
#272193=CARTESIAN_POINT('Ctrl Pts',(-1.51006890548561,-0.377622961933217,
18.683308574454));
#272194=CARTESIAN_POINT('Ctrl Pts',(-1.49499635161617,-0.433487595602833,
18.687450178897));
#272195=CARTESIAN_POINT('Ctrl Pts',(-1.47683588997844,-0.488401478367519,
18.69159178334));
#272196=CARTESIAN_POINT('Ctrl Pts',(-1.45869351899637,-0.543260658329841,
18.6957292620983));
#272197=CARTESIAN_POINT('Ctrl Pts',(-1.43746949749457,-0.597170472162358,
18.6998667408565));
#272198=CARTESIAN_POINT('Ctrl Pts',(-1.41328897637056,-0.649764972331879,
18.7040042196148));
#272199=CARTESIAN_POINT('Ctrl Pts',(-1.38912325789126,-0.702327275606414,
18.7081391655232));
#272200=CARTESIAN_POINT('Ctrl Pts',(-1.36200484454982,-0.75357538937617,
18.7122741114317));
#272201=CARTESIAN_POINT('Ctrl Pts',(-1.33210709816146,-0.803163077480445,
18.7164090573401));
#272202=CARTESIAN_POINT('Ctrl Pts',(-1.30221617470249,-0.852739449236975,
18.7205430596175));
#272203=CARTESIAN_POINT('Ctrl Pts',(-1.26954744603632,-0.900655702012691,
18.7246770618948));
#272204=CARTESIAN_POINT('Ctrl Pts',(-1.23431924712162,-0.946591911113297,
18.7288110641721));
#272205=CARTESIAN_POINT('Ctrl Pts',(-1.19905940702001,-0.992569379098057,
18.7329487795186));
#272206=CARTESIAN_POINT('Ctrl Pts',(-1.16123581917785,-1.0365628345512,
18.7370864948651));
#272207=CARTESIAN_POINT('Ctrl Pts',(-1.12110822496951,-1.07828409888383,
18.7412242102116));
#272208=CARTESIAN_POINT('Ctrl Pts',(-1.08096416148368,-1.12002248657243,
18.7453636237706));
#272209=CARTESIAN_POINT('Ctrl Pts',(-1.03851458757045,-1.15948646774434,
18.7495030373296));
#272210=CARTESIAN_POINT('Ctrl Pts',(-0.994055054977217,-1.19642584294817,
18.7536424508885));
#272211=CARTESIAN_POINT('Ctrl Pts',(-0.949509182631559,-1.2334369538704,
18.7577899031272));
#272212=CARTESIAN_POINT('Ctrl Pts',(-0.90294597044219,-1.26791334933861,
18.7619373553659));
#272213=CARTESIAN_POINT('Ctrl Pts',(-0.854692154271789,-1.29964671023561,
18.7660848076046));
#272214=CARTESIAN_POINT('Ctrl Pts',(-0.809136533122573,-1.32960564574675,
18.7700003479269));
#272215=CARTESIAN_POINT('Ctrl Pts',(-0.762074664077149,-1.35711994382657,
18.7739158882492));
#272216=CARTESIAN_POINT('Ctrl Pts',(-0.713800020992557,-1.38205274140715,
18.7778314285715));
#272217=CARTESIAN_POINT('Ctrl Pts',(-0.662644162089899,-1.40847362395714,
18.7819806633551));
#272218=CARTESIAN_POINT('Ctrl Pts',(-0.609912578938574,-1.43210558658674,
18.7861298981388));
#272219=CARTESIAN_POINT('Ctrl Pts',(-0.555940967516389,-1.45275940562673,
18.7902791329224));
#272220=CARTESIAN_POINT('Ctrl Pts',(-0.502065012393167,-1.47337661898021,
18.7944210138319));
#272221=CARTESIAN_POINT('Ctrl Pts',(-0.446953873401568,-1.49102598110697,
18.7985628947413));
#272222=CARTESIAN_POINT('Ctrl Pts',(-0.390966271700142,-1.50556488548083,
18.8027047756507));
#272223=CARTESIAN_POINT('Ctrl Pts',(-0.335034182048991,-1.52008937444187,
18.8068425498598));
#272224=CARTESIAN_POINT('Ctrl Pts',(-0.278227852725018,-1.53150938602532,
18.8109803240689));
#272225=CARTESIAN_POINT('Ctrl Pts',(-0.22092268181058,-1.5397316060475,
18.815118098278));
#272226=CARTESIAN_POINT('Ctrl Pts',(-0.163652336157003,-1.54794882929623,
18.8192533578961));
#272227=CARTESIAN_POINT('Ctrl Pts',(-0.105884263995698,-1.55297203957189,
18.8233886175142));
#272228=CARTESIAN_POINT('Ctrl Pts',(-0.0480034433414906,-1.55475911942248,
18.8275238771323));
#272229=CARTESIAN_POINT('Ctrl Pts',(0.00986441513524329,-1.5565457990637,
18.8316582106756));
#272230=CARTESIAN_POINT('Ctrl Pts',(0.0678444520235309,-1.55509777102806,
18.835792544219));
#272231=CARTESIAN_POINT('Ctrl Pts',(0.125549409195623,-1.55042497266093,
18.8399268777623));
#272232=CARTESIAN_POINT('Ctrl Pts',(0.183306533597198,-1.54574794992631,
18.8440649488827));
#272233=CARTESIAN_POINT('Ctrl Pts',(0.240787561214699,-1.53784037190848,
18.8482030200031));
#272234=CARTESIAN_POINT('Ctrl Pts',(0.297609450539051,-1.52676418118511,
18.8523410911236));
#272235=CARTESIAN_POINT('Ctrl Pts',(0.35445485067309,-1.51568340754106,
18.8564808744257));
#272236=CARTESIAN_POINT('Ctrl Pts',(0.410640062912466,-1.5014315344574,
18.8606206577279));
#272237=CARTESIAN_POINT('Ctrl Pts',(0.465794535428237,-1.48412118803189,
18.8647604410301));
#272238=CARTESIAN_POINT('Ctrl Pts',(0.521056353633815,-1.46677715093737,
18.868908281483));
#272239=CARTESIAN_POINT('Ctrl Pts',(0.575282933874055,-1.44636292780657,
18.8730561219358));
#272240=CARTESIAN_POINT('Ctrl Pts',(0.628121997755228,-1.42304005774117,
18.8772039623886));
#272241=CARTESIAN_POINT('Ctrl Pts',(0.677968997808009,-1.40103786807339,
18.8811169273067));
#272242=CARTESIAN_POINT('Ctrl Pts',(0.726581039451729,-1.37644771635597,
18.8850298922248));
#272243=CARTESIAN_POINT('Ctrl Pts',(0.773684537451322,-1.34944154616224,
18.8889428571429));
#272244=CARTESIAN_POINT('Ctrl Pts',(0.823545450020095,-1.32085444864224,
18.8930848850167));
#272245=CARTESIAN_POINT('Ctrl Pts',(0.871926305188375,-1.28943906380778,
18.8972269128904));
#272246=CARTESIAN_POINT('Ctrl Pts',(0.918486649111735,-1.25537346053017,
18.9013689407642));
#272247=CARTESIAN_POINT('Ctrl Pts',(0.9649640126152,-1.22136856939139,18.9055035866647));
#272248=CARTESIAN_POINT('Ctrl Pts',(1.00962688604308,-1.18472313970499,
18.9096382325652));
#272249=CARTESIAN_POINT('Ctrl Pts',(1.05216137632172,-1.14565993566014,
18.9137728784657));
#272250=CARTESIAN_POINT('Ctrl Pts',(1.0946534911311,-1.10663564877618,18.9179034051783));
#272251=CARTESIAN_POINT('Ctrl Pts',(1.13502104061593,-1.06519871093113,
18.9220339318909));
#272252=CARTESIAN_POINT('Ctrl Pts',(1.17298241452074,-1.02161269824973,
18.9261644586034));
#272253=CARTESIAN_POINT('Ctrl Pts',(1.2109206738195,-0.978053225005893,
18.9302924702464));
#272254=CARTESIAN_POINT('Ctrl Pts',(1.2464553190132,-0.93234766373174,18.9344204818894));
#272255=CARTESIAN_POINT('Ctrl Pts',(1.27934250116004,-0.88479546491015,
18.9385484935323));
#272256=CARTESIAN_POINT('Ctrl Pts',(1.31222239708508,-0.837253801374514,
18.9426755906059));
#272257=CARTESIAN_POINT('Ctrl Pts',(1.34245569726827,-0.787866741951971,
18.9468026876796));
#272258=CARTESIAN_POINT('Ctrl Pts',(1.36984101896112,-0.736963929084426,
18.9509297847532));
#272259=CARTESIAN_POINT('Ctrl Pts',(1.39725164353726,-0.686014084162731,
18.9550606950906));
#272260=CARTESIAN_POINT('Ctrl Pts',(1.42180878200753,-0.63354614784719,
18.959191605428));
#272261=CARTESIAN_POINT('Ctrl Pts',(1.44335701313008,-0.579914461492563,
18.9633225157654));
#272262=CARTESIAN_POINT('Ctrl Pts',(1.46491432766989,-0.526260167296834,
18.9674551674421));
#272263=CARTESIAN_POINT('Ctrl Pts',(1.48346003794147,-0.471441640916516,
18.9715878191189));
#272264=CARTESIAN_POINT('Ctrl Pts',(1.49888808133818,-0.415830217303106,
18.9757204707956));
#272265=CARTESIAN_POINT('Ctrl Pts',(1.51434673854817,-0.360108444133716,
18.9798613228788));
#272266=CARTESIAN_POINT('Ctrl Pts',(1.52667525381189,-0.303591141822869,
18.984002174962));
#272267=CARTESIAN_POINT('Ctrl Pts',(1.53581857345245,-0.246660818612296,
18.9881430270452));
#272268=CARTESIAN_POINT('Ctrl Pts',(1.54458556497539,-0.192073679519882,
18.9921134466016));
#272269=CARTESIAN_POINT('Ctrl Pts',(1.55042449470638,-0.137107278980882,
18.996083866158));
#272270=CARTESIAN_POINT('Ctrl Pts',(1.5533318590112,-0.0820998525017198,
19.0000542857144));
#272271=CARTESIAN_POINT('Ctrl Pts',(1.55639086283974,-0.0242234013400301,
19.0042317906124));
#272272=CARTESIAN_POINT('Ctrl Pts',(1.55621714226099,0.0339443710004242,
19.0084092955105));
#272273=CARTESIAN_POINT('Ctrl Pts',(1.5527761988485,0.0920126420097034,
19.0125868004085));
#272274=CARTESIAN_POINT('Ctrl Pts',(1.5493589106132,0.149681715742147,19.0167355865494));
#272275=CARTESIAN_POINT('Ctrl Pts',(1.54271916565345,0.207252128343795,
19.0208843726902));
#272276=CARTESIAN_POINT('Ctrl Pts',(1.53287509576863,0.26433726708945,19.025033158831));
#272277=CARTESIAN_POINT('Ctrl Pts',(1.5229288118468,0.322015138571926,19.0292250231077));
#272278=CARTESIAN_POINT('Ctrl Pts',(1.50971124661987,0.379197060509291,
19.0334168873844));
#272279=CARTESIAN_POINT('Ctrl Pts',(1.49329504324451,0.43548841984761,19.0376087516611));
#272280=CARTESIAN_POINT('Ctrl Pts',(1.47687883986916,0.491779779185915,
19.0418006159377));
#272281=CARTESIAN_POINT('Ctrl Pts',(1.45726411221541,0.547180037965144,
19.0459924802144));
#272282=CARTESIAN_POINT('Ctrl Pts',(1.43457668357356,0.601306900797836,
19.0501843444911));
#272283=CARTESIAN_POINT('Origin',(0.,0.,0.));
#272284=CARTESIAN_POINT('',(-1.95399958593193,0.00127207619237379,0.22586969212423));
#272285=CARTESIAN_POINT('',(0.861527879758777,1.75382031930251,3.92573008738128E-5));
#272286=CARTESIAN_POINT('Ctrl Pts',(-1.95399958593193,0.00127207619237379,
0.22586969212423));
#272287=CARTESIAN_POINT('Ctrl Pts',(-1.95395602836775,0.0681795954810932,
0.222037005420703));
#272288=CARTESIAN_POINT('Ctrl Pts',(-1.95047621447863,0.134982233331218,
0.218204318717176));
#272289=CARTESIAN_POINT('Ctrl Pts',(-1.94359078332685,0.201422111415151,
0.214371632013649));
#272290=CARTESIAN_POINT('Ctrl Pts',(-1.93653822890983,0.269474618994986,
0.210445918293744));
#272291=CARTESIAN_POINT('Ctrl Pts',(-1.92589346976546,0.337288960092626,
0.206520204573839));
#272292=CARTESIAN_POINT('Ctrl Pts',(-1.9116826354016,0.40445704531381,0.202594490853934));
#272293=CARTESIAN_POINT('Ctrl Pts',(-1.89749324764944,0.471523762254662,
0.198674701716329));
#272294=CARTESIAN_POINT('Ctrl Pts',(-1.87974856750535,0.537945683733757,
0.194754912578725));
#272295=CARTESIAN_POINT('Ctrl Pts',(-1.85852642413187,0.603320421338104,
0.19083512344112));
#272296=CARTESIAN_POINT('Ctrl Pts',(-1.83732958192574,0.668617218785931,
0.18692000749977));
#272297=CARTESIAN_POINT('Ctrl Pts',(-1.81266366201142,0.732868848475346,
0.18300489155842));
#272298=CARTESIAN_POINT('Ctrl Pts',(-1.78465700711252,0.795685469871221,
0.17908977561707));
#272299=CARTESIAN_POINT('Ctrl Pts',(-1.75666822735431,0.858461998798042,
0.175177158483539));
#272300=CARTESIAN_POINT('Ctrl Pts',(-1.72534314184954,0.919804890152479,
0.171264541350008));
#272301=CARTESIAN_POINT('Ctrl Pts',(-1.69085862348574,0.979343206125368,
0.167351924216477));
#272302=CARTESIAN_POINT('Ctrl Pts',(-1.65638440769107,1.03886373447512,
0.16344047601354));
#272303=CARTESIAN_POINT('Ctrl Pts',(-1.61875287845868,1.09658033418713,
0.159529027810603));
#272304=CARTESIAN_POINT('Ctrl Pts',(-1.57818652774778,1.15214724911159,
0.155617579607666));
#272305=CARTESIAN_POINT('Ctrl Pts',(-1.53761852548644,1.20771642629433,
0.15170597216058));
#272306=CARTESIAN_POINT('Ctrl Pts',(-1.4941157553654,1.26113535078223,0.147794364713494));
#272307=CARTESIAN_POINT('Ctrl Pts',(-1.44794258902418,1.31208927245441,
0.143882757266408));
#272308=CARTESIAN_POINT('Ctrl Pts',(-1.40172219393538,1.36309531292405,
0.139967148787221));
#272309=CARTESIAN_POINT('Ctrl Pts',(-1.35282628071841,1.41163095476592,
0.136051540308034));
#272310=CARTESIAN_POINT('Ctrl Pts',(-1.30155719667164,1.45741718934293,
0.132135931828847));
#272311=CARTESIAN_POINT('Ctrl Pts',(-1.25025852714807,1.50322984544876,
0.128218063798002));
#272312=CARTESIAN_POINT('Ctrl Pts',(-1.19658434270726,1.54628962916973,
0.124300195767158));
#272313=CARTESIAN_POINT('Ctrl Pts',(-1.14086913813976,1.58635860058192,
0.120382327736313));
#272314=CARTESIAN_POINT('Ctrl Pts',(-1.08506069260544,1.6264946285483,0.116457903042778));
#272315=CARTESIAN_POINT('Ctrl Pts',(-1.02720482132577,1.66362958935378,
0.112533478349243));
#272316=CARTESIAN_POINT('Ctrl Pts',(-0.967663207261701,1.69757000365581,
0.108609053655708));
#272317=CARTESIAN_POINT('Ctrl Pts',(-0.940612178557402,1.71298985976741,
0.106826103584545));
#272318=CARTESIAN_POINT('Ctrl Pts',(-0.913213507191092,1.72775098046652,
0.105043153513382));
#272319=CARTESIAN_POINT('Ctrl Pts',(-0.885502465630419,1.74183850668265,
0.10326020344222));
#272320=CARTESIAN_POINT('Ctrl Pts',(-0.825166121774214,1.7725118331976,
0.0993781159235467));
#272321=CARTESIAN_POINT('Ctrl Pts',(-0.763105599279648,1.8001116002205,
0.0954960284048736));
#272322=CARTESIAN_POINT('Ctrl Pts',(-0.699669805911684,1.82443913647332,
0.0916139408862006));
#272323=CARTESIAN_POINT('Ctrl Pts',(-0.636340329488619,1.84872590032945,
0.0877383596577921));
#272324=CARTESIAN_POINT('Ctrl Pts',(-0.57164062294732,1.86975114375477,
0.0838627784293837));
#272325=CARTESIAN_POINT('Ctrl Pts',(-0.505943004118793,1.88736262455927,
0.0799871972009753));
#272326=CARTESIAN_POINT('Ctrl Pts',(-0.440306865741454,1.90495762437397,
0.0761152427780247));
#272327=CARTESIAN_POINT('Ctrl Pts',(-0.37367514811737,1.91914506387478,
0.0722432883550741));
#272328=CARTESIAN_POINT('Ctrl Pts',(-0.306437506041051,1.92982176764885,
0.0683713339321236));
#272329=CARTESIAN_POINT('Ctrl Pts',(-0.239238675526287,1.94049230851279,
0.0645016145161243));
#272330=CARTESIAN_POINT('Ctrl Pts',(-0.171435108718065,1.94765605344516,
0.0606318951001249));
#272331=CARTESIAN_POINT('Ctrl Pts',(-0.103426987508651,1.95126083808774,
0.0567621756841256));
#272332=CARTESIAN_POINT('Ctrl Pts',(-0.0354337387159423,1.95486483441478,
0.0528933025211718));
#272333=CARTESIAN_POINT('Ctrl Pts',(0.0327634747013058,1.95491138939906,
0.049024429358218));
#272334=CARTESIAN_POINT('Ctrl Pts',(0.100760960714834,1.95140032509883,
0.0451555561952642));
#272335=CARTESIAN_POINT('Ctrl Pts',(0.168813418867247,1.9478864223008,0.0412835552661926));
#272336=CARTESIAN_POINT('Ctrl Pts',(0.236665324606256,1.9408091779182,0.0374115543371211));
#272337=CARTESIAN_POINT('Ctrl Pts',(0.30391575984376,1.93022050836649,0.0335395534080496));
#272338=CARTESIAN_POINT('Ctrl Pts',(0.371191768943996,1.91962781217643,
0.0296660800421098));
#272339=CARTESIAN_POINT('Ctrl Pts',(0.437865359858098,1.90552113363803,
0.0257926066761699));
#272340=CARTESIAN_POINT('Ctrl Pts',(0.503546370093836,1.88800345687324,
0.0219191333102301));
#272341=CARTESIAN_POINT('Ctrl Pts',(0.569342432687873,1.87045509467874,
0.0180388748439399));
#272342=CARTESIAN_POINT('Ctrl Pts',(0.634141962373302,1.84948395228774,
0.0141586163776498));
#272343=CARTESIAN_POINT('Ctrl Pts',(0.697571235538963,1.82524255137465,
0.0102783579113597));
#272344=CARTESIAN_POINT('Ctrl Pts',(0.753362940759582,1.80392007633468,
0.00686532437453106));
#272345=CARTESIAN_POINT('Ctrl Pts',(0.808094597965651,1.78006831145149,
0.00345229083770244));
#272346=CARTESIAN_POINT('Ctrl Pts',(0.861527879758777,1.75382031930251,
3.92573008738128E-5));
#272347=CARTESIAN_POINT('',(-0.861525859670488,1.75382131162756,0.));
#272348=CARTESIAN_POINT('Origin',(0.,0.,0.));
#272349=CARTESIAN_POINT('',(-1.953998900791,0.00207260887720313,0.124130307921729));
#272350=CARTESIAN_POINT('Ctrl Pts',(-0.861525859670491,1.75382131162756,
-2.22044604925031E-15));
#272351=CARTESIAN_POINT('Ctrl Pts',(-0.92465034722954,1.72281280577237,
0.00400987370320275));
#272352=CARTESIAN_POINT('Ctrl Pts',(-0.986146025991561,1.68836919186938,
0.00801974740640772));
#272353=CARTESIAN_POINT('Ctrl Pts',(-1.04563219790624,1.65068752545773,
0.0120296211096127));
#272354=CARTESIAN_POINT('Ctrl Pts',(-1.10690424482723,1.61187459199569,
0.0161598779706933));
#272355=CARTESIAN_POINT('Ctrl Pts',(-1.16604372940432,1.56962626415352,
0.0202901348317739));
#272356=CARTESIAN_POINT('Ctrl Pts',(-1.22266333358954,1.52420811331514,
0.0244203916928544));
#272357=CARTESIAN_POINT('Ctrl Pts',(-1.27759315554719,1.48014544323648,
0.0284273832160793));
#272358=CARTESIAN_POINT('Ctrl Pts',(-1.33015104229541,1.4330998336613,0.0324343747393041));
#272359=CARTESIAN_POINT('Ctrl Pts',(-1.38001546857801,1.38335581340645,
0.0364413662625289));
#272360=CARTESIAN_POINT('Ctrl Pts',(-1.42988102198453,1.33361066874931,
0.0404484483588601));
#272361=CARTESIAN_POINT('Ctrl Pts',(-1.47705266894162,1.2811673162302,0.0444555304551913));
#272362=CARTESIAN_POINT('Ctrl Pts',(-1.52124575697518,1.22634715594117,
0.0484626125515224));
#272363=CARTESIAN_POINT('Ctrl Pts',(-1.56545178522649,1.17151094371184,
0.0524708679651565));
#272364=CARTESIAN_POINT('Ctrl Pts',(-1.60667723309791,1.11429689771893,
0.0564791233787905));
#272365=CARTESIAN_POINT('Ctrl Pts',(-1.64467863203096,1.0550583857497,0.0604873787924245));
#272366=CARTESIAN_POINT('Ctrl Pts',(-1.68270143072715,0.995786514742109,
0.0644978913786586));
#272367=CARTESIAN_POINT('Ctrl Pts',(-1.71749632401162,0.934488297596708,
0.0685084039648928));
#272368=CARTESIAN_POINT('Ctrl Pts',(-1.74886467593283,0.871543656551046,
0.072518916551127));
#272369=CARTESIAN_POINT('Ctrl Pts',(-1.7802817510142,0.808501246204819,
0.0765356585002418));
#272370=CARTESIAN_POINT('Ctrl Pts',(-1.80826145814717,0.74380771951913,
0.0805524004493565));
#272371=CARTESIAN_POINT('Ctrl Pts',(-1.83265261212681,0.677864590655674,
0.0845691423984713));
#272372=CARTESIAN_POINT('Ctrl Pts',(-1.85706588858064,0.611861652192088,
0.0885895274827229));
#272373=CARTESIAN_POINT('Ctrl Pts',(-1.87788399325823,0.544607291841708,
0.0926099125669745));
#272374=CARTESIAN_POINT('Ctrl Pts',(-1.89500585440512,0.476517378245858,
0.0966302976512262));
#272375=CARTESIAN_POINT('Ctrl Pts',(-1.91215919769098,0.408302267038415,
0.100658075058124));
#272376=CARTESIAN_POINT('Ctrl Pts',(-1.92560264274347,0.339248985282941,
0.104685852465021));
#272377=CARTESIAN_POINT('Ctrl Pts',(-1.93528643133502,0.269782187496798,
0.108713629871919));
#272378=CARTESIAN_POINT('Ctrl Pts',(-1.93724361674103,0.255742289625824,
0.109527681839795));
#272379=CARTESIAN_POINT('Ctrl Pts',(-1.93904739689901,0.241685508467463,
0.110341733807671));
#272380=CARTESIAN_POINT('Ctrl Pts',(-1.94069761933797,0.227615356019609,
0.111155785775547));
#272381=CARTESIAN_POINT('Ctrl Pts',(-1.94946481043858,0.152864393717388,
0.115480626475622));
#272382=CARTESIAN_POINT('Ctrl Pts',(-1.95391883477712,0.0775566253238957,
0.119805467175698));
#272383=CARTESIAN_POINT('Ctrl Pts',(-1.95399890079015,0.00207260967928642,
0.124130307875774));
#272384=CARTESIAN_POINT('',(-1.95388395640249,0.000897708686404772,0.824130264813444));
#272385=CARTESIAN_POINT('Ctrl Pts',(-1.953998900791,0.00207260887720443,
0.124130307921729));
#272386=CARTESIAN_POINT('Ctrl Pts',(-1.95406971485036,-0.0646889473779068,
0.12795539715713));
#272387=CARTESIAN_POINT('Ctrl Pts',(-1.95071486305986,-0.131609446464987,
0.13178048639253));
#272388=CARTESIAN_POINT('Ctrl Pts',(-1.94391209993599,-0.198297119803763,
0.135605575627931));
#272389=CARTESIAN_POINT('Ctrl Pts',(-1.93711993049559,-0.264880942973053,
0.139424708197796));
#272390=CARTESIAN_POINT('Ctrl Pts',(-1.92689055170305,-0.331232150947945,
0.143243840767662));
#272391=CARTESIAN_POINT('Ctrl Pts',(-1.91325372797823,-0.396958653234087,
0.147062973337527));
#272392=CARTESIAN_POINT('Ctrl Pts',(-1.89962855986798,-0.462628978011944,
0.150878841632798));
#272393=CARTESIAN_POINT('Ctrl Pts',(-1.88260181766083,-0.527675151600647,
0.154694709928069));
#272394=CARTESIAN_POINT('Ctrl Pts',(-1.86225490420209,-0.591711645799947,
0.15851057822334));
#272395=CARTESIAN_POINT('Ctrl Pts',(-1.84191771893619,-0.655717523101673,
0.162324622089429));
#272396=CARTESIAN_POINT('Ctrl Pts',(-1.81826366361196,-0.71871418653411,
0.166138665955518));
#272397=CARTESIAN_POINT('Ctrl Pts',(-1.79142439797722,-0.780329818943215,
0.169952709821607));
#272398=CARTESIAN_POINT('Ctrl Pts',(-1.76458786151898,-0.841939185907573,
0.173766365852982));
#272399=CARTESIAN_POINT('Ctrl Pts',(-1.73456696517133,-0.902167328318251,
0.177580021884358));
#272400=CARTESIAN_POINT('Ctrl Pts',(-1.70154123168827,-0.960663019411473,
0.181393677915734));
#272401=CARTESIAN_POINT('Ctrl Pts',(-1.66848411293453,-1.01921430058263,
0.185210958170229));
#272402=CARTESIAN_POINT('Ctrl Pts',(-1.63241671219014,-1.07602939448073,
0.189028238424724));
#272403=CARTESIAN_POINT('Ctrl Pts',(-1.59356352779417,-1.13078348187626,
0.192845518679218));
#272404=CARTESIAN_POINT('Ctrl Pts',(-1.5546904210311,-1.1855656449893,0.196664756283148));
#272405=CARTESIAN_POINT('Ctrl Pts',(-1.51302901232075,-1.23828429714149,
0.200483993887078));
#272406=CARTESIAN_POINT('Ctrl Pts',(-1.46884405400318,-1.28864779711894,
0.204303231491008));
#272407=CARTESIAN_POINT('Ctrl Pts',(-1.42458132810623,-1.33909993919613,
0.208129191130555));
#272408=CARTESIAN_POINT('Ctrl Pts',(-1.37778655272207,-1.38718829192004,
0.211955150770102));
#272409=CARTESIAN_POINT('Ctrl Pts',(-1.32876043561764,-1.43265896316507,
0.215781110409649));
#272410=CARTESIAN_POINT('Ctrl Pts',(-1.3008665054816,-1.45852998460954,
0.217957930790131));
#272411=CARTESIAN_POINT('Ctrl Pts',(-1.27225085348762,-1.48355436721595,
0.220134751170613));
#272412=CARTESIAN_POINT('Ctrl Pts',(-1.24297306706696,-1.50769159795568,
0.222311571551095));
#272413=CARTESIAN_POINT('Ctrl Pts',(-1.19019641227937,-1.55120179630116,
0.226235546407139));
#272414=CARTESIAN_POINT('Ctrl Pts',(-1.13502956194456,-1.59202229000584,
0.230159521263182));
#272415=CARTESIAN_POINT('Ctrl Pts',(-1.07777745471449,-1.6298809030445,
0.234083496119226));
#272416=CARTESIAN_POINT('Ctrl Pts',(-1.02061138076857,-1.66768262558654,
0.238001574381064));
#272417=CARTESIAN_POINT('Ctrl Pts',(-0.961366675148951,-1.70253103344955,
0.241919652642901));
#272418=CARTESIAN_POINT('Ctrl Pts',(-0.900381093305233,-1.73419430480511,
0.245837730904739));
#272419=CARTESIAN_POINT('Ctrl Pts',(-0.839467503967435,-1.76582019817423,
0.249751183937729));
#272420=CARTESIAN_POINT('Ctrl Pts',(-0.776817553295469,-1.79426819851077,
0.253664636970718));
#272421=CARTESIAN_POINT('Ctrl Pts',(-0.712796163719197,-1.81935088121758,
0.257578090003708));
#272422=CARTESIAN_POINT('Ctrl Pts',(-0.648815159425008,-1.84441774153717,
0.261489074394488));
#272423=CARTESIAN_POINT('Ctrl Pts',(-0.583464887912403,-1.86612331741961,
0.265400058785267));
#272424=CARTESIAN_POINT('Ctrl Pts',(-0.51713155549024,-1.88432771945759,
0.269311043176047));
#272425=CARTESIAN_POINT('Ctrl Pts',(-0.450817509770402,-1.90252682848721,
0.273220890431257));
#272426=CARTESIAN_POINT('Ctrl Pts',(-0.383521443077999,-1.91722665508607,
0.277130737686467));
#272427=CARTESIAN_POINT('Ctrl Pts',(-0.315644359726697,-1.92833727293042,
0.281040584941677));
#272428=CARTESIAN_POINT('Ctrl Pts',(-0.247763930970189,-1.93944843837518,
0.284950624898498));
#272429=CARTESIAN_POINT('Ctrl Pts',(-0.179302912831436,-1.94696996714431,
0.28886066485532));
#272430=CARTESIAN_POINT('Ctrl Pts',(-0.110670350904324,-1.95086341742079,
0.292770704812142));
#272431=CARTESIAN_POINT('Ctrl Pts',(-0.0419664489043466,-1.95476091474168,
0.296684809057511));
#272432=CARTESIAN_POINT('Ctrl Pts',(0.0269088624428499,-1.95502277925515,
0.30059891330288));
#272433=CARTESIAN_POINT('Ctrl Pts',(0.0955445968728496,-1.95166268345952,
0.30451301754825));
#272434=CARTESIAN_POINT('Ctrl Pts',(0.16422050178672,-1.94830062109829,
0.308429412604124));
#272435=CARTESIAN_POINT('Ctrl Pts',(0.232656062905091,-1.94131242848719,
0.312345807659998));
#272436=CARTESIAN_POINT('Ctrl Pts',(0.300446258658313,-1.93076359134365,
0.316262202715873));
#272437=CARTESIAN_POINT('Ctrl Pts',(0.368351200806611,-1.92019689850547,
0.320185226934111));
#272438=CARTESIAN_POINT('Ctrl Pts',(0.435608117702528,-1.90605763224043,
0.32410825115235));
#272439=CARTESIAN_POINT('Ctrl Pts',(0.501823857525544,-1.88846202398094,
0.328031275370588));
#272440=CARTESIAN_POINT('Ctrl Pts',(0.53240861122868,-1.88033469132088,
0.329843302689274));
#272441=CARTESIAN_POINT('Ctrl Pts',(0.56277147105196,-1.8714706486461,0.331655330007959));
#272442=CARTESIAN_POINT('Ctrl Pts',(0.592875114421119,-1.86188482423058,
0.333467357326644));
#272443=CARTESIAN_POINT('Ctrl Pts',(0.6580782666512,-1.84112235501877,0.337392127882037));
#272444=CARTESIAN_POINT('Ctrl Pts',(0.722313696634057,-1.81689109617585,
0.341316898437429));
#272445=CARTESIAN_POINT('Ctrl Pts',(0.785187368964933,-1.78930064427919,
0.345241668992821));
#272446=CARTESIAN_POINT('Ctrl Pts',(0.847968839732872,-1.76175065260527,
0.349160684039334));
#272447=CARTESIAN_POINT('Ctrl Pts',(0.909392071410045,-1.73085144117634,
0.353079699085847));
#272448=CARTESIAN_POINT('Ctrl Pts',(0.969079276154258,-1.6967620211828,
0.356998714132359));
#272449=CARTESIAN_POINT('Ctrl Pts',(1.02869916732254,-1.66271104629271,
0.360913309422276));
#272450=CARTESIAN_POINT('Ctrl Pts',(1.08658649656621,-1.6254772505299,0.364827904712192));
#272451=CARTESIAN_POINT('Ctrl Pts',(1.14238615553471,-1.58526649861865,
0.368742500002108));
#272452=CARTESIAN_POINT('Ctrl Pts',(1.19815243861168,-1.5450797982826,0.37265475382417));
#272453=CARTESIAN_POINT('Ctrl Pts',(1.25183313215595,-1.50191996032999,
0.376567007646231));
#272454=CARTESIAN_POINT('Ctrl Pts',(1.30310164381818,-1.4560364370023,0.380479261468293));
#272455=CARTESIAN_POINT('Ctrl Pts',(1.35435689983018,-1.41016477701757,
0.384390503763657));
#272456=CARTESIAN_POINT('Ctrl Pts',(1.40320084736407,-1.36157115648459,
0.388301746059021));
#272457=CARTESIAN_POINT('Ctrl Pts',(1.44934095252709,-1.31054446827563,
0.392212988354385));
#272458=CARTESIAN_POINT('Ctrl Pts',(1.49548479582514,-1.25951364603512,
0.396124547527046));
#272459=CARTESIAN_POINT('Ctrl Pts',(1.53892403512438,-1.20604972982545,
0.400036106699708));
#272460=CARTESIAN_POINT('Ctrl Pts',(1.57940512122791,-1.15047618968802,
0.40394766587237));
#272461=CARTESIAN_POINT('Ctrl Pts',(1.61993011734768,-1.09484236868154,
0.407863467930867));
#272462=CARTESIAN_POINT('Ctrl Pts',(1.65749026776217,-1.03709475378983,
0.411779269989364));
#272463=CARTESIAN_POINT('Ctrl Pts',(1.69187482098419,-0.977586615149637,
0.415695072047861));
#272464=CARTESIAN_POINT('Ctrl Pts',(1.72628040799284,-0.918042074073651,
0.419613269488507));
#272465=CARTESIAN_POINT('Ctrl Pts',(1.7575063090594,-0.856735302355073,
0.423531466929153));
#272466=CARTESIAN_POINT('Ctrl Pts',(1.78538859830257,-0.794042538565279,
0.427449664369799));
#272467=CARTESIAN_POINT('Ctrl Pts',(1.81331908096952,-0.731241412836216,
0.431374634258292));
#272468=CARTESIAN_POINT('Ctrl Pts',(1.83789424193406,-0.667049970909388,
0.435299604146784));
#272469=CARTESIAN_POINT('Ctrl Pts',(1.85899926528549,-0.601861887535665,
0.439224574035277));
#272470=CARTESIAN_POINT('Ctrl Pts',(1.86867551159723,-0.571974408104326,
0.441024097057582));
#272471=CARTESIAN_POINT('Ctrl Pts',(1.87762302268613,-0.541877600403308,
0.442823620079887));
#272472=CARTESIAN_POINT('Ctrl Pts',(1.88583433470006,-0.511610068378626,
0.444623143102192));
#272473=CARTESIAN_POINT('Ctrl Pts',(1.90368746628818,-0.445802042673616,
0.448535687316633));
#272474=CARTESIAN_POINT('Ctrl Pts',(1.91812816343621,-0.378924298650098,
0.452448231531075));
#272475=CARTESIAN_POINT('Ctrl Pts',(1.92903299696811,-0.311364250690772,
0.456360775745517));
#272476=CARTESIAN_POINT('Ctrl Pts',(1.93992115319753,-0.243907525661809,
0.460267336312143));
#272477=CARTESIAN_POINT('Ctrl Pts',(1.94728409878175,-0.175771050509559,
0.464173896878769));
#272478=CARTESIAN_POINT('Ctrl Pts',(1.95104862591321,-0.107355760544837,
0.468080457445395));
#272479=CARTESIAN_POINT('Ctrl Pts',(1.95480862761923,-0.0390227141883073,
0.47198232184488));
#272480=CARTESIAN_POINT('Ctrl Pts',(1.95497877423996,0.0295879910690269,
0.475884186244366));
#272481=CARTESIAN_POINT('Ctrl Pts',(1.95153747598598,0.0980687504879788,
0.479786050643852));
#272482=CARTESIAN_POINT('Ctrl Pts',(1.94809838760666,0.166505534092153,
0.483685409410112));
#272483=CARTESIAN_POINT('Ctrl Pts',(1.94105247895137,0.234812045663115,
0.487584768176372));
#272484=CARTESIAN_POINT('Ctrl Pts',(1.93043024173676,0.302580702934179,
0.491484126942632));
#272485=CARTESIAN_POINT('Ctrl Pts',(1.91981115370218,0.370329268797202,
0.495382329664029));
#272486=CARTESIAN_POINT('Ctrl Pts',(1.90561791803515,0.437539809572893,
0.499280532385427));
#272487=CARTESIAN_POINT('Ctrl Pts',(1.88793266539845,0.503811721699204,
0.503178735106825));
#272488=CARTESIAN_POINT('Ctrl Pts',(1.87024654240509,0.570086895311284,
0.507077129673188));
#272489=CARTESIAN_POINT('Ctrl Pts',(1.84906819099268,0.635422872417174,
0.510975524239551));
#272490=CARTESIAN_POINT('Ctrl Pts',(1.82452998782281,0.699432858489848,
0.514873918805914));
#272491=CARTESIAN_POINT('Ctrl Pts',(1.79996570268938,0.763510881578643,
0.518776457024702));
#272492=CARTESIAN_POINT('Ctrl Pts',(1.77203461565791,0.826259639158054,
0.522678995243489));
#272493=CARTESIAN_POINT('Ctrl Pts',(1.7409174097096,0.887311992801872,0.526581533462276));
#272494=CARTESIAN_POINT('Ctrl Pts',(1.70978171060432,0.948400630254737,
0.530486390984793));
#272495=CARTESIAN_POINT('Ctrl Pts',(1.67545637146238,1.00779043017206,0.53439124850731));
#272496=CARTESIAN_POINT('Ctrl Pts',(1.6381668245706,1.06514104928703,0.538296106029828));
#272497=CARTESIAN_POINT('Ctrl Pts',(1.60081238762202,1.12259146808428,0.542207758658415));
#272498=CARTESIAN_POINT('Ctrl Pts',(1.56048373837106,1.17799522513034,0.546119411287002));
#272499=CARTESIAN_POINT('Ctrl Pts',(1.51744764577593,1.23104372072201,0.550031063915589));
#272500=CARTESIAN_POINT('Ctrl Pts',(1.49636826473821,1.25702724721393,0.551947018902973));
#272501=CARTESIAN_POINT('Ctrl Pts',(1.47463991823078,1.28244626566927,0.553862973890357));
#272502=CARTESIAN_POINT('Ctrl Pts',(1.45229707936367,1.30726783532364,0.555778928877742));
#272503=CARTESIAN_POINT('Ctrl Pts',(1.40659466211201,1.35804051197105,0.559698026839719));
#272504=CARTESIAN_POINT('Ctrl Pts',(1.35813616589249,1.40651401080766,0.563617124801696));
#272505=CARTESIAN_POINT('Ctrl Pts',(1.30718194018394,1.45237439224773,0.567536222763673));
#272506=CARTESIAN_POINT('Ctrl Pts',(1.25630440716111,1.4981657478951,0.571449421977428));
#272507=CARTESIAN_POINT('Ctrl Pts',(1.2029389623525,1.54135146580705,0.575362621191183));
#272508=CARTESIAN_POINT('Ctrl Pts',(1.14738442864059,1.58165260816436,0.579275820404938));
#272509=CARTESIAN_POINT('Ctrl Pts',(1.09189524003699,1.62190634696454,0.583184416782355));
#272510=CARTESIAN_POINT('Ctrl Pts',(1.03422247241362,1.65928196144433,0.587093013159773));
#272511=CARTESIAN_POINT('Ctrl Pts',(0.974698429202499,1.69354036624764,
0.59100160953719));
#272512=CARTESIAN_POINT('Ctrl Pts',(0.915211719349837,1.72777728424935,
0.594907754450934));
#272513=CARTESIAN_POINT('Ctrl Pts',(0.853876462352962,1.75890062628619,
0.598813899364678));
#272514=CARTESIAN_POINT('Ctrl Pts',(0.791053073003582,1.78671515236525,
0.602720044278422));
#272515=CARTESIAN_POINT('Ctrl Pts',(0.728247568779264,1.81452175995596,
0.606625077155853));
#272516=CARTESIAN_POINT('Ctrl Pts',(0.663955222543311,1.83902122269039,
0.610530110033284));
#272517=CARTESIAN_POINT('Ctrl Pts',(0.59855848983272,1.8600655188055,0.614435142910714));
#272518=CARTESIAN_POINT('Ctrl Pts',(0.533157976618605,1.88111103146511,
0.618340401533223));
#272519=CARTESIAN_POINT('Ctrl Pts',(0.466653418924475,1.89870083278995,
0.622245660155732));
#272520=CARTESIAN_POINT('Ctrl Pts',(0.399442837896673,1.91273663091735,
0.626150918778241));
#272521=CARTESIAN_POINT('Ctrl Pts',(0.332160863866813,1.92678733827108,
0.630060325678188));
#272522=CARTESIAN_POINT('Ctrl Pts',(0.264171851944922,1.93727640759385,
0.633969732578135));
#272523=CARTESIAN_POINT('Ctrl Pts',(0.195883442020762,1.94415680364062,
0.637879139478082));
#272524=CARTESIAN_POINT('Ctrl Pts',(0.127554293985283,1.95104130425418,
0.641790878572521));
#272525=CARTESIAN_POINT('Ctrl Pts',(0.0589258835932126,1.95431282358562,
0.64570261766696));
#272526=CARTESIAN_POINT('Ctrl Pts',(-0.00959242815166069,1.95397645464887,
0.649614356761399));
#272527=CARTESIAN_POINT('Ctrl Pts',(-0.0782288447553711,1.95363950591374,
0.653532838511659));
#272528=CARTESIAN_POINT('Ctrl Pts',(-0.146754293397251,1.94968228507878,
0.657451320261919));
#272529=CARTESIAN_POINT('Ctrl Pts',(-0.214763690333836,1.94216182572776,
0.66136980201218));
#272530=CARTESIAN_POINT('Ctrl Pts',(-0.246958672714578,1.93860171393135,
0.66322477289255));
#272531=CARTESIAN_POINT('Ctrl Pts',(-0.279038147342052,1.9342438321239,
0.665079743772919));
#272532=CARTESIAN_POINT('Ctrl Pts',(-0.310960116170037,1.92909818468411,
0.666934714653289));
#272533=CARTESIAN_POINT('Ctrl Pts',(-0.378397140896669,1.91822770374662,
0.670853449045919));
#272534=CARTESIAN_POINT('Ctrl Pts',(-0.445396648823328,1.90379532395704,
0.674772183438549));
#272535=CARTESIAN_POINT('Ctrl Pts',(-0.511553747936856,1.88584961303169,
0.678690917831179));
#272536=CARTESIAN_POINT('Ctrl Pts',(-0.57761148609735,1.86793085466266,
0.682603766699971));
#272537=CARTESIAN_POINT('Ctrl Pts',(-0.642828855711058,1.84650936526824,
0.686516615568762));
#272538=CARTESIAN_POINT('Ctrl Pts',(-0.706809520717932,1.82168501707142,
0.690429464437553));
#272539=CARTESIAN_POINT('Ctrl Pts',(-0.770715273941606,1.79688973447105,
0.694337731945927));
#272540=CARTESIAN_POINT('Ctrl Pts',(-0.833386742062816,1.76869968288066,
0.6982459994543));
#272541=CARTESIAN_POINT('Ctrl Pts',(-0.894442926679376,1.73726447350806,
0.702154266962674));
#272542=CARTESIAN_POINT('Ctrl Pts',(-0.955461025584627,1.70584887283385,
0.706060096566535));
#272543=CARTESIAN_POINT('Ctrl Pts',(-1.0148654035447,1.67119235450491,0.709965926170395));
#272544=CARTESIAN_POINT('Ctrl Pts',(-1.07229666946121,1.63349191998687,
0.713871755774256));
#272545=CARTESIAN_POINT('Ctrl Pts',(-1.12971179117575,1.59580208324026,
0.717776487430839));
#272546=CARTESIAN_POINT('Ctrl Pts',(-1.1851544910801,1.55507029866374,0.721681219087423));
#272547=CARTESIAN_POINT('Ctrl Pts',(-1.2382931114427,1.51153768400049,0.725585950744007));
#272548=CARTESIAN_POINT('Ctrl Pts',(-1.29143500306418,1.46800238943228,
0.729490922779209));
#272549=CARTESIAN_POINT('Ctrl Pts',(-1.34227215480009,1.42166623603719,
0.733395894814411));
#272550=CARTESIAN_POINT('Ctrl Pts',(-1.39050626367589,1.37281037681033,
0.737300866849613));
#272551=CARTESIAN_POINT('Ctrl Pts',(-1.43879191173385,1.32390231404769,
0.741210011431374));
#272552=CARTESIAN_POINT('Ctrl Pts',(-1.48446861997378,1.27246952289924,
0.745119156013136));
#272553=CARTESIAN_POINT('Ctrl Pts',(-1.52727594550763,1.21882902257609,
0.749028300594897));
#272554=CARTESIAN_POINT('Ctrl Pts',(-1.57010895751071,1.16515633535399,
0.752939790852796));
#272555=CARTESIAN_POINT('Ctrl Pts',(-1.61006887410968,1.10927370250086,
0.756851281110694));
#272556=CARTESIAN_POINT('Ctrl Pts',(-1.64693812859499,1.0515278410865,0.760762771368593));
#272557=CARTESIAN_POINT('Ctrl Pts',(-1.68387116070946,0.993682089012924,
0.76468102784888));
#272558=CARTESIAN_POINT('Ctrl Pts',(-1.71770261794877,0.93396710317401,
0.768599284329167));
#272559=CARTESIAN_POINT('Ctrl Pts',(-1.74826090204655,0.872754156893794,
0.772517540809453));
#272560=CARTESIAN_POINT('Ctrl Pts',(-1.76274864544053,0.843732977063809,
0.774375194015915));
#272561=CARTESIAN_POINT('Ctrl Pts',(-1.77650137211546,0.814375384895663,
0.776232847222377));
#272562=CARTESIAN_POINT('Ctrl Pts',(-1.78950466680477,0.784722274109725,
0.778090500428838));
#272563=CARTESIAN_POINT('Ctrl Pts',(-1.81966708733528,0.715938968114354,
0.78239950968779));
#272564=CARTESIAN_POINT('Ctrl Pts',(-1.84589697902349,0.645330203163963,
0.786708518946742));
#272565=CARTESIAN_POINT('Ctrl Pts',(-1.86799266684287,0.573340559023402,
0.791017528205694));
#272566=CARTESIAN_POINT('Ctrl Pts',(-1.89002192877661,0.501567336109809,
0.795313583364345));
#272567=CARTESIAN_POINT('Ctrl Pts',(-1.90794163694281,0.428421806118558,
0.799609638522996));
#272568=CARTESIAN_POINT('Ctrl Pts',(-1.92159819855776,0.354367553959984,
0.803905693681647));
#272569=CARTESIAN_POINT('Ctrl Pts',(-1.93518759565743,0.280677508992798,
0.808180620354927));
#272570=CARTESIAN_POINT('Ctrl Pts',(-1.9445555435709,0.206087959977226,
0.812455547028207));
#272571=CARTESIAN_POINT('Ctrl Pts',(-1.94959882342639,0.131074130530993,
0.816730473701487));
#272572=CARTESIAN_POINT('Ctrl Pts',(-1.9525087531185,0.0877917873179581,
0.819197070125765));
#272573=CARTESIAN_POINT('Ctrl Pts',(-1.95397982047966,0.0443685117972613,
0.821663666550042));
#272574=CARTESIAN_POINT('Ctrl Pts',(-1.95399979374754,0.000897794274978164,
0.82413026297432));
#272575=CARTESIAN_POINT('',(-1.95294106986963,-0.00171292579279444,1.52413030787577));
#272576=CARTESIAN_POINT('Ctrl Pts',(-1.9511716724286,0.000895704665025933,
0.824130307875774));
#272577=CARTESIAN_POINT('Ctrl Pts',(-1.94962095971081,-0.381081020904075,
0.845835633985312));
#272578=CARTESIAN_POINT('Ctrl Pts',(-1.6566714212464,-1.41732346558056,
0.904592888686698));
#272579=CARTESIAN_POINT('Ctrl Pts',(0.0263707153274739,-2.30948448311516,
1.00040207197994));
#272580=CARTESIAN_POINT('Ctrl Pts',(1.95483546415058,-1.23008919255452,
1.11155785775549));
#272581=CARTESIAN_POINT('Ctrl Pts',(2.09350030880432,0.975583768053607,
1.22271364353102));
#272582=CARTESIAN_POINT('Ctrl Pts',(0.315389825019358,2.28801419101323,
1.33386942930658));
#272583=CARTESIAN_POINT('Ctrl Pts',(-1.55282847017919,1.58079173016818,
1.43434165075483));
#272584=CARTESIAN_POINT('Ctrl Pts',(-1.94904571141455,0.461263095178057,
1.49776194361122));
#272585=CARTESIAN_POINT('Ctrl Pts',(-1.95294106986963,-0.00171292579279444,
1.52413030787577));
#272586=CARTESIAN_POINT('',(-1.954314499219,0.000110167652081693,2.22413030787577));
#272587=CARTESIAN_POINT('Ctrl Pts',(-1.95294106986963,-0.00171292579279444,
1.52413030787577));
#272588=CARTESIAN_POINT('Ctrl Pts',(-1.95451933662198,-0.189295062189897,
1.53481387220307));
#272589=CARTESIAN_POINT('Ctrl Pts',(-1.84359709592533,-1.02560727269399,
1.58254936512225));
#272590=CARTESIAN_POINT('Ctrl Pts',(-0.650213426172095,-2.21623829060653,
1.66733678663321));
#272591=CARTESIAN_POINT('Ctrl Pts',(1.50962798548894,-1.74800320177882,
1.77849257240879));
#272592=CARTESIAN_POINT('Ctrl Pts',(2.28728253437157,0.320671512699175,
1.88964835818433));
#272593=CARTESIAN_POINT('Ctrl Pts',(0.970743942497957,2.09574505604618,
2.00080414395987));
#272594=CARTESIAN_POINT('Ctrl Pts',(-1.2345895468568,1.95199388459953,2.11195992973542));
#272595=CARTESIAN_POINT('Ctrl Pts',(-1.95450450452585,0.658811978361127,
2.18640198437405));
#272596=CARTESIAN_POINT('Ctrl Pts',(-1.9572031630521,0.00601498584378786,
2.22379211042084));
#272597=CARTESIAN_POINT('Ctrl Pts',(-1.95719833082201,0.000110330218013179,
2.22413030787577));
#272598=CARTESIAN_POINT('',(-1.95399930646857,0.00164630506337263,2.924130286497));
#272599=CARTESIAN_POINT('Ctrl Pts',(-1.95399999689534,0.000110149923111962,
2.22413030787577));
#272600=CARTESIAN_POINT('Ctrl Pts',(-1.9540038404061,-0.0680716498362349,
2.22804190863548));
#272601=CARTESIAN_POINT('Ctrl Pts',(-1.95043473464766,-0.136391042845262,
2.23195350939518));
#272602=CARTESIAN_POINT('Ctrl Pts',(-1.94327546182087,-0.204441873120198,
2.23586511015488));
#272603=CARTESIAN_POINT('Ctrl Pts',(-1.93577088073319,-0.275774952084673,
2.23996537645204));
#272604=CARTESIAN_POINT('Ctrl Pts',(-1.924320940806,-0.346812366580474,
2.24406564274919));
#272605=CARTESIAN_POINT('Ctrl Pts',(-1.9089674010183,-0.41708447807302,
2.24816590904634));
#272606=CARTESIAN_POINT('Ctrl Pts',(-1.89436009320224,-0.483941136384349,
2.25206688906518));
#272607=CARTESIAN_POINT('Ctrl Pts',(-1.87621991406215,-0.550104598981535,
2.25596786908402));
#272608=CARTESIAN_POINT('Ctrl Pts',(-1.85463575962332,-0.615176559311583,
2.25986884910286));
#272609=CARTESIAN_POINT('Ctrl Pts',(-1.83306463621632,-0.680209233655742,
2.26376747397756));
#272610=CARTESIAN_POINT('Ctrl Pts',(-1.80805381687011,-0.744151245189555,
2.26766609885226));
#272611=CARTESIAN_POINT('Ctrl Pts',(-1.7797423449315,-0.806618364319666,
2.27156472372696));
#272612=CARTESIAN_POINT('Ctrl Pts',(-1.75143816735893,-0.869069388983415,
2.27546234413263));
#272613=CARTESIAN_POINT('Ctrl Pts',(-1.71983522921158,-0.930045826120616,
2.27935996453829));
#272614=CARTESIAN_POINT('Ctrl Pts',(-1.68512041365749,-0.989184103933541,
2.28325758494396));
#272615=CARTESIAN_POINT('Ctrl Pts',(-1.65040252829768,-1.04832761130108,
2.28715555001334));
#272616=CARTESIAN_POINT('Ctrl Pts',(-1.61257247167267,-1.10563221234015,
2.29105351508273));
#272617=CARTESIAN_POINT('Ctrl Pts',(-1.57186177757689,-1.16076119516153,
2.29495148015211));
#272618=CARTESIAN_POINT('Ctrl Pts',(-1.53110703945126,-1.21594982085118,
2.29885366234659));
#272619=CARTESIAN_POINT('Ctrl Pts',(-1.48746573983048,-1.26895773441807,
2.30275584454108));
#272620=CARTESIAN_POINT('Ctrl Pts',(-1.44121059456054,-1.31948020906963,
2.30665802673556));
#272621=CARTESIAN_POINT('Ctrl Pts',(-1.3949262893077,-1.37003453389676,
2.31056266892807));
#272622=CARTESIAN_POINT('Ctrl Pts',(-1.34602521209539,-1.41809995660916,
2.31446731112058));
#272623=CARTESIAN_POINT('Ctrl Pts',(-1.29481591562462,-1.46340962981839,
2.31837195331309));
#272624=CARTESIAN_POINT('Ctrl Pts',(-1.2435199544286,-1.50879598344797,
2.32228320357808));
#272625=CARTESIAN_POINT('Ctrl Pts',(-1.18990836652197,-1.55141697652738,
2.32619445384307));
#272626=CARTESIAN_POINT('Ctrl Pts',(-1.13432082705043,-1.59104753584537,
2.33010570410807));
#272627=CARTESIAN_POINT('Ctrl Pts',(-1.11458575519372,-1.60511745049347,
2.33149430316755));
#272628=CARTESIAN_POINT('Ctrl Pts',(-1.09460186721579,-1.61881085322814,
2.33288290222703));
#272629=CARTESIAN_POINT('Ctrl Pts',(-1.07438510093941,-1.63211906884253,
2.33427150128652));
#272630=CARTESIAN_POINT('Ctrl Pts',(-1.01734369373402,-1.66966806830466,
2.33818941987519));
#272631=CARTESIAN_POINT('Ctrl Pts',(-0.958218234290233,-1.70429765930014,
2.34210733846386));
#272632=CARTESIAN_POINT('Ctrl Pts',(-0.897339749246061,-1.73576996587192,
2.34602525705253));
#272633=CARTESIAN_POINT('Ctrl Pts',(-0.836553011177559,-1.76719484207577,
2.34993727113846));
#272634=CARTESIAN_POINT('Ctrl Pts',(-0.774018924193188,-1.79547165303807,
2.3538492852244));
#272635=CARTESIAN_POINT('Ctrl Pts',(-0.710096901862582,-1.82040610578111,
2.35776129931034));
#272636=CARTESIAN_POINT('Ctrl Pts',(-0.64625013137306,-1.84531120457998,
2.3616687079997));
#272637=CARTESIAN_POINT('Ctrl Pts',(-0.581019126684705,-1.8668815817236,
2.36557611668907));
#272638=CARTESIAN_POINT('Ctrl Pts',(-0.51478562865045,-1.88496996170628,
2.36948352537844));
#272639=CARTESIAN_POINT('Ctrl Pts',(-0.448593699509874,-1.90304698921677,
2.37338848173385));
#272640=CARTESIAN_POINT('Ctrl Pts',(-0.381400998594416,-1.91764622525208,
2.37729343808926));
#272641=CARTESIAN_POINT('Ctrl Pts',(-0.313605385924358,-1.92866992041646,
2.38119839444467));
#272642=CARTESIAN_POINT('Ctrl Pts',(-0.245829062863987,-1.93969047905373,
2.38510223973874));
#272643=CARTESIAN_POINT('Ctrl Pts',(-0.177450653924596,-1.94713743746912,
2.38900608503281));
#272644=CARTESIAN_POINT('Ctrl Pts',(-0.108877407863952,-1.95096430260957,
2.39290993032689));
#272645=CARTESIAN_POINT('Ctrl Pts',(-0.0403001469218326,-1.95479139180838,
2.39681400418643));
#272646=CARTESIAN_POINT('Ctrl Pts',(0.0284714824719405,-1.95499794207696,
2.40071807804598));
#272647=CARTESIAN_POINT('Ctrl Pts',(0.0970277471845426,-1.95158951018812,
2.40462215190552));
#272648=CARTESIAN_POINT('Ctrl Pts',(0.165657075602355,-1.94817744576965,
2.40853038652415));
#272649=CARTESIAN_POINT('Ctrl Pts',(0.234070088995972,-1.94114273490312,
2.41243862114279));
#272650=CARTESIAN_POINT('Ctrl Pts',(0.301860711858535,-1.9305429574698,
2.41634685576142));
#272651=CARTESIAN_POINT('Ctrl Pts',(0.369691881963554,-1.91993684004834,
2.42025742799151));
#272652=CARTESIAN_POINT('Ctrl Pts',(0.436899439237921,-1.90576151382809,
2.4241680002216));
#272653=CARTESIAN_POINT('Ctrl Pts',(0.503088834207008,-1.88812542615586,
2.42807857245169));
#272654=CARTESIAN_POINT('Ctrl Pts',(0.569392704334207,-1.87045883671025,
2.43199590805187));
#272655=CARTESIAN_POINT('Ctrl Pts',(0.634674429834119,-1.84931969125412,
2.43591324365206));
#272656=CARTESIAN_POINT('Ctrl Pts',(0.698556743561265,-1.82486560492138,
2.43983057925224));
#272657=CARTESIAN_POINT('Ctrl Pts',(0.728979687507331,-1.81321973215399,
2.44169614852218));
#272658=CARTESIAN_POINT('Ctrl Pts',(0.759085571541915,-1.80082272628931,
2.44356171779213));
#272659=CARTESIAN_POINT('Ctrl Pts',(0.788835631960881,-1.78769526087331,
2.44542728706207));
#272660=CARTESIAN_POINT('Ctrl Pts',(0.851314316603462,-1.76012601360684,
2.44934520562944));
#272661=CARTESIAN_POINT('Ctrl Pts',(0.912469980201015,-1.72922272457703,
2.4532631241968));
#272662=CARTESIAN_POINT('Ctrl Pts',(0.97192326330304,-1.69513455815471,
2.45718104276417));
#272663=CARTESIAN_POINT('Ctrl Pts',(1.03128694726609,-1.66109776434298,
2.46109305682783));
#272664=CARTESIAN_POINT('Ctrl Pts',(1.0889529191399,-1.623885861664,2.46500507089149));
#272665=CARTESIAN_POINT('Ctrl Pts',(1.14456304812394,-1.5836954975213,2.46891708495516));
#272666=CARTESIAN_POINT('Ctrl Pts',(1.20010771037732,-1.54355244727253,
2.47282449362092));
#272667=CARTESIAN_POINT('Ctrl Pts',(1.25360093951805,-1.50043818604334,
2.47673190228669));
#272668=CARTESIAN_POINT('Ctrl Pts',(1.30471200480384,-1.45459361490444,
2.48063931095245));
#272669=CARTESIAN_POINT('Ctrl Pts',(1.35579099219528,-1.40877781634738,
2.48454426728345));
#272670=CARTESIAN_POINT('Ctrl Pts',(1.40449041608053,-1.36023543478269,
2.48844922361445));
#272671=CARTESIAN_POINT('Ctrl Pts',(1.45051241974066,-1.30924776882686,
2.49235417994545));
#272672=CARTESIAN_POINT('Ctrl Pts',(1.49652132893811,-1.25827461019438,
2.49625802521433));
#272673=CARTESIAN_POINT('Ctrl Pts',(1.5398540007316,-1.20485791334639,2.50016187048321));
#272674=CARTESIAN_POINT('Ctrl Pts',(1.58025055554452,-1.14931465739424,
2.50406571575209));
#272675=CARTESIAN_POINT('Ctrl Pts',(1.62064947551981,-1.09376814946134,
2.50796978958571));
#272676=CARTESIAN_POINT('Ctrl Pts',(1.65811164993965,-1.03609523458316,
2.51187386341933));
#272677=CARTESIAN_POINT('Ctrl Pts',(1.69241958669902,-0.976643201254944,
2.51577793725294));
#272678=CARTESIAN_POINT('Ctrl Pts',(1.7267640870668,-0.91712780705251,2.51968617184469));
#272679=CARTESIAN_POINT('Ctrl Pts',(1.75794739462104,-0.855829937270136,
2.52359440643644));
#272680=CARTESIAN_POINT('Ctrl Pts',(1.7857977125298,-0.793122014524463,
2.52750264102819));
#272681=CARTESIAN_POINT('Ctrl Pts',(1.81366468839611,-0.730376584633669,
2.53141321323081));
#272682=CARTESIAN_POINT('Ctrl Pts',(1.83819453139249,-0.666219882852152,
2.53532378543343));
#272683=CARTESIAN_POINT('Ctrl Pts',(1.85926443526242,-0.601042227941037,
2.53923435763605));
#272684=CARTESIAN_POINT('Ctrl Pts',(1.88037077971888,-0.535751847694842,
2.54315169320815));
#272685=CARTESIAN_POINT('Ctrl Pts',(1.89800511549755,-0.469437465318987,
2.54706902878025));
#272686=CARTESIAN_POINT('Ctrl Pts',(1.91209531989201,-0.40250153744684,
2.55098636435235));
#272687=CARTESIAN_POINT('Ctrl Pts',(1.91880555827064,-0.370624353870048,
2.55285193384744));
#272688=CARTESIAN_POINT('Ctrl Pts',(1.92471274895798,-0.338606306352277,
2.55471750334253));
#272689=CARTESIAN_POINT('Ctrl Pts',(1.92981324471967,-0.306491175247436,
2.55658307283762));
#272690=CARTESIAN_POINT('Ctrl Pts',(1.94052489466023,-0.239045566376628,
2.56050099146844));
#272691=CARTESIAN_POINT('Ctrl Pts',(1.94771778341508,-0.170903868566048,
2.56441891009927));
#272692=CARTESIAN_POINT('Ctrl Pts',(1.95131155312682,-0.102465714430763,
2.56833682873009));
#272693=CARTESIAN_POINT('Ctrl Pts',(1.95489990684488,-0.0341307000734099,
2.57224884285834));
#272694=CARTESIAN_POINT('Ctrl Pts',(1.95489988071068,0.0344993966206616,
2.57616085698659));
#272695=CARTESIAN_POINT('Ctrl Pts',(1.95128252454568,0.103017034526457,
2.58007287111484));
#272696=CARTESIAN_POINT('Ctrl Pts',(1.9476694268928,0.171454010429994,2.58398027984654));
#272697=CARTESIAN_POINT('Ctrl Pts',(1.94044748240011,0.239778301551508,
2.58788768857825));
#272698=CARTESIAN_POINT('Ctrl Pts',(1.92963978130998,0.307581394733121,
2.59179509730996));
#272699=CARTESIAN_POINT('Ctrl Pts',(1.91883886325545,0.375341933925608,
2.5957000537077));
#272700=CARTESIAN_POINT('Ctrl Pts',(1.90445673004048,0.442581439342766,
2.59960501010544));
#272701=CARTESIAN_POINT('Ctrl Pts',(1.88656824028271,0.50889711608203,2.60350996650318));
#272702=CARTESIAN_POINT('Ctrl Pts',(1.86868484026439,0.575193924290699,
2.6074138118395));
#272703=CARTESIAN_POINT('Ctrl Pts',(1.8472971922513,0.640566950886118,2.61131765717583));
#272704=CARTESIAN_POINT('Ctrl Pts',(1.82253072672411,0.70462596471211,2.61522150251216));
#272705=CARTESIAN_POINT('Ctrl Pts',(1.79776281115086,0.768688729114502,
2.61912557641383));
#272706=CARTESIAN_POINT('Ctrl Pts',(1.76961586509378,0.831436870089212,
2.6230296503155));
#272707=CARTESIAN_POINT('Ctrl Pts',(1.73826376917769,0.892499338242987,
2.62693372421716));
#272708=CARTESIAN_POINT('Ctrl Pts',(1.70687825983113,0.953626883594127,
2.6308419588774));
#272709=CARTESIAN_POINT('Ctrl Pts',(1.67228100866933,1.01306473236957,2.63475019353765));
#272710=CARTESIAN_POINT('Ctrl Pts',(1.63469179150203,1.07046660237295,2.63865842819789));
#272711=CARTESIAN_POINT('Ctrl Pts',(1.59708009129986,1.12790280584593,2.64256900046935));
#272712=CARTESIAN_POINT('Ctrl Pts',(1.55647315440075,1.18330021014323,2.64647957274082));
#272713=CARTESIAN_POINT('Ctrl Pts',(1.51313235688074,1.23634399362011,2.65039014501229));
#272714=CARTESIAN_POINT('Ctrl Pts',(1.4697166010684,1.2894795167893,2.65430748065307));
#272715=CARTESIAN_POINT('Ctrl Pts',(1.42355787850931,1.34025293097346,2.65822481629384));
#272716=CARTESIAN_POINT('Ctrl Pts',(1.37495524514224,1.38838541977934,2.66214215193461));
#272717=CARTESIAN_POINT('Ctrl Pts',(1.3518090127958,1.41130775324426,2.66400772082746));
#272718=CARTESIAN_POINT('Ctrl Pts',(1.32810900083288,1.4336317093052,2.66587328972032));
#272719=CARTESIAN_POINT('Ctrl Pts',(1.3038900178082,1.4553304853057,2.66773885861317));
#272720=CARTESIAN_POINT('Ctrl Pts',(1.25302724643474,1.50090051942615,2.67165677721371));
#272721=CARTESIAN_POINT('Ctrl Pts',(1.19967168565047,1.54389136363152,2.67557469581425));
#272722=CARTESIAN_POINT('Ctrl Pts',(1.1441155533377,1.58401881321239,2.67949261441479));
#272723=CARTESIAN_POINT('Ctrl Pts',(1.08864314694684,1.62408578868229,2.68340462851239));
#272724=CARTESIAN_POINT('Ctrl Pts',(1.03097714640215,1.66129764807336,2.68731664260999));
#272725=CARTESIAN_POINT('Ctrl Pts',(0.97144428838517,1.69540909357117,2.69122865670758));
#272726=CARTESIAN_POINT('Ctrl Pts',(0.911981515095867,1.72948038155852,
2.69513606540823));
#272727=CARTESIAN_POINT('Ctrl Pts',(0.850656673890062,1.76045826106261,
2.69904347410888));
#272728=CARTESIAN_POINT('Ctrl Pts',(0.787825534997934,1.78814063384433,
2.70295088280953));
#272729=CARTESIAN_POINT('Ctrl Pts',(0.725033829644162,1.81580563285362,
2.70685583917597));
#272730=CARTESIAN_POINT('Ctrl Pts',(0.660738151075758,1.84017903006499,
2.71076079554242));
#272731=CARTESIAN_POINT('Ctrl Pts',(0.595317534095197,1.86110532576714,
2.71466575190886));
#272732=CARTESIAN_POINT('Ctrl Pts',(0.529915530980779,1.88202566739419,
2.71856959721371));
#272733=CARTESIAN_POINT('Ctrl Pts',(0.463389693183081,1.89950070472482,
2.72247344251856));
#272734=CARTESIAN_POINT('Ctrl Pts',(0.396135919437877,1.91342424290357,
2.72637728782341));
#272735=CARTESIAN_POINT('Ctrl Pts',(0.328878208069503,1.92734859628783,
2.73028136169345));
#272736=CARTESIAN_POINT('Ctrl Pts',(0.260892958381072,1.93772094046943,
2.73418543556349));
#272737=CARTESIAN_POINT('Ctrl Pts',(0.192586221880882,1.94448619103907,
2.73808950943354));
#272738=CARTESIAN_POINT('Ctrl Pts',(0.124206687618644,1.95125865166041,
2.74199774406217));
#272739=CARTESIAN_POINT('Ctrl Pts',(0.0555054732576298,1.95441629810444,
2.7459059786908));
#272740=CARTESIAN_POINT('Ctrl Pts',(-0.0131072953684214,1.95395603809506,
2.74981421331943));
#272741=CARTESIAN_POINT('Ctrl Pts',(-0.0817611029776405,1.95349550279285,
2.75372478555924));
#272742=CARTESIAN_POINT('Ctrl Pts',(-0.150325868425877,1.94941278361112,
2.75763535779905));
#272743=CARTESIAN_POINT('Ctrl Pts',(-0.218395344346425,1.94175680082955,
2.76154593003887));
#272744=CARTESIAN_POINT('Ctrl Pts',(-0.286582547032858,1.93408757695746,
2.76546326564826));
#272745=CARTESIAN_POINT('Ctrl Pts',(-0.354272265493934,1.9228328357604,
2.76938060125765));
#272746=CARTESIAN_POINT('Ctrl Pts',(-0.421068075163712,1.90809268015941,
2.77329793686704));
#272747=CARTESIAN_POINT('Ctrl Pts',(-0.452878523869282,1.90107291400978,
2.77516350604093));
#272748=CARTESIAN_POINT('Ctrl Pts',(-0.484486454340456,1.89326339210832,
2.77702907521482));
#272749=CARTESIAN_POINT('Ctrl Pts',(-0.515850472278009,1.88467882946951,
2.77889464438871));
#272750=CARTESIAN_POINT('Ctrl Pts',(-0.581718664664873,1.86665022023404,
2.78281256298898));
#272751=CARTESIAN_POINT('Ctrl Pts',(-0.646771323487212,1.84512860016864,
2.78673048158925));
#272752=CARTESIAN_POINT('Ctrl Pts',(-0.710611204335022,1.82020540496767,
2.79064840018953));
#272753=CARTESIAN_POINT('Ctrl Pts',(-0.774354875228049,1.79531977029237,
2.79456041428675));
#272754=CARTESIAN_POINT('Ctrl Pts',(-0.836888940942152,1.76704291187986,
2.79847242838397));
#272755=CARTESIAN_POINT('Ctrl Pts',(-0.897830131913202,1.73551636530133,
2.80238444248119));
#272756=CARTESIAN_POINT('Ctrl Pts',(-0.958699580202227,1.70402693317642,
2.80629185118132));
#272757=CARTESIAN_POINT('Ctrl Pts',(-1.01797944305589,1.6692956356774,2.81019925988145));
#272758=CARTESIAN_POINT('Ctrl Pts',(-1.07530700680656,1.63151182683814,
2.81410666858158));
#272759=CARTESIAN_POINT('Ctrl Pts',(-1.13259859112415,1.59375173154839,
2.81801162494743));
#272760=CARTESIAN_POINT('Ctrl Pts',(-1.18793989707555,1.55294319532719,
2.82191658131328));
#272761=CARTESIAN_POINT('Ctrl Pts',(-1.24099475083012,1.50932038627062,
2.82582153767913));
#272762=CARTESIAN_POINT('Ctrl Pts',(-1.29403450909828,1.46570998903831,
2.82972538298329));
#272763=CARTESIAN_POINT('Ctrl Pts',(-1.34478872681381,1.4192872208373,2.83362922828745));
#272764=CARTESIAN_POINT('Ctrl Pts',(-1.39295351444384,1.37032715312752,
2.8375330735916));
#272765=CARTESIAN_POINT('Ctrl Pts',(-1.44112112206026,1.3213642188687,2.84143714746088));
#272766=CARTESIAN_POINT('Ctrl Pts',(-1.48669865542713,1.26986404265072,
2.84534122133016));
#272767=CARTESIAN_POINT('Ctrl Pts',(-1.52941966529898,1.21613793929668,
2.84924529519944));
#272768=CARTESIAN_POINT('Ctrl Pts',(-1.57218620499653,1.16235457746187,
2.85315352982717));
#272769=CARTESIAN_POINT('Ctrl Pts',(-1.61208983884711,1.10634093992012,
2.8570617644549));
#272770=CARTESIAN_POINT('Ctrl Pts',(-1.64890559451535,1.04843995554156,
2.86096999908264));
#272771=CARTESIAN_POINT('Ctrl Pts',(-1.68574337059115,0.990504339162355,
2.86488057132147));
#272772=CARTESIAN_POINT('Ctrl Pts',(-1.71948935101782,0.930679557828923,
2.86879114356031));
#272773=CARTESIAN_POINT('Ctrl Pts',(-1.74996436960873,0.869333483250198,
2.87270171579914));
#272774=CARTESIAN_POINT('Ctrl Pts',(-1.78049209501533,0.807881310089891,
2.87661905140745));
#272775=CARTESIAN_POINT('Ctrl Pts',(-1.80773737248884,0.744903043680049,
2.88053638701575));
#272776=CARTESIAN_POINT('Ctrl Pts',(-1.8315693677346,0.680786053893797,
2.88445372262406));
#272777=CARTESIAN_POINT('Ctrl Pts',(-1.84291897886717,0.65025135071175,
2.88631929180412));
#272778=CARTESIAN_POINT('Ctrl Pts',(-1.85349519563914,0.619458599171217,
2.88818486098419));
#272779=CARTESIAN_POINT('Ctrl Pts',(-1.86328793786741,0.588450559178767,
2.89005043016426));
#272780=CARTESIAN_POINT('Ctrl Pts',(-1.88814446964756,0.509744072931565,
2.89478573091368));
#272781=CARTESIAN_POINT('Ctrl Pts',(-1.90803027275293,0.429397174052618,
2.8995210316631));
#272782=CARTESIAN_POINT('Ctrl Pts',(-1.92276472469617,0.347982490168748,
2.90425633241252));
#272783=CARTESIAN_POINT('Ctrl Pts',(-1.93730951742571,0.267615761443961,
2.90893068122289));
#272784=CARTESIAN_POINT('Ctrl Pts',(-1.94683466612875,0.186208584307251,
2.91360503003325));
#272785=CARTESIAN_POINT('Ctrl Pts',(-1.95121262866794,0.104332534363677,
2.91827937884362));
#272786=CARTESIAN_POINT('Ctrl Pts',(-1.95303926845357,0.0701709697138529,
2.92022968139475));
#272787=CARTESIAN_POINT('Ctrl Pts',(-1.95397042305096,0.0359280303751402,
2.92217998394587));
#272788=CARTESIAN_POINT('Ctrl Pts',(-1.95399930646857,0.00164630506337263,
2.924130286497));
#272789=CARTESIAN_POINT('',(-1.95135389229221,-0.00104612722430151,3.62413030787577));
#272790=CARTESIAN_POINT('Ctrl Pts',(-1.95261817115182,0.00164476589090098,
2.92413030787577));
#272791=CARTESIAN_POINT('Ctrl Pts',(-1.94901781276173,-0.449643694625046,
2.94982227723045));
#272792=CARTESIAN_POINT('Ctrl Pts',(-1.56887368220728,-1.55723649878973,
3.01256617517698));
#272793=CARTESIAN_POINT('Ctrl Pts',(0.273666914822965,-2.29338130550848,
3.11236200171536));
#272794=CARTESIAN_POINT('Ctrl Pts',(2.07538330807382,-1.01354601124164,
3.22351778749091));
#272795=CARTESIAN_POINT('Ctrl Pts',(1.97691764050528,1.19427301524132,3.33467357326646));
#272796=CARTESIAN_POINT('Ctrl Pts',(0.0684232320151593,2.3086380516957,
3.44582935904201));
#272797=CARTESIAN_POINT('Ctrl Pts',(-1.6425693175686,1.44115442383729,3.54231493724512));
#272798=CARTESIAN_POINT('Ctrl Pts',(-1.94944131033335,0.392737674719044,
3.60174858685637));
#272799=CARTESIAN_POINT('Ctrl Pts',(-1.95135389229221,-0.00104612722430151,
3.62413030787577));
#272800=CARTESIAN_POINT('',(-1.95399969426645,-0.00109307210263392,4.32413030787578));
#272801=CARTESIAN_POINT('Ctrl Pts',(-1.95135389229221,-0.00104612722430151,
3.62413030787577));
#272802=CARTESIAN_POINT('Ctrl Pts',(-1.95260750341136,-0.259153629688766,
3.63880051544822));
#272803=CARTESIAN_POINT('Ctrl Pts',(-1.7848815556947,-1.16758857717685,
3.6905226516125));
#272804=CARTESIAN_POINT('Ctrl Pts',(-0.409009355221126,-2.27314820012038,
3.77929671636865));
#272805=CARTESIAN_POINT('Ctrl Pts',(1.6882291036661,-1.57618967319729,3.8904525021442));
#272806=CARTESIAN_POINT('Ctrl Pts',(2.2397566354332,0.563898578107994,4.00160828791975));
#272807=CARTESIAN_POINT('Ctrl Pts',(0.740604968531764,2.18769185968862,
4.1127640736953));
#272808=CARTESIAN_POINT('Ctrl Pts',(-1.36516131740615,1.82092354038783,
4.22027108665239));
#272809=CARTESIAN_POINT('Ctrl Pts',(-1.95250978895003,0.582719763414392,
4.29072617101763));
#272810=CARTESIAN_POINT('Ctrl Pts',(-1.95643501159432,-0.00107728777549013,
4.32412932679103));
#272811=CARTESIAN_POINT('',(-1.95399923813581,0.00172550418305494,5.02413030787578));
#272812=CARTESIAN_POINT('Ctrl Pts',(-1.95399969426645,-0.00109307210263392,
4.32413030787578));
#272813=CARTESIAN_POINT('Ctrl Pts',(-1.95396406853087,-0.0647784193523055,
4.32777875366598));
#272814=CARTESIAN_POINT('Ctrl Pts',(-1.95081522176893,-0.128375053248821,
4.33142719945619));
#272815=CARTESIAN_POINT('Ctrl Pts',(-1.9445774776562,-0.191662289958832,
4.3350756452464));
#272816=CARTESIAN_POINT('Ctrl Pts',(-1.93787901614206,-0.259623897837666,
4.33899356385134));
#272817=CARTESIAN_POINT('Ctrl Pts',(-1.92760015463464,-0.327368813282832,
4.34291148245628));
#272818=CARTESIAN_POINT('Ctrl Pts',(-1.91376424398393,-0.394490073954503,
4.34682940106122));
#272819=CARTESIAN_POINT('Ctrl Pts',(-1.89994918475547,-0.461510179466701,
4.35074141516321));
#272820=CARTESIAN_POINT('Ctrl Pts',(-1.8825878138515,-0.527908017599158,
4.3546534292652));
#272821=CARTESIAN_POINT('Ctrl Pts',(-1.86175521833767,-0.593281979325559,
4.35856544336719));
#272822=CARTESIAN_POINT('Ctrl Pts',(-1.84094714788169,-0.658578979917066,
4.36247285207222));
#272823=CARTESIAN_POINT('Ctrl Pts',(-1.81667611725424,-0.722854031451185,
4.36638026077724));
#272824=CARTESIAN_POINT('Ctrl Pts',(-1.78906780717862,-0.785717749142202,
4.37028766948227));
#272825=CARTESIAN_POINT('Ctrl Pts',(-1.76147682439289,-0.848542012847915,
4.37419262585308));
#272826=CARTESIAN_POINT('Ctrl Pts',(-1.73055291435365,-0.909956250382317,
4.37809758222389));
#272827=CARTESIAN_POINT('Ctrl Pts',(-1.69647039580353,-0.969589705061996,
4.3820025385947));
#272828=CARTESIAN_POINT('Ctrl Pts',(-1.66239757461609,-1.02920619247335,
4.38590638390389));
#272829=CARTESIAN_POINT('Ctrl Pts',(-1.62516817297791,-1.08704247596307,
4.38981022921309));
#272830=CARTESIAN_POINT('Ctrl Pts',(-1.58500225835342,-1.14275274710436,
4.39371407452228));
#272831=CARTESIAN_POINT('Ctrl Pts',(-1.54483399206581,-1.19846628001104,
4.39761814839664));
#272832=CARTESIAN_POINT('Ctrl Pts',(-1.50172916122758,-1.25205315589847,
4.401522222271));
#272833=CARTESIAN_POINT('Ctrl Pts',(-1.45594985515803,-1.30319838062565,
4.40542629614536));
#272834=CARTESIAN_POINT('Ctrl Pts',(-1.41012175988938,-1.35439811326845,
4.40933453077824));
#272835=CARTESIAN_POINT('Ctrl Pts',(-1.36161382973086,-1.40315063430612,
4.41324276541112));
#272836=CARTESIAN_POINT('Ctrl Pts',(-1.31072629105317,-1.44917652131892,
4.41715100004399));
#272837=CARTESIAN_POINT('Ctrl Pts',(-1.25980831528837,-1.49522993754553,
4.42106157228802));
#272838=CARTESIAN_POINT('Ctrl Pts',(-1.20650828017215,-1.53855316369342,
4.42497214453205));
#272839=CARTESIAN_POINT('Ctrl Pts',(-1.15115870068675,-1.57890773822703,
4.42888271677608));
#272840=CARTESIAN_POINT('Ctrl Pts',(-1.09571339361134,-1.61933210635621,
4.43280005238958));
#272841=CARTESIAN_POINT('Ctrl Pts',(-1.0382118794749,-1.65677730721562,
4.43671738800309));
#272842=CARTESIAN_POINT('Ctrl Pts',(-0.97901401930995,-1.69104924528962,
4.4406347236166));
#272843=CARTESIAN_POINT('Ctrl Pts',(-0.950821974592702,-1.70737071380278,
4.44250029275171));
#272844=CARTESIAN_POINT('Ctrl Pts',(-0.922245533750066,-1.72297317790248,
4.44436586188682));
#272845=CARTESIAN_POINT('Ctrl Pts',(-0.893325153439702,-1.73783951221968,
4.44623143102194));
#272846=CARTESIAN_POINT('Ctrl Pts',(-0.832588891273433,-1.76906059468301,
4.45014934962686));
#272847=CARTESIAN_POINT('Ctrl Pts',(-0.770093377070202,-1.7971557769571,
4.45406726823179));
#272848=CARTESIAN_POINT('Ctrl Pts',(-0.706193219306302,-1.8219240206457,
4.45798518683672));
#272849=CARTESIAN_POINT('Ctrl Pts',(-0.6423893623357,-1.84665493732919,
4.4618972009387));
#272850=CARTESIAN_POINT('Ctrl Pts',(-0.577185518011613,-1.86806868977168,
4.46580921504068));
#272851=CARTESIAN_POINT('Ctrl Pts',(-0.510959848584841,-1.88601061320825,
4.46972122914266));
#272852=CARTESIAN_POINT('Ctrl Pts',(-0.444812142961179,-1.90393141461467,
4.47362863784767));
#272853=CARTESIAN_POINT('Ctrl Pts',(-0.377645473848739,-1.91838837618161,
4.47753604655269));
#272854=CARTESIAN_POINT('Ctrl Pts',(-0.309855164515936,-1.92927597222969,
4.4814434552577));
#272855=CARTESIAN_POINT('Ctrl Pts',(-0.242107401153447,-1.94015673509847,
4.4853484116285));
#272856=CARTESIAN_POINT('Ctrl Pts',(-0.173737258608705,-1.94747249838319,
4.4892533679993));
#272857=CARTESIAN_POINT('Ctrl Pts',(-0.105150779999663,-1.9511687045116,
4.49315832437011));
#272858=CARTESIAN_POINT('Ctrl Pts',(-0.0365838160270698,-1.95486385897326,
4.49706216967929));
#272859=CARTESIAN_POINT('Ctrl Pts',(0.032198870821327,-1.95494147424573,
4.50096601498848));
#272860=CARTESIAN_POINT('Ctrl Pts',(0.100787394650277,-1.95139895999757,
4.50486986029766));
#272861=CARTESIAN_POINT('Ctrl Pts',(0.169379934249911,-1.94785623833972,
4.50877393417202));
#272862=CARTESIAN_POINT('Ctrl Pts',(0.237777797108343,-1.94069299428809,
4.51267800804637));
#272863=CARTESIAN_POINT('Ctrl Pts',(0.305574204187586,-1.92995865389265,
4.51658208192072));
#272864=CARTESIAN_POINT('Ctrl Pts',(0.373442865145013,-1.91921287339652,
4.52049031655359));
#272865=CARTESIAN_POINT('Ctrl Pts',(0.440708304253144,-1.90488847821343,
4.52439855118647));
#272866=CARTESIAN_POINT('Ctrl Pts',(0.50697295311195,-1.8870862261203,4.52830678581934));
#272867=CARTESIAN_POINT('Ctrl Pts',(0.573277236485244,-1.86927332606282,
4.53221735806336));
#272868=CARTESIAN_POINT('Ctrl Pts',(0.638579070522587,-1.8479785816739,
4.53612793030738));
#272869=CARTESIAN_POINT('Ctrl Pts',(0.702497796749431,-1.82335209039894,
4.5400385025514));
#272870=CARTESIAN_POINT('Ctrl Pts',(0.766527070981792,-1.79868300738829,
4.5439558381649));
#272871=CARTESIAN_POINT('Ctrl Pts',(0.829168014267321,-1.77067087752169,
4.5478731737784));
#272872=CARTESIAN_POINT('Ctrl Pts',(0.890062419102886,-1.73951283125498,
4.5517905093919));
#272873=CARTESIAN_POINT('Ctrl Pts',(0.919062416390822,-1.72467430446961,
4.5536560785271));
#272874=CARTESIAN_POINT('Ctrl Pts',(0.947666698135512,-1.70912294044003,
4.5555216476623));
#272875=CARTESIAN_POINT('Ctrl Pts',(0.97583893887946,-1.69288344707089,
4.55738721679749));
#272876=CARTESIAN_POINT('Ctrl Pts',(1.03500401835615,-1.65877856615003,
4.56130513540242));
#272877=CARTESIAN_POINT('Ctrl Pts',(1.09249646371974,-1.6215005929131,4.56522305400735));
#272878=CARTESIAN_POINT('Ctrl Pts',(1.14795508174258,-1.58123847989523,
4.56914097261228));
#272879=CARTESIAN_POINT('Ctrl Pts',(1.2033301208026,-1.54103704393293,4.57305298671426));
#272880=CARTESIAN_POINT('Ctrl Pts',(1.25667702071132,-1.49786068027829,
4.57696500081624));
#272881=CARTESIAN_POINT('Ctrl Pts',(1.30766078230223,-1.45194327658787,
4.58087701491822));
#272882=CARTESIAN_POINT('Ctrl Pts',(1.35858452354176,-1.40607992890701,
4.58478442362324));
#272883=CARTESIAN_POINT('Ctrl Pts',(1.40715028771411,-1.35748227744352,
4.58869183232825));
#272884=CARTESIAN_POINT('Ctrl Pts',(1.45305505958132,-1.30642527295867,
4.59259924103327));
#272885=CARTESIAN_POINT('Ctrl Pts',(1.49893102109081,-1.25540031243141,
4.59650419740407));
#272886=CARTESIAN_POINT('Ctrl Pts',(1.54214897499646,-1.20191942571252,
4.60040915377487));
#272887=CARTESIAN_POINT('Ctrl Pts',(1.58244291927386,-1.14629420623156,
4.60431411014568));
#272888=CARTESIAN_POINT('Ctrl Pts',(1.62272539887643,-1.09068481357184,
4.60821795545486));
#272889=CARTESIAN_POINT('Ctrl Pts',(1.66008523195781,-1.03293269753834,
4.61212180076404));
#272890=CARTESIAN_POINT('Ctrl Pts',(1.69429799803567,-0.973380857553883,
4.61602564607323));
#272891=CARTESIAN_POINT('Ctrl Pts',(1.72851276722741,-0.913825530885028,
4.61992971994758));
#272892=CARTESIAN_POINT('Ctrl Pts',(1.75957986076182,-0.852470698897036,
4.62383379382194));
#272893=CARTESIAN_POINT('Ctrl Pts',(1.78732024914569,-0.789684954265806,
4.62773786769629));
#272894=CARTESIAN_POINT('Ctrl Pts',(1.81509020179009,-0.726832295859382,
4.63164610232916));
#272895=CARTESIAN_POINT('Ctrl Pts',(1.83952617446589,-0.662546132222402,
4.63555433696203));
#272896=CARTESIAN_POINT('Ctrl Pts',(1.86049726291968,-0.597215149396232,
4.6394625715949));
#272897=CARTESIAN_POINT('Ctrl Pts',(1.88148089469671,-0.531845090504163,
4.64337314383893));
#272898=CARTESIAN_POINT('Ctrl Pts',(1.89899539227486,-0.465429444442277,
4.64728371608295));
#272899=CARTESIAN_POINT('Ctrl Pts',(1.91296047745239,-0.398369441229001,
4.65119428832697));
#272900=CARTESIAN_POINT('Ctrl Pts',(1.92694971536895,-0.33119345714373,
4.65511162394047));
#272901=CARTESIAN_POINT('Ctrl Pts',(1.93737721412613,-0.263371377663411,
4.65902895955397));
#272902=CARTESIAN_POINT('Ctrl Pts',(1.94421438782664,-0.195311070264557,
4.66294629516747));
#272903=CARTESIAN_POINT('Ctrl Pts',(1.94747048367496,-0.162898425206187,
4.66481186430266));
#272904=CARTESIAN_POINT('Ctrl Pts',(1.94991306204641,-0.130431770493967,
4.66667743343785));
#272905=CARTESIAN_POINT('Ctrl Pts',(1.95154318759175,-0.0979550252118336,
4.66854300257304));
#272906=CARTESIAN_POINT('Ctrl Pts',(1.95496664646119,-0.0297499706961675,
4.67246092117797));
#272907=CARTESIAN_POINT('Ctrl Pts',(1.95481701751349,0.038770144406793,
4.6763788397829));
#272908=CARTESIAN_POINT('Ctrl Pts',(1.95105722451954,0.107199378030411,
4.68029675838782));
#272909=CARTESIAN_POINT('Ctrl Pts',(1.94730309772518,0.175525485312703,
4.68420877248981));
#272910=CARTESIAN_POINT('Ctrl Pts',(1.93994963147098,0.243760495698615,
4.6881207865918));
#272911=CARTESIAN_POINT('Ctrl Pts',(1.92901170863315,0.311496112265012,
4.69203280069378));
#272912=CARTESIAN_POINT('Ctrl Pts',(1.91808666240449,0.37915198745137,4.6959402093988));
#272913=CARTESIAN_POINT('Ctrl Pts',(1.90358561816303,0.44630915306549,4.69984761810382));
#272914=CARTESIAN_POINT('Ctrl Pts',(1.88557530377411,0.51256392166944,4.70375502680883));
#272915=CARTESIAN_POINT('Ctrl Pts',(1.86757629286366,0.578777108025924,
4.70765998317964));
#272916=CARTESIAN_POINT('Ctrl Pts',(1.84607250950989,0.644088547188653,
4.71156493955044));
#272917=CARTESIAN_POINT('Ctrl Pts',(1.82118153925018,0.708105783830585,
4.71546989592125));
#272918=CARTESIAN_POINT('Ctrl Pts',(1.7962976511187,0.772104805904206,4.71937374123044));
#272919=CARTESIAN_POINT('Ctrl Pts',(1.7680286674486,0.834809898173339,4.72327758653962));
#272920=CARTESIAN_POINT('Ctrl Pts',(1.7365411083581,0.895846515304052,4.72718143184881));
#272921=CARTESIAN_POINT('Ctrl Pts',(1.70505170571113,0.956886706050949,
4.73108550572317));
#272922=CARTESIAN_POINT('Ctrl Pts',(1.67034358132991,1.01625779169783,4.73498957959752));
#272923=CARTESIAN_POINT('Ctrl Pts',(1.63262937131469,1.07360948948889,4.73889365347188));
#272924=CARTESIAN_POINT('Ctrl Pts',(1.59487496745953,1.13102230973116,4.74280188810475));
#272925=CARTESIAN_POINT('Ctrl Pts',(1.55410835509141,1.18641103522474,4.74671012273762));
#272926=CARTESIAN_POINT('Ctrl Pts',(1.51058514758464,1.23945492531866,4.7506183573705));
#272927=CARTESIAN_POINT('Ctrl Pts',(1.46703590777817,1.29253054226644,4.75452892961452));
#272928=CARTESIAN_POINT('Ctrl Pts',(1.42072712316509,1.34325816920577,4.75843950185855));
#272929=CARTESIAN_POINT('Ctrl Pts',(1.37195239703345,1.39135280223032,4.76235007410257));
#272930=CARTESIAN_POINT('Ctrl Pts',(1.32309331457916,1.43953061535045,4.76626740971607));
#272931=CARTESIAN_POINT('Ctrl Pts',(1.27176014637439,1.48506601956992,4.77018474532957));
#272932=CARTESIAN_POINT('Ctrl Pts',(1.21828010083953,1.52771384620891,4.77410208094308));
#272933=CARTESIAN_POINT('Ctrl Pts',(1.19281107491446,1.5480241991911,4.77596765007825));
#272934=CARTESIAN_POINT('Ctrl Pts',(1.16685557093406,1.56768028400996,4.77783321921342));
#272935=CARTESIAN_POINT('Ctrl Pts',(1.14045106888306,1.58665918189241,4.77969878834859));
#272936=CARTESIAN_POINT('Ctrl Pts',(1.08499845236565,1.6265171403635,4.78361670695352));
#272937=CARTESIAN_POINT('Ctrl Pts',(1.02734374656688,1.66354366412415,4.78753462555845));
#272938=CARTESIAN_POINT('Ctrl Pts',(0.967807938556677,1.69748749452439,
4.79145254416337));
#272939=CARTESIAN_POINT('Ctrl Pts',(0.908361854042292,1.73138016984289,
4.79536455826536));
#272940=CARTESIAN_POINT('Ctrl Pts',(0.847040717511409,1.76219913028732,
4.79927657236734));
#272941=CARTESIAN_POINT('Ctrl Pts',(0.78419566740042,1.78973549867862,4.80318858646933));
#272942=CARTESIAN_POINT('Ctrl Pts',(0.721424601277155,1.8172394500325,4.80709599517434));
#272943=CARTESIAN_POINT('Ctrl Pts',(0.657133632955883,1.84146828759698,
4.81100340387936));
#272944=CARTESIAN_POINT('Ctrl Pts',(0.591698138622352,1.86225919590986,
4.81491081258438));
#272945=CARTESIAN_POINT('Ctrl Pts',(0.526303712350415,1.88303705561187,
4.81881576895518));
#272946=CARTESIAN_POINT('Ctrl Pts',(0.459766652759582,1.9003811175651,4.82272072532598));
#272947=CARTESIAN_POINT('Ctrl Pts',(0.392480473834731,1.91417738928723,
4.82662568169679));
#272948=CARTESIAN_POINT('Ctrl Pts',(0.325213439577279,1.92796973561133,
4.83052952700597));
#272949=CARTESIAN_POINT('Ctrl Pts',(0.257198190796686,1.93821619683129,
4.83443337231516));
#272950=CARTESIAN_POINT('Ctrl Pts',(0.188839725512325,1.94485360839021,
4.83833721762434));
#272951=CARTESIAN_POINT('Ctrl Pts',(0.120477257926878,1.95149140856113,
4.8422412914987));
#272952=CARTESIAN_POINT('Ctrl Pts',(0.0517720238259972,1.95451969456067,
4.84614536537306));
#272953=CARTESIAN_POINT('Ctrl Pts',(-0.0168663607248519,1.95392720587946,
4.85004943924741));
#272954=CARTESIAN_POINT('Ctrl Pts',(-0.0855778964895568,1.95333408575467,
4.85395767388028));
#272955=CARTESIAN_POINT('Ctrl Pts',(-0.154221947650849,1.94911249411899,
4.85786590851315));
#272956=CARTESIAN_POINT('Ctrl Pts',(-0.222390418021636,1.94130329984064,
4.86177414314602));
#272957=CARTESIAN_POINT('Ctrl Pts',(-0.290599661629359,1.93348943469133,
4.86568471539005));
#272958=CARTESIAN_POINT('Ctrl Pts',(-0.358332273144911,1.92208377800183,
4.86959528763407));
#272959=CARTESIAN_POINT('Ctrl Pts',(-0.425189585458391,1.90717849621312,
4.8735058598781));
#272960=CARTESIAN_POINT('Ctrl Pts',(-0.492162528088149,1.89224743560698,
4.8774231954916));
#272961=CARTESIAN_POINT('Ctrl Pts',(-0.558256676514778,1.87380480187081,
4.8813405311051));
#272962=CARTESIAN_POINT('Ctrl Pts',(-0.623088613897518,1.85199259696989,
4.8852578667186));
#272963=CARTESIAN_POINT('Ctrl Pts',(-0.653963798790631,1.84160487933519,
4.88712343585378));
#272964=CARTESIAN_POINT('Ctrl Pts',(-0.684553012127485,1.83045365138825,
4.88898900498896));
#272965=CARTESIAN_POINT('Ctrl Pts',(-0.714816674560956,1.81855797866596,
4.89085457412414));
#272966=CARTESIAN_POINT('Ctrl Pts',(-0.77837399005539,1.79357564132026,
4.89477249272907));
#272967=CARTESIAN_POINT('Ctrl Pts',(-0.840746204620179,1.76520778252149,
4.898690411334));
#272968=CARTESIAN_POINT('Ctrl Pts',(-0.901548157631753,1.73358787474728,
4.90260832993892));
#272969=CARTESIAN_POINT('Ctrl Pts',(-0.962258479002415,1.70201561978505,
4.90652034404091));
#272970=CARTESIAN_POINT('Ctrl Pts',(-1.0214028024615,1.66720126770328,4.91043235814289));
#272971=CARTESIAN_POINT('Ctrl Pts',(-1.07861522978388,1.62932660509742,
4.91434437224487));
#272972=CARTESIAN_POINT('Ctrl Pts',(-1.1357603040926,1.59149653022865,4.91825178094988));
#272973=CARTESIAN_POINT('Ctrl Pts',(-1.1909775908175,1.55061357015786,4.9221591896549));
#272974=CARTESIAN_POINT('Ctrl Pts',(-1.24392675285296,1.50690485218434,
4.92606659835991));
#272975=CARTESIAN_POINT('Ctrl Pts',(-1.29684268339119,1.4632235663001,4.92997155473072));
#272976=CARTESIAN_POINT('Ctrl Pts',(-1.34749293447195,1.41672035297581,
4.93387651110152));
#272977=CARTESIAN_POINT('Ctrl Pts',(-1.39556835769231,1.36766405195427,
4.93778146747232));
#272978=CARTESIAN_POINT('Ctrl Pts',(-1.44363010220478,1.31862170872587,
4.94168531278151));
#272979=CARTESIAN_POINT('Ctrl Pts',(-1.48911812903031,1.26702807103927,
4.94558915809069));
#272980=CARTESIAN_POINT('Ctrl Pts',(-1.53175977084458,1.21318918739913,
4.94949300339987));
#272981=CARTESIAN_POINT('Ctrl Pts',(-1.5744039092727,1.15934715156088,4.95339707727423));
#272982=CARTESIAN_POINT('Ctrl Pts',(-1.61420102839992,1.10325999600695,
4.95730115114859));
#272983=CARTESIAN_POINT('Ctrl Pts',(-1.65091956898821,1.04526579238574,
4.96120522502295));
#272984=CARTESIAN_POINT('Ctrl Pts',(-1.68767724228383,0.987209781564125,
4.96511345965582));
#272985=CARTESIAN_POINT('Ctrl Pts',(-1.72134952549778,0.927243082981232,
4.96902169428869));
#272986=CARTESIAN_POINT('Ctrl Pts',(-1.75174948485069,0.865730756254706,
4.97292992892156));
#272987=CARTESIAN_POINT('Ctrl Pts',(-1.78216762716618,0.804181637494288,
4.97684050116558));
#272988=CARTESIAN_POINT('Ctrl Pts',(-1.80930935590143,0.741085502680043,
4.98075107340961));
#272989=CARTESIAN_POINT('Ctrl Pts',(-1.83303595225885,0.676827302734235,
4.98466164565363));
#272990=CARTESIAN_POINT('Ctrl Pts',(-1.85680358397568,0.612457967660123,
4.98857898126713));
#272991=CARTESIAN_POINT('Ctrl Pts',(-1.87714414903812,0.546923025771801,
4.99249631688063));
#272992=CARTESIAN_POINT('Ctrl Pts',(-1.89396907145856,0.480621635341562,
4.99641365249413));
#272993=CARTESIAN_POINT('Ctrl Pts',(-1.90198167468339,0.449046646673181,
4.99827922162931));
#272994=CARTESIAN_POINT('Ctrl Pts',(-1.90919768693769,0.417297961276106,
5.0001447907645));
#272995=CARTESIAN_POINT('Ctrl Pts',(-1.91561166762039,0.38541917294892,
5.00201035989968));
#272996=CARTESIAN_POINT('Ctrl Pts',(-1.93495299057814,0.289288864636548,
5.00763597321668));
#272997=CARTESIAN_POINT('Ctrl Pts',(-1.94706313315768,0.191658470633638,
5.01326158653369));
#272998=CARTESIAN_POINT('Ctrl Pts',(-1.95176526863315,0.0934255647955626,
5.01888719985069));
#272999=CARTESIAN_POINT('Ctrl Pts',(-1.9532260755329,0.0629076634335931,
5.02063490252572));
#273000=CARTESIAN_POINT('Ctrl Pts',(-1.95397221085221,0.0323318000566485,
5.02238260520075));
#273001=CARTESIAN_POINT('Ctrl Pts',(-1.95399923813581,0.00172550418305494,
5.02413030787578));
#273002=CARTESIAN_POINT('',(-1.95079228797786,3.78500716371835E-5,5.72413030787577));
#273003=CARTESIAN_POINT('Ctrl Pts',(-1.9546671565405,0.0017197843226782,
5.02413066805192));
#273004=CARTESIAN_POINT('Ctrl Pts',(-1.94988360819336,-0.518201249319763,
5.05380916059302));
#273005=CARTESIAN_POINT('Ctrl Pts',(-1.46932115474053,-1.69501948412908,
5.12053958172598));
#273006=CARTESIAN_POINT('Ctrl Pts',(0.517818131704895,-2.25085667576551,
5.22432193145079));
#273007=CARTESIAN_POINT('Ctrl Pts',(2.17203334564338,-0.785342306114842,
5.33547771722633));
#273008=CARTESIAN_POINT('Ctrl Pts',(1.83757553579813,1.39921676040448,5.44663350300188));
#273009=CARTESIAN_POINT('Ctrl Pts',(-0.179331995427646,2.30267918472736,
5.55778928877743));
#273010=CARTESIAN_POINT('Ctrl Pts',(-1.72107917867584,1.30007497440903,
5.65028822373539));
#273011=CARTESIAN_POINT('Ctrl Pts',(-1.95084822744177,0.32391356113618,
5.70573523010151));
#273012=CARTESIAN_POINT('Ctrl Pts',(-1.95079228797786,3.78500716371835E-5,
5.72413030787577));
#273013=CARTESIAN_POINT('',(-1.95399922102775,-0.00174477016505668,6.42413030787577));
#273014=CARTESIAN_POINT('Ctrl Pts',(-1.95079228797786,3.78500716371835E-5,
5.72413030787577));
#273015=CARTESIAN_POINT('Ctrl Pts',(-1.95073555246167,-0.328446807559118,
5.74278715869335));
#273016=CARTESIAN_POINT('Ctrl Pts',(-1.71625531119408,-1.30936792044859,
5.7984959381028));
#273017=CARTESIAN_POINT('Ctrl Pts',(-0.163096070439655,-2.30388607881722,
5.89125664610408));
#273018=CARTESIAN_POINT('Ctrl Pts',(1.84739289128347,-1.38622902061525,
6.00241243187962));
#273019=CARTESIAN_POINT('Ctrl Pts',(2.16644354493716,0.800633348643864,
6.11356821765517));
#273020=CARTESIAN_POINT('Ctrl Pts',(0.501939091571552,2.25445082907413,
6.22472400343072));
#273021=CARTESIAN_POINT('Ctrl Pts',(-1.47623102002116,1.68605736602827,
6.32824460474009));
#273022=CARTESIAN_POINT('Ctrl Pts',(-1.94977076795257,0.513689648483756,
6.3947132774576));
#273023=CARTESIAN_POINT('Ctrl Pts',(-1.95452816085295,-0.00174022619192097,
6.42413002158326));
#273024=CARTESIAN_POINT('',(-1.95399973054014,0.00102618178129684,7.12413030787578));
#273025=CARTESIAN_POINT('Ctrl Pts',(-1.95399922102775,-0.00174477016505668,
6.42413030787577));
#273026=CARTESIAN_POINT('Ctrl Pts',(-1.95391274289347,-0.0985931748455416,
6.42965921107939));
#273027=CARTESIAN_POINT('Ctrl Pts',(-1.94662244500826,-0.195131146519569,
6.43518811428301));
#273028=CARTESIAN_POINT('Ctrl Pts',(-1.9322863978956,-0.290491439646095,
6.44071701748663));
#273029=CARTESIAN_POINT('Ctrl Pts',(-1.92682520998912,-0.326818083628763,
6.44282320331836));
#273030=CARTESIAN_POINT('Ctrl Pts',(-1.92034203116191,-0.362974145946528,
6.44492938915009));
#273031=CARTESIAN_POINT('Ctrl Pts',(-1.91284727552396,-0.398912647731989,
6.44703557498182));
#273032=CARTESIAN_POINT('Ctrl Pts',(-1.89890556054757,-0.46576530748182,
6.45095349358675));
#273033=CARTESIAN_POINT('Ctrl Pts',(-1.88142727460356,-0.532018896690245,
6.45487141219167));
#273034=CARTESIAN_POINT('Ctrl Pts',(-1.86047923850533,-0.597271297728789,
6.4587893307966));
#273035=CARTESIAN_POINT('Ctrl Pts',(-1.83956277216473,-0.662425360074588,
6.46270134489859));
#273036=CARTESIAN_POINT('Ctrl Pts',(-1.8151870826716,-0.726580764134181,
6.46661335900057));
#273037=CARTESIAN_POINT('Ctrl Pts',(-1.78746985563884,-0.789346258103795,
6.47052537310256));
#273038=CARTESIAN_POINT('Ctrl Pts',(-1.75978525855835,-0.852037861742691,
6.47443278180757));
#273039=CARTESIAN_POINT('Ctrl Pts',(-1.72876713429301,-0.913342357046629,
6.47834019051259));
#273040=CARTESIAN_POINT('Ctrl Pts',(-1.69458216108227,-0.972886066989219,
6.4822475992176));
#273041=CARTESIAN_POINT('Ctrl Pts',(-1.66041864275012,-1.03239240662118,
6.4861525555884));
#273042=CARTESIAN_POINT('Ctrl Pts',(-1.62309246250114,-1.09013972735596,
6.49005751195921));
#273043=CARTESIAN_POINT('Ctrl Pts',(-1.58281666067281,-1.14577808440229,
6.49396246833001));
#273044=CARTESIAN_POINT('Ctrl Pts',(-1.54255231835727,-1.20140061088944,
6.49786631363919));
#273045=CARTESIAN_POINT('Ctrl Pts',(-1.49934030881723,-1.25491496658702,
6.50177015894838));
#273046=CARTESIAN_POINT('Ctrl Pts',(-1.45343648464424,-1.3060009131333,
6.50567400425756));
#273047=CARTESIAN_POINT('Ctrl Pts',(-1.40752997286077,-1.35708985069672,
6.50957807813192));
#273048=CARTESIAN_POINT('Ctrl Pts',(-1.35893166425077,-1.40574973262428,
6.51348215200628));
#273049=CARTESIAN_POINT('Ctrl Pts',(-1.30793588972586,-1.45169545992505,
6.51738622588064));
#273050=CARTESIAN_POINT('Ctrl Pts',(-1.25688576656164,-1.49769015378796,
6.5212944605135));
#273051=CARTESIAN_POINT('Ctrl Pts',(-1.20343344445735,-1.54096459032305,
6.52520269514637));
#273052=CARTESIAN_POINT('Ctrl Pts',(-1.14790736046466,-1.58127312371743,
6.52911092977924));
#273053=CARTESIAN_POINT('Ctrl Pts',(-1.09234806495694,-1.62160576663594,
6.53302150202327));
#273054=CARTESIAN_POINT('Ctrl Pts',(-1.03471295185424,-1.65896870823414,
6.53693207426729));
#273055=CARTESIAN_POINT('Ctrl Pts',(-0.975358172148888,-1.69316048737926,
6.54084264651131));
#273056=CARTESIAN_POINT('Ctrl Pts',(-0.915900737824142,-1.72741140151051,
6.54475998212481));
#273057=CARTESIAN_POINT('Ctrl Pts',(-0.854718139270463,-1.7584799841879,
6.54867731773831));
#273058=CARTESIAN_POINT('Ctrl Pts',(-0.79218896246577,-1.78621181491653,
6.55259465335181));
#273059=CARTESIAN_POINT('Ctrl Pts',(-0.76241043088079,-1.79941866073574,
6.55446022248699));
#273060=CARTESIAN_POINT('Ctrl Pts',(-0.732326754472248,-1.81186945472834,
6.55632579162218));
#273061=CARTESIAN_POINT('Ctrl Pts',(-0.701979991915673,-1.82355150487999,
6.55819136075737));
#273062=CARTESIAN_POINT('Ctrl Pts',(-0.638248156210868,-1.84808520924376,
6.5621092793623));
#273063=CARTESIAN_POINT('Ctrl Pts',(-0.573102123664993,-1.86932251147531,
6.56602719796722));
#273064=CARTESIAN_POINT('Ctrl Pts',(-0.506916001839037,-1.88710152537682,
6.56994511657215));
#273065=CARTESIAN_POINT('Ctrl Pts',(-0.44082962587064,-1.9048537453986,
6.57385713067414));
#273066=CARTESIAN_POINT('Ctrl Pts',(-0.373706742743016,-1.91915789406084,
6.57776914477612));
#273067=CARTESIAN_POINT('Ctrl Pts',(-0.305939909450436,-1.92990071553058,
6.58168115887811));
#273068=CARTESIAN_POINT('Ctrl Pts',(-0.238252854287599,-1.94063089007316,
6.58558856758312));
#273069=CARTESIAN_POINT('Ctrl Pts',(-0.169923838093017,-1.94780798720893,
6.58949597628814));
#273070=CARTESIAN_POINT('Ctrl Pts',(-0.101357215031177,-1.95136944604581,
6.59340338499316));
#273071=CARTESIAN_POINT('Ctrl Pts',(-0.0328336251630234,-1.95492866967055,
6.59730834136396));
#273072=CARTESIAN_POINT('Ctrl Pts',(0.0359267855861521,-1.95487673091302,
6.60121329773476));
#273073=CARTESIAN_POINT('Ctrl Pts',(0.104514465942167,-1.95120289216904,
6.60511825410557));
#273074=CARTESIAN_POINT('Ctrl Pts',(0.173082631319818,-1.9475300987277,
6.60902209941475));
#273075=CARTESIAN_POINT('Ctrl Pts',(0.241477672862865,-1.9402374773509,
6.61292594472394));
#273076=CARTESIAN_POINT('Ctrl Pts',(0.309291786723594,-1.92936637025354,
6.61682979003312));
#273077=CARTESIAN_POINT('Ctrl Pts',(0.377109871014345,-1.91849462666671,
6.62073386390748));
#273078=CARTESIAN_POINT('Ctrl Pts',(0.444346474763577,-1.90404406179105,
6.62463793778184));
#273079=CARTESIAN_POINT('Ctrl Pts',(0.510602456442851,-1.88610740189273,
6.6285420116562));
#273080=CARTESIAN_POINT('Ctrl Pts',(0.576929050295117,-1.86815162603687,
6.63245024628907));
#273081=CARTESIAN_POINT('Ctrl Pts',(0.642272460613658,-1.84670246932343,
6.63635848092194));
#273082=CARTESIAN_POINT('Ctrl Pts',(0.706248203474354,-1.82190270736097,
6.64026671555481));
#273083=CARTESIAN_POINT('Ctrl Pts',(0.770262211798635,-1.7970881120516,
6.64417728779884));
#273084=CARTESIAN_POINT('Ctrl Pts',(0.83290647589306,-1.76891912479073,
6.64808786004286));
#273085=CARTESIAN_POINT('Ctrl Pts',(0.893818610961755,-1.73758576499072,
6.65199843228689));
#273086=CARTESIAN_POINT('Ctrl Pts',(0.954836094109801,-1.70619821386627,
6.65591576790039));
#273087=CARTESIAN_POINT('Ctrl Pts',(1.01411504441724,-1.67163561492152,
6.65983310351389));
#273088=CARTESIAN_POINT('Ctrl Pts',(1.07132043821504,-1.63413234429245,
6.66375043912739));
#273089=CARTESIAN_POINT('Ctrl Pts',(1.0985636023358,-1.61627200475131,6.66561600826256));
#273090=CARTESIAN_POINT('Ctrl Pts',(1.12533695126987,-1.59774533089602,
6.66748157739774));
#273091=CARTESIAN_POINT('Ctrl Pts',(1.15160701602777,-1.57858078052269,
6.66934714653291));
#273092=CARTESIAN_POINT('Ctrl Pts',(1.20677729812938,-1.53833292958698,
6.67326506513784));
#273093=CARTESIAN_POINT('Ctrl Pts',(1.25994459082221,-1.49510946894049,
6.67718298374277));
#273094=CARTESIAN_POINT('Ctrl Pts',(1.31077002566914,-1.44913696378477,
6.6811009023477));
#273095=CARTESIAN_POINT('Ctrl Pts',(1.36151886399635,-1.40323374153646,
6.68501291644968));
#273096=CARTESIAN_POINT('Ctrl Pts',(1.40993248696035,-1.35459002436953,
6.68892493055167));
#273097=CARTESIAN_POINT('Ctrl Pts',(1.45570288401229,-1.30347424733989,
6.69283694465366));
#273098=CARTESIAN_POINT('Ctrl Pts',(1.50141939811739,-1.25241864607612,
6.69674435335867));
#273099=CARTESIAN_POINT('Ctrl Pts',(1.54449853961188,-1.19889712941683,
6.70065176206369));
#273100=CARTESIAN_POINT('Ctrl Pts',(1.58466849750097,-1.14321553218456,
6.70455917076871));
#273101=CARTESIAN_POINT('Ctrl Pts',(1.62481324426692,-1.08756888135697,
6.70846412713951));
#273102=CARTESIAN_POINT('Ctrl Pts',(1.66205214211782,-1.02976523726008,
6.71236908351031));
#273103=CARTESIAN_POINT('Ctrl Pts',(1.69615410631377,-0.970142900625954,
6.71627403988112));
#273104=CARTESIAN_POINT('Ctrl Pts',(1.73024636761423,-0.910537528096824,
6.7201778851903));
#273105=CARTESIAN_POINT('Ctrl Pts',(1.76120322295931,-0.849114917102498,
6.72408173049949));
#273106=CARTESIAN_POINT('Ctrl Pts',(1.78883829480519,-0.786240138277388,
6.72798557580867));
#273107=CARTESIAN_POINT('Ctrl Pts',(1.81647498464935,-0.723361678214043,
6.73188964968303));
#273108=CARTESIAN_POINT('Ctrl Pts',(1.84078930926984,-0.659031332907956,
6.73579372355738));
#273109=CARTESIAN_POINT('Ctrl Pts',(1.8616427630243,-0.593634755450892,
6.73969779743174));
#273110=CARTESIAN_POINT('Ctrl Pts',(1.88251844130321,-0.528168481729042,
6.74360603206461));
#273111=CARTESIAN_POINT('Ctrl Pts',(1.8999257379916,-0.461634177661315,
6.74751426669748));
#273112=CARTESIAN_POINT('Ctrl Pts',(1.91377614856796,-0.394432317606417,
6.75142250133035));
#273113=CARTESIAN_POINT('Ctrl Pts',(1.92763484341517,-0.32719026246799,
6.75533307357438));
#273114=CARTESIAN_POINT('Ctrl Pts',(1.93793234435327,-0.259280343150828,
6.7592436458184));
#273115=CARTESIAN_POINT('Ctrl Pts',(1.94463182551026,-0.191110081399764,
6.76315421806243));
#273116=CARTESIAN_POINT('Ctrl Pts',(1.9513428934795,-0.122821918574689,
6.76707155367593));
#273117=CARTESIAN_POINT('Ctrl Pts',(1.95444349962448,-0.0542730058415149,
6.77098888928943));
#273118=CARTESIAN_POINT('Ctrl Pts',(1.95394892397752,0.0141280744304211,
6.77490622490293));
#273119=CARTESIAN_POINT('Ctrl Pts',(1.95371339014712,0.0467030071802761,
6.77677179403811));
#273120=CARTESIAN_POINT('Ctrl Pts',(1.9526632350996,0.0792444735219877,
6.77863736317329));
#273121=CARTESIAN_POINT('Ctrl Pts',(1.95080422311103,0.111708921273798,
6.78050293230847));
#273122=CARTESIAN_POINT('Ctrl Pts',(1.94690007529929,0.179888149503358,
6.7844208509134));
#273123=CARTESIAN_POINT('Ctrl Pts',(1.93940965139226,0.247997782538903,
6.78833876951833));
#273124=CARTESIAN_POINT('Ctrl Pts',(1.92833958366678,0.315630242631857,
6.79225668812326));
#273125=CARTESIAN_POINT('Ctrl Pts',(1.91728619909734,0.383160777161784,
6.79616870222524));
#273126=CARTESIAN_POINT('Ctrl Pts',(1.90266395606301,0.450215084383322,
6.80008071632723));
#273127=CARTESIAN_POINT('Ctrl Pts',(1.88453139914629,0.516388812457961,
6.80399273042921));
#273128=CARTESIAN_POINT('Ctrl Pts',(1.86642018868192,0.582484637877146,
6.80790013913423));
#273129=CARTESIAN_POINT('Ctrl Pts',(1.84480700089815,0.64770147075974,6.81180754783924));
#273130=CARTESIAN_POINT('Ctrl Pts',(1.81980143302252,0.711645097200267,
6.81571495654426));
#273131=CARTESIAN_POINT('Ctrl Pts',(1.79481155892613,0.77554859189247,6.81961991291506));
#273132=CARTESIAN_POINT('Ctrl Pts',(1.76643370692484,0.838180008129233,
6.82352486928586));
#273133=CARTESIAN_POINT('Ctrl Pts',(1.73482683566997,0.899161748652228,
6.82742982565667));
#273134=CARTESIAN_POINT('Ctrl Pts',(1.70322895739177,0.960126138284474,
6.83133367096585));
#273135=CARTESIAN_POINT('Ctrl Pts',(1.66840410996748,1.01944134743096,6.83523751627504));
#273136=CARTESIAN_POINT('Ctrl Pts',(1.63055798594328,1.07675282886863,6.83914136158422));
#273137=CARTESIAN_POINT('Ctrl Pts',(1.59270964607673,1.13406766582053,6.84304543545857));
#273138=CARTESIAN_POINT('Ctrl Pts',(1.55183995163655,1.18937813305157,6.84694950933293));
#273139=CARTESIAN_POINT('Ctrl Pts',(1.50819784603678,1.24235874738741,6.85085358320728));
#273140=CARTESIAN_POINT('Ctrl Pts',(1.4645092289548,1.29539582570149,6.85476181784015));
#273141=CARTESIAN_POINT('Ctrl Pts',(1.4180426174066,1.3460977152817,6.85867005247303));
#273142=CARTESIAN_POINT('Ctrl Pts',(1.36908651935444,1.39417290983649,6.8625782871059));
#273143=CARTESIAN_POINT('Ctrl Pts',(1.32010113945727,1.44227685934627,6.86648885934992));
#273144=CARTESIAN_POINT('Ctrl Pts',(1.26862367837227,1.48775066133684,6.87039943159394));
#273145=CARTESIAN_POINT('Ctrl Pts',(1.21497658622953,1.53034241100286,6.87431000383797));
#273146=CARTESIAN_POINT('Ctrl Pts',(1.1612367109638,1.57300782347873,6.87822733945147));
#273147=CARTESIAN_POINT('Ctrl Pts',(1.10532011607045,1.61278095022153,6.88214467506497));
#273148=CARTESIAN_POINT('Ctrl Pts',(1.04757839517192,1.64945309298841,6.88606201067847));
#273149=CARTESIAN_POINT('Ctrl Pts',(1.0200798137511,1.66691762102912,6.88792757981365));
#273150=CARTESIAN_POINT('Ctrl Pts',(0.99216765700178,1.68367952315546,6.88979314894883));
#273151=CARTESIAN_POINT('Ctrl Pts',(0.963881644802451,1.69972002836141,
6.89165871808401));
#273152=CARTESIAN_POINT('Ctrl Pts',(0.904477631643619,1.73340701030902,
6.89557663668894));
#273153=CARTESIAN_POINT('Ctrl Pts',(0.843187582883122,1.76404291221313,
6.89949455529386));
#273154=CARTESIAN_POINT('Ctrl Pts',(0.780357559123363,1.79141231432605,
6.90341247389879));
#273155=CARTESIAN_POINT('Ctrl Pts',(0.717622223410446,1.81874046935559,
6.90732448800077));
#273156=CARTESIAN_POINT('Ctrl Pts',(0.653351966055132,1.84281169964799,
6.91123650210276));
#273157=CARTESIAN_POINT('Ctrl Pts',(0.587918284448726,1.8634559535473,6.91514851620474));
#273158=CARTESIAN_POINT('Ctrl Pts',(0.522561634282116,1.88407590411287,
6.91905592490975));
#273159=CARTESIAN_POINT('Ctrl Pts',(0.456044746888122,1.90127674330248,
6.92296333361477));
#273160=CARTESIAN_POINT('Ctrl Pts',(0.388758282549127,1.91493681299135,
6.92687074231978));
#273161=CARTESIAN_POINT('Ctrl Pts',(0.321514047961584,1.92858830946488,
6.93077569869059));
#273162=CARTESIAN_POINT('Ctrl Pts',(0.25350167555272,1.93870334695118,6.9346806550614));
#273163=CARTESIAN_POINT('Ctrl Pts',(0.18512462780308,1.94521075263859,6.9385856114322));
#273164=CARTESIAN_POINT('Ctrl Pts',(0.116767035101388,1.95171630679988,
6.94248945674139));
#273165=CARTESIAN_POINT('Ctrl Pts',(0.0480454625343314,1.95461622026885,
6.94639330205057));
#273166=CARTESIAN_POINT('Ctrl Pts',(-0.0206306555021805,1.95389108602643,
6.95029714735975));
#273167=CARTESIAN_POINT('Ctrl Pts',(-0.0893107944379186,1.95316590932833,
6.95420122123411));
#273168=CARTESIAN_POINT('Ctrl Pts',(-0.157944981674803,1.94881527129698,
6.95810529510846));
#273169=CARTESIAN_POINT('Ctrl Pts',(-0.22612475266668,1.94087186496982,
6.96200936898282));
#273170=CARTESIAN_POINT('Ctrl Pts',(-0.294377186106019,1.93291999297408,
6.96591760361569));
#273171=CARTESIAN_POINT('Ctrl Pts',(-0.362173747218213,1.92136776820417,
6.96982583824856));
#273172=CARTESIAN_POINT('Ctrl Pts',(-0.429113068040347,1.90629955013293,
6.97373407288143));
#273173=CARTESIAN_POINT('Ctrl Pts',(-0.496092426914868,1.89122231939025,
6.97764464512546));
#273174=CARTESIAN_POINT('Ctrl Pts',(-0.562213051426074,1.8726250432057,
6.98155521736948));
#273175=CARTESIAN_POINT('Ctrl Pts',(-0.627088444737639,1.85064207303209,
6.9854657896135));
#273176=CARTESIAN_POINT('Ctrl Pts',(-0.69207604061893,1.82862108311606,
6.989383125227));
#273177=CARTESIAN_POINT('Ctrl Pts',(-0.75581365023548,1.80320289443677,
6.99330046084051));
#273178=CARTESIAN_POINT('Ctrl Pts',(-0.817935278905976,1.77456977307769,
6.99721779645401));
#273179=CARTESIAN_POINT('Ctrl Pts',(-0.84751972213716,1.76093370184922,
6.99908336558919));
#273180=CARTESIAN_POINT('Ctrl Pts',(-0.87673803298852,1.74656915631899,
7.00094893472438));
#273181=CARTESIAN_POINT('Ctrl Pts',(-0.9055529027555,1.73149933303801,7.00281450385956));
#273182=CARTESIAN_POINT('Ctrl Pts',(-0.966067580142368,1.69985089938206,
7.00673242246449));
#273183=CARTESIAN_POINT('Ctrl Pts',(-1.02504123378782,1.66496341253867,
7.01065034106942));
#273184=CARTESIAN_POINT('Ctrl Pts',(-1.08210522136569,1.62701084504471,
7.01456825967435));
#273185=CARTESIAN_POINT('Ctrl Pts',(-1.13908321060705,1.58911547400353,
7.01848027377633));
#273186=CARTESIAN_POINT('Ctrl Pts',(-1.19415683917951,1.54816446004565,
7.02239228787832));
#273187=CARTESIAN_POINT('Ctrl Pts',(-1.24698179293194,1.5043777478068,7.02630430198031));
#273188=CARTESIAN_POINT('Ctrl Pts',(-1.29974455879966,1.4606425832328,7.03021171068532));
#273189=CARTESIAN_POINT('Ctrl Pts',(-1.35026353034211,1.41407866273953,
7.03411911939034));
#273190=CARTESIAN_POINT('Ctrl Pts',(-1.39822466545501,1.36494827188184,
7.03802652809535));
#273191=CARTESIAN_POINT('Ctrl Pts',(-1.4461556996132,1.31584871581709,7.04193148446616));
#273192=CARTESIAN_POINT('Ctrl Pts',(-1.49153173891609,1.26418623580297,
7.04583644083696));
#273193=CARTESIAN_POINT('Ctrl Pts',(-1.53407421973957,1.21026124796692,
7.04974139720776));
#273194=CARTESIAN_POINT('Ctrl Pts',(-1.57660459612112,1.15635160319199,
7.05364524251695));
#273195=CARTESIAN_POINT('Ctrl Pts',(-1.61630270994416,1.10018111456041,
7.05754908782613));
#273196=CARTESIAN_POINT('Ctrl Pts',(-1.65293025542248,1.04208328396005,
7.06145293313532));
#273197=CARTESIAN_POINT('Ctrl Pts',(-1.68955994539699,0.983982051805635,
7.06535700700968));
#273198=CARTESIAN_POINT('Ctrl Pts',(-1.72311844991441,0.923953671155186,
7.06926108088404));
#273199=CARTESIAN_POINT('Ctrl Pts',(-1.75341176577964,0.862359078125545,
7.0731651547584));
#273200=CARTESIAN_POINT('Ctrl Pts',(-1.78373736668246,0.800698840788064,
7.07707338939127));
#273201=CARTESIAN_POINT('Ctrl Pts',(-1.81079061662371,0.737469502159592,
7.08098162402414));
#273202=CARTESIAN_POINT('Ctrl Pts',(-1.83442477262436,0.673054049525057,
7.08488985865701));
#273203=CARTESIAN_POINT('Ctrl Pts',(-1.85807306479435,0.608600068425758,
7.08880043090104));
#273204=CARTESIAN_POINT('Ctrl Pts',(-1.87829804813884,0.542959031597052,
7.09271100314506));
#273205=CARTESIAN_POINT('Ctrl Pts',(-1.89500304837502,0.476528537077671,
7.09662157538908));
#273206=CARTESIAN_POINT('Ctrl Pts',(-1.91173694005769,0.409983150427166,
7.10053891100258));
#273207=CARTESIAN_POINT('Ctrl Pts',(-1.92493860358043,0.342646063501762,
7.10445624661608));
#273208=CARTESIAN_POINT('Ctrl Pts',(-1.93456274107396,0.274923627301158,
7.10837358222958));
#273209=CARTESIAN_POINT('Ctrl Pts',(-1.93914608435421,0.242671888057907,
7.11023915136476));
#273210=CARTESIAN_POINT('Ctrl Pts',(-1.94291881149136,0.21033280354338,
7.11210472049994));
#273211=CARTESIAN_POINT('Ctrl Pts',(-1.94588018410544,0.177950299538276,
7.11397028963512));
#273212=CARTESIAN_POINT('Ctrl Pts',(-1.95125613063908,0.119164515767483,
7.117356962382));
#273213=CARTESIAN_POINT('Ctrl Pts',(-1.95396869021499,0.0601314865954855,
7.12074363512889));
#273214=CARTESIAN_POINT('Ctrl Pts',(-1.95399973054014,0.00102618178129684,
7.12413030787578));
#273215=CARTESIAN_POINT('',(-1.95143063279042,0.00110697429861677,7.82413030787578));
#273216=CARTESIAN_POINT('Ctrl Pts',(-1.95653239756848,0.00101057639789689,
7.12413127700382));
#273217=CARTESIAN_POINT('Ctrl Pts',(-1.95277222847162,-0.587284438719568,
7.1577962098061));
#273218=CARTESIAN_POINT('Ctrl Pts',(-1.35742546160988,-1.82964434792259,
7.22851307120022));
#273219=CARTESIAN_POINT('Ctrl Pts',(0.756007498599133,-2.18241702119978,
7.33628186118621));
#273220=CARTESIAN_POINT('Ctrl Pts',(2.24367588325968,-0.548096636770858,
7.44743764696176));
#273221=CARTESIAN_POINT('Ctrl Pts',(1.67707667939426,1.58805075605049,7.55859343273731));
#273222=CARTESIAN_POINT('Ctrl Pts',(-0.425022500941536,2.27020863932239,
7.66974921851285));
#273223=CARTESIAN_POINT('Ctrl Pts',(-1.78903345425891,1.15826657200137,
7.75826151022568));
#273224=CARTESIAN_POINT('Ctrl Pts',(-1.95273655968318,0.25458387806612,
7.80972187334665));
#273225=CARTESIAN_POINT('Ctrl Pts',(-1.95143063279042,0.00110697429861677,
7.82413030787578));
#273226=CARTESIAN_POINT('',(-1.95399933299106,-0.00161451865900695,8.52413033064835));
#273227=CARTESIAN_POINT('Ctrl Pts',(-1.95143063279042,0.00110697429861677,
7.82413030787578));
#273228=CARTESIAN_POINT('Ctrl Pts',(-1.94937831074373,-0.397243224947184,
7.8467738019385));
#273229=CARTESIAN_POINT('Ctrl Pts',(-1.63702841788431,-1.45037623606872,
7.90646922459306));
#273230=CARTESIAN_POINT('Ctrl Pts',(0.0846950054830772,-2.30809838360649,
8.00321657583951));
#273231=CARTESIAN_POINT('Ctrl Pts',(1.98528689602104,-1.18030815164845,
8.11437236161505));
#273232=CARTESIAN_POINT('Ctrl Pts',(2.06818731211289,1.02815010303738,8.2255281473906));
#273233=CARTESIAN_POINT('Ctrl Pts',(0.257494186475546,2.29525339261092,
8.33668393316614));
#273234=CARTESIAN_POINT('Ctrl Pts',(-1.574992175394,1.54810389090286,8.4362179866612));
#273235=CARTESIAN_POINT('Ctrl Pts',(-1.94901851619721,0.44514694611732,
8.49870011156441));
#273236=CARTESIAN_POINT('Ctrl Pts',(-1.9524979245119,-0.00161287803163724,
8.52413030787577));
#273237=CARTESIAN_POINT('',(-1.95430622668274,-0.000195118721719283,9.22413030787577));
#273238=CARTESIAN_POINT('Ctrl Pts',(-1.95399933299106,-0.00161451865900695,
8.52413033064835));
#273239=CARTESIAN_POINT('Ctrl Pts',(-1.9539320163729,-0.0830856284773361,
8.52876425028391));
#273240=CARTESIAN_POINT('Ctrl Pts',(-1.94876546240929,-0.164338261234181,
8.53339816991947));
#273241=CARTESIAN_POINT('Ctrl Pts',(-1.93860446546909,-0.244803444549495,
8.53803208955503));
#273242=CARTESIAN_POINT('Ctrl Pts',(-1.92831626862875,-0.326275926985445,
8.54272401866726));
#273243=CARTESIAN_POINT('Ctrl Pts',(-1.91290789145434,-0.406941059896342,
8.54741594777949));
#273244=CARTESIAN_POINT('Ctrl Pts',(-1.89253714684451,-0.486229521742185,
8.55210787689172));
#273245=CARTESIAN_POINT('Ctrl Pts',(-1.88256924209821,-0.525027309957497,
8.55440375283356));
#273246=CARTESIAN_POINT('Ctrl Pts',(-1.87141388570986,-0.563495796774266,
8.5566996287754));
#273247=CARTESIAN_POINT('Ctrl Pts',(-1.85909368766508,-0.601570162561162,
8.55899550471724));
#273248=CARTESIAN_POINT('Ctrl Pts',(-1.8380692358398,-0.666544172423249,
8.56291342332217));
#273249=CARTESIAN_POINT('Ctrl Pts',(-1.81359276004705,-0.730543630978053,
8.5668313419271));
#273250=CARTESIAN_POINT('Ctrl Pts',(-1.78577378172853,-0.79317589505164,
8.57074926053202));
#273251=CARTESIAN_POINT('Ctrl Pts',(-1.75799672802768,-0.855713769112257,
8.574661274634));
#273252=CARTESIAN_POINT('Ctrl Pts',(-1.72688736713501,-0.916888091937685,
8.57857328873598));
#273253=CARTESIAN_POINT('Ctrl Pts',(-1.69260462824858,-0.976322473587231,
8.58248530283796));
#273254=CARTESIAN_POINT('Ctrl Pts',(-1.65836224852688,-1.03568688643971,
8.58639271154298));
#273255=CARTESIAN_POINT('Ctrl Pts',(-1.62095415485611,-1.09331500201994,
8.59030012024799));
#273256=CARTESIAN_POINT('Ctrl Pts',(-1.58058610395774,-1.14885315335586,
8.594207528953));
#273257=CARTESIAN_POINT('Ctrl Pts',(-1.54024338850793,-1.20435644831538,
8.59811248532381));
#273258=CARTESIAN_POINT('Ctrl Pts',(-1.49694468948603,-1.25777198394912,
8.60201744169461));
#273259=CARTESIAN_POINT('Ctrl Pts',(-1.45093931600466,-1.30877465641413,
8.60592239806541));
#273260=CARTESIAN_POINT('Ctrl Pts',(-1.40494703224824,-1.35976281729269,
8.6098262433746));
#273261=CARTESIAN_POINT('Ctrl Pts',(-1.35624993218061,-1.40833911273824,
8.61373008868378));
#273262=CARTESIAN_POINT('Ctrl Pts',(-1.30513670778591,-1.45421256148809,
8.61763393399296));
#273263=CARTESIAN_POINT('Ctrl Pts',(-1.25402049077697,-1.50008869606999,
8.62153800786732));
#273264=CARTESIAN_POINT('Ctrl Pts',(-1.2004882364131,-1.54326134310115,
8.62544208174167));
#273265=CARTESIAN_POINT('Ctrl Pts',(-1.14486312844721,-1.58347858120091,
8.62934615561603));
#273266=CARTESIAN_POINT('Ctrl Pts',(-1.08917873813962,-1.62373868073751,
8.6332543902489));
#273267=CARTESIAN_POINT('Ctrl Pts',(-1.03139744233148,-1.66103679664842,
8.63716262488177));
#273268=CARTESIAN_POINT('Ctrl Pts',(-0.971872107326577,-1.6951638879473,
8.64107085951464));
#273269=CARTESIAN_POINT('Ctrl Pts',(-0.912311168756344,-1.72931139149794,
8.64498143175866));
#273270=CARTESIAN_POINT('Ctrl Pts',(-0.851004554076599,-1.76028387386122,
8.64889200400269));
#273271=CARTESIAN_POINT('Ctrl Pts',(-0.788327949779091,-1.78791919381081,
8.65280257624671));
#273272=CARTESIAN_POINT('Ctrl Pts',(-0.725542945737033,-1.81560230929203,
8.65671991186021));
#273273=CARTESIAN_POINT('Ctrl Pts',(-0.661383682812903,-1.83993656860672,
8.66063724747371));
#273274=CARTESIAN_POINT('Ctrl Pts',(-0.596243113116256,-1.86080900418647,
8.66455458308721));
#273275=CARTESIAN_POINT('Ctrl Pts',(-0.565220946964255,-1.87074917154403,
8.6664201522224));
#273276=CARTESIAN_POINT('Ctrl Pts',(-0.533976400546536,-1.87990494439288,
8.6682857213576));
#273277=CARTESIAN_POINT('Ctrl Pts',(-0.502552650317926,-1.88826821020173,
8.67015129049279));
#273278=CARTESIAN_POINT('Ctrl Pts',(-0.436559011521794,-1.90583206998708,
8.67406920909772));
#273279=CARTESIAN_POINT('Ctrl Pts',(-0.369512513301717,-1.9199669785106,
8.67798712770265));
#273280=CARTESIAN_POINT('Ctrl Pts',(-0.301802455051448,-1.93055206563431,
8.68190504630758));
#273281=CARTESIAN_POINT('Ctrl Pts',(-0.234194439308534,-1.94112120049246,
8.68581706040956));
#273282=CARTESIAN_POINT('Ctrl Pts',(-0.165925330327548,-1.94815105591516,
8.68972907451155));
#273283=CARTESIAN_POINT('Ctrl Pts',(-0.0973975601784948,-1.95157108896173,
8.69364108861354));
#273284=CARTESIAN_POINT('Ctrl Pts',(-0.0289504639679613,-1.95498709579331,
8.69754849731855));
#273285=CARTESIAN_POINT('Ctrl Pts',(0.0397541996598223,-1.95480169567058,
8.70145590602357));
#273286=CARTESIAN_POINT('Ctrl Pts',(0.108307701137618,-1.95099601277765,
8.70536331472858));
#273287=CARTESIAN_POINT('Ctrl Pts',(0.176818177657025,-1.94719271837466,
8.70926827109939));
#273288=CARTESIAN_POINT('Ctrl Pts',(0.245177190141463,-1.93977367556684,
8.71317322747019));
#273289=CARTESIAN_POINT('Ctrl Pts',(0.312976394490285,-1.92877209034449,
8.717078183841));
#273290=CARTESIAN_POINT('Ctrl Pts',(0.38075630820264,-1.91777363535919,
8.72098202915019));
#273291=CARTESIAN_POINT('Ctrl Pts',(0.447976244614836,-1.90319474023785,
8.72488587445937));
#273292=CARTESIAN_POINT('Ctrl Pts',(0.514235177137632,-1.88512020375207,
8.72878971976855));
#273293=CARTESIAN_POINT('Ctrl Pts',(0.58049798903657,-1.86704460902518,
8.73269379364291));
#273294=CARTESIAN_POINT('Ctrl Pts',(0.645799211414756,-1.845473098534,8.73659786751727));
#273295=CARTESIAN_POINT('Ctrl Pts',(0.709751935731432,-1.82054063116578,
8.74050194139163));
#273296=CARTESIAN_POINT('Ctrl Pts',(0.773772817529424,-1.79558159207294,
8.7444101760245));
#273297=CARTESIAN_POINT('Ctrl Pts',(0.836441873899648,-1.76725462666114,
8.74831841065737));
#273298=CARTESIAN_POINT('Ctrl Pts',(0.897392132113103,-1.73574288453719,
8.75222664529025));
#273299=CARTESIAN_POINT('Ctrl Pts',(0.958378846173423,-1.7042122944661,
8.75613721753427));
#273300=CARTESIAN_POINT('Ctrl Pts',(1.01764429153029,-1.66949338529711,
8.76004778977829));
#273301=CARTESIAN_POINT('Ctrl Pts',(1.0748485293495,-1.63181391063908,8.76395836202231));
#273302=CARTESIAN_POINT('Ctrl Pts',(1.1321517024068,-1.59406926899451,8.76787569763581));
#273303=CARTESIAN_POINT('Ctrl Pts',(1.18738615716273,-1.55335413417732,
8.77179303324932));
#273304=CARTESIAN_POINT('Ctrl Pts',(1.24024391104561,-1.50993742953617,
8.77571036886282));
#273305=CARTESIAN_POINT('Ctrl Pts',(1.26541658041269,-1.48926091056487,
8.77757593799799));
#273306=CARTESIAN_POINT('Ctrl Pts',(1.29005074412221,-1.46797223198639,
8.77944150713316));
#273307=CARTESIAN_POINT('Ctrl Pts',(1.31411617499479,-1.44610327384218,
8.78130707626834));
#273308=CARTESIAN_POINT('Ctrl Pts',(1.36465646190966,-1.40017584270702,
8.78522499487327));
#273309=CARTESIAN_POINT('Ctrl Pts',(1.4128864653487,-1.35150454386662,8.78914291347819));
#273310=CARTESIAN_POINT('Ctrl Pts',(1.45849354319493,-1.30035094665197,
8.79306083208312));
#273311=CARTESIAN_POINT('Ctrl Pts',(1.50403188885132,-1.24927444051444,
8.79697284618511));
#273312=CARTESIAN_POINT('Ctrl Pts',(1.54695482921322,-1.19572342466037,
8.80088486028709));
#273313=CARTESIAN_POINT('Ctrl Pts',(1.58698488859974,-1.1399977909435,8.80479687438908));
#273314=CARTESIAN_POINT('Ctrl Pts',(1.62696782282021,-1.08433775992078,
8.80870428309409));
#273315=CARTESIAN_POINT('Ctrl Pts',(1.66406435402609,-1.02650859297274,
8.81261169179911));
#273316=CARTESIAN_POINT('Ctrl Pts',(1.69803700493591,-0.966843487782949,
8.81651910050412));
#273317=CARTESIAN_POINT('Ctrl Pts',(1.73198833422303,-0.90721582909281,
8.82042405687493));
#273318=CARTESIAN_POINT('Ctrl Pts',(1.76281942949986,-0.845754944393178,
8.82432901324573));
#273319=CARTESIAN_POINT('Ctrl Pts',(1.79033678388323,-0.78282194672521,
8.82823396961654));
#273320=CARTESIAN_POINT('Ctrl Pts',(1.81784630886381,-0.719906855131373,
8.83213781492572));
#273321=CARTESIAN_POINT('Ctrl Pts',(1.84204376765398,-0.655520932583686,
8.83604166023491));
#273322=CARTESIAN_POINT('Ctrl Pts',(1.86278297148862,-0.590047117722006,
8.8399455055441));
#273323=CARTESIAN_POINT('Ctrl Pts',(1.88352338957723,-0.524569469451849,
8.84384957941845));
#273324=CARTESIAN_POINT('Ctrl Pts',(1.90080500461284,-0.458004272158418,
8.84775365329281));
#273325=CARTESIAN_POINT('Ctrl Pts',(1.91453142947546,-0.39074979916904,
8.85165772716716));
#273326=CARTESIAN_POINT('Ctrl Pts',(1.92827248324649,-0.323423649866621,
8.85556596180004));
#273327=CARTESIAN_POINT('Ctrl Pts',(1.93845068668766,-0.25540724176912,
8.85947419643291));
#273328=CARTESIAN_POINT('Ctrl Pts',(1.94502095399775,-0.187108226729025,
8.86338243106578));
#273329=CARTESIAN_POINT('Ctrl Pts',(1.95159515114614,-0.118768360370054,
8.86729300330981));
#273330=CARTESIAN_POINT('Ctrl Pts',(1.95455709614358,-0.0501460422143237,
8.87120357555382));
#273331=CARTESIAN_POINT('Ctrl Pts',(1.95391383943899,0.0183496062298952,
8.87511414779785));
#273332=CARTESIAN_POINT('Ctrl Pts',(1.95326947021621,0.0869637185073052,
8.87903148341135));
#273333=CARTESIAN_POINT('Ctrl Pts',(1.94900748521415,0.155450233086523,
8.88294881902485));
#273334=CARTESIAN_POINT('Ctrl Pts',(1.94118685446954,0.223404556879756,
8.88686615463835));
#273335=CARTESIAN_POINT('Ctrl Pts',(1.93746240275688,0.25576672892183,8.88873172377353));
#273336=CARTESIAN_POINT('Ctrl Pts',(1.93293160515096,0.288008343806086,
8.89059729290871));
#273337=CARTESIAN_POINT('Ctrl Pts',(1.92760485918677,0.320086717686857,
8.89246286204389));
#273338=CARTESIAN_POINT('Ctrl Pts',(1.91641805472947,0.387455144550988,
8.89638078064882));
#273339=CARTESIAN_POINT('Ctrl Pts',(1.90167307614851,0.454370121717464,
8.90029869925375));
#273340=CARTESIAN_POINT('Ctrl Pts',(1.88342018786656,0.520427128363525,
8.90421661785868));
#273341=CARTESIAN_POINT('Ctrl Pts',(1.86519480761717,0.586384583735182,
8.90812863196066));
#273342=CARTESIAN_POINT('Ctrl Pts',(1.84347213961137,0.651486164384399,
8.91204064606265));
#273343=CARTESIAN_POINT('Ctrl Pts',(1.81835371609044,0.71533611902384,8.91595266016463));
#273344=CARTESIAN_POINT('Ctrl Pts',(1.7932648630947,0.779110906657251,8.91986006886965));
#273345=CARTESIAN_POINT('Ctrl Pts',(1.76478837315675,0.841636538986938,
8.92376747757466));
#273346=CARTESIAN_POINT('Ctrl Pts',(1.73307545102905,0.902532814384301,
8.92767488627968));
#273347=CARTESIAN_POINT('Ctrl Pts',(1.70138243229252,0.963390870585568,
8.93157984265049));
#273348=CARTESIAN_POINT('Ctrl Pts',(1.66645723735186,1.02262116302438,8.93548479902129));
#273349=CARTESIAN_POINT('Ctrl Pts',(1.62849836781698,1.07986529994136,8.93938975539209));
#273350=CARTESIAN_POINT('Ctrl Pts',(1.59055029856743,1.137093149413,8.94329360070128));
#273351=CARTESIAN_POINT('Ctrl Pts',(1.54957053996758,1.19233555540075,8.94719744601046));
#273352=CARTESIAN_POINT('Ctrl Pts',(1.50580158876996,1.24526205083824,8.95110129131965));
#273353=CARTESIAN_POINT('Ctrl Pts',(1.46203007495597,1.29819164505466,8.95500536519401));
#273354=CARTESIAN_POINT('Ctrl Pts',(1.41546935980839,1.34880468205008,8.95890943906836));
#273355=CARTESIAN_POINT('Ctrl Pts',(1.3664018278686,1.39680422565131,8.96281351294272));
#273356=CARTESIAN_POINT('Ctrl Pts',(1.31728200230992,1.4448549246651,8.96672174757559));
#273357=CARTESIAN_POINT('Ctrl Pts',(1.26565038050763,1.4902862269339,8.97062998220846));
#273358=CARTESIAN_POINT('Ctrl Pts',(1.21182504330288,1.53283921675562,8.97453821684133));
#273359=CARTESIAN_POINT('Ctrl Pts',(1.15796751184157,1.57541765856599,8.97844878908536));
#273360=CARTESIAN_POINT('Ctrl Pts',(1.10191405515166,1.61511407730049,8.98235936132938));
#273361=CARTESIAN_POINT('Ctrl Pts',(1.04401225770631,1.65171256753679,8.9862699335734));
#273362=CARTESIAN_POINT('Ctrl Pts',(0.986010318587284,1.68837435518747,
8.9901872691869));
#273363=CARTESIAN_POINT('Ctrl Pts',(0.926154087418501,1.72192728033022,
8.9941046048004));
#273364=CARTESIAN_POINT('Ctrl Pts',(0.864815494984659,1.75220151798657,
8.9980219404139));
#273365=CARTESIAN_POINT('Ctrl Pts',(0.835603960377922,1.76661914489812,
8.99988750954908));
#273366=CARTESIAN_POINT('Ctrl Pts',(0.806056514829847,1.78029387776113,
9.00175307868426));
#273367=CARTESIAN_POINT('Ctrl Pts',(0.77621466080163,1.7932113094548,9.00361864781944));
#273368=CARTESIAN_POINT('Ctrl Pts',(0.713543193474069,1.82033946300654,
9.00753656642437));
#273369=CARTESIAN_POINT('Ctrl Pts',(0.649323458916591,1.8442320195025,9.0114544850293));
#273370=CARTESIAN_POINT('Ctrl Pts',(0.583922606928159,1.8647118783121,9.01537240363423));
#273371=CARTESIAN_POINT('Ctrl Pts',(0.518620317355696,1.88516087293106,
9.01928441773621));
#273372=CARTESIAN_POINT('Ctrl Pts',(0.452140908689718,1.90220723124397,
9.02319643183819));
#273373=CARTESIAN_POINT('Ctrl Pts',(0.384871960076454,1.91572168499156,
9.02710844594018));
#273374=CARTESIAN_POINT('Ctrl Pts',(0.317682203460918,1.92922022892322,
9.03101585464519));
#273375=CARTESIAN_POINT('Ctrl Pts',(0.249705232869922,1.93919502950697,
9.03492326335021));
#273376=CARTESIAN_POINT('Ctrl Pts',(0.181342494852364,1.94556698665472,
9.03883067205523));
#273377=CARTESIAN_POINT('Ctrl Pts',(0.113022662067911,1.95193494468958,
9.04273562842603));
#273378=CARTESIAN_POINT('Ctrl Pts',(0.044318030841683,1.95470449918397,
9.04664058479684));
#273379=CARTESIAN_POINT('Ctrl Pts',(-0.0243626330771243,1.95384811643831,
9.05054554116764));
#273380=CARTESIAN_POINT('Ctrl Pts',(-0.0930237555613264,1.95299197735582,
9.05444938647683));
#273381=CARTESIAN_POINT('Ctrl Pts',(-0.161660432605449,1.94851195519506,
9.05835323178601));
#273382=CARTESIAN_POINT('Ctrl Pts',(-0.22986350742114,1.94043262391562,
9.0622570770952));
#273383=CARTESIAN_POINT('Ctrl Pts',(-0.298070575440003,1.93235281960162,
9.06616115096955));
#273384=CARTESIAN_POINT('Ctrl Pts',(-0.36584350260625,1.92067334819781,
9.07006522484391));
#273385=CARTESIAN_POINT('Ctrl Pts',(-0.43277967871086,1.90547047988021,
9.07396929871827));
#273386=CARTESIAN_POINT('Ctrl Pts',(-0.499787191904258,1.89025140913771,
9.07787753335114));
#273387=CARTESIAN_POINT('Ctrl Pts',(-0.565955693689586,1.87150155667804,
9.08178576798401));
#273388=CARTESIAN_POINT('Ctrl Pts',(-0.630895165440094,1.84934780131384,
9.08569400261688));
#273389=CARTESIAN_POINT('Ctrl Pts',(-0.695873479084083,1.82718079524428,
9.0896045748609));
#273390=CARTESIAN_POINT('Ctrl Pts',(-0.75962084305028,1.80160601754062,
9.09351514710492));
#273391=CARTESIAN_POINT('Ctrl Pts',(-0.821767380670605,1.77279845782474,
9.09742571934895));
#273392=CARTESIAN_POINT('Ctrl Pts',(-0.884021401280499,1.74394107517811,
9.10134305496245));
#273393=CARTESIAN_POINT('Ctrl Pts',(-0.94466863516237,1.71183998146086,
9.10526039057595));
#273394=CARTESIAN_POINT('Ctrl Pts',(-1.00336472363941,1.67671560837132,
9.10917772618945));
#273395=CARTESIAN_POINT('Ctrl Pts',(-1.03131780752665,1.65998818116222,
9.11104329532463));
#273396=CARTESIAN_POINT('Ctrl Pts',(-1.05882881364094,1.64257570288164,
9.11290886445981));
#273397=CARTESIAN_POINT('Ctrl Pts',(-1.08586313347053,1.62450523402344,
9.11477443359499));
#273398=CARTESIAN_POINT('Ctrl Pts',(-1.14248049445749,1.5866606621978,9.11868145259301));
#273399=CARTESIAN_POINT('Ctrl Pts',(-1.19723251652673,1.5457754581117,9.12258847159102));
#273400=CARTESIAN_POINT('Ctrl Pts',(-1.24977243038037,1.50206020926631,
9.12649549058904));
#273401=CARTESIAN_POINT('Ctrl Pts',(-1.30447872619442,1.45654244649299,
9.13056360797599));
#273402=CARTESIAN_POINT('Ctrl Pts',(-1.35678601891319,1.40795638949954,
9.13463172536294));
#273403=CARTESIAN_POINT('Ctrl Pts',(-1.40633472210552,1.3565908187071,9.13869984274989));
#273404=CARTESIAN_POINT('Ctrl Pts',(-1.45379225699105,1.3073930958457,9.14259626809244));
#273405=CARTESIAN_POINT('Ctrl Pts',(-1.4987189765413,1.25564614837589,9.146492693435));
#273406=CARTESIAN_POINT('Ctrl Pts',(-1.5408332642137,1.20164422850217,9.15038911877756));
#273407=CARTESIAN_POINT('Ctrl Pts',(-1.58292212734437,1.14767490977501,
9.15428319183461));
#273408=CARTESIAN_POINT('Ctrl Pts',(-1.62220162238339,1.09145370826315,
9.15817726489165));
#273409=CARTESIAN_POINT('Ctrl Pts',(-1.65842965663595,1.0333087989514,9.1620713379487));
#273410=CARTESIAN_POINT('Ctrl Pts',(-1.69464843478071,0.975178745415278,
9.16596441608673));
#273411=CARTESIAN_POINT('Ctrl Pts',(-1.7278170382089,0.915126379811159,
9.16985749422477));
#273412=CARTESIAN_POINT('Ctrl Pts',(-1.75773710396939,0.853508215150441,
9.17375057236281));
#273413=CARTESIAN_POINT('Ctrl Pts',(-1.7876599434774,0.791884338161662,
9.17764401140967));
#273414=CARTESIAN_POINT('Ctrl Pts',(-1.81433343401215,0.728694820586261,
9.18153745045653));
#273415=CARTESIAN_POINT('Ctrl Pts',(-1.83760633974216,0.664318402680099,
9.1854308895034));
#273416=CARTESIAN_POINT('Ctrl Pts',(-1.86090435888048,0.599872517244304,
9.18932852989605));
#273417=CARTESIAN_POINT('Ctrl Pts',(-1.88079430434863,0.534237642789977,
9.1932261702887));
#273418=CARTESIAN_POINT('Ctrl Pts',(-1.89717441254307,0.467808987078976,
9.19712381068135));
#273419=CARTESIAN_POINT('Ctrl Pts',(-1.91356497607487,0.401337930304608,
9.20102393891748));
#273420=CARTESIAN_POINT('Ctrl Pts',(-1.92644115296945,0.33407257033215,
9.2049240671536));
#273421=CARTESIAN_POINT('Ctrl Pts',(-1.935752581741,0.266416858105946,9.20882419538972));
#273422=CARTESIAN_POINT('Ctrl Pts',(-1.94507957848799,0.198648030858228,
9.21273084433303));
#273423=CARTESIAN_POINT('Ctrl Pts',(-1.95082989748065,0.130488041793009,
9.21663749327635));
#273424=CARTESIAN_POINT('Ctrl Pts',(-1.95300519580194,0.0623434452900937,
9.22054414221966));
#273425=CARTESIAN_POINT('Ctrl Pts',(-1.95367081146085,0.0414920015784572,
9.2217395307717));
#273426=CARTESIAN_POINT('Ctrl Pts',(-1.95400207064188,0.0206419743383481,
9.22293491932373));
#273427=CARTESIAN_POINT('Ctrl Pts',(-1.95399999026116,-0.000195088146951379,
9.22413030787577));
#273428=CARTESIAN_POINT('',(-1.95399923014638,0.00173452798668402,9.92413030787578));
#273429=CARTESIAN_POINT('Ctrl Pts',(-1.95718185414804,-0.000195405825525797,
9.22413030787577));
#273430=CARTESIAN_POINT('Ctrl Pts',(-1.95719676559863,-0.0106706459447958,
9.22473027837403));
#273431=CARTESIAN_POINT('Ctrl Pts',(-1.9571199413354,-0.0211456613651047,
9.22533024887228));
#273432=CARTESIAN_POINT('Ctrl Pts',(-1.94650003891758,-0.678424664968078,
9.26298214796238));
#273433=CARTESIAN_POINT('Ctrl Pts',(-1.2207993775171,-1.9606479215337,9.33708600514608));
#273434=CARTESIAN_POINT('Ctrl Pts',(0.98549264484445,-2.08885031520166,
9.44824179092163));
#273435=CARTESIAN_POINT('Ctrl Pts',(2.28948607134397,-0.304540508771072,
9.55939757669718));
#273436=CARTESIAN_POINT('Ctrl Pts',(1.49726895966604,1.7586008798989,9.67055336247273));
#273437=CARTESIAN_POINT('Ctrl Pts',(-0.665819550192416,2.21160026201443,
9.78170914824828));
#273438=CARTESIAN_POINT('Ctrl Pts',(-1.84711996695996,1.01628998128808,
9.86623464117473));
#273439=CARTESIAN_POINT('Ctrl Pts',(-1.95463561301669,0.184694303118807,
9.91370820550933));
#273440=CARTESIAN_POINT('Ctrl Pts',(-1.95307033066634,0.00174189496380082,
9.92412984125209));
#273441=CARTESIAN_POINT('',(-1.95399983006808,-0.000814919564481316,10.6241303079163));
#273442=CARTESIAN_POINT('Ctrl Pts',(-1.95399923014638,0.00173452798668402,
9.92413030787578));
#273443=CARTESIAN_POINT('Ctrl Pts',(-1.95405962454448,-0.0663016226432694,
9.92800408460677));
#273444=CARTESIAN_POINT('Ctrl Pts',(-1.95056232198822,-0.134411719177273,
9.93187786133777));
#273445=CARTESIAN_POINT('Ctrl Pts',(-1.94351084834083,-0.202191944403128,
9.93575163806877));
#273446=CARTESIAN_POINT('Ctrl Pts',(-1.93646276771955,-0.269939555159191,
9.93962355081696));
#273447=CARTESIAN_POINT('Ctrl Pts',(-1.92586395926989,-0.33735711184642,
9.94349546356515));
#273448=CARTESIAN_POINT('Ctrl Pts',(-1.91176993307524,-0.40404420920177,
9.94736737631334));
#273449=CARTESIAN_POINT('Ctrl Pts',(-1.89767765412431,-0.470723039323177,
9.95123880905851));
#273450=CARTESIAN_POINT('Ctrl Pts',(-1.88009112231765,-0.536671100075149,
9.95511024180368));
#273451=CARTESIAN_POINT('Ctrl Pts',(-1.85911690417107,-0.601498409495291,
9.95898167454884));
#273452=CARTESIAN_POINT('Ctrl Pts',(-1.83812279022283,-0.666387213045117,
9.96285677967205));
#273453=CARTESIAN_POINT('Ctrl Pts',(-1.81373472523136,-0.730152663798364,
9.96673188479526));
#273454=CARTESIAN_POINT('Ctrl Pts',(-1.78610878838271,-0.792421223884144,
9.97060698991846));
#273455=CARTESIAN_POINT('Ctrl Pts',(-1.75847015739071,-0.854718396430472,
9.97448387565603));
#273456=CARTESIAN_POINT('Ctrl Pts',(-1.7275909193593,-0.915516861522571,
9.97836076139359));
#273457=CARTESIAN_POINT('Ctrl Pts',(-1.69367353785893,-0.974467006704897,
9.98223764713116));
#273458=CARTESIAN_POINT('Ctrl Pts',(-1.65969279940653,-1.03352726951292,
9.98612177480938));
#273459=CARTESIAN_POINT('Ctrl Pts',(-1.62266285436743,-1.09073189453974,
9.99000590248759));
#273460=CARTESIAN_POINT('Ctrl Pts',(-1.58282959514847,-1.1457602160671,
9.9938900301658));
#273461=CARTESIAN_POINT('Ctrl Pts',(-1.54819819099351,-1.19360234799779,
9.99726692671033));
#273462=CARTESIAN_POINT('Ctrl Pts',(-1.51144864042195,-1.23979981747353,
10.0006438232549));
#273463=CARTESIAN_POINT('Ctrl Pts',(-1.47276553818141,-1.28416419103837,
10.0040207197994));
#273464=CARTESIAN_POINT('Ctrl Pts',(-1.42788490770719,-1.33563630523962,
10.0079386384043));
#273465=CARTESIAN_POINT('Ctrl Pts',(-1.38021357834289,-1.38485492894223,
10.0118565570092));
#273466=CARTESIAN_POINT('Ctrl Pts',(-1.33000664865851,-1.43150211823949,
10.0157744756142));
#273467=CARTESIAN_POINT('Ctrl Pts',(-1.27987538337502,-1.47807900784599,
10.0196864897162));
#273468=CARTESIAN_POINT('Ctrl Pts',(-1.22721645911195,-1.52209182193203,
10.0235985038181));
#273469=CARTESIAN_POINT('Ctrl Pts',(-1.17232401053735,-1.56325698921119,
10.0275105179201));
#273470=CARTESIAN_POINT('Ctrl Pts',(-1.11749618379432,-1.60437369502478,
10.0314179266251));
#273471=CARTESIAN_POINT('Ctrl Pts',(-1.06044044645612,-1.64264911813421,
10.0353253353302));
#273472=CARTESIAN_POINT('Ctrl Pts',(-1.00148505280831,-1.67783899376595,
10.0392327440352));
#273473=CARTESIAN_POINT('Ctrl Pts',(-0.942566660237059,-1.71300678383093,
10.043137700406));
#273474=CARTESIAN_POINT('Ctrl Pts',(-0.881751397842195,-1.74509261627888,
10.0470426567768));
#273475=CARTESIAN_POINT('Ctrl Pts',(-0.819396331698406,-1.77389561462877,
10.0509476131476));
#273476=CARTESIAN_POINT('Ctrl Pts',(-0.757059007192297,-1.8026904177767,
10.0548514584568));
#273477=CARTESIAN_POINT('Ctrl Pts',(-0.69318319504812,-1.82820403486895,
10.058755303766));
#273478=CARTESIAN_POINT('Ctrl Pts',(-0.628148753351215,-1.85028244969878,
10.0626591490751));
#273479=CARTESIAN_POINT('Ctrl Pts',(-0.563110503970661,-1.87236215719165,
10.0665632229495));
#273480=CARTESIAN_POINT('Ctrl Pts',(-0.496913957008386,-1.89100610739543,
10.0704672968238));
#273481=CARTESIAN_POINT('Ctrl Pts',(-0.429955323980053,-1.90610976058075,
10.0743713706982));
#273482=CARTESIAN_POINT('Ctrl Pts',(-0.362925329929332,-1.9212295104527,
10.0782796053311));
#273483=CARTESIAN_POINT('Ctrl Pts',(-0.295132109727523,-1.93280132493636,
10.0821878399639));
#273484=CARTESIAN_POINT('Ctrl Pts',(-0.226982304187082,-1.94077176236309,
10.0860960745968));
#273485=CARTESIAN_POINT('Ctrl Pts',(-0.158791736573707,-1.94874696710425,
10.0900066468408));
#273486=CARTESIAN_POINT('Ctrl Pts',(-0.0902446501664814,-1.95311647649373,
10.0939172190848));
#273487=CARTESIAN_POINT('Ctrl Pts',(-0.0217502250042049,-1.95387894397587,
10.0978277913289));
#273488=CARTESIAN_POINT('Ctrl Pts',(0.0468626618756505,-1.9546427301523,
10.1017451269424));
#273489=CARTESIAN_POINT('Ctrl Pts',(0.115422214466668,-1.95178704391515,
10.1056624625559));
#273490=CARTESIAN_POINT('Ctrl Pts',(0.183522714763041,-1.94536254029063,
10.1095797981693));
#273491=CARTESIAN_POINT('Ctrl Pts',(0.215954501053342,-1.94230297203981,
10.1114453673045));
#273492=CARTESIAN_POINT('Ctrl Pts',(0.248282302472955,-1.93843475375679,
10.1133109364397));
#273493=CARTESIAN_POINT('Ctrl Pts',(0.280463230798123,-1.93376740487844,
10.1151765055749));
#273494=CARTESIAN_POINT('Ctrl Pts',(0.348047034276776,-1.92396541327105,
10.1190944241799));
#273495=CARTESIAN_POINT('Ctrl Pts',(0.415250500290206,-1.91059669162971,
10.1230123427848));
#273496=CARTESIAN_POINT('Ctrl Pts',(0.481668161728989,-1.89370319268269,
10.1269302613897));
#273497=CARTESIAN_POINT('Ctrl Pts',(0.547985728368301,-1.87683515309923,
10.1308422754917));
#273498=CARTESIAN_POINT('Ctrl Pts',(0.613519367818316,-1.85645299892549,
10.1347542895937));
#273499=CARTESIAN_POINT('Ctrl Pts',(0.677871328599324,-1.83265011987094,
10.1386663036957));
#273500=CARTESIAN_POINT('Ctrl Pts',(0.742147531390295,-1.80887526262416,
10.1425737124007));
#273501=CARTESIAN_POINT('Ctrl Pts',(0.805244359098048,-1.78168784806091,
10.1464811211057));
#273502=CARTESIAN_POINT('Ctrl Pts',(0.866778587305234,-1.75123124703425,
10.1503885298107));
#273503=CARTESIAN_POINT('Ctrl Pts',(0.928274195929873,-1.72079376091732,
10.1542934861815));
#273504=CARTESIAN_POINT('Ctrl Pts',(0.988208710551904,-1.68709137611959,
10.1581984425523));
#273505=CARTESIAN_POINT('Ctrl Pts',(1.046219741459,-1.650315197949,10.1621033989231));
#273506=CARTESIAN_POINT('Ctrl Pts',(1.10421426671942,-1.61354948355735,
10.1660072442323));
#273507=CARTESIAN_POINT('Ctrl Pts',(1.16028597941404,-1.57371197523036,
10.1699110895415));
#273508=CARTESIAN_POINT('Ctrl Pts',(1.21409950582571,-1.53103833719269,
10.1738149348507));
#273509=CARTESIAN_POINT('Ctrl Pts',(1.26791618295084,-1.48836220066785,
10.177719008725));
#273510=CARTESIAN_POINT('Ctrl Pts',(1.31947402743773,-1.44284991242812,
10.1816230825994));
#273511=CARTESIAN_POINT('Ctrl Pts',(1.36847037087042,-1.39477770417001,
10.1855271564737));
#273512=CARTESIAN_POINT('Ctrl Pts',(1.417518932053,-1.34665426305713,10.1894353911066));
#273513=CARTESIAN_POINT('Ctrl Pts',(1.46400019225624,-1.29596580238125,
10.1933436257395));
#273514=CARTESIAN_POINT('Ctrl Pts',(1.50764876301083,-1.24302502283418,
10.1972518603724));
#273515=CARTESIAN_POINT('Ctrl Pts',(1.55132344104799,-1.19005257810617,
10.2011624326164));
#273516=CARTESIAN_POINT('Ctrl Pts',(1.59216176513657,-1.13482552900091,
10.2050730048604));
#273517=CARTESIAN_POINT('Ctrl Pts',(1.62994074259063,-1.07768695623688,
10.2089835771044));
#273518=CARTESIAN_POINT('Ctrl Pts',(1.66778505912221,-1.02044956180305,
10.2129009127179));
#273519=CARTESIAN_POINT('Ctrl Pts',(1.70255921943757,-0.961294469294182,
10.2168182483314));
#273520=CARTESIAN_POINT('Ctrl Pts',(1.73408580198429,-0.900590046223309,
10.2207355839449));
#273521=CARTESIAN_POINT('Ctrl Pts',(1.74909983834462,-0.871680524746696,
10.2226011530801));
#273522=CARTESIAN_POINT('Ctrl Pts',(1.76337803026822,-0.842419918247882,
10.2244667222153));
#273523=CARTESIAN_POINT('Ctrl Pts',(1.77690512200243,-0.812849424802369,
10.2263322913505));
#273524=CARTESIAN_POINT('Ctrl Pts',(1.80531363465236,-0.750747847196636,
10.2302502099554));
#273525=CARTESIAN_POINT('Ctrl Pts',(1.83051900333678,-0.68703193119432,
10.2341681285603));
#273526=CARTESIAN_POINT('Ctrl Pts',(1.8523366304931,-0.62206511502693,10.2380860471652));
#273527=CARTESIAN_POINT('Ctrl Pts',(1.87412137737377,-0.557196207161326,
10.2419980612672));
#273528=CARTESIAN_POINT('Ctrl Pts',(1.8925283599387,-0.491080603094183,
10.2459100753692));
#273529=CARTESIAN_POINT('Ctrl Pts',(1.90742038369684,-0.424103147663155,
10.2498220894712));
#273530=CARTESIAN_POINT('Ctrl Pts',(1.92229487590236,-0.357204541071136,
10.2537294981762));
#273531=CARTESIAN_POINT('Ctrl Pts',(1.93366252106905,-0.289446576072365,
10.2576369068812));
#273532=CARTESIAN_POINT('Ctrl Pts',(1.94143599774202,-0.221228991480406,
10.2615443155862));
#273533=CARTESIAN_POINT('Ctrl Pts',(1.94920459569248,-0.153054221021664,
10.265449271957));
#273534=CARTESIAN_POINT('Ctrl Pts',(1.95338344422542,-0.0844208908608971,
10.2693542283278));
#273535=CARTESIAN_POINT('Ctrl Pts',(1.95393662721973,-0.0157371156567165,
10.2732591846986));
#273536=CARTESIAN_POINT('Ctrl Pts',(1.95448965281909,0.0529271172276451,
10.2771630300078));
#273537=CARTESIAN_POINT('Ctrl Pts',(1.95141905679734,0.121641274970306,
10.281066875317));
#273538=CARTESIAN_POINT('Ctrl Pts',(1.9447410116955,0.189995782662541,10.2849707206262));
#273539=CARTESIAN_POINT('Ctrl Pts',(1.93806257560263,0.258354292424093,
10.2888747945005));
#273540=CARTESIAN_POINT('Ctrl Pts',(1.92777632148089,0.326352620970326,
10.2927788683749));
#273541=CARTESIAN_POINT('Ctrl Pts',(1.91395024154316,0.393586677743139,
10.2966829422492));
#273542=CARTESIAN_POINT('Ctrl Pts',(1.90010942648983,0.460892389070508,
10.3005911768821));
#273543=CARTESIAN_POINT('Ctrl Pts',(1.88272135598796,0.527431720296417,
10.304499411515));
#273544=CARTESIAN_POINT('Ctrl Pts',(1.86190487862007,0.59281213126147,10.3084076461479));
#273545=CARTESIAN_POINT('Ctrl Pts',(1.84107595040562,0.658231647856704,
10.3123182183919));
#273546=CARTESIAN_POINT('Ctrl Pts',(1.81681470801753,0.722490404341941,
10.3162287906359));
#273547=CARTESIAN_POINT('Ctrl Pts',(1.78928851404671,0.785215011000507,
10.3201393628799));
#273548=CARTESIAN_POINT('Ctrl Pts',(1.76171471327864,0.848048100424074,
10.3240566984934));
#273549=CARTESIAN_POINT('Ctrl Pts',(1.73086491185874,0.909341305167467,
10.3279740341069));
#273550=CARTESIAN_POINT('Ctrl Pts',(1.69695242853623,0.96874581562193,10.3318913697204));
#273551=CARTESIAN_POINT('Ctrl Pts',(1.68080214466305,0.99703627427289,10.3337569388556));
#273552=CARTESIAN_POINT('Ctrl Pts',(1.66395788216242,1.02489880606965,10.3356225079908));
#273553=CARTESIAN_POINT('Ctrl Pts',(1.64644598563396,1.05229825448387,10.337488077126));
#273554=CARTESIAN_POINT('Ctrl Pts',(1.60966890569531,1.10984037751821,10.341405995731));
#273555=CARTESIAN_POINT('Ctrl Pts',(1.56979861387346,1.16556638933122,10.3453239143359));
#273556=CARTESIAN_POINT('Ctrl Pts',(1.52704039622133,1.21912412342149,10.3492418329408));
#273557=CARTESIAN_POINT('Ctrl Pts',(1.48434661738156,1.27260114327792,10.3531538470428));
#273558=CARTESIAN_POINT('Ctrl Pts',(1.43877385480222,1.32391598927017,10.3570658611448));
#273559=CARTESIAN_POINT('Ctrl Pts',(1.39057108368565,1.37274471815313,10.3609778752468));
#273560=CARTESIAN_POINT('Ctrl Pts',(1.34242505901485,1.421515963685,10.3648852839518));
#273561=CARTESIAN_POINT('Ctrl Pts',(1.29165551877425,1.4678065562625,10.3687926926568));
#273562=CARTESIAN_POINT('Ctrl Pts',(1.23855099435898,1.51132638247745,10.3727001013618));
#273563=CARTESIAN_POINT('Ctrl Pts',(1.18547979894815,1.55481889515374,10.3766050577326));
#273564=CARTESIAN_POINT('Ctrl Pts',(1.13007690599375,1.59554377988425,10.3805100141034));
#273565=CARTESIAN_POINT('Ctrl Pts',(1.07266575709322,1.63324957479242,10.3844149704742));
#273566=CARTESIAN_POINT('Ctrl Pts',(1.01527094315726,1.67094464142158,10.3883188157834));
#273567=CARTESIAN_POINT('Ctrl Pts',(0.955869418588534,1.70562205356739,
10.3922226610926));
#273568=CARTESIAN_POINT('Ctrl Pts',(0.894814094910756,1.73707332474742,
10.3961265064018));
#273569=CARTESIAN_POINT('Ctrl Pts',(0.833755196521393,1.76852643735938,
10.4000305802762));
#273570=CARTESIAN_POINT('Ctrl Pts',(0.771042745283283,1.79675281099617,
10.4039346541505));
#273571=CARTESIAN_POINT('Ctrl Pts',(0.707053141642332,1.82159047397973,
10.4078387280249));
#273572=CARTESIAN_POINT('Ctrl Pts',(0.642995341216151,1.84645460765028,
10.4117469626578));
#273573=CARTESIAN_POINT('Ctrl Pts',(0.577658131479498,1.86792264481257,
10.4156551972906));
#273574=CARTESIAN_POINT('Ctrl Pts',(0.511435782531989,1.88588160825273,
10.4195634319235));
#273575=CARTESIAN_POINT('Ctrl Pts',(0.445173824370667,1.90385131339012,
10.4234740041675));
#273576=CARTESIAN_POINT('Ctrl Pts',(0.378026154340807,1.91830766413244,
10.4273845764115));
#273577=CARTESIAN_POINT('Ctrl Pts',(0.310397256258584,1.92918883039145,
10.4312951486555));
#273578=CARTESIAN_POINT('Ctrl Pts',(0.242651393395549,1.9400888157243,10.435212484269));
#273579=CARTESIAN_POINT('Ctrl Pts',(0.174423130244239,1.94740122317494,
10.4391298198825));
#273580=CARTESIAN_POINT('Ctrl Pts',(0.106121215206654,1.95111616457941,
10.443047155496));
#273581=CARTESIAN_POINT('Ctrl Pts',(0.0735935083316315,1.95288534667329,
10.4449127246312));
#273582=CARTESIAN_POINT('Ctrl Pts',(0.0410490824634399,1.95383939184425,
10.4467782937664));
#273583=CARTESIAN_POINT('Ctrl Pts',(0.00853176193233716,1.95398137376955,
10.4486438629016));
#273584=CARTESIAN_POINT('Ctrl Pts',(-0.0597585054663083,1.95427955281647,
10.4525617815065));
#273585=CARTESIAN_POINT('Ctrl Pts',(-0.128199965837453,1.95099396842147,
10.4564797001114));
#273586=CARTESIAN_POINT('Ctrl Pts',(-0.196385405575358,1.94410616286174,
10.4603976187163));
#273587=CARTESIAN_POINT('Ctrl Pts',(-0.264468086381559,1.93722873757592,
10.4643096328183));
#273588=CARTESIAN_POINT('Ctrl Pts',(-0.332295026796115,1.92675991422756,
10.4682216469203));
#273589=CARTESIAN_POINT('Ctrl Pts',(-0.399459038952325,1.91273324752807,
10.4721336610223));
#273590=CARTESIAN_POINT('Ctrl Pts',(-0.466543982646745,1.89872309364437,
10.4760410697273));
#273591=CARTESIAN_POINT('Ctrl Pts',(-0.532967068755224,1.88116351479865,
10.4799484784323));
#273592=CARTESIAN_POINT('Ctrl Pts',(-0.59832808697045,1.86013964538749,
10.4838558871373));
#273593=CARTESIAN_POINT('Ctrl Pts',(-0.663648083866068,1.83912897079626,
10.4877608435081));
#273594=CARTESIAN_POINT('Ctrl Pts',(-0.727906867860279,1.81465846888872,
10.4916657998789));
#273595=CARTESIAN_POINT('Ctrl Pts',(-0.79071777670186,1.7868635643517,10.4955707562498));
#273596=CARTESIAN_POINT('Ctrl Pts',(-0.853510814206847,1.75907656818766,
10.4994746015589));
#273597=CARTESIAN_POINT('Ctrl Pts',(-0.914856344709965,1.72796724608777,
10.5033784468681));
#273598=CARTESIAN_POINT('Ctrl Pts',(-0.974387836881763,1.6937190863118,
10.5072822921773));
#273599=CARTESIAN_POINT('Ctrl Pts',(-1.03392281454644,1.65946892134979,
10.5111863660517));
#273600=CARTESIAN_POINT('Ctrl Pts',(-1.09164311788173,1.62207980138402,
10.515090439926));
#273601=CARTESIAN_POINT('Ctrl Pts',(-1.14720856340261,1.58178017184934,
10.5189945138004));
#273602=CARTESIAN_POINT('Ctrl Pts',(-1.20283322768021,1.54143759306922,
10.5229027484332));
#273603=CARTESIAN_POINT('Ctrl Pts',(-1.25629805194379,1.49817860368856,
10.5268109830661));
#273604=CARTESIAN_POINT('Ctrl Pts',(-1.30729433089059,1.45227322925865,
10.530719217699));
#273605=CARTESIAN_POINT('Ctrl Pts',(-1.35832111196475,1.40634039769643,
10.534629789943));
#273606=CARTESIAN_POINT('Ctrl Pts',(-1.40687606141522,1.35775837889213,
10.538540362187));
#273607=CARTESIAN_POINT('Ctrl Pts',(-1.45268791200197,1.30683351285593,
10.5424509344311));
#273608=CARTESIAN_POINT('Ctrl Pts',(-1.49857899459168,1.25582057181108,
10.5463682700446));
#273609=CARTESIAN_POINT('Ctrl Pts',(-1.54171720044315,1.20245707875382,
10.5502856056581));
#273610=CARTESIAN_POINT('Ctrl Pts',(-1.58187259387785,1.14708112038258,
10.5542029412716));
#273611=CARTESIAN_POINT('Ctrl Pts',(-1.60099596496339,1.12070919595175,
10.5560685104068));
#273612=CARTESIAN_POINT('Ctrl Pts',(-1.61944348781101,1.09388124861885,
10.557934079542));
#273613=CARTESIAN_POINT('Ctrl Pts',(-1.63719398309528,1.06663576806547,
10.5597996486772));
#273614=CARTESIAN_POINT('Ctrl Pts',(-1.67525271209658,1.00821889888604,
10.5637996041157));
#273615=CARTESIAN_POINT('Ctrl Pts',(-1.71025039317968,0.947656606513882,
10.5677995595543));
#273616=CARTESIAN_POINT('Ctrl Pts',(-1.74194395780078,0.885295006131485,
10.5717995149929));
#273617=CARTESIAN_POINT('Ctrl Pts',(-1.77358357467427,0.823039555622688,
10.5757926618383));
#273618=CARTESIAN_POINT('Ctrl Pts',(-1.80193003757505,0.758991291439256,
10.5797858086838));
#273619=CARTESIAN_POINT('Ctrl Pts',(-1.82678404858984,0.693524361372909,
10.5837789555292));
#273620=CARTESIAN_POINT('Ctrl Pts',(-1.85159550625389,0.628169519340802,
10.5877652655796));
#273621=CARTESIAN_POINT('Ctrl Pts',(-1.87292624176117,0.561401274733641,
10.5917515756301));
#273622=CARTESIAN_POINT('Ctrl Pts',(-1.89062411321434,0.493615703288001,
10.5957378856805));
#273623=CARTESIAN_POINT('Ctrl Pts',(-1.90830416947359,0.425898366776875,
10.5997201829949));
#273624=CARTESIAN_POINT('Ctrl Pts',(-1.92235850832266,0.357166185273823,
10.6037024803093));
#273625=CARTESIAN_POINT('Ctrl Pts',(-1.93268440510735,0.287831531029609,
10.6076847776237));
#273626=CARTESIAN_POINT('Ctrl Pts',(-1.9430020556683,0.218552247188954,
10.6116638946899));
#273627=CARTESIAN_POINT('Ctrl Pts',(-1.94959711577114,0.148671905876252,
10.6156430117561));
#273628=CARTESIAN_POINT('Ctrl Pts',(-1.95241799906493,0.0786127020736065,
10.6196221288223));
#273629=CARTESIAN_POINT('Ctrl Pts',(-1.95348331470874,0.0521546185476659,
10.6211248551734));
#273630=CARTESIAN_POINT('Ctrl Pts',(-1.95401087610628,0.0256711001595666,
10.6226275815246));
#273631=CARTESIAN_POINT('Ctrl Pts',(-1.95399983006838,-0.000814918850473378,
10.6241303078758));
#273632=CARTESIAN_POINT('',(-1.95399956009588,-0.00131116173880527,11.3241303078758));
#273633=CARTESIAN_POINT('Ctrl Pts',(-1.95399983006808,-0.000814919564467043,
10.6241303079163));
#273634=CARTESIAN_POINT('Ctrl Pts',(-1.9539685147891,-0.0759021459440577,
10.6283905009516));
#273635=CARTESIAN_POINT('Ctrl Pts',(-1.94960488516428,-0.150851560010165,
10.6326506939869));
#273636=CARTESIAN_POINT('Ctrl Pts',(-1.94098145165923,-0.225182158073955,
10.6369108870221));
#273637=CARTESIAN_POINT('Ctrl Pts',(-1.93233214265287,-0.299735792760608,
10.6411838632058));
#273638=CARTESIAN_POINT('Ctrl Pts',(-1.91939756216364,-0.373666572052315,
10.6454568393895));
#273639=CARTESIAN_POINT('Ctrl Pts',(-1.90230107844747,-0.446504878962826,
10.6497298155732));
#273640=CARTESIAN_POINT('Ctrl Pts',(-1.88512890787792,-0.519665644125383,
10.6540217084024));
#273641=CARTESIAN_POINT('Ctrl Pts',(-1.86375805156586,-0.591723931865959,
10.6583136012317));
#273642=CARTESIAN_POINT('Ctrl Pts',(-1.83836197564382,-0.66222446836925,
10.6626054940609));
#273643=CARTESIAN_POINT('Ctrl Pts',(-1.82189249635873,-0.707944410658504,
10.6653888075248));
#273644=CARTESIAN_POINT('Ctrl Pts',(-1.80373115748422,-0.753009659755936,
10.6681721209887));
#273645=CARTESIAN_POINT('Ctrl Pts',(-1.78393560091633,-0.797301556365778,
10.6709554344526));
#273646=CARTESIAN_POINT('Ctrl Pts',(-1.75607047527468,-0.859648844238558,
10.6748733530575));
#273647=CARTESIAN_POINT('Ctrl Pts',(-1.7248776172163,-0.920657320442244,
10.6787912716625));
#273648=CARTESIAN_POINT('Ctrl Pts',(-1.6905079878465,-0.979948336917393,
10.6827091902674));
#273649=CARTESIAN_POINT('Ctrl Pts',(-1.65619015525919,-1.03914999881003,
10.6866212043694));
#273650=CARTESIAN_POINT('Ctrl Pts',(-1.61870529764365,-1.09663891563633,
10.6905332184714));
#273651=CARTESIAN_POINT('Ctrl Pts',(-1.5782517579668,-1.15205789284858,
10.6944452325734));
#273652=CARTESIAN_POINT('Ctrl Pts',(-1.53784584199584,-1.20741162837635,
10.6983526412784));
#273653=CARTESIAN_POINT('Ctrl Pts',(-1.49447847345894,-1.26069986838858,
10.7022600499834));
#273654=CARTESIAN_POINT('Ctrl Pts',(-1.44839211859912,-1.31159302787868,
10.7061674586884));
#273655=CARTESIAN_POINT('Ctrl Pts',(-1.40233468806056,-1.36245424624218,
10.7100724150592));
#273656=CARTESIAN_POINT('Ctrl Pts',(-1.35356198573122,-1.41092300207031,
10.71397737143));
#273657=CARTESIAN_POINT('Ctrl Pts',(-1.30235671910202,-1.45670277552074,
10.7178823278009));
#273658=CARTESIAN_POINT('Ctrl Pts',(-1.25116602170253,-1.50246952343533,
10.7217861731101));
#273659=CARTESIAN_POINT('Ctrl Pts',(-1.19754450055124,-1.54554848005739,
10.7256900184192));
#273660=CARTESIAN_POINT('Ctrl Pts',(-1.1418103631971,-1.58568127140851,
10.7295938637284));
#273661=CARTESIAN_POINT('Ctrl Pts',(-1.08607296268026,-1.6258164124834,
10.7334979376028));
#273662=CARTESIAN_POINT('Ctrl Pts',(-1.02822310109709,-1.66300476044023,
10.7374020114772));
#273663=CARTESIAN_POINT('Ctrl Pts',(-0.968609094096294,-1.69703047198156,
10.7413060853515));
#273664=CARTESIAN_POINT('Ctrl Pts',(-0.908931553592955,-1.73109244635338,
10.7452143199844));
#273665=CARTESIAN_POINT('Ctrl Pts',(-0.847486543551229,-1.76198481331922,
10.7491225546173));
#273666=CARTESIAN_POINT('Ctrl Pts',(-0.784647296834283,-1.78953754349291,
10.7530307892502));
#273667=CARTESIAN_POINT('Ctrl Pts',(-0.721770464420032,-1.81710675363144,
10.7569413614942));
#273668=CARTESIAN_POINT('Ctrl Pts',(-0.657498196058105,-1.84133217802094,
10.7608519337382));
#273669=CARTESIAN_POINT('Ctrl Pts',(-0.592221388308868,-1.86209286213914,
10.7647625059822));
#273670=CARTESIAN_POINT('Ctrl Pts',(-0.52683168374006,-1.88288945204516,
10.7686798415957));
#273671=CARTESIAN_POINT('Ctrl Pts',(-0.460434448035369,-1.90020921780993,
10.7725971772092));
#273672=CARTESIAN_POINT('Ctrl Pts',(-0.393432475219139,-1.91398194543286,
10.7765145128228));
#273673=CARTESIAN_POINT('Ctrl Pts',(-0.361523845269081,-1.92054098915428,
10.7783800819579));
#273674=CARTESIAN_POINT('Ctrl Pts',(-0.329478159965262,-1.9262963267367,
10.7802456510931));
#273675=CARTESIAN_POINT('Ctrl Pts',(-0.29733921643378,-1.93124451853476,
10.7821112202283));
#273676=CARTESIAN_POINT('Ctrl Pts',(-0.229843586048967,-1.94163631390749,
10.7860291388332));
#273677=CARTESIAN_POINT('Ctrl Pts',(-0.161668555654476,-1.948506087794,
10.7899470574381));
#273678=CARTESIAN_POINT('Ctrl Pts',(-0.0932141343151712,-1.95177537774301,
10.793864976043));
#273679=CARTESIAN_POINT('Ctrl Pts',(-0.0248628772764009,-1.95503974070551,
10.797776990145));
#273680=CARTESIAN_POINT('Ctrl Pts',(0.0437664476449764,-1.95471436531483,
10.801689004247));
#273681=CARTESIAN_POINT('Ctrl Pts',(0.112266166666696,-1.95077223371207,
10.805601018349));
#273682=CARTESIAN_POINT('Ctrl Pts',(0.180685244773023,-1.94683474296193,
10.809508427054));
#273683=CARTESIAN_POINT('Ctrl Pts',(0.248974531204067,-1.93928898016744,
10.813415835759));
#273684=CARTESIAN_POINT('Ctrl Pts',(0.316725626858963,-1.92815997191384,
10.817323244464));
#273685=CARTESIAN_POINT('Ctrl Pts',(0.384434201154495,-1.9170379483526,
10.8212282008348));
#273686=CARTESIAN_POINT('Ctrl Pts',(0.451604770365875,-1.90233721994039,
10.8251331572056));
#273687=CARTESIAN_POINT('Ctrl Pts',(0.517834898997069,-1.88413455394796,
10.8290381135764));
#273688=CARTESIAN_POINT('Ctrl Pts',(0.584046183434645,-1.8659370670873,
10.8329419588856));
#273689=CARTESIAN_POINT('Ctrl Pts',(0.649317084352055,-1.84423975094801,
10.8368458041948));
#273690=CARTESIAN_POINT('Ctrl Pts',(0.713257969600139,-1.81916988453577,
10.840749649504));
#273691=CARTESIAN_POINT('Ctrl Pts',(0.777202598505579,-1.7940985503148,
10.8446537233783));
#273692=CARTESIAN_POINT('Ctrl Pts',(0.839816600080803,-1.76565445574872,
10.8485577972527));
#273693=CARTESIAN_POINT('Ctrl Pts',(0.900729753407535,-1.73401323850956,
10.852461871127));
#273694=CARTESIAN_POINT('Ctrl Pts',(0.961707824799248,-1.7023382997097,
10.8563701057599));
#273695=CARTESIAN_POINT('Ctrl Pts',(1.02098099298303,-1.66745966542983,
10.8602783403928));
#273696=CARTESIAN_POINT('Ctrl Pts',(1.07820402153073,-1.62959875059935,
10.8641865750256));
#273697=CARTESIAN_POINT('Ctrl Pts',(1.13546127657767,-1.59171519022554,
10.8680971472696));
#273698=CARTESIAN_POINT('Ctrl Pts',(1.19066555611156,-1.55084609201704,
10.8720077195137));
#273699=CARTESIAN_POINT('Ctrl Pts',(1.2435032811134,-1.50725432155964,10.8759182917577));
#273700=CARTESIAN_POINT('Ctrl Pts',(1.29643238943057,-1.46358715874752,
10.8798356273712));
#273701=CARTESIAN_POINT('Ctrl Pts',(1.34698641197762,-1.41718825790193,
10.8837529629847));
#273702=CARTESIAN_POINT('Ctrl Pts',(1.39488795320832,-1.36835799336076,
10.8876702985982));
#273703=CARTESIAN_POINT('Ctrl Pts',(1.41770030468006,-1.34510335209972,
10.8895358677334));
#273704=CARTESIAN_POINT('Ctrl Pts',(1.4399116600572,-1.32129777398009,10.8914014368686));
#273705=CARTESIAN_POINT('Ctrl Pts',(1.46149538198817,-1.29697619424076,
10.8932670060037));
#273706=CARTESIAN_POINT('Ctrl Pts',(1.50682378291525,-1.24589796402959,
10.8971849246087));
#273707=CARTESIAN_POINT('Ctrl Pts',(1.54956120552918,-1.19233919937936,
10.9011028432136));
#273708=CARTESIAN_POINT('Ctrl Pts',(1.5894248336085,-1.13659346219684,10.9050207618185));
#273709=CARTESIAN_POINT('Ctrl Pts',(1.62922838516937,-1.08093173668033,
10.9089327759205));
#273710=CARTESIAN_POINT('Ctrl Pts',(1.66616645372537,-1.02308997668234,
10.9128447900225));
#273711=CARTESIAN_POINT('Ctrl Pts',(1.69999529315344,-0.963396078078033,
10.9167568041245));
#273712=CARTESIAN_POINT('Ctrl Pts',(1.73378430776737,-0.903772453785764,
10.9206642128295));
#273713=CARTESIAN_POINT('Ctrl Pts',(1.76447112129018,-0.842301447179175,
10.9245716215345));
#273714=CARTESIAN_POINT('Ctrl Pts',(1.79185532432582,-0.779339782562925,
10.9284790302395));
#273715=CARTESIAN_POINT('Ctrl Pts',(1.8192223407237,-0.716417633404564,
10.9323839866103));
#273716=CARTESIAN_POINT('Ctrl Pts',(1.84329066253446,-0.652007132170347,
10.9362889429811));
#273717=CARTESIAN_POINT('Ctrl Pts',(1.8639065886548,-0.586488046569769,
10.940193899352));
#273718=CARTESIAN_POINT('Ctrl Pts',(1.88451664900813,-0.520987602852581,
10.9440977446611));
#273719=CARTESIAN_POINT('Ctrl Pts',(1.90167611609606,-0.454379669965605,
10.9480015899703));
#273720=CARTESIAN_POINT('Ctrl Pts',(1.91528067306263,-0.387060645626431,
10.9519054352795));
#273721=CARTESIAN_POINT('Ctrl Pts',(1.92888602655869,-0.319737679844125,
10.9558095091539));
#273722=CARTESIAN_POINT('Ctrl Pts',(1.93893596177339,-0.251704022650568,
10.9597135830282));
#273723=CARTESIAN_POINT('Ctrl Pts',(1.94537731985309,-0.183365982126458,
10.9636176569026));
#273724=CARTESIAN_POINT('Ctrl Pts',(1.95182554279661,-0.114955110479479,
10.9675258915355));
#273725=CARTESIAN_POINT('Ctrl Pts',(1.95465746721037,-0.0462396988173985,
10.9714341261683));
#273726=CARTESIAN_POINT('Ctrl Pts',(1.95387194510453,0.0223701169744634,
10.9753423608012));
#273727=CARTESIAN_POINT('Ctrl Pts',(1.95308595315862,0.091020969982767,
10.9792529330452));
#273728=CARTESIAN_POINT('Ctrl Pts',(1.94867824014254,0.159565610423876,
10.9831635052893));
#273729=CARTESIAN_POINT('Ctrl Pts',(1.94069965165146,0.227598027407773,
10.9870740775333));
#273730=CARTESIAN_POINT('Ctrl Pts',(1.93270726412062,0.295748107061931,
10.9909914131468));
#273731=CARTESIAN_POINT('Ctrl Pts',(1.92113175793174,0.363383710495605,
10.9949087487603));
#273732=CARTESIAN_POINT('Ctrl Pts',(1.90607511418001,0.430108892146699,
10.9988260843738));
#273733=CARTESIAN_POINT('Ctrl Pts',(1.8989046257067,0.461885704681965,11.000691653509));
#273734=CARTESIAN_POINT('Ctrl Pts',(1.89094535045098,0.493456257333144,
11.0025572226442));
#273735=CARTESIAN_POINT('Ctrl Pts',(1.8822121994957,0.524779226027066,11.0044227917794));
#273736=CARTESIAN_POINT('Ctrl Pts',(1.86387153660521,0.590561211531077,
11.0083407103843));
#273737=CARTESIAN_POINT('Ctrl Pts',(1.84204176826305,0.655511113583888,
11.0122586289892));
#273738=CARTESIAN_POINT('Ctrl Pts',(1.8168162123231,0.719232125700695,11.0161765475941));
#273739=CARTESIAN_POINT('Ctrl Pts',(1.79162867258112,0.782857107005847,
11.0200885616961));
#273740=CARTESIAN_POINT('Ctrl Pts',(1.76305568148216,0.84525642020697,11.0240005757981));
#273741=CARTESIAN_POINT('Ctrl Pts',(1.73124058994447,0.906047471012826,
11.0279125899001));
#273742=CARTESIAN_POINT('Ctrl Pts',(1.69946295254735,0.966766955890282,
11.0318199986051));
#273743=CARTESIAN_POINT('Ctrl Pts',(1.66445102182194,1.02588150472803,11.0357274073101));
#273744=CARTESIAN_POINT('Ctrl Pts',(1.62639586916403,1.08302930558973,11.0396348160151));
#273745=CARTESIAN_POINT('Ctrl Pts',(1.5883646003534,1.14014123984066,11.0435397723859));
#273746=CARTESIAN_POINT('Ctrl Pts',(1.54729417039366,1.19528846612587,11.0474447287567));
#273747=CARTESIAN_POINT('Ctrl Pts',(1.50342033842383,1.24813592449444,11.0513496851275));
#273748=CARTESIAN_POINT('Ctrl Pts',(1.45955898969995,1.30096834638702,11.0552535304367));
#273749=CARTESIAN_POINT('Ctrl Pts',(1.41289613648942,1.35150192101288,11.0591573757459));
#273750=CARTESIAN_POINT('Ctrl Pts',(1.36370828778775,1.39943406626358,11.0630612210551));
#273751=CARTESIAN_POINT('Ctrl Pts',(1.31451755920018,1.44736901788033,11.0669652949294));
#273752=CARTESIAN_POINT('Ctrl Pts',(1.26280189572413,1.49270189623786,11.0708693688038));
#273753=CARTESIAN_POINT('Ctrl Pts',(1.2088738718207,1.53516773091061,11.0747734426781));
#273754=CARTESIAN_POINT('Ctrl Pts',(1.15488837423927,1.5776788234573,11.078681677311));
#273755=CARTESIAN_POINT('Ctrl Pts',(1.0986861979647,1.61731646942391,11.0825899119438));
#273756=CARTESIAN_POINT('Ctrl Pts',(1.04061133452346,1.65385732469923,11.0864981465767));
#273757=CARTESIAN_POINT('Ctrl Pts',(0.982501735079602,1.69042003595783,
11.0904087188207));
#273758=CARTESIAN_POINT('Ctrl Pts',(0.922517648943269,1.72388203048328,
11.0943192910648));
#273759=CARTESIAN_POINT('Ctrl Pts',(0.861027793049799,1.75406588804292,
11.0982298633088));
#273760=CARTESIAN_POINT('Ctrl Pts',(0.799431589903674,1.78430194885266,
11.1021471989223));
#273761=CARTESIAN_POINT('Ctrl Pts',(0.736324871501352,1.8112483639733,11.1060645345358));
#273762=CARTESIAN_POINT('Ctrl Pts',(0.672095623599954,1.83477613695453,
11.1099818701493));
#273763=CARTESIAN_POINT('Ctrl Pts',(0.641507460040964,1.84598086675665,
11.1118474392844));
#273764=CARTESIAN_POINT('Ctrl Pts',(0.610664917406567,1.85641098761622,
11.1137130084196));
#273765=CARTESIAN_POINT('Ctrl Pts',(0.579610802906014,1.86605662217272,
11.1155785775548));
#273766=CARTESIAN_POINT('Ctrl Pts',(0.514393443406147,1.88631360990501,
11.1194964961597));
#273767=CARTESIAN_POINT('Ctrl Pts',(0.447983410876055,1.90318773630915,
11.1234144147647));
#273768=CARTESIAN_POINT('Ctrl Pts',(0.380764717166862,1.91654225890295,
11.1273323333696));
#273769=CARTESIAN_POINT('Ctrl Pts',(0.313647325453663,1.92987665555084,
11.1312443474716));
#273770=CARTESIAN_POINT('Ctrl Pts',(0.245724169844897,1.9397018802542,11.1351563615736));
#273771=CARTESIAN_POINT('Ctrl Pts',(0.17739444888597,1.94593093646831,11.1390683756756));
#273772=CARTESIAN_POINT('Ctrl Pts',(0.109145168713203,1.95215265956044,
11.1429757843806));
#273773=CARTESIAN_POINT('Ctrl Pts',(0.0404907613303627,1.95478657761763,
11.1468831930856));
#273774=CARTESIAN_POINT('Ctrl Pts',(-0.0281611624639135,1.95379705929983,
11.1507906017906));
#273775=CARTESIAN_POINT('Ctrl Pts',(-0.096769999528806,1.95280816201501,
11.1546955581614));
#273776=CARTESIAN_POINT('Ctrl Pts',(-0.165375865315554,1.94820034651441,
11.1586005145322));
#273777=CARTESIAN_POINT('Ctrl Pts',(-0.233569397092006,1.93999003521721,
11.162505470903));
#273778=CARTESIAN_POINT('Ctrl Pts',(-0.301743526035585,1.93178205996705,
11.1664093162122));
#273779=CARTESIAN_POINT('Ctrl Pts',(-0.369505065683895,1.91997368248687,
11.1703131615214));
#273780=CARTESIAN_POINT('Ctrl Pts',(-0.43644984764403,1.90463317478498,
11.1742170068306));
#273781=CARTESIAN_POINT('Ctrl Pts',(-0.503398549135946,1.88929176891589,
11.178121080705));
#273782=CARTESIAN_POINT('Ctrl Pts',(-0.569529919061022,1.8704179346261,
11.1820251545793));
#273783=CARTESIAN_POINT('Ctrl Pts',(-0.634451836961836,1.84813064110083,
11.1859292284537));
#273784=CARTESIAN_POINT('Ctrl Pts',(-0.699442945259962,1.82581959493941,
11.1898374630866));
#273785=CARTESIAN_POINT('Ctrl Pts',(-0.763221562947385,1.80008798943833,
11.1937456977194));
#273786=CARTESIAN_POINT('Ctrl Pts',(-0.82541351117599,1.77110376194285,
11.1976539323523));
#273787=CARTESIAN_POINT('Ctrl Pts',(-0.887642657936773,1.74210219826882,
11.2015645045963));
#273788=CARTESIAN_POINT('Ctrl Pts',(-0.948282812127677,1.709844371824,11.2054750768404));
#273789=CARTESIAN_POINT('Ctrl Pts',(-1.00698497578881,1.67454389567297,
11.2093856490844));
#273790=CARTESIAN_POINT('Ctrl Pts',(-1.06578866536411,1.63918236703447,
11.2133029846979));
#273791=CARTESIAN_POINT('Ctrl Pts',(-1.12264726733472,1.6007679611778,11.2172203203114));
#273792=CARTESIAN_POINT('Ctrl Pts',(-1.17724202376935,1.55955673749673,
11.2211376559249));
#273793=CARTESIAN_POINT('Ctrl Pts',(-1.20324191313156,1.53993054395428,
11.2230032250601));
#273794=CARTESIAN_POINT('Ctrl Pts',(-1.22872886914824,1.51967060984118,
11.2248687941952));
#273795=CARTESIAN_POINT('Ctrl Pts',(-1.25367138196224,1.49880754803573,
11.2267343633304));
#273796=CARTESIAN_POINT('Ctrl Pts',(-1.3079287206718,1.45342422120985,11.2307925276864));
#273797=CARTESIAN_POINT('Ctrl Pts',(-1.35984680323557,1.40498323572559,
11.2348506920425));
#273798=CARTESIAN_POINT('Ctrl Pts',(-1.40905733704925,1.35376269002646,
11.2389088563985));
#273799=CARTESIAN_POINT('Ctrl Pts',(-1.45582513564135,1.30508465344787,
11.2427655797167));
#273800=CARTESIAN_POINT('Ctrl Pts',(-1.50014735042896,1.25389683588597,
11.2466223030348));
#273801=CARTESIAN_POINT('Ctrl Pts',(-1.54174049822195,1.20048000239168,
11.250479026353));
#273802=CARTESIAN_POINT('Ctrl Pts',(-1.58329453093444,1.14711340322331,
11.2543321227265));
#273803=CARTESIAN_POINT('Ctrl Pts',(-1.62212427238269,1.09152233964788,
11.2581852191001));
#273804=CARTESIAN_POINT('Ctrl Pts',(-1.65798463175839,1.03402270809348,
11.2620383154736));
#273805=CARTESIAN_POINT('Ctrl Pts',(-1.69382437880148,0.976556127003494,
11.2658891971091));
#273806=CARTESIAN_POINT('Ctrl Pts',(-1.72669786015049,0.917183582291981,
11.2697400787445));
#273807=CARTESIAN_POINT('Ctrl Pts',(-1.75640286533857,0.856250532630753,
11.2735909603799));
#273808=CARTESIAN_POINT('Ctrl Pts',(-1.78610165457326,0.795330233581561,
11.2774410361949));
#273809=CARTESIAN_POINT('Ctrl Pts',(-1.81263306292323,0.732850533811338,
11.2812911120099));
#273810=CARTESIAN_POINT('Ctrl Pts',(-1.83584141958589,0.669180306145414,
11.2851411878249));
#273811=CARTESIAN_POINT('Ctrl Pts',(-1.85906597067962,0.605465650382825,
11.2889939501631));
#273812=CARTESIAN_POINT('Ctrl Pts',(-1.87896266653266,0.540559285055208,
11.2928467125012));
#273813=CARTESIAN_POINT('Ctrl Pts',(-1.89542497282366,0.474847525418879,
11.2966994748393));
#273814=CARTESIAN_POINT('Ctrl Pts',(-1.91189397277362,0.409109047040911,
11.3005538037306));
#273815=CARTESIAN_POINT('Ctrl Pts',(-1.92492570561245,0.342565020072114,
11.3044081326218));
#273816=CARTESIAN_POINT('Ctrl Pts',(-1.93446485725264,0.275611531062305,
11.3082624615131));
#273817=CARTESIAN_POINT('Ctrl Pts',(-1.94401756415766,0.20856290022976,
11.3121222674584));
#273818=CARTESIAN_POINT('Ctrl Pts',(-1.95006774392593,0.141104150990945,
11.3159820734036));
#273819=CARTESIAN_POINT('Ctrl Pts',(-1.95261207530983,0.0736347971697302,
11.3198418793489));
#273820=CARTESIAN_POINT('Ctrl Pts',(-1.95355436648917,0.0486475736564669,
11.3212713555245));
#273821=CARTESIAN_POINT('Ctrl Pts',(-1.9540163153482,0.0236588741376556,
11.3227008317002));
#273822=CARTESIAN_POINT('Ctrl Pts',(-1.95399956009588,-0.00131116173880527,
11.3241303078758));
#273823=CARTESIAN_POINT('',(-1.95399932181806,0.00162798481247529,12.0241303078758));
#273824=CARTESIAN_POINT('Ctrl Pts',(-1.95604828032066,-0.00131253645946981,
11.3241303078758));
#273825=CARTESIAN_POINT('Ctrl Pts',(-1.95666788006178,-0.0815157866439698,
11.3287169216192));
#273826=CARTESIAN_POINT('Ctrl Pts',(-1.91576572910727,-0.80898595490767,
11.3703554639544));
#273827=CARTESIAN_POINT('Ctrl Pts',(-1.00369601420896,-2.08016482602406,
11.4490459348816));
#273828=CARTESIAN_POINT('Ctrl Pts',(1.20363141497037,-1.97123382916792,
11.560201720657));
#273829=CARTESIAN_POINT('Ctrl Pts',(2.3089364786395,-0.057478082500643,
11.6713575064327));
#273830=CARTESIAN_POINT('Ctrl Pts',(1.3002225757448,1.90890351927077,11.7825132922081));
#273831=CARTESIAN_POINT('Ctrl Pts',(-0.89895074918647,2.12752883479819,
11.8936690779838));
#273832=CARTESIAN_POINT('Ctrl Pts',(-1.89602525605444,0.874547554056413,
11.9742080832062));
#273833=CARTESIAN_POINT('Ctrl Pts',(-1.95616528042983,0.114289761396843,
12.0176951598369));
#273834=CARTESIAN_POINT('Ctrl Pts',(-1.95515771590482,0.00162894993460125,
12.0241303078758));
#273835=CARTESIAN_POINT('',(-1.95370249770292,0.000308414297733195,12.7241302921614));
#273836=CARTESIAN_POINT('Ctrl Pts',(-1.95399932181806,0.00162798481247529,
12.0241303078758));
#273837=CARTESIAN_POINT('Ctrl Pts',(-1.9540554909094,-0.0657893310810446,
12.0279834768089));
#273838=CARTESIAN_POINT('Ctrl Pts',(-1.95061836818367,-0.133329609715946,
12.031836645742));
#273839=CARTESIAN_POINT('Ctrl Pts',(-1.94367633872893,-0.200594841073482,
12.035689814675));
#273840=CARTESIAN_POINT('Ctrl Pts',(-1.9367409886327,-0.267795352366316,
12.0395392762345));
#273841=CARTESIAN_POINT('Ctrl Pts',(-1.92630746402906,-0.334720838234257,
12.043388737794));
#273842=CARTESIAN_POINT('Ctrl Pts',(-1.9124161765106,-0.400974273265233,
12.0472381993535));
#273843=CARTESIAN_POINT('Ctrl Pts',(-1.89853315627626,-0.467188278115878,
12.051085369938));
#273844=CARTESIAN_POINT('Ctrl Pts',(-1.88119655565532,-0.532730528746946,
12.0549325405225));
#273845=CARTESIAN_POINT('Ctrl Pts',(-1.86049823265094,-0.597212128395529,
12.0587797111069));
#273846=CARTESIAN_POINT('Ctrl Pts',(-1.83980463332279,-0.661679012349574,
12.0626260037078));
#273847=CARTESIAN_POINT('Ctrl Pts',(-1.81575098950706,-0.725085242231116,
12.0664722963087));
#273848=CARTESIAN_POINT('Ctrl Pts',(-1.78847902146685,-0.787057043531779,
12.0703185889096));
#273849=CARTESIAN_POINT('Ctrl Pts',(-1.76118407533488,-0.849081059389693,
12.0741681222177));
#273850=CARTESIAN_POINT('Ctrl Pts',(-1.73066559046174,-0.909667765005355,
12.0780176555258));
#273851=CARTESIAN_POINT('Ctrl Pts',(-1.69711300844451,-0.968464473570616,
12.081867188834));
#273852=CARTESIAN_POINT('Ctrl Pts',(-1.66354753547827,-1.02728377191368,
12.0857182011382));
#273853=CARTESIAN_POINT('Ctrl Pts',(-1.62694591854707,-1.08431127521329,
12.0895692134424));
#273854=CARTESIAN_POINT('Ctrl Pts',(-1.58754146245115,-1.13922258799519,
12.0934202257466));
#273855=CARTESIAN_POINT('Ctrl Pts',(-1.54806429116053,-1.19423523162126,
12.0972783445341));
#273856=CARTESIAN_POINT('Ctrl Pts',(-1.50577426642181,-1.24712348582285,
12.1011364633216));
#273857=CARTESIAN_POINT('Ctrl Pts',(-1.46094509962579,-1.29759601412743,
12.1049945821091));
#273858=CARTESIAN_POINT('Ctrl Pts',(-1.41839446150562,-1.34550317904688,
12.1086566045844));
#273859=CARTESIAN_POINT('Ctrl Pts',(-1.37355682168725,-1.39123398319979,
12.1123186270596));
#273860=CARTESIAN_POINT('Ctrl Pts',(-1.3266942071601,-1.43457257769965,
12.1159806495348));
#273861=CARTESIAN_POINT('Ctrl Pts',(-1.27655690992226,-1.48093960216542,
12.1198985681397));
#273862=CARTESIAN_POINT('Ctrl Pts',(-1.22388643151331,-1.52476709658075,
12.1238164867447));
#273863=CARTESIAN_POINT('Ctrl Pts',(-1.16897046839485,-1.56576628013913,
12.1277344053496));
#273864=CARTESIAN_POINT('Ctrl Pts',(-1.11413726643054,-1.60670367583915,
12.1316464194516));
#273865=CARTESIAN_POINT('Ctrl Pts',(-1.05706568690618,-1.64482092808708,
12.1355584335536));
#273866=CARTESIAN_POINT('Ctrl Pts',(-0.998078554773395,-1.67986761338549,
12.1394704476556));
#273867=CARTESIAN_POINT('Ctrl Pts',(-0.939160864915841,-1.71487304016737,
12.1433778563606));
#273868=CARTESIAN_POINT('Ctrl Pts',(-0.878332521961585,-1.74681482895347,
12.1472852650656));
#273869=CARTESIAN_POINT('Ctrl Pts',(-0.815946062527566,-1.77548529226399,
12.1511926737706));
#273870=CARTESIAN_POINT('Ctrl Pts',(-0.753598757546154,-1.80413776166515,
12.1550976301414));
#273871=CARTESIAN_POINT('Ctrl Pts',(-0.689695721890799,-1.82952277334644,
12.1590025865122));
#273872=CARTESIAN_POINT('Ctrl Pts',(-0.624613489224658,-1.85147886541505,
12.162907542883));
#273873=CARTESIAN_POINT('Ctrl Pts',(-0.559549774145845,-1.8734287104046,
12.1668113881922));
#273874=CARTESIAN_POINT('Ctrl Pts',(-0.493307994009486,-1.89195141535257,
12.1707152335014));
#273875=CARTESIAN_POINT('Ctrl Pts',(-0.426282322391558,-1.90693455095251,
12.1746190788106));
#273876=CARTESIAN_POINT('Ctrl Pts',(-0.359252726506088,-1.92191856379593,
12.1785231526849));
#273877=CARTESIAN_POINT('Ctrl Pts',(-0.291439628667888,-1.93336249102916,
12.1824272265593));
#273878=CARTESIAN_POINT('Ctrl Pts',(-0.22324816053472,-1.94120484720646,
12.1863313004336));
#273879=CARTESIAN_POINT('Ctrl Pts',(-0.154984017487743,-1.94905556135837,
12.1902395350665));
#273880=CARTESIAN_POINT('Ctrl Pts',(-0.0863411890446798,-1.9532969879008,
12.1941477696994));
#273881=CARTESIAN_POINT('Ctrl Pts',(-0.0177297011688613,-1.95391956274982,
12.1980560043323));
#273882=CARTESIAN_POINT('Ctrl Pts',(0.0509228249235043,-1.95454250997616,
12.2019665765763));
#273883=CARTESIAN_POINT('Ctrl Pts',(0.119543481598909,-1.95154231920351,
12.2058771488203));
#273884=CARTESIAN_POINT('Ctrl Pts',(0.18772530006829,-1.94496149363278,
12.2097877210643));
#273885=CARTESIAN_POINT('Ctrl Pts',(0.256025039599139,-1.93836928646571,
12.2137050566778));
#273886=CARTESIAN_POINT('Ctrl Pts',(0.323883939875557,-1.92818415766703,
12.2176223922913));
#273887=CARTESIAN_POINT('Ctrl Pts',(0.390904045973118,-1.91449994171895,
12.2215397279048));
#273888=CARTESIAN_POINT('Ctrl Pts',(0.42282131161165,-1.9079830502829,12.22340529704));
#273889=CARTESIAN_POINT('Ctrl Pts',(0.454548547372225,-1.90067330553549,
12.2252708661752));
#273890=CARTESIAN_POINT('Ctrl Pts',(0.486044131895434,-1.89258476741466,
12.2271364353103));
#273891=CARTESIAN_POINT('Ctrl Pts',(0.552188631314071,-1.87559786867538,
12.2310543539153));
#273892=CARTESIAN_POINT('Ctrl Pts',(0.617572821896984,-1.85510552414462,
12.2349722725202));
#273893=CARTESIAN_POINT('Ctrl Pts',(0.68179806575538,-1.83119288922064,
12.2388901911251));
#273894=CARTESIAN_POINT('Ctrl Pts',(0.745926518899189,-1.80731629185577,
12.2428022052271));
#273895=CARTESIAN_POINT('Ctrl Pts',(0.808899034363604,-1.78002980427668,
12.2467142193291));
#273896=CARTESIAN_POINT('Ctrl Pts',(0.870330156739797,-1.74946889605654,
12.2506262334311));
#273897=CARTESIAN_POINT('Ctrl Pts',(0.93168895966685,-1.71894396549662,
12.2545336421361));
#273898=CARTESIAN_POINT('Ctrl Pts',(0.991509534952271,-1.68515248802175,
12.2584410508411));
#273899=CARTESIAN_POINT('Ctrl Pts',(1.04942622590129,-1.64827807010546,
12.2623484595461));
#273900=CARTESIAN_POINT('Ctrl Pts',(1.10730656767539,-1.61142679499386,
12.2662534159169));
#273901=CARTESIAN_POINT('Ctrl Pts',(1.16328498136309,-1.57149668123188,
12.2701583722877));
#273902=CARTESIAN_POINT('Ctrl Pts',(1.21702163959142,-1.52871656259956,
12.2740633286585));
#273903=CARTESIAN_POINT('Ctrl Pts',(1.27074300834321,-1.48594861602337,
12.2779671739677));
#273904=CARTESIAN_POINT('Ctrl Pts',(1.32222350315288,-1.44033258059323,
12.2818710192769));
#273905=CARTESIAN_POINT('Ctrl Pts',(1.37115493142929,-1.39213869783766,
12.2857748645861));
#273906=CARTESIAN_POINT('Ctrl Pts',(1.42008922457854,-1.34394199339161,
12.2896789384604));
#273907=CARTESIAN_POINT('Ctrl Pts',(1.46647380620244,-1.29316748899696,
12.2935830123348));
#273908=CARTESIAN_POINT('Ctrl Pts',(1.51003734737879,-1.24012225587691,
12.2974870862091));
#273909=CARTESIAN_POINT('Ctrl Pts',(1.55364731630747,-1.18702048991128,
12.301395320842));
#273910=CARTESIAN_POINT('Ctrl Pts',(1.59442993185607,-1.13164354647098,
12.3053035554749));
#273911=CARTESIAN_POINT('Ctrl Pts',(1.63215483794644,-1.07433076143617,
12.3092117901078));
#273912=CARTESIAN_POINT('Ctrl Pts',(1.66990230822993,-1.01698369621663,
12.3131223623518));
#273913=CARTESIAN_POINT('Ctrl Pts',(1.70458818076787,-0.957698909690016,
12.3170329345958));
#273914=CARTESIAN_POINT('Ctrl Pts',(1.73602750630394,-0.896841400335714,
12.3209435068398));
#273915=CARTESIAN_POINT('Ctrl Pts',(1.7675212064332,-0.835878637377611,
12.3248608424533));
#273916=CARTESIAN_POINT('Ctrl Pts',(1.7957569506424,-0.773338170923284,
12.3287781780668));
#273917=CARTESIAN_POINT('Ctrl Pts',(1.8205978078482,-0.709605257913402,
12.3326955136803));
#273918=CARTESIAN_POINT('Ctrl Pts',(1.83242787324641,-0.679253465997395,
12.3345610828155));
#273919=CARTESIAN_POINT('Ctrl Pts',(1.8434887128893,-0.648631452940076,
12.3364266519507));
#273920=CARTESIAN_POINT('Ctrl Pts',(1.85376957305606,-0.617781814244768,
12.3382922210859));
#273921=CARTESIAN_POINT('Ctrl Pts',(1.8753606106448,-0.552993878423696,
12.3422101396908));
#273922=CARTESIAN_POINT('Ctrl Pts',(1.89359397391154,-0.486944101538939,
12.3461280582957));
#273923=CARTESIAN_POINT('Ctrl Pts',(1.90832506892014,-0.420013608506845,
12.3500459769006));
#273924=CARTESIAN_POINT('Ctrl Pts',(1.92303396341805,-0.353183983137696,
12.3539579910026));
#273925=CARTESIAN_POINT('Ctrl Pts',(1.93425095987221,-0.285476752365371,
12.3578700051046));
#273926=CARTESIAN_POINT('Ctrl Pts',(1.94188088816484,-0.217289245431345,
12.3617820192066));
#273927=CARTESIAN_POINT('Ctrl Pts',(1.94950183416659,-0.149182011862786,
12.3656894279116));
#273928=CARTESIAN_POINT('Ctrl Pts',(1.95354404418813,-0.0805961115949446,
12.3695968366166));
#273929=CARTESIAN_POINT('Ctrl Pts',(1.95396352987359,-0.011938338408627,
12.3735042453216));
#273930=CARTESIAN_POINT('Ctrl Pts',(1.95438275228505,0.0566763443772267,
12.3774092016925));
#273931=CARTESIAN_POINT('Ctrl Pts',(1.95118375756041,0.125362319778213,
12.3813141580633));
#273932=CARTESIAN_POINT('Ctrl Pts',(1.94437456419064,0.193709974261689,
12.3852191144341));
#273933=CARTESIAN_POINT('Ctrl Pts',(1.93756730821343,0.262038182060291,
12.3891229597433));
#273934=CARTESIAN_POINT('Ctrl Pts',(1.92715194147817,0.330027770748407,
12.3930268050524));
#273935=CARTESIAN_POINT('Ctrl Pts',(1.91318842773897,0.397273256041339,
12.3969306503616));
#273936=CARTESIAN_POINT('Ctrl Pts',(1.89922409645384,0.46452267847175,12.400834724236));
#273937=CARTESIAN_POINT('Ctrl Pts',(1.88171130825211,0.531027429868459,
12.4047387981103));
#273938=CARTESIAN_POINT('Ctrl Pts',(1.86076096062313,0.596393030996247,
12.4086428719847));
#273939=CARTESIAN_POINT('Ctrl Pts',(1.83978828520522,0.66182829537597,12.4125511066175));
#273940=CARTESIAN_POINT('Ctrl Pts',(1.81537088939659,0.72612151724033,12.4164593412504));
#273941=CARTESIAN_POINT('Ctrl Pts',(1.78766899671218,0.788895150317236,
12.4203675758833));
#273942=CARTESIAN_POINT('Ctrl Pts',(1.75995053484516,0.85170632984636,12.4242781481273));
#273943=CARTESIAN_POINT('Ctrl Pts',(1.72894388842041,0.91299567267797,12.4281887203713));
#273944=CARTESIAN_POINT('Ctrl Pts',(1.6948554637872,0.972409870821289,12.4320992926154));
#273945=CARTESIAN_POINT('Ctrl Pts',(1.66070808292043,1.03192682634868,12.4360166282289));
#273946=CARTESIAN_POINT('Ctrl Pts',(1.62346855284891,1.08956175148456,12.4399339638424));
#273947=CARTESIAN_POINT('Ctrl Pts',(1.58338633786399,1.14499070086428,12.4438512994559));
#273948=CARTESIAN_POINT('Ctrl Pts',(1.56429781685795,1.17138786142477,12.4457168685911));
#273949=CARTESIAN_POINT('Ctrl Pts',(1.54456516290423,1.19728520154391,12.4475824377263));
#273950=CARTESIAN_POINT('Ctrl Pts',(1.52421833582585,1.22265058979755,12.4494480068614));
#273951=CARTESIAN_POINT('Ctrl Pts',(1.48148756222014,1.27592094289543,12.4533659254664));
#273952=CARTESIAN_POINT('Ctrl Pts',(1.43587597248702,1.32705421430028,12.4572838440713));
#273953=CARTESIAN_POINT('Ctrl Pts',(1.387625404141,1.37572226040816,12.4612017626762));
#273954=CARTESIAN_POINT('Ctrl Pts',(1.33944755185965,1.42431696129111,12.4651137767782));
#273955=CARTESIAN_POINT('Ctrl Pts',(1.28863895757512,1.47045346370681,12.4690257908802));
#273956=CARTESIAN_POINT('Ctrl Pts',(1.23548187243687,1.51383636595238,12.4729378049822));
#273957=CARTESIAN_POINT('Ctrl Pts',(1.18238736618313,1.55716819591618,12.4768452136872));
#273958=CARTESIAN_POINT('Ctrl Pts',(1.12695023920267,1.59775255410474,12.4807526223922));
#273959=CARTESIAN_POINT('Ctrl Pts',(1.06948844639271,1.63533191219168,12.4846600310973));
#273960=CARTESIAN_POINT('Ctrl Pts',(1.01206271725846,1.67288768504543,12.4885649874681));
#273961=CARTESIAN_POINT('Ctrl Pts',(0.952615253736853,1.70744193029679,
12.4924699438389));
#273962=CARTESIAN_POINT('Ctrl Pts',(0.891494578602756,1.73877928913416,
12.4963749002097));
#273963=CARTESIAN_POINT('Ctrl Pts',(0.830391293889959,1.77010773167813,
12.5002787455189));
#273964=CARTESIAN_POINT('Ctrl Pts',(0.767616180191292,1.79822088045845,
12.504182590828));
#273965=CARTESIAN_POINT('Ctrl Pts',(0.70354245591668,1.82294926224586,12.5080864361372));
#273966=CARTESIAN_POINT('Ctrl Pts',(0.639464980207017,1.84767909184857,
12.5119905100116));
#273967=CARTESIAN_POINT('Ctrl Pts',(0.57408920283838,1.86902358627734,12.515894583886));
#273968=CARTESIAN_POINT('Ctrl Pts',(0.507806712048847,1.88686203607952,
12.5197986577603));
#273969=CARTESIAN_POINT('Ctrl Pts',(0.441453580834311,1.90471949717201,
12.5237068923932));
#273970=CARTESIAN_POINT('Ctrl Pts',(0.374192283648423,1.9190633284824,12.5276151270261));
#273971=CARTESIAN_POINT('Ctrl Pts',(0.306426925951779,1.92982344763757,
12.5315233616589));
#273972=CARTESIAN_POINT('Ctrl Pts',(0.238621036129936,1.94059000268433,
12.535433933903));
#273973=CARTESIAN_POINT('Ctrl Pts',(0.170310975093264,1.94776852818752,
12.539344506147));
#273974=CARTESIAN_POINT('Ctrl Pts',(0.101905523011608,1.95134088881972,
12.543255078391));
#273975=CARTESIAN_POINT('Ctrl Pts',(0.0333817630921084,1.95491942788141,
12.5471724140045));
#273976=CARTESIAN_POINT('Ctrl Pts',(-0.0352372254569389,1.95487935441795,
12.551089749618));
#273977=CARTESIAN_POINT('Ctrl Pts',(-0.103543987799294,1.95125463294533,
12.5550070852315));
#273978=CARTESIAN_POINT('Ctrl Pts',(-0.13607400312618,1.94952841666723,
12.5568726543667));
#273979=CARTESIAN_POINT('Ctrl Pts',(-0.168533302538319,1.94698996459378,
12.5587382235018));
#273980=CARTESIAN_POINT('Ctrl Pts',(-0.200878643321318,1.94364702830977,
12.560603792637));
#273981=CARTESIAN_POINT('Ctrl Pts',(-0.268807732653197,1.9366264617623,
12.5645217112419));
#273982=CARTESIAN_POINT('Ctrl Pts',(-0.336503158662888,1.9260265627108,
12.5684396298468));
#273983=CARTESIAN_POINT('Ctrl Pts',(-0.403558074281079,1.91187261099754,
12.5723575484517));
#273984=CARTESIAN_POINT('Ctrl Pts',(-0.47051193472534,1.89773999001058,
12.5762695625537));
#273985=CARTESIAN_POINT('Ctrl Pts',(-0.536826723058539,1.88006404713187,
12.5801815766557));
#273986=CARTESIAN_POINT('Ctrl Pts',(-0.602101190726571,1.85892177245995,
12.5840935907577));
#273987=CARTESIAN_POINT('Ctrl Pts',(-0.667298814388258,1.83780438741405,
12.5880009994627));
#273988=CARTESIAN_POINT('Ctrl Pts',(-0.731458083890375,1.81322892578366,
12.5919084081677));
#273989=CARTESIAN_POINT('Ctrl Pts',(-0.794190214627478,1.78532291280596,
12.5958158168727));
#273990=CARTESIAN_POINT('Ctrl Pts',(-0.856882973964803,1.75743441395986,
12.5997207732435));
#273991=CARTESIAN_POINT('Ctrl Pts',(-0.918149922826318,1.72621970971303,
12.6036257296144));
#273992=CARTESIAN_POINT('Ctrl Pts',(-0.977621135074021,1.69185487446666,
12.6075306859852));
#273993=CARTESIAN_POINT('Ctrl Pts',(-1.03707542621546,1.65749981690947,
12.6114345312943));
#273994=CARTESIAN_POINT('Ctrl Pts',(-1.09473456928394,1.61999665364559,
12.6153383766035));
#273995=CARTESIAN_POINT('Ctrl Pts',(-1.15025380299516,1.57956708901369,
12.6192422219127));
#273996=CARTESIAN_POINT('Ctrl Pts',(-1.20577628728657,1.53913515728244,
12.623146295787));
#273997=CARTESIAN_POINT('Ctrl Pts',(-1.2591582173127,1.49577677567557,12.6270503696613));
#273998=CARTESIAN_POINT('Ctrl Pts',(-1.31008584493853,1.44975552383555,
12.6309544435357));
#273999=CARTESIAN_POINT('Ctrl Pts',(-1.36106774857662,1.40368522494297,
12.6348626781685));
#274000=CARTESIAN_POINT('Ctrl Pts',(-1.40958976402385,1.35494672257884,
12.6387709128014));
#274001=CARTESIAN_POINT('Ctrl Pts',(-1.45537389526011,1.30384156437637,
12.6426791474343));
#274002=CARTESIAN_POINT('Ctrl Pts',(-1.50118541111011,1.25270583892319,
12.6465897196783));
#274003=CARTESIAN_POINT('Ctrl Pts',(-1.54425547511677,1.19920102368488,
12.6505002919223));
#274004=CARTESIAN_POINT('Ctrl Pts',(-1.58434720475194,1.14366076036329,
12.6544108641663));
#274005=CARTESIAN_POINT('Ctrl Pts',(-1.62450827339006,1.08802443966234,
12.6583281997798));
#274006=CARTESIAN_POINT('Ctrl Pts',(-1.66168046053407,1.03034605811188,
12.6622455353933));
#274007=CARTESIAN_POINT('Ctrl Pts',(-1.69567137881452,0.970986392834244,
12.6661628710068));
#274008=CARTESIAN_POINT('Ctrl Pts',(-1.71185901609634,0.942717290988959,
12.6680284401421));
#274009=CARTESIAN_POINT('Ctrl Pts',(-1.72732583476716,0.914067205865857,
12.6698940092773));
#274010=CARTESIAN_POINT('Ctrl Pts',(-1.74205490144005,0.88507667485291,
12.6717595784125));
#274011=CARTESIAN_POINT('Ctrl Pts',(-1.77651139766982,0.817257569628513,
12.6761238044224));
#274012=CARTESIAN_POINT('Ctrl Pts',(-1.80705483983964,0.747321895345659,
12.6804880304322));
#274013=CARTESIAN_POINT('Ctrl Pts',(-1.83343982526576,0.67573249672445,
12.6848522564421));
#274014=CARTESIAN_POINT('Ctrl Pts',(-1.8586008869996,0.60746392468978,12.689014038542));
#274015=CARTESIAN_POINT('Ctrl Pts',(-1.8799804781929,0.537692051207313,
12.693175820642));
#274016=CARTESIAN_POINT('Ctrl Pts',(-1.89741215384907,0.466843783749794,
12.697337602742));
#274017=CARTESIAN_POINT('Ctrl Pts',(-1.9148071043119,0.396144779987412,
12.7014906167662));
#274018=CARTESIAN_POINT('Ctrl Pts',(-1.92827058971641,0.324374272716027,
12.7056436307904));
#274019=CARTESIAN_POINT('Ctrl Pts',(-1.93768523310141,0.251976065174288,
12.7097966448147));
#274020=CARTESIAN_POINT('Ctrl Pts',(-1.94707437508419,0.179773962331943,
12.7139384095885));
#274021=CARTESIAN_POINT('Ctrl Pts',(-1.95243646025069,0.106947933259381,
12.7180801743623));
#274022=CARTESIAN_POINT('Ctrl Pts',(-1.95370500604768,0.033952162585741,
12.7222219391361));
#274023=CARTESIAN_POINT('Ctrl Pts',(-1.95389983693685,0.0227410333228769,
12.7228580562676));
#274024=CARTESIAN_POINT('Ctrl Pts',(-1.95399820468377,0.0115259205146458,
12.7234941733992));
#274025=CARTESIAN_POINT('Ctrl Pts',(-1.9539999756484,0.000308489971946228,
12.7241302905307));
#274026=CARTESIAN_POINT('',(-1.95402820026386,-0.00178509135925994,13.4241303078758));
#274027=CARTESIAN_POINT('Ctrl Pts',(-1.95083582512995,0.000307685056475884,
12.7241303078758));
#274028=CARTESIAN_POINT('Ctrl Pts',(-1.95035082451635,-0.344675762667878,
12.7437253266466));
#274029=CARTESIAN_POINT('Ctrl Pts',(-1.69859020752685,-1.34264473489564,
12.800372274009));
#274030=CARTESIAN_POINT('Ctrl Pts',(-0.104847311655371,-2.30727077595995,
12.8940711499638));
#274031=CARTESIAN_POINT('Ctrl Pts',(1.88181988362473,-1.33912109906285,
13.0052269357391));
#274032=CARTESIAN_POINT('Ctrl Pts',(2.1455280618664,0.85510275879836,13.1163827215148));
#274033=CARTESIAN_POINT('Ctrl Pts',(0.44483095739769,2.26641055673969,13.2275385072902));
#274034=CARTESIAN_POINT('Ctrl Pts',(-1.50056042635302,1.65383118156618,
13.3301210360774));
#274035=CARTESIAN_POINT('Ctrl Pts',(-1.94943588392903,0.497535626713033,
13.3956516362725));
#274036=CARTESIAN_POINT('Ctrl Pts',(-1.95402820026386,-0.00178509135925994,
13.4241303078758));
#274037=CARTESIAN_POINT('',(-1.95413348876404,0.000767679038905043,14.1241303078758));
#274038=CARTESIAN_POINT('Ctrl Pts',(-1.95402820026386,-0.00178509135925994,
13.4241303078758));
#274039=CARTESIAN_POINT('Ctrl Pts',(-1.95541067725083,-0.152101261135744,
13.4327035648643));
#274040=CARTESIAN_POINT('Ctrl Pts',(-1.87089950475814,-0.950516301187075,
13.4783287504445));
#274041=CARTESIAN_POINT('Ctrl Pts',(-0.775036692012782,-2.17573195003328,
13.5610058646171));
#274042=CARTESIAN_POINT('Ctrl Pts',(1.40791228892896,-1.83092172935965,
13.6721616503923));
#274043=CARTESIAN_POINT('Ctrl Pts',(2.30180316472699,0.190246112222753,
13.7833174361682));
#274044=CARTESIAN_POINT('Ctrl Pts',(1.08820620248698,2.03722817897972,13.8944732219435));
#274045=CARTESIAN_POINT('Ctrl Pts',(-1.12173196396984,2.01896230607907,
14.0056290077192));
#274046=CARTESIAN_POINT('Ctrl Pts',(-1.93638948072713,0.733314628616374,
14.0821813696965));
#274047=CARTESIAN_POINT('Ctrl Pts',(-1.95705073983529,0.0435387888036669,
14.1216818030821));
#274048=CARTESIAN_POINT('Ctrl Pts',(-1.95683651916685,0.000768740921214415,
14.1241303078758));
#274049=CARTESIAN_POINT('',(-1.95399956106643,0.00130971454563185,14.8241303078238));
#274050=CARTESIAN_POINT('Ctrl Pts',(-1.95399984921942,0.000767626538767374,
14.1241303078758));
#274051=CARTESIAN_POINT('Ctrl Pts',(-1.95402643386531,-0.0669038145125677,
14.1280100028959));
#274052=CARTESIAN_POINT('Ctrl Pts',(-1.95053334135365,-0.134718102982957,
14.1318896979161));
#274053=CARTESIAN_POINT('Ctrl Pts',(-1.94350227311917,-0.20227435423359,
14.1357693929362));
#274054=CARTESIAN_POINT('Ctrl Pts',(-1.93648251703331,-0.269721915548593,
14.1396428459907));
#274055=CARTESIAN_POINT('Ctrl Pts',(-1.92593613721697,-0.336911768377198,
14.1435162990451));
#274056=CARTESIAN_POINT('Ctrl Pts',(-1.91189683763907,-0.403443282538866,
14.1473897520996));
#274057=CARTESIAN_POINT('Ctrl Pts',(-1.89787010835416,-0.469915226732554,
14.151259737001));
#274058=CARTESIAN_POINT('Ctrl Pts',(-1.88035676061684,-0.535729511362023,
14.1551297219024));
#274059=CARTESIAN_POINT('Ctrl Pts',(-1.85944208487721,-0.600492408767574,
14.1589997068038));
#274060=CARTESIAN_POINT('Ctrl Pts',(-1.83853862212686,-0.665220584828008,
14.1628676168894));
#274061=CARTESIAN_POINT('Ctrl Pts',(-1.81423760121725,-0.728898014171866,
14.166735526975));
#274062=CARTESIAN_POINT('Ctrl Pts',(-1.78667452646286,-0.791144826494302,
14.1706034370606));
#274063=CARTESIAN_POINT('Ctrl Pts',(-1.75911632835618,-0.85338062568496,
14.1744706628091));
#274064=CARTESIAN_POINT('Ctrl Pts',(-1.72829742601706,-0.914185851384229,
14.1783378885577));
#274065=CARTESIAN_POINT('Ctrl Pts',(-1.69440120631608,-0.973201187851012,
14.1822051143062));
#274066=CARTESIAN_POINT('Ctrl Pts',(-1.66047473866568,-1.03226918779851,
14.1860757910486));
#274067=CARTESIAN_POINT('Ctrl Pts',(-1.62346571708041,-1.08954367020213,
14.1899464677911));
#274068=CARTESIAN_POINT('Ctrl Pts',(-1.58360266826016,-1.14469148205065,
14.1938171445336));
#274069=CARTESIAN_POINT('Ctrl Pts',(-1.54372302155348,-1.19986225594409,
14.1976894329202));
#274070=CARTESIAN_POINT('Ctrl Pts',(-1.50098729627419,-1.25290420366035,
14.2015617213069));
#274071=CARTESIAN_POINT('Ctrl Pts',(-1.45566457516665,-1.30351702888949,
14.2054340096936));
#274072=CARTESIAN_POINT('Ctrl Pts',(-1.41025760552753,-1.35422393620596,
14.209313496117));
#274073=CARTESIAN_POINT('Ctrl Pts',(-1.36225438800566,-1.40249234297613,
14.2131929825405));
#274074=CARTESIAN_POINT('Ctrl Pts',(-1.31196066470999,-1.44805911973707,
14.2170724689639));
#274075=CARTESIAN_POINT('Ctrl Pts',(-1.26499588012766,-1.4906098341097,
14.2206951723993));
#274076=CARTESIAN_POINT('Ctrl Pts',(-1.21603438180848,-1.53080491841486,
14.2243178758348));
#274077=CARTESIAN_POINT('Ctrl Pts',(-1.16534810818424,-1.56846414901693,
14.2279405792703));
#274078=CARTESIAN_POINT('Ctrl Pts',(-1.1105313952005,-1.60919224140752,
14.2318584978752));
#274079=CARTESIAN_POINT('Ctrl Pts',(-1.05346818430586,-1.64712400283433,
14.2357764164801));
#274080=CARTESIAN_POINT('Ctrl Pts',(-0.994475457487556,-1.68200314044146,
14.239694335085));
#274081=CARTESIAN_POINT('Ctrl Pts',(-0.935571635714056,-1.71682971341122,
14.243606349187));
#274082=CARTESIAN_POINT('Ctrl Pts',(-0.874744489147849,-1.74861254445149,
14.247518363289));
#274083=CARTESIAN_POINT('Ctrl Pts',(-0.812341816209655,-1.77713724108106,
14.251430377391));
#274084=CARTESIAN_POINT('Ctrl Pts',(-0.750012606473188,-1.80562835716922,
14.255337786096));
#274085=CARTESIAN_POINT('Ctrl Pts',(-0.686111999261733,-1.83086875287559,
14.259245194801));
#274086=CARTESIAN_POINT('Ctrl Pts',(-0.621012754626721,-1.85268970920414,
14.263152603506));
#274087=CARTESIAN_POINT('Ctrl Pts',(-0.555954367019157,-1.87449697045195,
14.2670575598768));
#274088=CARTESIAN_POINT('Ctrl Pts',(-0.48969929964492,-1.89288889344172,
14.2709625162476));
#274089=CARTESIAN_POINT('Ctrl Pts',(-0.422639218570995,-1.90774528984498,
14.2748674726184));
#274090=CARTESIAN_POINT('Ctrl Pts',(-0.355598217833756,-1.92259745921718,
14.2787713179276));
#274091=CARTESIAN_POINT('Ctrl Pts',(-0.287753138159825,-1.9339159926138,
14.2826751632368));
#274092=CARTESIAN_POINT('Ctrl Pts',(-0.21950793033573,-1.94163134207288,
14.286579008546));
#274093=CARTESIAN_POINT('Ctrl Pts',(-0.151258726841537,-1.94934714325586,
14.2904830824203));
#274094=CARTESIAN_POINT('Ctrl Pts',(-0.0826098377990403,-1.95345928894754,
14.2943871562947));
#274095=CARTESIAN_POINT('Ctrl Pts',(-0.0139706505631757,-1.95395005589264,
14.298291230169));
#274096=CARTESIAN_POINT('Ctrl Pts',(0.0547416887419765,-1.95444134587158,
14.3021994648019));
#274097=CARTESIAN_POINT('Ctrl Pts',(0.123443812729814,-1.9513035512105,
14.3061076994348));
#274098=CARTESIAN_POINT('Ctrl Pts',(0.191727031081185,-1.94457109552538,
14.3100159340677));
#274099=CARTESIAN_POINT('Ctrl Pts',(0.260051091303008,-1.93783461299313,
14.3139265063117));
#274100=CARTESIAN_POINT('Ctrl Pts',(0.327955260822571,-1.92749926447036,
14.3178370785557));
#274101=CARTESIAN_POINT('Ctrl Pts',(0.395039467697114,-1.91365091355806,
14.3217476507997));
#274102=CARTESIAN_POINT('Ctrl Pts',(0.462239697304064,-1.89977861179969,
14.3256649864132));
#274103=CARTESIAN_POINT('Ctrl Pts',(0.528616658251948,-1.88238130595424,
14.3295823220267));
#274104=CARTESIAN_POINT('Ctrl Pts',(0.593784740514013,-1.86159492960545,
14.3334996576402));
#274105=CARTESIAN_POINT('Ctrl Pts',(0.624820009090008,-1.8516957465957,
14.3353652267754));
#274106=CARTESIAN_POINT('Ctrl Pts',(0.655581390671758,-1.8410286354368,
14.3372307959106));
#274107=CARTESIAN_POINT('Ctrl Pts',(0.686029009967765,-1.82961203469005,
14.3390963650457));
#274108=CARTESIAN_POINT('Ctrl Pts',(0.749972656904149,-1.8056358058668,
14.3430142836507));
#274109=CARTESIAN_POINT('Ctrl Pts',(0.812784777378005,-1.7782557751123,
14.3469322022556));
#274110=CARTESIAN_POINT('Ctrl Pts',(0.874078152400699,-1.74759932006618,
14.3508501208605));
#274111=CARTESIAN_POINT('Ctrl Pts',(0.935279155184495,-1.71698906585968,
14.3547621349625));
#274112=CARTESIAN_POINT('Ctrl Pts',(0.994965518577663,-1.68311240526268,
14.3586741490645));
#274113=CARTESIAN_POINT('Ctrl Pts',(1.05276852114657,-1.64614532799594,
14.3625861631665));
#274114=CARTESIAN_POINT('Ctrl Pts',(1.11050347545034,-1.6092217700165,14.3664935718715));
#274115=CARTESIAN_POINT('Ctrl Pts',(1.16635905979217,-1.56921528460179,
14.3704009805765));
#274116=CARTESIAN_POINT('Ctrl Pts',(1.21999139515354,-1.5263475999101,14.3743083892815));
#274117=CARTESIAN_POINT('Ctrl Pts',(1.27359007025038,-1.48350681946557,
14.3782133456523));
#274118=CARTESIAN_POINT('Ctrl Pts',(1.32496788084573,-1.43780870831795,
14.3821183020231));
#274119=CARTESIAN_POINT('Ctrl Pts',(1.37381147447616,-1.38951719406333,
14.3860232583939));
#274120=CARTESIAN_POINT('Ctrl Pts',(1.42264117083421,-1.34123942000016,
14.3899271037031));
#274121=CARTESIAN_POINT('Ctrl Pts',(1.46893773196347,-1.29037005336541,
14.3938309490123));
#274122=CARTESIAN_POINT('Ctrl Pts',(1.512423694745,-1.23721080159117,14.3977347943215));
#274123=CARTESIAN_POINT('Ctrl Pts',(1.55591220357432,-1.18404843741039,
14.4016388681959));
#274124=CARTESIAN_POINT('Ctrl Pts',(1.59658947785309,-1.12859630430256,
14.4055429420702));
#274125=CARTESIAN_POINT('Ctrl Pts',(1.63421865207261,-1.07118877758217,
14.4094470159446));
#274126=CARTESIAN_POINT('Ctrl Pts',(1.67188792950531,-1.01372006891107,
14.4133552505775));
#274127=CARTESIAN_POINT('Ctrl Pts',(1.70650235362224,-0.954292219893747,
14.4172634852103));
#274128=CARTESIAN_POINT('Ctrl Pts',(1.73786925291926,-0.893267294687242,
14.4211717198432));
#274129=CARTESIAN_POINT('Ctrl Pts',(1.76925491352942,-0.832205868973619,
14.4250822920872));
#274130=CARTESIAN_POINT('Ctrl Pts',(1.79738898201236,-0.769545914793622,
14.4289928643313));
#274131=CARTESIAN_POINT('Ctrl Pts',(1.82212668193712,-0.705670146012158,
14.4329034365753));
#274132=CARTESIAN_POINT('Ctrl Pts',(1.8469071659339,-0.641683903520521,
14.4368207721888));
#274133=CARTESIAN_POINT('Ctrl Pts',(1.86827940447334,-0.576478116851078,
14.4407381078023));
#274134=CARTESIAN_POINT('Ctrl Pts',(1.88614853348424,-0.510450496752881,
14.4446554434158));
#274135=CARTESIAN_POINT('Ctrl Pts',(1.89465842358414,-0.479005886875614,
14.446521012551));
#274136=CARTESIAN_POINT('Ctrl Pts',(1.90237456301791,-0.447375030903409,
14.4483865816862));
#274137=CARTESIAN_POINT('Ctrl Pts',(1.90929082390855,-0.415601431348128,
14.4502521508214));
#274138=CARTESIAN_POINT('Ctrl Pts',(1.92381580007209,-0.348873067067548,
14.4541700694263));
#274139=CARTESIAN_POINT('Ctrl Pts',(1.93486722982208,-0.281249887143623,
14.4580879880312));
#274140=CARTESIAN_POINT('Ctrl Pts',(1.94234218761738,-0.213126315131955,
14.4620059066361));
#274141=CARTESIAN_POINT('Ctrl Pts',(1.94980588027048,-0.145105408813827,
14.4659179207381));
#274142=CARTESIAN_POINT('Ctrl Pts',(1.95370374478881,-0.0765860921174858,
14.4698299348401));
#274143=CARTESIAN_POINT('Ctrl Pts',(1.95398373116002,-0.00797360407566831,
14.4737419489421));
#274144=CARTESIAN_POINT('Ctrl Pts',(1.95426338791883,0.0605581102938482,
14.4776493576471));
#274145=CARTESIAN_POINT('Ctrl Pts',(1.95093362319341,0.129182288571518,
14.4815567663521));
#274146=CARTESIAN_POINT('Ctrl Pts',(1.94399428818267,0.197489765590924,
14.4854641750572));
#274147=CARTESIAN_POINT('Ctrl Pts',(1.93705930837763,0.265754372059655,
14.489369131428));
#274148=CARTESIAN_POINT('Ctrl Pts',(1.92651930171783,0.333702183235872,
14.4932740877988));
#274149=CARTESIAN_POINT('Ctrl Pts',(1.91242612898619,0.400926802759444,
14.4971790441696));
#274150=CARTESIAN_POINT('Ctrl Pts',(1.89833696612862,0.46813229513088,14.5010828894787));
#274151=CARTESIAN_POINT('Ctrl Pts',(1.88069674501712,0.534614523082058,
14.5049867347879));
#274152=CARTESIAN_POINT('Ctrl Pts',(1.85960853023193,0.599976761457181,
14.5088905800971));
#274153=CARTESIAN_POINT('Ctrl Pts',(1.83851908075864,0.665342826708067,
14.5127946539714));
#274154=CARTESIAN_POINT('Ctrl Pts',(1.81398139030327,0.729588304806202,
14.5166987278458));
#274155=CARTESIAN_POINT('Ctrl Pts',(1.78614798482388,0.792332869638516,
14.5206028017201));
#274156=CARTESIAN_POINT('Ctrl Pts',(1.75828491595114,0.855144304358821,
14.524511036353));
#274157=CARTESIAN_POINT('Ctrl Pts',(1.72711932220709,0.916451182948067,
14.5284192709859));
#274158=CARTESIAN_POINT('Ctrl Pts',(1.69285095732083,0.975895299864676,
14.5323275056188));
#274159=CARTESIAN_POINT('Ctrl Pts',(1.65856209568363,1.03537497176801,14.5362380778628));
#274160=CARTESIAN_POINT('Ctrl Pts',(1.62116703730577,1.09298925190883,14.5401486501068));
#274161=CARTESIAN_POINT('Ctrl Pts',(1.58090885585488,1.14840898180031,14.5440592223508));
#274162=CARTESIAN_POINT('Ctrl Pts',(1.54058104752112,1.20392456060753,14.5479765579643));
#274163=CARTESIAN_POINT('Ctrl Pts',(1.49738054259637,1.25723763189034,14.5518938935778));
#274164=CARTESIAN_POINT('Ctrl Pts',(1.45159007873062,1.30805284424247,14.5558112291913));
#274165=CARTESIAN_POINT('Ctrl Pts',(1.42978309446835,1.33225278550745,14.5576767983265));
#274166=CARTESIAN_POINT('Ctrl Pts',(1.40738923910176,1.35588676737919,14.5595423674617));
#274167=CARTESIAN_POINT('Ctrl Pts',(1.38444174273771,1.3789260534798,14.5614079365968));
#274168=CARTESIAN_POINT('Ctrl Pts',(1.3362492521751,1.42731131348196,14.5653258552018));
#274169=CARTESIAN_POINT('Ctrl Pts',(1.2854215092442,1.47326312640682,14.5692437738067));
#274170=CARTESIAN_POINT('Ctrl Pts',(1.23223411854782,1.5164811495982,14.5731616924116));
#274171=CARTESIAN_POINT('Ctrl Pts',(1.17912688395893,1.55963404102681,14.5770737065136));
#274172=CARTESIAN_POINT('Ctrl Pts',(1.12366743790186,1.60006101162009,14.5809857206156));
#274173=CARTESIAN_POINT('Ctrl Pts',(1.06616805780133,1.63749860229685,14.5848977347176));
#274174=CARTESIAN_POINT('Ctrl Pts',(1.00873636852802,1.67489211977704,14.5888051434226));
#274175=CARTESIAN_POINT('Ctrl Pts',(0.949269924912657,1.70930297941689,
14.5927125521276));
#274176=CARTESIAN_POINT('Ctrl Pts',(0.888112444611049,1.7405092029998,14.5966199608326));
#274177=CARTESIAN_POINT('Ctrl Pts',(0.826993347440678,1.77169584120133,
14.6005249172034));
#274178=CARTESIAN_POINT('Ctrl Pts',(0.764185756086352,1.79968160994729,
14.6044298735742));
#274179=CARTESIAN_POINT('Ctrl Pts',(0.700059261816433,1.82428973300434,
14.608334829945));
#274180=CARTESIAN_POINT('Ctrl Pts',(0.635951013201532,1.84889085441052,
14.6122386752542));
#274181=CARTESIAN_POINT('Ctrl Pts',(0.570525065692171,1.87011606175263,
14.6161425205634));
#274182=CARTESIAN_POINT('Ctrl Pts',(0.504170647569705,1.88783684626854,
14.6200463658726));
#274183=CARTESIAN_POINT('Ctrl Pts',(0.437812344480365,1.90555866831387,
14.623950439747));
#274184=CARTESIAN_POINT('Ctrl Pts',(0.370525938794869,1.91977553572203,
14.6278545136213));
#274185=CARTESIAN_POINT('Ctrl Pts',(0.302713698029415,1.93040939104257,
14.6317585874957));
#274186=CARTESIAN_POINT('Ctrl Pts',(0.234829186511242,1.94105457937202,
14.6356668221286));
#274187=CARTESIAN_POINT('Ctrl Pts',(0.166418208443643,1.94810905848887,
14.6395750567615));
#274188=CARTESIAN_POINT('Ctrl Pts',(0.0978900520182863,1.95154644774749,
14.6434832913943));
#274189=CARTESIAN_POINT('Ctrl Pts',(0.0293209072190169,1.95498589299308,
14.6473938636384));
#274190=CARTESIAN_POINT('Ctrl Pts',(-0.0393650634138969,1.95480394398451,
14.6513044358824));
#274191=CARTESIAN_POINT('Ctrl Pts',(-0.107759489808657,1.9510263689546,
14.6552150081264));
#274192=CARTESIAN_POINT('Ctrl Pts',(-0.176272204972246,1.94724226057508,
14.6591323437399));
#274193=CARTESIAN_POINT('Ctrl Pts',(-0.244491880700859,1.93985016757965,
14.6630496793534));
#274194=CARTESIAN_POINT('Ctrl Pts',(-0.312017046916634,1.92892751611703,
14.6669670149669));
#274195=CARTESIAN_POINT('Ctrl Pts',(-0.344174839449375,1.92372577609436,
14.6688325841021));
#274196=CARTESIAN_POINT('Ctrl Pts',(-0.376175295340427,1.9177240530037,
14.6706981532373));
#274197=CARTESIAN_POINT('Ctrl Pts',(-0.407976251362151,1.91093468709019,
14.6725637223725));
#274198=CARTESIAN_POINT('Ctrl Pts',(-0.47476206749868,1.89667620557556,
14.6764816409774));
#274199=CARTESIAN_POINT('Ctrl Pts',(-0.540932054278828,1.87888403280015,
14.6803995595823));
#274200=CARTESIAN_POINT('Ctrl Pts',(-0.606084415364867,1.85762689511426,
14.6843174781872));
#274201=CARTESIAN_POINT('Ctrl Pts',(-0.671138588523441,1.83640179301783,
14.6882294922892));
#274202=CARTESIAN_POINT('Ctrl Pts',(-0.735177715747694,1.81172224090109,
14.6921415063912));
#274203=CARTESIAN_POINT('Ctrl Pts',(-0.797811107533291,1.78370777783148,
14.6960535204932));
#274204=CARTESIAN_POINT('Ctrl Pts',(-0.860370764504758,1.7557262946336,
14.6999609291982));
#274205=CARTESIAN_POINT('Ctrl Pts',(-0.921527525735173,1.72441789746557,
14.7038683379033));
#274206=CARTESIAN_POINT('Ctrl Pts',(-0.980908508555638,1.68995103415547,
14.7077757466083));
#274207=CARTESIAN_POINT('Ctrl Pts',(-1.04025222319486,1.65550580264142,
14.7116807029791));
#274208=CARTESIAN_POINT('Ctrl Pts',(-1.09782194571756,1.61790628359267,
14.7155856593499));
#274209=CARTESIAN_POINT('Ctrl Pts',(-1.1532687452085,1.57736717390886,14.7194906157207));
#274210=CARTESIAN_POINT('Ctrl Pts',(-1.20869976864335,1.53683959865577,
14.7233944610299));
#274211=CARTESIAN_POINT('Ctrl Pts',(-1.26200867120127,1.49337438334165,
14.7272983063391));
#274212=CARTESIAN_POINT('Ctrl Pts',(-1.31287643101941,1.44722889581218,
14.7312021516482));
#274213=CARTESIAN_POINT('Ctrl Pts',(-1.36374716908006,1.40108070652322,
14.7351062255226));
#274214=CARTESIAN_POINT('Ctrl Pts',(-1.41217611800806,1.35225226588987,
14.739010299397));
#274215=CARTESIAN_POINT('Ctrl Pts',(-1.45787957732774,1.30103925306298,
14.7429143732713));
#274216=CARTESIAN_POINT('Ctrl Pts',(-1.50363174501301,1.24977166007546,
14.7468226079042));
#274217=CARTESIAN_POINT('Ctrl Pts',(-1.54665229802001,1.19611479085303,
14.7507308425371));
#274218=CARTESIAN_POINT('Ctrl Pts',(-1.58669715029207,1.14039824327075,
14.7546390771699));
#274219=CARTESIAN_POINT('Ctrl Pts',(-1.62676595437416,1.08464837025244,
14.758549649414));
#274220=CARTESIAN_POINT('Ctrl Pts',(-1.66385524983905,1.02683678119652,
14.762460221658));
#274221=CARTESIAN_POINT('Ctrl Pts',(-1.69776526619505,0.967320578144422,
14.766370793902));
#274222=CARTESIAN_POINT('Ctrl Pts',(-1.73173393022585,0.907701441289936,
14.7702881295155));
#274223=CARTESIAN_POINT('Ctrl Pts',(-1.76251212021033,0.846372245822791,
14.774205465129));
#274224=CARTESIAN_POINT('Ctrl Pts',(-1.78994721212184,0.783712305516029,
14.7781228007425));
#274225=CARTESIAN_POINT('Ctrl Pts',(-1.80301274077191,0.75387149988175,
14.7799883698777));
#274226=CARTESIAN_POINT('Ctrl Pts',(-1.8153207795147,0.7237291370088,14.7818539390128));
#274227=CARTESIAN_POINT('Ctrl Pts',(-1.8268588358628,0.693327335268145,
14.783719508148));
#274228=CARTESIAN_POINT('Ctrl Pts',(-1.85454088667258,0.620387474766188,
14.788195372889));
#274229=CARTESIAN_POINT('Ctrl Pts',(-1.87787906227524,0.545713210096145,
14.79267123763));
#274230=CARTESIAN_POINT('Ctrl Pts',(-1.8966828185995,0.469798132850119,
14.797147102371));
#274231=CARTESIAN_POINT('Ctrl Pts',(-1.91557621125608,0.393521173170883,
14.8016443032798));
#274232=CARTESIAN_POINT('Ctrl Pts',(-1.92989163872075,0.315991707952488,
14.8061415041886));
#274233=CARTESIAN_POINT('Ctrl Pts',(-1.93948425663725,0.237732661315694,
14.8106387050974));
#274234=CARTESIAN_POINT('Ctrl Pts',(-1.94907687455376,0.1594736146789,14.8151359060062));
#274235=CARTESIAN_POINT('Ctrl Pts',(-1.95394649182682,0.0804851892759246,
14.819633106915));
#274236=CARTESIAN_POINT('Ctrl Pts',(-1.95399956106643,0.00130971454563252,
14.8241303078238));
#274237=CARTESIAN_POINT('',(-1.95399944231052,-0.00147629610118066,15.5241303078758));
#274238=CARTESIAN_POINT('Ctrl Pts',(-1.95399956106705,0.00130971363016174,
14.8241303078758));
#274239=CARTESIAN_POINT('Ctrl Pts',(-1.95404586063319,-0.0677659452257072,
14.8280538349129));
#274240=CARTESIAN_POINT('Ctrl Pts',(-1.95042499795379,-0.136864374352902,
14.8319773619499));
#274241=CARTESIAN_POINT('Ctrl Pts',(-1.94315626763052,-0.205571689607818,
14.835900888987));
#274242=CARTESIAN_POINT('Ctrl Pts',(-1.93588716306388,-0.274282542379846,
14.8398246180337));
#274243=CARTESIAN_POINT('Ctrl Pts',(-1.92496987030036,-0.342601759347549,
14.8437483470805));
#274244=CARTESIAN_POINT('Ctrl Pts',(-1.91047548303559,-0.410121236611718,
14.8476720761272));
#274245=CARTESIAN_POINT('Ctrl Pts',(-1.8959446266587,-0.477810598627981,
14.8516056776102));
#274246=CARTESIAN_POINT('Ctrl Pts',(-1.87781875978922,-0.544695714643512,
14.8555392790933));
#274247=CARTESIAN_POINT('Ctrl Pts',(-1.85622038180967,-0.610378484347524,
14.8594728805763));
#274248=CARTESIAN_POINT('Ctrl Pts',(-1.83463860778333,-0.676010759813655,
14.8634034580667));
#274249=CARTESIAN_POINT('Ctrl Pts',(-1.80958986356056,-0.740442093694928,
14.8673340355571));
#274250=CARTESIAN_POINT('Ctrl Pts',(-1.78124471143847,-0.803295262012971,
14.8712646130476));
#274251=CARTESIAN_POINT('Ctrl Pts',(-1.75284094456976,-0.866278403968806,
14.8752033185524));
#274252=CARTESIAN_POINT('Ctrl Pts',(-1.72112737001053,-0.927676426106799,
14.8791420240572));
#274253=CARTESIAN_POINT('Ctrl Pts',(-1.68632081344798,-0.987136319933643,
14.883080729562));
#274254=CARTESIAN_POINT('Ctrl Pts',(-1.65157774273774,-1.04648776114666,
14.8870122510158));
#274255=CARTESIAN_POINT('Ctrl Pts',(-1.61375329407324,-1.10390778401485,
14.8909437724697));
#274256=CARTESIAN_POINT('Ctrl Pts',(-1.573103708595,-1.15907753062711,14.8948752939235));
#274257=CARTESIAN_POINT('Ctrl Pts',(-1.53259476845624,-1.21405639293761,
14.8987932125284));
#274258=CARTESIAN_POINT('Ctrl Pts',(-1.48911974745898,-1.26701818210528,
14.9027111311334));
#274259=CARTESIAN_POINT('Ctrl Pts',(-1.44290681470613,-1.3176251075608,
14.9066290497383));
#274260=CARTESIAN_POINT('Ctrl Pts',(-1.3967635271974,-1.36815576580132,
14.9105410638403));
#274261=CARTESIAN_POINT('Ctrl Pts',(-1.34789084593812,-1.41633824326813,
14.9144530779423));
#274262=CARTESIAN_POINT('Ctrl Pts',(-1.29655866312948,-1.46186580542261,
14.9183650920442));
#274263=CARTESIAN_POINT('Ctrl Pts',(-1.24528691084912,-1.50733977050637,
14.9222725007493));
#274264=CARTESIAN_POINT('Ctrl Pts',(-1.19156177366926,-1.55016470264205,
14.9261799094543));
#274265=CARTESIAN_POINT('Ctrl Pts',(-1.13569037152903,-1.5900702437365,
14.9300873181593));
#274266=CARTESIAN_POINT('Ctrl Pts',(-1.07985403491722,-1.62995073965879,
14.9339922745301));
#274267=CARTESIAN_POINT('Ctrl Pts',(-1.02187450480552,-1.66691519382847,
14.9378972309009));
#274268=CARTESIAN_POINT('Ctrl Pts',(-0.962091173610014,-1.70073412785823,
14.9418021872717));
#274269=CARTESIAN_POINT('Ctrl Pts',(-0.902324852326635,-1.73454343952195,
14.9457060325809));
#274270=CARTESIAN_POINT('Ctrl Pts',(-0.840756176772905,-1.76520876562135,
14.9496098778901));
#274271=CARTESIAN_POINT('Ctrl Pts',(-0.777751097026513,-1.79254546136885,
14.9535137231993));
#274272=CARTESIAN_POINT('Ctrl Pts',(-0.714742328412924,-1.81988375764508,
14.9574177970736));
#274273=CARTESIAN_POINT('Ctrl Pts',(-0.650297440949275,-1.84389284319112,
14.961321870948));
#274274=CARTESIAN_POINT('Ctrl Pts',(-0.584802739996737,-1.86443604215653,
14.9652259448224));
#274275=CARTESIAN_POINT('Ctrl Pts',(-0.519238238204495,-1.88500113499301,
14.9691341794552));
#274276=CARTESIAN_POINT('Ctrl Pts',(-0.452622160354177,-1.90209282208422,
14.9730424140881));
#274277=CARTESIAN_POINT('Ctrl Pts',(-0.385355395870925,-1.91562449840076,
14.976950648721));
#274278=CARTESIAN_POINT('Ctrl Pts',(-0.318048397483143,-1.92916426834537,
14.980861220965));
#274279=CARTESIAN_POINT('Ctrl Pts',(-0.250090424695966,-1.93913971830562,
14.9847717932091));
#274280=CARTESIAN_POINT('Ctrl Pts',(-0.181889169252525,-1.94551595472991,
14.9886823654531));
#274281=CARTESIAN_POINT('Ctrl Pts',(-0.113569959131261,-1.9519032189118,
14.9925997010666));
#274282=CARTESIAN_POINT('Ctrl Pts',(-0.0450071178671433,-1.95467882572272,
14.9965170366801));
#274283=CARTESIAN_POINT('Ctrl Pts',(0.0233908491985165,-1.95385999195791,
15.0004343722936));
#274284=CARTESIAN_POINT('Ctrl Pts',(0.0559642993326093,-1.95347003532689,
15.0022999414288));
#274285=CARTESIAN_POINT('Ctrl Pts',(0.0885004216232417,-1.95226562528409,
15.0041655105639));
#274286=CARTESIAN_POINT('Ctrl Pts',(0.120955691704299,-1.95025273250529,
15.0060310796991));
#274287=CARTESIAN_POINT('Ctrl Pts',(0.189115645727107,-1.94602541660517,
15.009948998304));
#274288=CARTESIAN_POINT('Ctrl Pts',(0.257189004158087,-1.93821219483261,
15.0138669169089));
#274289=CARTESIAN_POINT('Ctrl Pts',(0.324768225269652,-1.92682163156199,
15.0177848355139));
#274290=CARTESIAN_POINT('Ctrl Pts',(0.392245601052069,-1.91544823445053,
15.0216968496158));
#274291=CARTESIAN_POINT('Ctrl Pts',(0.459229836267934,-1.90050827659049,
15.0256088637178));
#274292=CARTESIAN_POINT('Ctrl Pts',(0.52531686116011,-1.88206221878579,
15.0295208778198));
#274293=CARTESIAN_POINT('Ctrl Pts',(0.591326085467733,-1.86363787650062,
15.0334282865248));
#274294=CARTESIAN_POINT('Ctrl Pts',(0.656439725564638,-1.84171576321858,
15.0373356952299));
#274295=CARTESIAN_POINT('Ctrl Pts',(0.720264091534097,-1.81640734375485,
15.0412431039349));
#274296=CARTESIAN_POINT('Ctrl Pts',(0.784048400604479,-1.79111480814346,
15.0451480603057));
#274297=CARTESIAN_POINT('Ctrl Pts',(0.846544584390473,-1.76244036314053,
15.0490530166765));
#274298=CARTESIAN_POINT('Ctrl Pts',(0.907375803439642,-1.73054475565709,
15.0529579730473));
#274299=CARTESIAN_POINT('Ctrl Pts',(0.968189714425392,-1.69865822330327,
15.0568618183565));
#274300=CARTESIAN_POINT('Ctrl Pts',(1.02733916561554,-1.6635525762057,15.0607656636657));
#274301=CARTESIAN_POINT('Ctrl Pts',(1.08447058888164,-1.62543518537366,
15.0646695089749));
#274302=CARTESIAN_POINT('Ctrl Pts',(1.14160535711974,-1.58731556281698,
15.0685735828492));
#274303=CARTESIAN_POINT('Ctrl Pts',(1.19672145505932,-1.54618412159655,
15.0724776567236));
#274304=CARTESIAN_POINT('Ctrl Pts',(1.24949458333011,-1.50229134532178,
15.076381730598));
#274305=CARTESIAN_POINT('Ctrl Pts',(1.3023239544513,-1.45835179041306,15.0802899652308));
#274306=CARTESIAN_POINT('Ctrl Pts',(1.35280499365664,-1.41164534250131,
15.0841981998637));
#274307=CARTESIAN_POINT('Ctrl Pts',(1.40064756563739,-1.36246188822809,
15.0881064344966));
#274308=CARTESIAN_POINT('Ctrl Pts',(1.44851875343587,-1.3132490161225,15.0920170067406));
#274309=CARTESIAN_POINT('Ctrl Pts',(1.49374800925436,-1.26155655936768,
15.0959275789846));
#274310=CARTESIAN_POINT('Ctrl Pts',(1.53608495973236,-1.20770815865591,
15.0998381512287));
#274311=CARTESIAN_POINT('Ctrl Pts',(1.57849513234272,-1.15376662665621,
15.1037554868422));
#274312=CARTESIAN_POINT('Ctrl Pts',(1.61800273271483,-1.09766211072205,
15.1076728224557));
#274313=CARTESIAN_POINT('Ctrl Pts',(1.65440073172345,-1.03974718988459,
15.1115901580692));
#274314=CARTESIAN_POINT('Ctrl Pts',(1.67173470313451,-1.01216612473229,
15.1134557272043));
#274315=CARTESIAN_POINT('Ctrl Pts',(1.68836409592214,-0.984174819782734,
15.1153212963395));
#274316=CARTESIAN_POINT('Ctrl Pts',(1.70427032758818,-0.95581308345433,
15.1171868654746));
#274317=CARTESIAN_POINT('Ctrl Pts',(1.73767531902174,-0.89625004055497,
15.1211047840796));
#274318=CARTESIAN_POINT('Ctrl Pts',(1.7680203237141,-0.834815447264566,
15.1250227026845));
#274319=CARTESIAN_POINT('Ctrl Pts',(1.79509156488076,-0.771856381520527,
15.1289406212894));
#274320=CARTESIAN_POINT('Ctrl Pts',(1.82212200830776,-0.708992198296166,
15.1328526353914));
#274321=CARTESIAN_POINT('Ctrl Pts',(1.84588828711157,-0.644608550526538,
15.1367646494934));
#274322=CARTESIAN_POINT('Ctrl Pts',(1.86622211267582,-0.579077737579145,
15.1406766635954));
#274323=CARTESIAN_POINT('Ctrl Pts',(1.88653200035639,-0.51362407041887,
15.1445840723004));
#274324=CARTESIAN_POINT('Ctrl Pts',(1.90341731483462,-0.447026387783651,
15.1484914810054));
#274325=CARTESIAN_POINT('Ctrl Pts',(1.91675825132557,-0.379675922301295,
15.1523988897104));
#274326=CARTESIAN_POINT('Ctrl Pts',(1.93009081489281,-0.312367726738288,
15.1563038460812));
#274327=CARTESIAN_POINT('Ctrl Pts',(1.93988331776019,-0.244308167001138,
15.160208802452));
#274328=CARTESIAN_POINT('Ctrl Pts',(1.94606650057897,-0.175901038440164,
15.1641137588228));
#274329=CARTESIAN_POINT('Ctrl Pts',(1.95224792412148,-0.107513373485817,
15.168017604132));
#274330=CARTESIAN_POINT('Ctrl Pts',(1.95482202199657,-0.038778825736158,
15.1719214494412));
#274331=CARTESIAN_POINT('Ctrl Pts',(1.953771328377,0.0298930830122975,15.1758252947503));
#274332=CARTESIAN_POINT('Ctrl Pts',(1.95272057324065,0.0985690124136654,
15.1797293686247));
#274333=CARTESIAN_POINT('Ctrl Pts',(1.94804461534932,0.167181803690281,
15.1836334424991));
#274334=CARTESIAN_POINT('Ctrl Pts',(1.93977808374912,0.235323151871166,
15.1875375163734));
#274335=CARTESIAN_POINT('Ctrl Pts',(1.9315027421103,0.303537121550285,15.1914457510063));
#274336=CARTESIAN_POINT('Ctrl Pts',(1.91962924927223,0.37127815611275,15.1953539856392));
#274337=CARTESIAN_POINT('Ctrl Pts',(1.90424386649369,0.438145292022133,
15.199262220272));
#274338=CARTESIAN_POINT('Ctrl Pts',(1.88884928133971,0.505052422808323,
15.2031727925161));
#274339=CARTESIAN_POINT('Ctrl Pts',(1.8699387612331,0.571084141675299,15.2070833647601));
#274340=CARTESIAN_POINT('Ctrl Pts',(1.84764848835242,0.635854593039192,
15.2109939370041));
#274341=CARTESIAN_POINT('Ctrl Pts',(1.82531966424652,0.700737065474845,
15.2149112726176));
#274342=CARTESIAN_POINT('Ctrl Pts',(1.79959960526362,0.764353460855958,
15.2188286082311));
#274343=CARTESIAN_POINT('Ctrl Pts',(1.77067231048155,0.826338652668465,
15.2227459438446));
#274344=CARTESIAN_POINT('Ctrl Pts',(1.75689614381259,0.855858120003723,
15.2246115129798));
#274345=CARTESIAN_POINT('Ctrl Pts',(1.74239324672286,0.885008005651919,
15.226477082115));
#274346=CARTESIAN_POINT('Ctrl Pts',(1.72718699236919,0.913751111293806,
15.2283426512502));
#274347=CARTESIAN_POINT('Ctrl Pts',(1.69525203712161,0.974115075423408,
15.2322605698551));
#274348=CARTESIAN_POINT('Ctrl Pts',(1.66008537049449,1.03292267800056,15.23617848846));
#274349=CARTESIAN_POINT('Ctrl Pts',(1.62186271066378,1.0898061055795,15.2400964070649));
#274350=CARTESIAN_POINT('Ctrl Pts',(1.58369765432871,1.1466038069351,15.2440084211669));
#274351=CARTESIAN_POINT('Ctrl Pts',(1.54248601726698,1.20148268337229,15.2479204352689));
#274352=CARTESIAN_POINT('Ctrl Pts',(1.49844937390611,1.25409946728336,15.2518324493709));
#274353=CARTESIAN_POINT('Ctrl Pts',(1.45446457244015,1.30665430837648,15.2557398580759));
#274354=CARTESIAN_POINT('Ctrl Pts',(1.40766168382216,1.3569519702945,15.2596472667809));
#274355=CARTESIAN_POINT('Ctrl Pts',(1.3583044794147,1.40467965785867,15.2635546754859));
#274356=CARTESIAN_POINT('Ctrl Pts',(1.30897825215094,1.45237739098249,15.2674596318567));
#274357=CARTESIAN_POINT('Ctrl Pts',(1.25710124200206,1.49750800810701,15.2713645882275));
#274358=CARTESIAN_POINT('Ctrl Pts',(1.20297518228468,1.53979437289761,15.2752695445984));
#274359=CARTESIAN_POINT('Ctrl Pts',(1.14886452283863,1.58206870611793,15.2791733899075));
#274360=CARTESIAN_POINT('Ctrl Pts',(1.0925064716272,1.62150009079892,15.2830772352167));
#274361=CARTESIAN_POINT('Ctrl Pts',(1.03423565650843,1.65785180483859,15.2869810805259));
#274362=CARTESIAN_POINT('Ctrl Pts',(0.975961429707744,1.69420564722476,
15.2908851544003));
#274363=CARTESIAN_POINT('Ctrl Pts',(0.915774635395799,1.7274792027814,15.2947892282746));
#274364=CARTESIAN_POINT('Ctrl Pts',(0.85403712532951,1.75748018155509,15.298693302149));
#274365=CARTESIAN_POINT('Ctrl Pts',(0.792233818641646,1.78751313380884,
15.3026015367818));
#274366=CARTESIAN_POINT('Ctrl Pts',(0.72887694127389,1.8142663333555,15.3065097714147));
#274367=CARTESIAN_POINT('Ctrl Pts',(0.66435017186063,1.83759485446296,15.3104180060476));
#274368=CARTESIAN_POINT('Ctrl Pts',(0.59978480740128,1.86093732893204,15.3143285782916));
#274369=CARTESIAN_POINT('Ctrl Pts',(0.534048629164836,1.88085090566003,
15.3182391505356));
#274370=CARTESIAN_POINT('Ctrl Pts',(0.467539689018546,1.89724079631249,
15.3221497227796));
#274371=CARTESIAN_POINT('Ctrl Pts',(0.4009157210687,1.91365903342661,15.3260670583932));
#274372=CARTESIAN_POINT('Ctrl Pts',(0.333516806699145,1.92654132891995,
15.3299843940067));
#274373=CARTESIAN_POINT('Ctrl Pts',(0.265749507083569,1.93584431178875,
15.3339017296202));
#274374=CARTESIAN_POINT('Ctrl Pts',(0.233476402348129,1.94027471025791,
15.3357672987554));
#274375=CARTESIAN_POINT('Ctrl Pts',(0.201119796147725,1.94389408762178,
15.3376328678906));
#274376=CARTESIAN_POINT('Ctrl Pts',(0.168723617269851,1.94670191374421,
15.3394984370257));
#274377=CARTESIAN_POINT('Ctrl Pts',(0.100687761852009,1.95259868486726,
15.3434163556307));
#274378=CARTESIAN_POINT('Ctrl Pts',(0.0322073647878031,1.95493615796299,
15.3473342742356));
#274379=CARTESIAN_POINT('Ctrl Pts',(-0.0363132450550216,1.95366254717481,
15.3512521928405));
#274380=CARTESIAN_POINT('Ctrl Pts',(-0.104730590847791,1.95239085578298,
15.3551642069425));
#274381=CARTESIAN_POINT('Ctrl Pts',(-0.173187541255314,1.94751889014242,
15.3590762210445));
#274382=CARTESIAN_POINT('Ctrl Pts',(-0.241275528199328,1.93904670379342,
15.3629882351465));
#274383=CARTESIAN_POINT('Ctrl Pts',(-0.309283358937298,1.93058449127895,
15.3668956438515));
#274384=CARTESIAN_POINT('Ctrl Pts',(-0.376922602996216,1.91853053588878,
15.3708030525565));
#274385=CARTESIAN_POINT('Ctrl Pts',(-0.443787416982026,1.90293686929662,
15.3747104612615));
#274386=CARTESIAN_POINT('Ctrl Pts',(-0.510610265849078,1.8873529894672,
15.3786154176323));
#274387=CARTESIAN_POINT('Ctrl Pts',(-0.576659170782764,1.868233916762,15.3825203740031));
#274388=CARTESIAN_POINT('Ctrl Pts',(-0.641537667170822,1.84568291469608,
15.3864253303739));
#274389=CARTESIAN_POINT('Ctrl Pts',(-0.70639770393955,1.82313832897667,
15.3903291756831));
#274390=CARTESIAN_POINT('Ctrl Pts',(-0.770087528791084,1.79716391378434,
15.3942330209923));
#274391=CARTESIAN_POINT('Ctrl Pts',(-0.832226799177427,1.76791248503168,
15.3981368663015));
#274392=CARTESIAN_POINT('Ctrl Pts',(-0.89436970773915,1.73865934364501,
15.4020409401758));
#274393=CARTESIAN_POINT('Ctrl Pts',(-0.954961437599773,1.70612901961545,
15.4059450140502));
#274394=CARTESIAN_POINT('Ctrl Pts',(-1.01364421897853,1.67052129508468,
15.4098490879245));
#274395=CARTESIAN_POINT('Ctrl Pts',(-1.07238954140798,1.63487562169647,
15.4137573225574));
#274396=CARTESIAN_POINT('Ctrl Pts',(-1.12922143379994,1.59614625812135,
15.4176655571903));
#274397=CARTESIAN_POINT('Ctrl Pts',(-1.18381008911126,1.55457700771573,
15.4215737918232));
#274398=CARTESIAN_POINT('Ctrl Pts',(-1.2384313952384,1.51298289372021,15.4254843640672));
#274399=CARTESIAN_POINT('Ctrl Pts',(-1.29080641881575,1.46854583067027,
15.4293949363112));
#274400=CARTESIAN_POINT('Ctrl Pts',(-1.34063968711691,1.42154888390342,
15.4333055085552));
#274401=CARTESIAN_POINT('Ctrl Pts',(-1.39055914249879,1.37447065549917,
15.4372228441687));
#274402=CARTESIAN_POINT('Ctrl Pts',(-1.43792772942498,1.32482406278651,
15.4411401797822));
#274403=CARTESIAN_POINT('Ctrl Pts',(-1.48248856441694,1.27292719995018,
15.4450575153957));
#274404=CARTESIAN_POINT('Ctrl Pts',(-1.50370995737396,1.24821213974798,
15.4469230845309));
#274405=CARTESIAN_POINT('Ctrl Pts',(-1.52429517046379,1.2229871747464,15.4487886536661));
#274406=CARTESIAN_POINT('Ctrl Pts',(-1.54421993964279,1.19728892837511,
15.4506542228012));
#274407=CARTESIAN_POINT('Ctrl Pts',(-1.58608153931649,1.14329735174773,
15.454573751685));
#274408=CARTESIAN_POINT('Ctrl Pts',(-1.62519387850404,1.08699708252043,
15.4584932805689));
#274409=CARTESIAN_POINT('Ctrl Pts',(-1.66129293659796,1.02869907106488,
15.4624128094527));
#274410=CARTESIAN_POINT('Ctrl Pts',(-1.69733844138664,0.970487545278667,
15.4663265236771));
#274411=CARTESIAN_POINT('Ctrl Pts',(-1.73037927662693,0.910284569449585,
15.4702402379015));
#274412=CARTESIAN_POINT('Ctrl Pts',(-1.76019243483317,0.848433021726573,
15.4741539521259));
#274413=CARTESIAN_POINT('Ctrl Pts',(-1.78997153867594,0.786652124522111,
15.4780631958731));
#274414=CARTESIAN_POINT('Ctrl Pts',(-1.81653007025389,0.723226832147985,
15.4819724396202));
#274415=CARTESIAN_POINT('Ctrl Pts',(-1.83968996959911,0.658526245305715,
15.4858816833674));
#274416=CARTESIAN_POINT('Ctrl Pts',(-1.86283217533394,0.5938750881677,15.4897879405456));
#274417=CARTESIAN_POINT('Ctrl Pts',(-1.88258073813993,0.527951031449829,
15.4936941977238));
#274418=CARTESIAN_POINT('Ctrl Pts',(-1.89880565127024,0.461143251825488,
15.497600454902));
#274419=CARTESIAN_POINT('Ctrl Pts',(-1.91502356470393,0.394364294185336,
15.5015050268561));
#274420=CARTESIAN_POINT('Ctrl Pts',(-1.92772073426583,0.326702847837579,
15.5054095988102));
#274421=CARTESIAN_POINT('Ctrl Pts',(-1.93681746653096,0.258561600669126,
15.5093141707643));
#274422=CARTESIAN_POINT('Ctrl Pts',(-1.94591515674891,0.19041317772614,
15.5132191538985));
#274423=CARTESIAN_POINT('Ctrl Pts',(-1.95141158638116,0.121785339361323,
15.5171241370327));
#274424=CARTESIAN_POINT('Ctrl Pts',(-1.95327870347652,0.0530877249942702,
15.5210291201669));
#274425=CARTESIAN_POINT('Ctrl Pts',(-1.95377296771858,0.0349020555576315,
15.5220628494032));
#274426=CARTESIAN_POINT('Ctrl Pts',(-1.95401318365985,0.0167115111454544,
15.5230965786395));
#274427=CARTESIAN_POINT('Ctrl Pts',(-1.95399944231052,-0.00147629610118066,
15.5241303078758));
#274428=CARTESIAN_POINT('',(-1.9542420472437,-0.000492779743085885,16.2241302604684));
#274429=CARTESIAN_POINT('Ctrl Pts',(-1.95209224254652,-0.00148915573612675,
15.5241311214624));
#274430=CARTESIAN_POINT('Ctrl Pts',(-1.95364004303147,-0.222253404836076,
15.5366907505006));
#274431=CARTESIAN_POINT('Ctrl Pts',(-1.81714905168899,-1.09243017089523,
15.5863023081303));
#274432=CARTESIAN_POINT('Ctrl Pts',(-0.537454058353606,-2.24624899054346,
15.6729657943525));
#274433=CARTESIAN_POINT('Ctrl Pts',(1.5959832982511,-1.66952948583204,15.7841215801279));
#274434=CARTESIAN_POINT('Ctrl Pts',(2.2681682583395,0.43577992637193,15.8952773659034));
#274435=CARTESIAN_POINT('Ctrl Pts',(0.863660870300283,2.14209740522327,
16.0064331516791));
#274436=CARTESIAN_POINT('Ctrl Pts',(-1.30121699004713,1.89067897567588,
16.1160505996986));
#274437=CARTESIAN_POINT('Ctrl Pts',(-1.9549464319646,0.619678012551105,
16.1886161191264));
#274438=CARTESIAN_POINT('Ctrl Pts',(-1.95705348401711,-0.000483876568800027,
16.2241297099623));
#274439=CARTESIAN_POINT('',(-1.953999187747,0.0017816520611407,16.9241302923036));
#274440=CARTESIAN_POINT('Ctrl Pts',(-1.95399993766937,-0.000493546448478972,
16.2241303078758));
#274441=CARTESIAN_POINT('Ctrl Pts',(-1.95399316389338,-0.027311605637371,
16.2256684463272));
#274442=CARTESIAN_POINT('Ctrl Pts',(-1.95343431063418,-0.0541219966759405,
16.2272065847787));
#274443=CARTESIAN_POINT('Ctrl Pts',(-1.95232417177688,-0.0809093832366167,
16.2287447232302));
#274444=CARTESIAN_POINT('Ctrl Pts',(-1.94949644604203,-0.149141732594158,
16.2326626418351));
#274445=CARTESIAN_POINT('Ctrl Pts',(-1.9430817925214,-0.217361090421165,
16.23658056044));
#274446=CARTESIAN_POINT('Ctrl Pts',(-1.93308041068442,-0.285159825059866,
16.2404984790448));
#274447=CARTESIAN_POINT('Ctrl Pts',(-1.92309410143939,-0.352856383551347,
16.2444104931467));
#274448=CARTESIAN_POINT('Ctrl Pts',(-1.90953186281156,-0.420133094167381,
16.2483225072486));
#274449=CARTESIAN_POINT('Ctrl Pts',(-1.89244585101954,-0.486584731530828,
16.2522345213504));
#274450=CARTESIAN_POINT('Ctrl Pts',(-1.87537995364044,-0.552958139071596,
16.2561419300553));
#274451=CARTESIAN_POINT('Ctrl Pts',(-1.8547986436603,-0.61850792821327,
16.2600493387601));
#274452=CARTESIAN_POINT('Ctrl Pts',(-1.83080528357202,-0.682838204587869,
16.263956747465));
#274453=CARTESIAN_POINT('Ctrl Pts',(-1.80682698198983,-0.747128106548239,
16.2678617038356));
#274454=CARTESIAN_POINT('Ctrl Pts',(-1.77944104973901,-0.810199554116817,
16.2717666602062));
#274455=CARTESIAN_POINT('Ctrl Pts',(-1.74880046681653,-0.871672488531269,
16.2756716165768));
#274456=CARTESIAN_POINT('Ctrl Pts',(-1.71816860193657,-0.933127932297529,
16.2795754618858));
#274457=CARTESIAN_POINT('Ctrl Pts',(-1.68428414405233,-0.992985325723271,
16.2834793071948));
#274458=CARTESIAN_POINT('Ctrl Pts',(-1.64734716498844,-1.0508869197038,
16.2873831525037));
#274459=CARTESIAN_POINT('Ctrl Pts',(-1.61040802331153,-1.10879190374881,
16.2912872263779));
#274460=CARTESIAN_POINT('Ctrl Pts',(-1.57041627235939,-1.16474044764703,
16.295191300252));
#274461=CARTESIAN_POINT('Ctrl Pts',(-1.52761568809808,-1.21840318018159,
16.2990953741261));
#274462=CARTESIAN_POINT('Ctrl Pts',(-1.48476948920408,-1.27212310366054,
16.3030036087587));
#274463=CARTESIAN_POINT('Ctrl Pts',(-1.43910879018471,-1.32355196871172,
16.3069118433913));
#274464=CARTESIAN_POINT('Ctrl Pts',(-1.39091746281637,-1.37239375240215,
16.310820078024));
#274465=CARTESIAN_POINT('Ctrl Pts',(-1.34269731103114,-1.42126474956339,
16.3147306502678));
#274466=CARTESIAN_POINT('Ctrl Pts',(-1.29194388205237,-1.46754525424671,
16.3186412225115));
#274467=CARTESIAN_POINT('Ctrl Pts',(-1.23897561054832,-1.51097830443273,
16.3225517947553));
#274468=CARTESIAN_POINT('Ctrl Pts',(-1.18591572994759,-1.55448647246536,
16.3264691303686));
#274469=CARTESIAN_POINT('Ctrl Pts',(-1.13063375764106,-1.59513706573119,
16.3303864659819));
#274470=CARTESIAN_POINT('Ctrl Pts',(-1.07347795000258,-1.6327158634797,
16.3343038015952));
#274471=CARTESIAN_POINT('Ctrl Pts',(-1.04625840048215,-1.65061217163273,
16.3361693707319));
#274472=CARTESIAN_POINT('Ctrl Pts',(-1.01861423899964,-1.66781246799583,
16.3380349398686));
#274473=CARTESIAN_POINT('Ctrl Pts',(-0.9905848842623,-1.6842973570813,16.3399005090053));
#274474=CARTESIAN_POINT('Ctrl Pts',(-0.931719882550855,-1.71891759837199,
16.3438184276108));
#274475=CARTESIAN_POINT('Ctrl Pts',(-0.870920931029039,-1.75051690307593,
16.3477363462163));
#274476=CARTESIAN_POINT('Ctrl Pts',(-0.808530647667815,-1.77887441709129,
16.3516542648218));
#274477=CARTESIAN_POINT('Ctrl Pts',(-0.746234389642191,-1.8071891948883,
16.3555662789244));
#274478=CARTESIAN_POINT('Ctrl Pts',(-0.682352003608599,-1.83227167611146,
16.3594782930269));
#274479=CARTESIAN_POINT('Ctrl Pts',(-0.617252257112829,-1.85394596768329,
16.3633903071295));
#274480=CARTESIAN_POINT('Ctrl Pts',(-0.552229148933675,-1.8755947433152,
16.3672977158351));
#274481=CARTESIAN_POINT('Ctrl Pts',(-0.485991991036962,-1.89384314303914,
16.3712051245408));
#274482=CARTESIAN_POINT('Ctrl Pts',(-0.418929475171209,-1.90856335887305,
16.3751125332464));
#274483=CARTESIAN_POINT('Ctrl Pts',(-0.351909048504303,-1.92327433613183,
16.3790174896178));
#274484=CARTESIAN_POINT('Ctrl Pts',(-0.284064770837009,-1.93446141676652,
16.3829224459892));
#274485=CARTESIAN_POINT('Ctrl Pts',(-0.215798931230133,-1.94204706979,16.3868274023607));
#274486=CARTESIAN_POINT('Ctrl Pts',(-0.147552515029612,-1.94963056449796,
16.3907312476705));
#274487=CARTESIAN_POINT('Ctrl Pts',(-0.0788852636999524,-1.95361461147805,
16.3946350929803));
#274488=CARTESIAN_POINT('Ctrl Pts',(-0.0102062543892486,-1.95397334484669,
16.3985389382901));
#274489=CARTESIAN_POINT('Ctrl Pts',(0.0584767759899475,-1.95433209921871,
16.4024430121651));
#274490=CARTESIAN_POINT('Ctrl Pts',(0.127171073771154,-1.95106511856314,
16.40634708604));
#274491=CARTESIAN_POINT('Ctrl Pts',(0.195467709344648,-1.94419864587021,
16.410251159915));
#274492=CARTESIAN_POINT('Ctrl Pts',(0.263837131913595,-1.93732485524848,
16.4141593945485));
#274493=CARTESIAN_POINT('Ctrl Pts',(0.331807556064612,-1.9268439660771,
16.418067629182));
#274494=CARTESIAN_POINT('Ctrl Pts',(0.398976332539859,-1.91283399333895,
16.4219758638155));
#274495=CARTESIAN_POINT('Ctrl Pts',(0.466185284310451,-1.89881564089193,
16.4258864360601));
#274496=CARTESIAN_POINT('Ctrl Pts',(0.532591158464872,-1.88126412966425,
16.4297970083048));
#274497=CARTESIAN_POINT('Ctrl Pts',(0.597805386096926,-1.86030769507453,
16.4337075805494));
#274498=CARTESIAN_POINT('Ctrl Pts',(0.663132402315464,-1.83931501614486,
16.4376249161635));
#274499=CARTESIAN_POINT('Ctrl Pts',(0.727263199095435,-1.814905835472,16.4415422517776));
#274500=CARTESIAN_POINT('Ctrl Pts',(0.789828950992136,-1.78725662068285,
16.4454595873917));
#274501=CARTESIAN_POINT('Ctrl Pts',(0.819624900796952,-1.77408911943775,
16.4473251565216));
#274502=CARTESIAN_POINT('Ctrl Pts',(0.849066259865159,-1.76018745667784,
16.4491907256515));
#274503=CARTESIAN_POINT('Ctrl Pts',(0.878115358073886,-1.74557423729693,
16.4510562947813));
#274504=CARTESIAN_POINT('Ctrl Pts',(0.93912194340399,-1.71488472643146,
16.4549742133857));
#274505=CARTESIAN_POINT('Ctrl Pts',(0.998638812367975,-1.68093224684657,
16.45889213199));
#274506=CARTESIAN_POINT('Ctrl Pts',(1.05629462308656,-1.6438849318728,16.4628100505943));
#274507=CARTESIAN_POINT('Ctrl Pts',(1.11386354356105,-1.6068934490901,16.4667220646957));
#274508=CARTESIAN_POINT('Ctrl Pts',(1.16957656159134,-1.56681665120158,
16.4706340787971));
#274509=CARTESIAN_POINT('Ctrl Pts',(1.22308593495831,-1.52386902183461,
16.4745460928984));
#274510=CARTESIAN_POINT('Ctrl Pts',(1.27653231471146,-1.48097195232674,
16.4784535016028));
#274511=CARTESIAN_POINT('Ctrl Pts',(1.32777982013092,-1.43521106985662,
16.4823609103072));
#274512=CARTESIAN_POINT('Ctrl Pts',(1.37651030909296,-1.38684367142112,
16.4862683190116));
#274513=CARTESIAN_POINT('Ctrl Pts',(1.42521021424511,-1.33850662891575,
16.4901732753818));
#274514=CARTESIAN_POINT('Ctrl Pts',(1.47139588819428,-1.28756666126125,
16.494078231752));
#274515=CARTESIAN_POINT('Ctrl Pts',(1.51478406114057,-1.23431975116437,
16.4979831881222));
#274516=CARTESIAN_POINT('Ctrl Pts',(1.5581598890236,-1.1810879911978,16.5018870334308));
#274517=CARTESIAN_POINT('Ctrl Pts',(1.59873948540423,-1.12555097299784,
16.5057908787394));
#274518=CARTESIAN_POINT('Ctrl Pts',(1.63627931118113,-1.0680383962202,16.509694724048));
#274519=CARTESIAN_POINT('Ctrl Pts',(1.67382133486708,-1.01052245215434,
16.5135987979217));
#274520=CARTESIAN_POINT('Ctrl Pts',(1.70832296786059,-0.951031133220822,
16.5175028717955));
#274521=CARTESIAN_POINT('Ctrl Pts',(1.73958453519513,-0.889922269026882,
16.5214069456692));
#274522=CARTESIAN_POINT('Ctrl Pts',(1.77087941947939,-0.828748278189293,
16.5253151803015));
#274523=CARTESIAN_POINT('Ctrl Pts',(1.79892712227707,-0.765953740510865,
16.5292234149338));
#274524=CARTESIAN_POINT('Ctrl Pts',(1.82357487496324,-0.701919279834076,
16.5331316495661));
#274525=CARTESIAN_POINT('Ctrl Pts',(1.8482373700759,-0.637846518573021,
16.5370422218095));
#274526=CARTESIAN_POINT('Ctrl Pts',(1.86949571557832,-0.572532826192455,
16.5409527940529));
#274527=CARTESIAN_POINT('Ctrl Pts',(1.88724697473463,-0.506374225602937,
16.5448633662964));
#274528=CARTESIAN_POINT('Ctrl Pts',(1.90502893485162,-0.440101203124977,
16.5487807019093));
#274529=CARTESIAN_POINT('Ctrl Pts',(1.91929160048593,-0.372980836894027,
16.5526980375223));
#274530=CARTESIAN_POINT('Ctrl Pts',(1.92998326678699,-0.305418712462424,
16.5566153731352));
#274531=CARTESIAN_POINT('Ctrl Pts',(1.93507500379461,-0.273243319067745,
16.5584809422757));
#274532=CARTESIAN_POINT('Ctrl Pts',(1.93935760399372,-0.24096779895067,
16.5603465114162));
#274533=CARTESIAN_POINT('Ctrl Pts',(1.94282963590388,-0.208636060769936,
16.5622120805567));
#274534=CARTESIAN_POINT('Ctrl Pts',(1.95012131870425,-0.140735538741785,
16.5661299991607));
#274535=CARTESIAN_POINT('Ctrl Pts',(1.95386357534866,-0.0723175288653932,
16.5700479177647));
#274536=CARTESIAN_POINT('Ctrl Pts',(1.95399633371426,-0.00378521217720786,
16.5739658363687));
#274537=CARTESIAN_POINT('Ctrl Pts',(1.95412889200624,0.0646438228180311,
16.5778778504698));
#274538=CARTESIAN_POINT('Ctrl Pts',(1.95066274689834,0.133186334766387,
16.5817898645709));
#274539=CARTESIAN_POINT('Ctrl Pts',(1.94358956775634,0.201433840525196,
16.585701878672));
#274540=CARTESIAN_POINT('Ctrl Pts',(1.93652471547539,0.269601002285023,
16.5896092873761));
#274541=CARTESIAN_POINT('Ctrl Pts',(1.92586131293985,0.337473360588105,
16.5935166960802));
#274542=CARTESIAN_POINT('Ctrl Pts',(1.91164305261644,0.404644089766898,
16.5974241047843));
#274543=CARTESIAN_POINT('Ctrl Pts',(1.8974337158352,0.471772661830811,16.6013290611542));
#274544=CARTESIAN_POINT('Ctrl Pts',(1.87967404861689,0.53819999808793,16.605234017524));
#274545=CARTESIAN_POINT('Ctrl Pts',(1.85845915694204,0.60352759835675,16.6091389738939));
#274546=CARTESIAN_POINT('Ctrl Pts',(1.83725030145551,0.668836611224643,
16.6130428192022));
#274547=CARTESIAN_POINT('Ctrl Pts',(1.81258832499304,0.733046041599784,
16.6169466645105));
#274548=CARTESIAN_POINT('Ctrl Pts',(1.78461820633659,0.795772491112862,
16.6208505098187));
#274549=CARTESIAN_POINT('Ctrl Pts',(1.75664645006534,0.858502613179624,
16.6247545836921));
#274550=CARTESIAN_POINT('Ctrl Pts',(1.72536636974336,0.919749133749592,
16.6286586575656));
#274551=CARTESIAN_POINT('Ctrl Pts',(1.69097036370414,0.979150258680603,
16.632562731439));
#274552=CARTESIAN_POINT('Ctrl Pts',(1.65653770019385,1.03861469023553,16.636470966071));
#274553=CARTESIAN_POINT('Ctrl Pts',(1.61898273063974,1.09622937460925,16.6403792007029));
#274554=CARTESIAN_POINT('Ctrl Pts',(1.57854243913934,1.15165957115635,16.6442874353349));
#274555=CARTESIAN_POINT('Ctrl Pts',(1.53807795930705,1.20712292186583,16.648198007578));
#274556=CARTESIAN_POINT('Ctrl Pts',(1.49472503345375,1.26039880276027,16.6521085798211));
#274557=CARTESIAN_POINT('Ctrl Pts',(1.44876060395979,1.31118599459194,16.6560191520642));
#274558=CARTESIAN_POINT('Ctrl Pts',(1.40271667857609,1.36206102332372,16.6599364876767));
#274559=CARTESIAN_POINT('Ctrl Pts',(1.35405258373583,1.41043842576115,16.6638538232893));
#274560=CARTESIAN_POINT('Ctrl Pts',(1.30308107517443,1.45605484495683,16.6677711589019));
#274561=CARTESIAN_POINT('Ctrl Pts',(1.27880670019815,1.47777894329889,16.6696367280454));
#274562=CARTESIAN_POINT('Ctrl Pts',(1.25400947284102,1.49887745941012,16.6715022971888));
#274563=CARTESIAN_POINT('Ctrl Pts',(1.22872551090253,1.51932538281216,16.6733678663323));
#274564=CARTESIAN_POINT('Ctrl Pts',(1.17562616299812,1.56226847065926,16.6772857849413));
#274565=CARTESIAN_POINT('Ctrl Pts',(1.12016746720938,1.60250976330026,16.6812037035503));
#274566=CARTESIAN_POINT('Ctrl Pts',(1.0626556220808,1.63978017699326,16.6851216221593));
#274567=CARTESIAN_POINT('Ctrl Pts',(1.00523045023266,1.67699442227417,16.6890336362654));
#274568=CARTESIAN_POINT('Ctrl Pts',(0.945758679412449,1.71124640897584,
16.6929456503715));
#274569=CARTESIAN_POINT('Ctrl Pts',(0.884579017944451,1.74230765394991,
16.6968576644776));
#274570=CARTESIAN_POINT('Ctrl Pts',(0.823471379894613,1.77333233224509,
16.7007650731867));
#274571=CARTESIAN_POINT('Ctrl Pts',(0.760660280836818,1.80117350717616,
16.7046724818958));
#274572=CARTESIAN_POINT('Ctrl Pts',(0.696511243825545,1.82564730636139,
16.7085798906049));
#274573=CARTESIAN_POINT('Ctrl Pts',(0.632402467480672,1.85010574551144,
16.7124848469797));
#274574=CARTESIAN_POINT('Ctrl Pts',(0.566957877471911,1.87120082625279,
16.7163898033546));
#274575=CARTESIAN_POINT('Ctrl Pts',(0.50056387830783,1.8887963902267,16.7202947597295));
#274576=CARTESIAN_POINT('Ctrl Pts',(0.434188769962954,1.90638694780513,
16.7241986050427));
#274577=CARTESIAN_POINT('Ctrl Pts',(0.366865264016026,1.9204798392786,16.728102450356));
#274578=CARTESIAN_POINT('Ctrl Pts',(0.298994117277603,1.93098899992553,
16.7320062956692));
#274579=CARTESIAN_POINT('Ctrl Pts',(0.231118996770347,1.94149877587037,
16.7359103695476));
#274580=CARTESIAN_POINT('Ctrl Pts',(0.162696658351408,1.94842433167081,
16.739814443426));
#274581=CARTESIAN_POINT('Ctrl Pts',(0.0941354173468984,1.95173116058563,
16.7437185173044));
#274582=CARTESIAN_POINT('Ctrl Pts',(0.0255011073450798,1.95504151374636,
16.7476267519413));
#274583=CARTESIAN_POINT('Ctrl Pts',(-0.0432719083604364,1.95472541954719,
16.7515349865782));
#274584=CARTESIAN_POINT('Ctrl Pts',(-0.111773871146991,1.95080050280105,
16.755443221215));
#274585=CARTESIAN_POINT('Ctrl Pts',(-0.180316806639969,1.9468732384658,
16.759353793463));
#274586=CARTESIAN_POINT('Ctrl Pts',(-0.248587877520439,1.93933290973836,
16.763264365711));
#274587=CARTESIAN_POINT('Ctrl Pts',(-0.316183825544045,1.92824889173165,
16.767174937959));
#274588=CARTESIAN_POINT('Ctrl Pts',(-0.383896681359458,1.91714570381746,
16.7710922735764));
#274589=CARTESIAN_POINT('Ctrl Pts',(-0.450931603554621,1.90248669937868,
16.7750096091938));
#274590=CARTESIAN_POINT('Ctrl Pts',(-0.516897729096984,1.88439187475811,
16.7789269448112));
#274591=CARTESIAN_POINT('Ctrl Pts',(-0.548313052522219,1.87577450086955,
16.78079251391));
#274592=CARTESIAN_POINT('Ctrl Pts',(-0.579486230068499,1.86637860719992,
16.7826580830089));
#274593=CARTESIAN_POINT('Ctrl Pts',(-0.610376663439658,1.85622098057539,
16.7845236521078));
#274594=CARTESIAN_POINT('Ctrl Pts',(-0.675250274141671,1.8348887477971,
16.7884415707076));
#274595=CARTESIAN_POINT('Ctrl Pts',(-0.739132979750126,1.81010914982836,
16.7923594893073));
#274596=CARTESIAN_POINT('Ctrl Pts',(-0.801632660703622,1.78199356825249,
16.7962774079071));
#274597=CARTESIAN_POINT('Ctrl Pts',(-0.86403815145392,1.75392035829038,
16.8001894220039));
#274598=CARTESIAN_POINT('Ctrl Pts',(-0.925064309086546,1.72252134266924,
16.8041014361007));
#274599=CARTESIAN_POINT('Ctrl Pts',(-0.984335501314149,1.68795723312311,
16.8080134501975));
#274600=CARTESIAN_POINT('Ctrl Pts',(-1.04353691685918,1.65343381398339,
16.8119208588974));
#274601=CARTESIAN_POINT('Ctrl Pts',(-1.10098704719417,1.6157529476028,16.8158282675974));
#274602=CARTESIAN_POINT('Ctrl Pts',(-1.15633320473661,1.57512206499165,
16.8197356762973));
#274603=CARTESIAN_POINT('Ctrl Pts',(-1.21164462640057,1.53451668278493,
16.823640632663));
#274604=CARTESIAN_POINT('Ctrl Pts',(-1.26485429900329,1.49096524750577,
16.8275455890287));
#274605=CARTESIAN_POINT('Ctrl Pts',(-1.31563830423586,1.44471860665923,
16.8314505453945));
#274606=CARTESIAN_POINT('Ctrl Pts',(-1.36640786009908,1.39848512418395,
16.8353543906986));
#274607=CARTESIAN_POINT('Ctrl Pts',(-1.41475275512536,1.34955828953871,
16.8392582360028));
#274608=CARTESIAN_POINT('Ctrl Pts',(-1.46038337990191,1.29822817089534,
16.8431620813069));
#274609=CARTESIAN_POINT('Ctrl Pts',(-1.506016676294,1.24689504693826,16.8470661551763));
#274610=CARTESIAN_POINT('Ctrl Pts',(-1.54893506200075,1.1931587289922,16.8509702290457));
#274611=CARTESIAN_POINT('Ctrl Pts',(-1.58888815056499,1.13734359144199,
16.8548743029151));
#274612=CARTESIAN_POINT('Ctrl Pts',(-1.62888381905042,1.08146896902481,
16.8587825375431));
#274613=CARTESIAN_POINT('Ctrl Pts',(-1.66590759656421,1.02351150631851,
16.8626907721711));
#274614=CARTESIAN_POINT('Ctrl Pts',(-1.69975211727543,0.963825056645488,
16.8665990067991));
#274615=CARTESIAN_POINT('Ctrl Pts',(-1.7336168812265,0.90410290703963,16.8705095790383));
#274616=CARTESIAN_POINT('Ctrl Pts',(-1.76429838408449,0.84265015251891,
16.8744201512775));
#274617=CARTESIAN_POINT('Ctrl Pts',(-1.79163626743338,0.779843244003176,
16.8783307235167));
#274618=CARTESIAN_POINT('Ctrl Pts',(-1.81902143189563,0.716927710378318,
16.8822480591255));
#274619=CARTESIAN_POINT('Ctrl Pts',(-1.84305126298817,0.652653808977684,
16.8861653947343));
#274620=CARTESIAN_POINT('Ctrl Pts',(-1.86361465725008,0.587415023031145,
16.8900827303431));
#274621=CARTESIAN_POINT('Ctrl Pts',(-1.87340764881474,0.556346082158551,
16.8919482995232));
#274622=CARTESIAN_POINT('Ctrl Pts',(-1.88241520042632,0.525058482026375,
16.8938138687033));
#274623=CARTESIAN_POINT('Ctrl Pts',(-1.89062940432749,0.493595437065913,
16.8956794378834));
#274624=CARTESIAN_POINT('Ctrl Pts',(-1.91275769521846,0.408836960215565,
16.9007051053724));
#274625=CARTESIAN_POINT('Ctrl Pts',(-1.92919629943473,0.322535927961186,
16.9057307728614));
#274626=CARTESIAN_POINT('Ctrl Pts',(-1.93977379464525,0.235358504430079,
16.9107564403505));
#274627=CARTESIAN_POINT('Ctrl Pts',(-1.94915641929425,0.158028945155436,
16.9152143910015));
#274628=CARTESIAN_POINT('Ctrl Pts',(-1.95392785941723,0.080009888355393,
16.9196723416526));
#274629=CARTESIAN_POINT('Ctrl Pts',(-1.953999187747,0.0017816520611407,
16.9241302923036));
#274630=CARTESIAN_POINT('',(-1.95094246698047,-0.000563023513259459,17.6241303078758));
#274631=CARTESIAN_POINT('Ctrl Pts',(-1.95354848948922,0.00178096791722124,
16.9241303078758));
#274632=CARTESIAN_POINT('Ctrl Pts',(-1.94920835895243,-0.481881162347818,
16.9516986131368));
#274633=CARTESIAN_POINT('Ctrl Pts',(-1.52352210899758,-1.62241065435048,
17.0163188469899));
#274634=CARTESIAN_POINT('Ctrl Pts',(0.389143425895551,-2.27663321337086,
17.1179910094344));
#274635=CARTESIAN_POINT('Ctrl Pts',(2.12392328477785,-0.907436657176078,
17.2291467952101));
#274636=CARTESIAN_POINT('Ctrl Pts',(1.91407877620591,1.29259189050651,17.3403025809855));
#274637=CARTESIAN_POINT('Ctrl Pts',(-0.0482603607290702,2.30914753798913,
17.4514583667612));
#274638=CARTESIAN_POINT('Ctrl Pts',(-1.68087886701888,1.37488706274673,
17.5460676090578));
#274639=CARTESIAN_POINT('Ctrl Pts',(-1.9500108862808,0.36039877990176,17.6036249227627));
#274640=CARTESIAN_POINT('Ctrl Pts',(-1.95094246698047,-0.000563023513259459,
17.6241303078758));
#274641=CARTESIAN_POINT('',(-1.95561232558833,-0.0014928043343815,18.3241303078758));
#274642=CARTESIAN_POINT('Ctrl Pts',(-1.95094246698047,-0.000563023513259459,
17.6241303078758));
#274643=CARTESIAN_POINT('Ctrl Pts',(-1.95169419343994,-0.291836274002239,
17.6406768513546));
#274644=CARTESIAN_POINT('Ctrl Pts',(-1.75385900573772,-1.23437415643904,
17.6942753234252));
#274645=CARTESIAN_POINT('Ctrl Pts',(-0.293683595883821,-2.29090409153417,
17.7849257240878));
#274646=CARTESIAN_POINT('Ctrl Pts',(1.76567929076945,-1.48891520582879,
17.8960815098634));
#274647=CARTESIAN_POINT('Ctrl Pts',(2.20841865870259,0.676296302087549,
18.0072372956388));
#274648=CARTESIAN_POINT('Ctrl Pts',(0.629172532386841,2.22230403884525,
18.1183930814145));
#274649=CARTESIAN_POINT('Ctrl Pts',(-1.41900919557561,1.75790052996025,
18.2240240854933));
#274650=CARTESIAN_POINT('Ctrl Pts',(-1.9509415634449,0.550122899281012,
18.2926031609805));
#274651=CARTESIAN_POINT('Ctrl Pts',(-1.95561232558833,-0.0014928043343815,
18.3241303078758));
#274652=CARTESIAN_POINT('',(-1.95561294514167,0.00149323284471017,19.0241303078758));
#274653=CARTESIAN_POINT('Ctrl Pts',(-1.95561232558833,-0.0014928043343815,
18.3241303078758));
#274654=CARTESIAN_POINT('Ctrl Pts',(-1.95643082468325,-0.0981573186656843,
18.3296550895723));
#274655=CARTESIAN_POINT('Ctrl Pts',(-1.90597210246247,-0.842244556469267,
18.372231799861));
#274656=CARTESIAN_POINT('Ctrl Pts',(-0.950834908026892,-2.10485633930825,
18.4518604387409));
#274657=CARTESIAN_POINT('Ctrl Pts',(1.25304999289457,-1.9401976262354,18.5630162245168));
#274658=CARTESIAN_POINT('Ctrl Pts',(2.30963487490165,0.000858495533198333,
18.6741720102921));
#274659=CARTESIAN_POINT('Ctrl Pts',(1.25162020209078,1.94114985842893,18.7853277960678));
#274660=CARTESIAN_POINT('Ctrl Pts',(-0.952466446087789,2.10412033278024,
18.8964835818432));
#274661=CARTESIAN_POINT('Ctrl Pts',(-1.90620395697742,0.841282306943821,
18.9760844191126));
#274662=CARTESIAN_POINT('Ctrl Pts',(-1.9564186700096,0.0976720719330024,
19.0186333277901));
#274663=CARTESIAN_POINT('Ctrl Pts',(-1.95561294514167,0.00149323284471017,
19.0241303078758));
#274664=CARTESIAN_POINT('Origin',(0.00633869323629521,0.000406037882227006,
19.0313468175703));
#274665=CARTESIAN_POINT('',(-1.47320923595053,1.28365515116407,19.0459999669866));
#274666=CARTESIAN_POINT('Origin',(0.,0.,19.046));
#274667=CARTESIAN_POINT('',(-1.95399969215015,-0.00109684872514523,18.4258696921242));
#274668=CARTESIAN_POINT('Ctrl Pts',(-1.47320923595053,1.28365515116407,
19.0459999669866));
#274669=CARTESIAN_POINT('Ctrl Pts',(-1.42581084117245,1.33805274610456,
19.0419127014303));
#274670=CARTESIAN_POINT('Ctrl Pts',(-1.37545460949829,1.38975536399569,
19.0378254358741));
#274671=CARTESIAN_POINT('Ctrl Pts',(-1.32247459452319,1.43846339781057,
19.0337381703178));
#274672=CARTESIAN_POINT('Ctrl Pts',(-1.26932992720409,1.48732280742145,
19.0296382022763));
#274673=CARTESIAN_POINT('Ctrl Pts',(-1.21354549144269,1.53316875258888,
19.0255382342349));
#274674=CARTESIAN_POINT('Ctrl Pts',(-1.15548848752197,1.57574184281696,
19.0214382661934));
#274675=CARTESIAN_POINT('Ctrl Pts',(-1.0973329601268,1.61838718012091,19.017331340454));
#274676=CARTESIAN_POINT('Ctrl Pts',(-1.03689752655318,1.65774836347391,
19.0132244147147));
#274677=CARTESIAN_POINT('Ctrl Pts',(-0.974575828299399,1.69361092193412,
19.0091174889753));
#274678=CARTESIAN_POINT('Ctrl Pts',(-0.912074034894885,1.72957711481143,
19.0049986951798));
#274679=CARTESIAN_POINT('Ctrl Pts',(-0.847675457691548,1.76202429151714,
19.0008799013843));
#274680=CARTESIAN_POINT('Ctrl Pts',(-0.781795983461404,1.79078503462689,
18.9967611075888));
#274681=CARTESIAN_POINT('Ctrl Pts',(-0.757494229514739,1.80139435582357,
18.9952417585876));
#274682=CARTESIAN_POINT('Ctrl Pts',(-0.732991117784341,1.81150253783091,
18.9937224095863));
#274683=CARTESIAN_POINT('Ctrl Pts',(-0.708307999362921,1.82110290155128,
18.9922030605851));
#274684=CARTESIAN_POINT('Ctrl Pts',(-0.644556172088405,1.84589882560043,
18.9882788694256));
#274685=CARTESIAN_POINT('Ctrl Pts',(-0.579376664124773,1.86739131888459,
18.9843546782661));
#274686=CARTESIAN_POINT('Ctrl Pts',(-0.51314437284014,1.88541742132147,
18.9804304871067));
#274687=CARTESIAN_POINT('Ctrl Pts',(-0.447011520927206,1.90341645985544,
18.9765121876217));
#274688=CARTESIAN_POINT('Ctrl Pts',(-0.379829492183832,1.91795930969979,
18.9725938881367));
#274689=CARTESIAN_POINT('Ctrl Pts',(-0.311991705435798,1.92893161510181,
18.9686755886518));
#274690=CARTESIAN_POINT('Ctrl Pts',(-0.24423390183834,1.93989098376757,
18.9647619089806));
#274691=CARTESIAN_POINT('Ctrl Pts',(-0.175822357499235,1.94728809182404,
18.9608482293093));
#274692=CARTESIAN_POINT('Ctrl Pts',(-0.107162381747267,1.95105925690079,
18.9569345496381));
#274693=CARTESIAN_POINT('Ctrl Pts',(-0.0385456533880884,1.95482804660447,
18.9530233351067));
#274694=CARTESIAN_POINT('Ctrl Pts',(0.0303187076642368,1.95497539760276,
18.9491121205753));
#274695=CARTESIAN_POINT('Ctrl Pts',(0.0990200711887029,1.95148943771207,
18.9452009060439));
#274696=CARTESIAN_POINT('Ctrl Pts',(0.167701515547227,1.94800448853515,
18.9412908255239));
#274697=CARTESIAN_POINT('Ctrl Pts',(0.236219566972794,1.94088834477837,
18.937380745004));
#274698=CARTESIAN_POINT('Ctrl Pts',(0.304165193452798,1.93018121819994,
18.933470664484));
#274699=CARTESIAN_POINT('Ctrl Pts',(0.372114216289481,1.9194735564109,18.9295603885132));
#274700=CARTESIAN_POINT('Ctrl Pts',(0.43949027364022,1.90517463419125,18.9256501125424));
#274701=CARTESIAN_POINT('Ctrl Pts',(0.505892824047464,1.88737607555497,
18.9217398365716));
#274702=CARTESIAN_POINT('Ctrl Pts',(0.572364360708856,1.86955902582336,
18.9178254981772));
#274703=CARTESIAN_POINT('Ctrl Pts',(0.637859897647259,1.84823521057338,
18.9139111597827));
#274704=CARTESIAN_POINT('Ctrl Pts',(0.701993375156466,1.82354635291687,
18.9099968213883));
#274705=CARTESIAN_POINT('Ctrl Pts',(0.766164417825701,1.79884303415636,
18.9060801902327));
#274706=CARTESIAN_POINT('Ctrl Pts',(0.828971365391464,1.77077094949238,
18.902163559077));
#274707=CARTESIAN_POINT('Ctrl Pts',(0.890050050998562,1.73951915962931,
18.8982469279214));
#274708=CARTESIAN_POINT('Ctrl Pts',(0.951231951283219,1.70821455848875,
18.8943236781914));
#274709=CARTESIAN_POINT('Ctrl Pts',(1.01067933662763,1.67371977322852,18.8904004284614));
#274710=CARTESIAN_POINT('Ctrl Pts',(1.06805520883447,1.63626833706503,18.8864771787315));
#274711=CARTESIAN_POINT('Ctrl Pts',(1.09430899175348,1.61913148428662,18.8846819964922));
#274712=CARTESIAN_POINT('Ctrl Pts',(1.12012948878298,1.60137615623275,18.8828868142529));
#274713=CARTESIAN_POINT('Ctrl Pts',(1.14548677551538,1.58302749411353,18.8810916320137));
#274714=CARTESIAN_POINT('Ctrl Pts',(1.20092748359473,1.54291031474283,18.8771666783888));
#274715=CARTESIAN_POINT('Ctrl Pts',(1.25436369953291,1.49980083127761,18.873241724764));
#274716=CARTESIAN_POINT('Ctrl Pts',(1.30545543201943,1.45392644759319,18.8693167711392));
#274717=CARTESIAN_POINT('Ctrl Pts',(1.35647230034779,1.40811928314266,18.8653975687061));
#274718=CARTESIAN_POINT('Ctrl Pts',(1.40515114237818,1.35955558495761,18.861478366273));
#274719=CARTESIAN_POINT('Ctrl Pts',(1.45118286073189,1.3085046063037,18.8575591638399));
#274720=CARTESIAN_POINT('Ctrl Pts',(1.49716272292246,1.25751113816586,18.8536443765102));
#274721=CARTESIAN_POINT('Ctrl Pts',(1.54050105766794,1.20403631694402,18.8497295891806));
#274722=CARTESIAN_POINT('Ctrl Pts',(1.58092496836611,1.14838680086311,18.845814801851));
#274723=CARTESIAN_POINT('Ctrl Pts',(1.6213247329099,1.09277052554944,18.8419023529161));
#274724=CARTESIAN_POINT('Ctrl Pts',(1.65881323989536,1.03498252806685,18.8379899039812));
#274725=CARTESIAN_POINT('Ctrl Pts',(1.69315831477619,0.975361943641562,
18.8340774550464));
#274726=CARTESIAN_POINT('Ctrl Pts',(1.72749453418746,0.915756731675726,
18.83016601489));
#274727=CARTESIAN_POINT('Ctrl Pts',(1.75868868634086,0.854320295252809,
18.8262545747335));
#274728=CARTESIAN_POINT('Ctrl Pts',(1.78655328498693,0.791418574398155,
18.8223431345771));
#274729=CARTESIAN_POINT('Ctrl Pts',(1.81442015830947,0.728511718674476,
18.8184313751173));
#274730=CARTESIAN_POINT('Ctrl Pts',(1.83895674239513,0.664139789928554,
18.8145196156575));
#274731=CARTESIAN_POINT('Ctrl Pts',(1.86002339623353,0.598689373100854,
18.8106078561977));
#274732=CARTESIAN_POINT('Ctrl Pts',(1.88111288826538,0.533168001991905,
18.8066918560303));
#274733=CARTESIAN_POINT('Ctrl Pts',(1.89872479260933,0.466566276707873,
18.8027758558629));
#274734=CARTESIAN_POINT('Ctrl Pts',(1.91276944054903,0.39928569634003,18.7988598556955));
#274735=CARTESIAN_POINT('Ctrl Pts',(1.9268226857782,0.331963930844073,18.7949414583881));
#274736=CARTESIAN_POINT('Ctrl Pts',(1.93730425376752,0.263962967355806,
18.7910230610807));
#274737=CARTESIAN_POINT('Ctrl Pts',(1.94417613596757,0.195691472308317,
18.7871046637733));
#274738=CARTESIAN_POINT('Ctrl Pts',(1.95105987668993,0.127302163971462,
18.7831795046501));
#274739=CARTESIAN_POINT('Ctrl Pts',(1.95432147595897,0.0586418813374403,
18.7792543455269));
#274740=CARTESIAN_POINT('Ctrl Pts',(1.95397502420171,-0.00987951395203889,
18.7753291864037));
#274741=CARTESIAN_POINT('Ctrl Pts',(1.953817649304,-0.0410051969617995,
18.7735461920832));
#274742=CARTESIAN_POINT('Ctrl Pts',(1.95291649744364,-0.0721022797467864,
18.7717631977627));
#274743=CARTESIAN_POINT('Ctrl Pts',(1.95127640791245,-0.103132826608546,
18.7699802034423));
#274744=CARTESIAN_POINT('Ctrl Pts',(1.9476772661379,-0.171228705140731,
18.7660674601313));
#274745=CARTESIAN_POINT('Ctrl Pts',(1.94050187012511,-0.239274528996423,
18.7621547168202));
#274746=CARTESIAN_POINT('Ctrl Pts',(1.92975404797098,-0.306863673867736,
18.7582419735092));
#274747=CARTESIAN_POINT('Ctrl Pts',(1.91902265009754,-0.374349532410877,
18.7543352094555));
#274748=CARTESIAN_POINT('Ctrl Pts',(1.90472973637868,-0.441379613629611,
18.7504284454018));
#274749=CARTESIAN_POINT('Ctrl Pts',(1.88693106645239,-0.507550145755895,
18.7465216813482));
#274750=CARTESIAN_POINT('Ctrl Pts',(1.86915376980208,-0.573641217953406,
18.7426196086757));
#274751=CARTESIAN_POINT('Ctrl Pts',(1.8478792046855,-0.638874316687479,
18.7387175360033));
#274752=CARTESIAN_POINT('Ctrl Pts',(1.82321424775281,-0.702855466501586,
18.7348154633308));
#274753=CARTESIAN_POINT('Ctrl Pts',(1.79856510893852,-0.766795583955237,
18.7309158931338));
#274754=CARTESIAN_POINT('Ctrl Pts',(1.77053006806591,-0.829484885686202,
18.7270163229367));
#274755=CARTESIAN_POINT('Ctrl Pts',(1.73926546778139,-0.89054569370874,
18.7231167527396));
#274756=CARTESIAN_POINT('Ctrl Pts',(1.70801011323798,-0.951588444490264,
18.7192183357451));
#274757=CARTESIAN_POINT('Ctrl Pts',(1.67352731978124,-1.01100321848788,
18.7153199187506));
#274758=CARTESIAN_POINT('Ctrl Pts',(1.63602030203372,-1.06843510394105,
18.7114215017561));
#274759=CARTESIAN_POINT('Ctrl Pts',(1.59851141418806,-1.12586985294531,
18.7075228903867));
#274760=CARTESIAN_POINT('Ctrl Pts',(1.55797827466797,-1.1813211053985,18.7036242790173));
#274761=CARTESIAN_POINT('Ctrl Pts',(1.51466751281931,-1.23446276801277,
18.6997256676478));
#274762=CARTESIAN_POINT('Ctrl Pts',(1.47131074123148,-1.28766088389482,
18.695822914719));
#274763=CARTESIAN_POINT('Ctrl Pts',(1.42517077092788,-1.33854413022793,
18.6919201617903));
#274764=CARTESIAN_POINT('Ctrl Pts',(1.37653397585288,-1.38682018060117,
18.6880174088615));
#274765=CARTESIAN_POINT('Ctrl Pts',(1.32786825384278,-1.43512494335511,
18.6841123347542));
#274766=CARTESIAN_POINT('Ctrl Pts',(1.27670312001706,-1.48081909566736,
18.680207260647));
#274767=CARTESIAN_POINT('Ctrl Pts',(1.22335908468114,-1.52364974647329,
18.6763021865397));
#274768=CARTESIAN_POINT('Ctrl Pts',(1.16992237404742,-1.56655480753509,
18.6723903280956));
#274769=CARTESIAN_POINT('Ctrl Pts',(1.11429960723626,-1.60658615033506,
18.6684784696515));
#274770=CARTESIAN_POINT('Ctrl Pts',(1.05684064036482,-1.64353395488906,
18.6645666112073));
#274771=CARTESIAN_POINT('Ctrl Pts',(1.02894326166577,-1.66147278936285,
18.6626673324285));
#274772=CARTESIAN_POINT('Ctrl Pts',(1.00061341462232,-1.67868543812271,
18.6607680536497));
#274773=CARTESIAN_POINT('Ctrl Pts',(0.971893015866229,-1.6951519004828,
18.6588687748708));
#274774=CARTESIAN_POINT('Ctrl Pts',(0.912626357980133,-1.72913165820057,
18.6549494732423));
#274775=CARTESIAN_POINT('Ctrl Pts',(0.851458535485548,-1.76006659392973,
18.6510301716139));
#274776=CARTESIAN_POINT('Ctrl Pts',(0.788734919209241,-1.78773969783635,
18.6471108699854));
#274777=CARTESIAN_POINT('Ctrl Pts',(0.72610563165396,-1.81537118474679,
18.6431974625118));
#274778=CARTESIAN_POINT('Ctrl Pts',(0.661925640058772,-1.8397503786959,
18.6392840550382));
#274779=CARTESIAN_POINT('Ctrl Pts',(0.596565939931027,-1.86070553267147,
18.6353706475646));
#274780=CARTESIAN_POINT('Ctrl Pts',(0.531283030199932,-1.88163606666588,
18.6314618379106));
#274781=CARTESIAN_POINT('Ctrl Pts',(0.46482363052957,-1.89915040096931,
18.6275530282567));
#274782=CARTESIAN_POINT('Ctrl Pts',(0.397578104515613,-1.913125100669,18.6236442186027));
#274783=CARTESIAN_POINT('Ctrl Pts',(0.330374695937586,-1.92709104768945,
18.6197378571271));
#274784=CARTESIAN_POINT('Ctrl Pts',(0.262386617923052,-1.93752165815829,
18.6158314956514));
#274785=CARTESIAN_POINT('Ctrl Pts',(0.194017255254432,-1.94434392653757,
18.6119251341758));
#274786=CARTESIAN_POINT('Ctrl Pts',(0.125667303993895,-1.95116425794054,
18.6080198817931));
#274787=CARTESIAN_POINT('Ctrl Pts',(0.0569367718664548,-1.9543782322859,
18.6041146294104));
#274788=CARTESIAN_POINT('Ctrl Pts',(-0.0117647544452431,-1.95396458272734,
18.6002093770277));
#274789=CARTESIAN_POINT('Ctrl Pts',(-0.0804702979021206,-1.9535509089817,
18.5963038962954));
#274790=CARTESIAN_POINT('Ctrl Pts',(-0.149146340665118,-1.94950919572022,
18.5923984155631));
#274791=CARTESIAN_POINT('Ctrl Pts',(-0.217384028907364,-1.9418702799044,
18.5884929348308));
#274792=CARTESIAN_POINT('Ctrl Pts',(-0.28569416176618,-1.93422325422523,
18.5845833078406));
#274793=CARTESIAN_POINT('Ctrl Pts',(-0.353564521924234,-1.92297145924986,
18.5806736808504));
#274794=CARTESIAN_POINT('Ctrl Pts',(-0.420593115150671,-1.90819742990285,
18.5767640538602));
#274795=CARTESIAN_POINT('Ctrl Pts',(-0.487661725079951,-1.89341458032087,
18.5728520927858));
#274796=CARTESIAN_POINT('Ctrl Pts',(-0.553887094051403,-1.87510544224461,
18.5689401317114));
#274797=CARTESIAN_POINT('Ctrl Pts',(-0.61888186044793,-1.85340261217268,
18.565028170637));
#274798=CARTESIAN_POINT('Ctrl Pts',(-0.683988474229122,-1.83166243440465,
18.5611094775957));
#274799=CARTESIAN_POINT('Ctrl Pts',(-0.747859801662094,-1.80651708861102,
18.5571907845544));
#274800=CARTESIAN_POINT('Ctrl Pts',(-0.81012875650471,-1.77814718116475,
18.5532720915131));
#274801=CARTESIAN_POINT('Ctrl Pts',(-0.839338956356765,-1.76483893360568,
18.5514338431085));
#274802=CARTESIAN_POINT('Ctrl Pts',(-0.868196910416859,-1.75082177012659,
18.5495955947039));
#274803=CARTESIAN_POINT('Ctrl Pts',(-0.896666821613518,-1.73611768351616,
18.5477573462993));
#274804=CARTESIAN_POINT('Ctrl Pts',(-0.957361315609888,-1.70477030451191,
18.5438384174349));
#274805=CARTESIAN_POINT('Ctrl Pts',(-1.01652969689966,-1.67017445412417,
18.5399194885705));
#274806=CARTESIAN_POINT('Ctrl Pts',(-1.0738023578566,-1.63250252565245,
18.536000559706));
#274807=CARTESIAN_POINT('Ctrl Pts',(-1.13098907038735,-1.59488713101221,
18.5320875119333));
#274808=CARTESIAN_POINT('Ctrl Pts',(-1.18628530129918,-1.55420508805625,
18.5281744641605));
#274809=CARTESIAN_POINT('Ctrl Pts',(-1.23934556821764,-1.51067486989732,
18.5242614163877));
#274810=CARTESIAN_POINT('Ctrl Pts',(-1.2923437780468,-1.46719556287761,
18.5203529451534));
#274811=CARTESIAN_POINT('Ctrl Pts',(-1.34311083921788,-1.42087500670096,
18.5164444739192));
#274812=CARTESIAN_POINT('Ctrl Pts',(-1.39133134932632,-1.3719741529569,
18.5125360026849));
#274813=CARTESIAN_POINT('Ctrl Pts',(-1.43952182110403,-1.32310376135466,
18.5086299661812));
#274814=CARTESIAN_POINT('Ctrl Pts',(-1.48516854423479,-1.27165661002935,
18.5047239296776));
#274815=CARTESIAN_POINT('Ctrl Pts',(-1.52799142088666,-1.21793194296593,
18.5008178931739));
#274816=CARTESIAN_POINT('Ctrl Pts',(-1.57080229168217,-1.16422233819366,
18.4969129517698));
#274817=CARTESIAN_POINT('Ctrl Pts',(-1.61079058138535,-1.10823686957285,
18.4930080103657));
#274818=CARTESIAN_POINT('Ctrl Pts',(-1.64771629625348,-1.05030805341134,
18.4891030689616));
#274819=CARTESIAN_POINT('Ctrl Pts',(-1.68464430805058,-0.992375633842908,
18.4851978846543));
#274820=CARTESIAN_POINT('Ctrl Pts',(-1.71850910468994,-0.932500042688802,
18.481292700347));
#274821=CARTESIAN_POINT('Ctrl Pts',(-1.74911486508527,-0.871041439162183,
18.4773875160397));
#274822=CARTESIAN_POINT('Ctrl Pts',(-1.77975331029039,-0.809517202148931,
18.473478161269));
#274823=CARTESIAN_POINT('Ctrl Pts',(-1.80712555385027,-0.746407019901457,
18.4695688064982));
#274824=CARTESIAN_POINT('Ctrl Pts',(-1.8310829286302,-0.682093328276309,
18.4656594517275));
#274825=CARTESIAN_POINT('Ctrl Pts',(-1.85505468953874,-0.617741017017433,
18.461747749434));
#274826=CARTESIAN_POINT('Ctrl Pts',(-1.87560735349436,-0.552184227264455,
18.4578360471406));
#274827=CARTESIAN_POINT('Ctrl Pts',(-1.89264224981713,-0.485820248864909,
18.4539243448471));
#274828=CARTESIAN_POINT('Ctrl Pts',(-1.90970656556094,-0.419341659270481,
18.4500058870082));
#274829=CARTESIAN_POINT('Ctrl Pts',(-1.92324089160671,-0.352053580509883,
18.4460874291693));
#274830=CARTESIAN_POINT('Ctrl Pts',(-1.93319788949831,-0.284362304181293,
18.4421689713304));
#274831=CARTESIAN_POINT('Ctrl Pts',(-1.93787600823236,-0.252558759440938,
18.4403279534629));
#274832=CARTESIAN_POINT('Ctrl Pts',(-1.9417652074676,-0.22066626547931,
18.4384869355955));
#274833=CARTESIAN_POINT('Ctrl Pts',(-1.94486454898216,-0.188727014792367,
18.436645917728));
#274834=CARTESIAN_POINT('Ctrl Pts',(-1.95091178404236,-0.126409210948082,
18.4330538425267));
#274835=CARTESIAN_POINT('Ctrl Pts',(-1.95396449707421,-0.0637957113532713,
18.4294617673255));
#274836=CARTESIAN_POINT('Ctrl Pts',(-1.95399969215015,-0.00109684872514523,
18.4258696921242));
#274837=CARTESIAN_POINT('',(-1.95134777043173,-0.00103525977712474,17.7258696921242));
#274838=CARTESIAN_POINT('Ctrl Pts',(-1.95645114732722,-0.00108114071341489,
18.4258687145873));
#274839=CARTESIAN_POINT('Ctrl Pts',(-1.952565755839,0.583424133764486,18.392423972777));
#274840=CARTESIAN_POINT('Ctrl Pts',(-1.3640428686297,1.82206153794779,18.3219420881096));
#274841=CARTESIAN_POINT('Ctrl Pts',(0.742083973805834,2.18684491535976,
18.2144230605852));
#274842=CARTESIAN_POINT('Ctrl Pts',(2.23963755709721,0.563107605485782,
18.1033116320136));
#274843=CARTESIAN_POINT('Ctrl Pts',(1.68811978691671,-1.57585659307529,
17.9922002034423));
#274844=CARTESIAN_POINT('Ctrl Pts',(-0.407879737212788,-2.27303301670108,
17.8810887748708));
#274845=CARTESIAN_POINT('Ctrl Pts',(-1.78439856374539,-1.16847809341345,
17.7923119377648));
#274846=CARTESIAN_POINT('Ctrl Pts',(-1.95259122315044,-0.259714155535947,
17.7405722435159));
#274847=CARTESIAN_POINT('Ctrl Pts',(-1.95134777043173,-0.00103525977712474,
17.7258696921242));
#274848=CARTESIAN_POINT('',(-1.95399929689543,0.00165762847613276,17.0258696715309));
#274849=CARTESIAN_POINT('Ctrl Pts',(-1.95134777043173,-0.00103525977712474,
17.7258696921242));
#274850=CARTESIAN_POINT('Ctrl Pts',(-1.94945884600364,0.391922894462037,
17.7035351006588));
#274851=CARTESIAN_POINT('Ctrl Pts',(-1.64362033274317,1.43922352125159,
17.6441633663363));
#274852=CARTESIAN_POINT('Ctrl Pts',(0.0645653811787344,2.30843805668281,
17.5477544891566));
#274853=CARTESIAN_POINT('Ctrl Pts',(1.97418123894165,1.19819262885406,17.4366430605851));
#274854=CARTESIAN_POINT('Ctrl Pts',(2.07759448914051,-1.00829461665569,
17.3255316320136));
#274855=CARTESIAN_POINT('Ctrl Pts',(0.280191065138641,-2.29228039229647,
17.2144202034423));
#274856=CARTESIAN_POINT('Ctrl Pts',(-1.56609907861032,-1.56118274288362,
17.1145328901458));
#274857=CARTESIAN_POINT('Ctrl Pts',(-1.94902844534429,-0.451721645161182,
17.0516827197064));
#274858=CARTESIAN_POINT('Ctrl Pts',(-1.95268185958658,0.00165614916274905,
17.0258696921242));
#274859=CARTESIAN_POINT('',(-1.95399999965015,3.69758055297757E-5,16.3258696921745));
#274860=CARTESIAN_POINT('Ctrl Pts',(-1.95399929689543,0.00165762847613276,
17.0258696715309));
#274861=CARTESIAN_POINT('Ctrl Pts',(-1.95392944244911,0.0840014956052798,
17.0211845557084));
#274862=CARTESIAN_POINT('Ctrl Pts',(-1.9486506380379,0.166119521674429,
17.0164994398858));
#274863=CARTESIAN_POINT('Ctrl Pts',(-1.93827107857988,0.24742923420808,
17.0118143240633));
#274864=CARTESIAN_POINT('Ctrl Pts',(-1.92774884814808,0.329856579519055,
17.0070648095503));
#274865=CARTESIAN_POINT('Ctrl Pts',(-1.91198475580092,0.411453222331514,
17.0023152950372));
#274866=CARTESIAN_POINT('Ctrl Pts',(-1.89114037462833,0.491634095085596,
16.9975657805242));
#274867=CARTESIAN_POINT('Ctrl Pts',(-1.88328682180889,0.521843901463097,
16.9957763024493));
#274868=CARTESIAN_POINT('Ctrl Pts',(-1.87471257563528,0.55185295002992,
16.9939868243743));
#274869=CARTESIAN_POINT('Ctrl Pts',(-1.86542801643474,0.581630738097954,
16.9921973462993));
#274870=CARTESIAN_POINT('Ctrl Pts',(-1.84509919017844,0.646830115565059,
16.9882792293387));
#274871=CARTESIAN_POINT('Ctrl Pts',(-1.82130773338751,0.711091673200386,
16.9843611123781));
#274872=CARTESIAN_POINT('Ctrl Pts',(-1.79415901651518,0.774021591079526,
16.9804429954175));
#274873=CARTESIAN_POINT('Ctrl Pts',(-1.76705118104201,0.836856747091851,
16.9765307784817));
#274874=CARTESIAN_POINT('Ctrl Pts',(-1.73659631207985,0.898363795000412,
16.972618561546));
#274875=CARTESIAN_POINT('Ctrl Pts',(-1.70294935694726,0.958164645388731,
16.9687063446102));
#274876=CARTESIAN_POINT('Ctrl Pts',(-1.66934196849415,1.01789517378,16.9647987281927));
#274877=CARTESIAN_POINT('Ctrl Pts',(-1.63255018881405,1.07592306269883,
16.9608911117753));
#274878=CARTESIAN_POINT('Ctrl Pts',(-1.59277603073726,1.13189244891414,
16.9569834953578));
#274879=CARTESIAN_POINT('Ctrl Pts',(-1.5530268014057,1.18782675590623,16.9530783280676));
#274880=CARTESIAN_POINT('Ctrl Pts',(-1.51029918592256,1.24170471945634,
16.9491731607774));
#274881=CARTESIAN_POINT('Ctrl Pts',(-1.46483904964484,1.29319857664459,
16.9452679934872));
#274882=CARTESIAN_POINT('Ctrl Pts',(-1.41939181376794,1.34467782121942,
16.9413639343816));
#274883=CARTESIAN_POINT('Ctrl Pts',(-1.37121392181844,1.39377393392444,
16.9374598752761));
#274884=CARTESIAN_POINT('Ctrl Pts',(-1.3205909817362,1.44019285477918,16.9335558161705));
#274885=CARTESIAN_POINT('Ctrl Pts',(-1.26996504484116,1.48661452357422,
16.9296515259496));
#274886=CARTESIAN_POINT('Ctrl Pts',(-1.21689413671791,1.53035835532792,
16.9257472357288));
#274887=CARTESIAN_POINT('Ctrl Pts',(-1.16169876999093,1.57116898130072,
16.9218429455079));
#274888=CARTESIAN_POINT('Ctrl Pts',(-1.10644461140303,1.61202307709334,
16.9179344965958));
#274889=CARTESIAN_POINT('Ctrl Pts',(-1.04906187445869,1.64993743891098,
16.9140260476837));
#274890=CARTESIAN_POINT('Ctrl Pts',(-0.989901207589153,1.68469926076245,
16.9101175987716));
#274891=CARTESIAN_POINT('Ctrl Pts',(-0.930705129006683,1.71948188994625,
16.9062068103851));
#274892=CARTESIAN_POINT('Ctrl Pts',(-0.869729439220855,1.75110799716119,
16.9022960219985));
#274893=CARTESIAN_POINT('Ctrl Pts',(-0.807348105016895,1.77941143003119,
16.8983852336119));
#274894=CARTESIAN_POINT('Ctrl Pts',(-0.74485905837139,1.80776373379978,
16.8944676925553));
#274895=CARTESIAN_POINT('Ctrl Pts',(-0.680959980998942,1.83278173348723,
16.8905501514987));
#274896=CARTESIAN_POINT('Ctrl Pts',(-0.616042625149195,1.85434826394593,
16.8866326104421));
#274897=CARTESIAN_POINT('Ctrl Pts',(-0.585404645907629,1.86452666545131,
16.8847837128707));
#274898=CARTESIAN_POINT('Ctrl Pts',(-0.554540039311765,1.87393701832972,
16.8829348152994));
#274899=CARTESIAN_POINT('Ctrl Pts',(-0.523490742810242,1.88257096604404,
16.881085917728));
#274900=CARTESIAN_POINT('Ctrl Pts',(-0.457692198149527,1.90086771535206,
16.8771678009547));
#274901=CARTESIAN_POINT('Ctrl Pts',(-0.390802818928335,1.9157469518832,
16.8732496841813));
#274902=CARTESIAN_POINT('Ctrl Pts',(-0.32321059275063,1.92708352510569,
16.869331567408));
#274903=CARTESIAN_POINT('Ctrl Pts',(-0.255720149132896,1.93840302734963,
16.8654193506616));
#274904=CARTESIAN_POINT('Ctrl Pts',(-0.187529440249675,1.946190372983,16.8615071339152));
#274905=CARTESIAN_POINT('Ctrl Pts',(-0.119040137275175,1.95037059189209,
16.8575949171688));
#274906=CARTESIAN_POINT('Ctrl Pts',(-0.050631373407831,1.954545895127,16.853687300943));
#274907=CARTESIAN_POINT('Ctrl Pts',(0.0180747985636558,1.9551224660021,
16.8497796847171));
#274908=CARTESIAN_POINT('Ctrl Pts',(0.0866698429625813,1.95207692940643,
16.8458720684912));
#274909=CARTESIAN_POINT('Ctrl Pts',(0.155221894890366,1.94903330162423,
16.8419669013938));
#274910=CARTESIAN_POINT('Ctrl Pts',(0.223662467116329,1.94237209146302,
16.8380617342965));
#274911=CARTESIAN_POINT('Ctrl Pts',(0.291582837074114,1.93212200679041,
16.8341565671991));
#274912=CARTESIAN_POINT('Ctrl Pts',(0.359483932985028,1.92187483082711,
16.8302525082873));
#274913=CARTESIAN_POINT('Ctrl Pts',(0.42686463353449,1.90804087547645,16.8263484493754));
#274914=CARTESIAN_POINT('Ctrl Pts',(0.49332296545365,1.89070051879086,16.8224443904636));
#274915=CARTESIAN_POINT('Ctrl Pts',(0.559785231609485,1.87335913558135,
16.8185401004372));
#274916=CARTESIAN_POINT('Ctrl Pts',(0.625324545432984,1.85251106559555,
16.8146358104108));
#274917=CARTESIAN_POINT('Ctrl Pts',(0.689552498035929,1.82828699947585,
16.8107315203843));
#274918=CARTESIAN_POINT('Ctrl Pts',(0.753848863651919,1.80403713086231,
16.8068230716663));
#274919=CARTESIAN_POINT('Ctrl Pts',(0.816830619331629,1.77640426357738,
16.8029146229483));
#274920=CARTESIAN_POINT('Ctrl Pts',(0.878128760066116,1.74556749532774,
16.7990061742303));
#274921=CARTESIAN_POINT('Ctrl Pts',(0.939463591938396,1.71471226915915,
16.7950953860379));
#274922=CARTESIAN_POINT('Ctrl Pts',(0.999112376041192,1.68064956929513,
16.7911845978456));
#274923=CARTESIAN_POINT('Ctrl Pts',(1.05673264645341,1.64360339313339,16.7872738096532));
#274924=CARTESIAN_POINT('Ctrl Pts',(1.11445240851875,1.60649325015438,16.7833562687889));
#274925=CARTESIAN_POINT('Ctrl Pts',(1.17013626735915,1.56638963661305,16.7794387279245));
#274926=CARTESIAN_POINT('Ctrl Pts',(1.22347325827623,1.52355806790649,16.7755211870602));
#274927=CARTESIAN_POINT('Ctrl Pts',(1.24864586748505,1.50334353532201,16.773672287759));
#274928=CARTESIAN_POINT('Ctrl Pts',(1.27329624906766,1.48252192830883,16.7718233884578));
#274929=CARTESIAN_POINT('Ctrl Pts',(1.2973946303134,1.461123941777,16.7699744891565));
#274930=CARTESIAN_POINT('Ctrl Pts',(1.34846299905584,1.41577814633084,16.7660563724033));
#274931=CARTESIAN_POINT('Ctrl Pts',(1.39725238884547,1.36766186930103,16.7621382556502));
#274932=CARTESIAN_POINT('Ctrl Pts',(1.44344716950006,1.31703313126978,16.758220138897));
#274933=CARTESIAN_POINT('Ctrl Pts',(1.48957238854848,1.26648063164221,16.7543079221717));
#274934=CARTESIAN_POINT('Ctrl Pts',(1.53311042369732,1.21342354005044,16.7503957054464));
#274935=CARTESIAN_POINT('Ctrl Pts',(1.57378037375586,1.15815859673054,16.7464834887212));
#274936=CARTESIAN_POINT('Ctrl Pts',(1.6144024985005,1.10295864152247,16.7425758725177));
#274937=CARTESIAN_POINT('Ctrl Pts',(1.65216294620333,1.04555638516053,16.7386682563143));
#274938=CARTESIAN_POINT('Ctrl Pts',(1.6868204325988,0.986282326804649,16.7347606401108));
#274939=CARTESIAN_POINT('Ctrl Pts',(1.72145619714115,0.927045418932637,
16.7308554730367));
#274940=CARTESIAN_POINT('Ctrl Pts',(1.75299261053317,0.86593945992652,16.7269503059625));
#274941=CARTESIAN_POINT('Ctrl Pts',(1.78123203824553,0.803323363240291,
16.7230451388883));
#274942=CARTESIAN_POINT('Ctrl Pts',(1.80946345233201,0.740725035397593,
16.7191410800005));
#274943=CARTESIAN_POINT('Ctrl Pts',(1.83439953594026,0.676617868775745,
16.7152370211127));
#274944=CARTESIAN_POINT('Ctrl Pts',(1.85588972070514,0.611383140576348,
16.7113329622249));
#274945=CARTESIAN_POINT('Ctrl Pts',(1.87738117765369,0.54614455058809,16.7074286722232));
#274946=CARTESIAN_POINT('Ctrl Pts',(1.8954261792976,0.479778734483987,16.7035243822215));
#274947=CARTESIAN_POINT('Ctrl Pts',(1.90992378050061,0.412682871801403,
16.6996200922198));
#274948=CARTESIAN_POINT('Ctrl Pts',(1.92443682395765,0.345515541340018,
16.6957116435275));
#274949=CARTESIAN_POINT('Ctrl Pts',(1.9353948220809,0.277617094127129,16.6918031948352));
#274950=CARTESIAN_POINT('Ctrl Pts',(1.94274802045342,0.2093946728652,16.6878947461429));
#274951=CARTESIAN_POINT('Ctrl Pts',(1.950105620218,0.141131415818891,16.6839839579767));
#274952=CARTESIAN_POINT('Ctrl Pts',(1.95385409912709,0.0725442899996735,
16.6800731698106));
#274953=CARTESIAN_POINT('Ctrl Pts',(1.95399581835698,0.00404250460009209,
16.6761623816445));
#274954=CARTESIAN_POINT('Ctrl Pts',(1.95413778229033,-0.0645775613149842,
16.6722448408071));
#274955=CARTESIAN_POINT('Ctrl Pts',(1.9506605819423,-0.133111501725674,
16.6683272999696));
#274956=CARTESIAN_POINT('Ctrl Pts',(1.94361854554447,-0.201154043995133,
16.6644097591322));
#274957=CARTESIAN_POINT('Ctrl Pts',(1.94029502749426,-0.233267001758994,
16.6625608596165));
#274958=CARTESIAN_POINT('Ctrl Pts',(1.93617821866225,-0.26527063846103,
16.6607119601008));
#274959=CARTESIAN_POINT('Ctrl Pts',(1.93127775061767,-0.297123290856094,
16.658863060585));
#274960=CARTESIAN_POINT('Ctrl Pts',(1.92089286702049,-0.364624207987812,
16.6549449437687));
#274961=CARTESIAN_POINT('Ctrl Pts',(1.90694425660678,-0.431713827933215,
16.6510268269523));
#274962=CARTESIAN_POINT('Ctrl Pts',(1.88947742054759,-0.497987025173156,
16.6471087101359));
#274963=CARTESIAN_POINT('Ctrl Pts',(1.87203688661393,-0.564160426093595,
16.6431964933463));
#274964=CARTESIAN_POINT('Ctrl Pts',(1.85108876575637,-0.629519372412166,
16.6392842765567));
#274965=CARTESIAN_POINT('Ctrl Pts',(1.82672992672002,-0.693666904807687,
16.635372059767));
#274966=CARTESIAN_POINT('Ctrl Pts',(1.80239973214376,-0.757739003746423,
16.6314644434979));
#274967=CARTESIAN_POINT('Ctrl Pts',(1.77466695866875,-0.820602060268188,
16.6275568272288));
#274968=CARTESIAN_POINT('Ctrl Pts',(1.74367832738289,-0.881874078661569,
16.6236492109596));
#274969=CARTESIAN_POINT('Ctrl Pts',(1.71270911845958,-0.943107694347085,
16.619744043819));
#274970=CARTESIAN_POINT('Ctrl Pts',(1.67848832119053,-1.00275181207261,
16.6158388766783));
#274971=CARTESIAN_POINT('Ctrl Pts',(1.64121020734743,-1.06044568710453,
16.6119337095376));
#274972=CARTESIAN_POINT('Ctrl Pts',(1.60394267207081,-1.11812319010393,
16.6080296505826));
#274973=CARTESIAN_POINT('Ctrl Pts',(1.56361980935094,-1.17385113611301,
16.6041255916276));
#274974=CARTESIAN_POINT('Ctrl Pts',(1.52048021258001,-1.22729618395587,
16.6002215326726));
#274975=CARTESIAN_POINT('Ctrl Pts',(1.47733806200913,-1.28074439566605,
16.5963172426031));
#274976=CARTESIAN_POINT('Ctrl Pts',(1.43137915727873,-1.33190905976387,
16.5924129525336));
#274977=CARTESIAN_POINT('Ctrl Pts',(1.38288237295785,-1.3804898922348,16.5885086624641));
#274978=CARTESIAN_POINT('Ctrl Pts',(1.33433393183387,-1.42912247103352,
16.5846002137035));
#274979=CARTESIAN_POINT('Ctrl Pts',(1.28324256445431,-1.47516537690042,
16.580691764943));
#274980=CARTESIAN_POINT('Ctrl Pts',(1.22992328793101,-1.51835592197777,
16.5767833161824));
#274981=CARTESIAN_POINT('Ctrl Pts',(1.17657209617025,-1.56157231955335,
16.5728725279477));
#274982=CARTESIAN_POINT('Ctrl Pts',(1.12099073931128,-1.60193266937518,
16.5689617397129));
#274983=CARTESIAN_POINT('Ctrl Pts',(1.06352424536954,-1.63921694095417,
16.5650509514782));
#274984=CARTESIAN_POINT('Ctrl Pts',(1.00595852530987,-1.67656559045628,
16.5611334105723));
#274985=CARTESIAN_POINT('Ctrl Pts',(0.946501597619499,-1.71082731556612,
16.5572158696665));
#274986=CARTESIAN_POINT('Ctrl Pts',(0.885523377905878,-1.74182787530289,
16.5532983287606));
#274987=CARTESIAN_POINT('Ctrl Pts',(0.856744466079466,-1.75645871200858,
16.551449429845));
#274988=CARTESIAN_POINT('Ctrl Pts',(0.827626992125715,-1.77036385166465,
16.5496005309293));
#274989=CARTESIAN_POINT('Ctrl Pts',(0.798211179823588,-1.78352878092972,
16.5477516320137));
#274990=CARTESIAN_POINT('Ctrl Pts',(0.735874300842777,-1.81142740205085,
16.5438335152278));
#274991=CARTESIAN_POINT('Ctrl Pts',(0.671949444664659,-1.83610924804977,
16.5399153984419));
#274992=CARTESIAN_POINT('Ctrl Pts',(0.606801614227519,-1.85739274279052,
16.535997281656));
#274993=CARTESIAN_POINT('Ctrl Pts',(0.541751885503323,-1.87864418815559,
16.5320850648972));
#274994=CARTESIAN_POINT('Ctrl Pts',(0.475483301232471,-1.89650728686393,
16.5281728481384));
#274995=CARTESIAN_POINT('Ctrl Pts',(0.408381873685793,-1.91084804347308,
16.5242606313797));
#274996=CARTESIAN_POINT('Ctrl Pts',(0.341359353198165,-1.92517193625428,
16.5203530151418));
#274997=CARTESIAN_POINT('Ctrl Pts',(0.273506413221159,-1.93598161080183,
16.5164453989039));
#274998=CARTESIAN_POINT('Ctrl Pts',(0.205223543266017,-1.9431930674252,
16.5125377826661));
#274999=CARTESIAN_POINT('Ctrl Pts',(0.136983470128228,-1.9504000042123,
16.5086326155569));
#275000=CARTESIAN_POINT('Ctrl Pts',(0.068314489600747,-1.95401314515249,
16.5047274484478));
#275001=CARTESIAN_POINT('Ctrl Pts',(-0.000374961877715423,-1.95399996402344,
16.5008222813386));
#275002=CARTESIAN_POINT('Ctrl Pts',(-0.0690449210593987,-1.95398678663484,
16.4969182224153));
#275003=CARTESIAN_POINT('Ctrl Pts',(-0.137734848010914,-1.95034933012595,
16.493014163492));
#275004=CARTESIAN_POINT('Ctrl Pts',(-0.206035279610768,-1.94310716728535,
16.4891101045687));
#275005=CARTESIAN_POINT('Ctrl Pts',(-0.274339754492164,-1.93586457571975,
16.485205814531));
#275006=CARTESIAN_POINT('Ctrl Pts',(-0.342254199379061,-1.925016908578,
16.4813015244933));
#275007=CARTESIAN_POINT('Ctrl Pts',(-0.409375065767647,-1.91063551090409,
16.4773972344557));
#275008=CARTESIAN_POINT('Ctrl Pts',(-0.476567426575125,-1.89623879474988,
16.4734887857269));
#275009=CARTESIAN_POINT('Ctrl Pts',(-0.542964040064954,-1.87830093956203,
16.4695803369982));
#275010=CARTESIAN_POINT('Ctrl Pts',(-0.608173330622478,-1.85694404867771,
16.4656718882695));
#275011=CARTESIAN_POINT('Ctrl Pts',(-0.673421653404437,-1.83557437423216,
16.4617611000666));
#275012=CARTESIAN_POINT('Ctrl Pts',(-0.737480780057206,-1.8107817686867,
16.4578503118638));
#275013=CARTESIAN_POINT('Ctrl Pts',(-0.799978686095661,-1.78273668885583,
16.4539395236609));
#275014=CARTESIAN_POINT('Ctrl Pts',(-0.862584505884696,-1.75464318420658,
16.4500219827866));
#275015=CARTESIAN_POINT('Ctrl Pts',(-0.923623287534398,-1.72328622133261,
16.4461044419124));
#275016=CARTESIAN_POINT('Ctrl Pts',(-0.982747968393865,-1.68888200612646,
16.4421869010381));
#275017=CARTESIAN_POINT('Ctrl Pts',(-1.01065209972749,-1.67264479815193,
16.4403380018395));
#275018=CARTESIAN_POINT('Ctrl Pts',(-1.03813031028421,-1.65572946599459,
16.4384891026409));
#275019=CARTESIAN_POINT('Ctrl Pts',(-1.06514858527807,-1.63816192462166,
16.4366402034423));
#275020=CARTESIAN_POINT('Ctrl Pts',(-1.12237316433513,-1.60095395481743,
16.4327242436563));
#275021=CARTESIAN_POINT('Ctrl Pts',(-1.17775982360252,-1.56066973669982,
16.4288082838704));
#275022=CARTESIAN_POINT('Ctrl Pts',(-1.23095822858698,-1.51751699808404,
16.4248923240845));
#275023=CARTESIAN_POINT('Ctrl Pts',(-1.28407650419064,-1.47442925769944,
16.4209822626603));
#275024=CARTESIAN_POINT('Ctrl Pts',(-1.33501268735557,-1.4284818792864,
16.4170722012361));
#275025=CARTESIAN_POINT('Ctrl Pts',(-1.3834449916962,-1.37992606865394,
16.4131621398119));
#275026=CARTESIAN_POINT('Ctrl Pts',(-1.43182040739025,-1.33142729173871,
16.4092566711508));
#275027=CARTESIAN_POINT('Ctrl Pts',(-1.47769743890976,-1.28032651433722,
16.4053512024897));
#275028=CARTESIAN_POINT('Ctrl Pts',(-1.52078842845766,-1.22691424144856,
16.4014457338286));
#275029=CARTESIAN_POINT('Ctrl Pts',(-1.56385248865943,-1.17353534810395,
16.3975427058568));
#275030=CARTESIAN_POINT('Ctrl Pts',(-1.60413365205027,-1.11784820716031,
16.393639677885));
#275031=CARTESIAN_POINT('Ctrl Pts',(-1.6413831816081,-1.06017793371399,
16.3897366499133));
#275032=CARTESIAN_POINT('Ctrl Pts',(-1.6786222472096,-1.00252386071987,
16.3858347183611));
#275033=CARTESIAN_POINT('Ctrl Pts',(-1.71283110250474,-0.942888174647101,
16.3819327868089));
#275034=CARTESIAN_POINT('Ctrl Pts',(-1.74380421683398,-0.881625120644844,
16.3780308552567));
#275035=CARTESIAN_POINT('Ctrl Pts',(-1.77477928560832,-0.820358200861631,
16.3741286774874));
#275036=CARTESIAN_POINT('Ctrl Pts',(-1.80251798820246,-0.757464149983337,
16.3702264997181));
#275037=CARTESIAN_POINT('Ctrl Pts',(-1.8268614954187,-0.693320327522964,
16.3663243219488));
#275038=CARTESIAN_POINT('Ctrl Pts',(-1.85123096816227,-0.629108087305018,
16.3624179819977));
#275039=CARTESIAN_POINT('Ctrl Pts',(-1.87219784364341,-0.563643876634213,
16.3585116420465));
#275040=CARTESIAN_POINT('Ctrl Pts',(-1.88965243210149,-0.49732251693738,
16.3546053020954));
#275041=CARTESIAN_POINT('Ctrl Pts',(-1.90711756295254,-0.430961099817349,
16.3506966027549));
#275042=CARTESIAN_POINT('Ctrl Pts',(-1.92106608512885,-0.3637419856602,
16.3467879034144));
#275043=CARTESIAN_POINT('Ctrl Pts',(-1.93143953667531,-0.296069782597726,
16.3428792040738));
#275044=CARTESIAN_POINT('Ctrl Pts',(-1.94183081966495,-0.228281254410631,
16.3389637858751));
#275045=CARTESIAN_POINT('Ctrl Pts',(-1.94863471911459,-0.160038572711775,
16.3350483676763));
#275046=CARTESIAN_POINT('Ctrl Pts',(-1.95184474547632,-0.0917501474466611,
16.3311329494776));
#275047=CARTESIAN_POINT('Ctrl Pts',(-1.95328309287062,-0.0611514957619569,
16.3293785303766));
#275048=CARTESIAN_POINT('Ctrl Pts',(-1.95400057833122,-0.0305436375502851,
16.3276241112755));
#275049=CARTESIAN_POINT('Ctrl Pts',(-1.95399999965015,3.69758055581722E-5,
16.3258696921745));
#275050=CARTESIAN_POINT('',(-1.95399927660164,-0.00168138046293059,15.625869711382));
#275051=CARTESIAN_POINT('Ctrl Pts',(-1.95399999965013,3.69766827344706E-5,
16.3258696921242));
#275052=CARTESIAN_POINT('Ctrl Pts',(-1.9539999621663,0.00201777642562759,
16.3257560530398));
#275053=CARTESIAN_POINT('Ctrl Pts',(-1.953996912733,0.00399857278929908,
16.3256424139553));
#275054=CARTESIAN_POINT('Ctrl Pts',(-1.95399085137439,0.00597935993164894,
16.3255287748708));
#275055=CARTESIAN_POINT('Ctrl Pts',(-1.95378186420173,0.0742741319649818,
16.3216106580765));
#275056=CARTESIAN_POINT('Ctrl Pts',(-1.94998765241292,0.142693315948708,
16.3176925412822));
#275057=CARTESIAN_POINT('Ctrl Pts',(-1.94259283162147,0.210829529556217,
16.3137744244879));
#275058=CARTESIAN_POINT('Ctrl Pts',(-1.9352091461905,0.278863141447944,
16.3098622077207));
#275059=CARTESIAN_POINT('Ctrl Pts',(-1.92423566498077,0.346614143558209,
16.3059499909535));
#275060=CARTESIAN_POINT('Ctrl Pts',(-1.9097090145515,0.413675573053036,
16.3020377741863));
#275061=CARTESIAN_POINT('Ctrl Pts',(-1.89519944654936,0.480658142525099,
16.2981301579399));
#275062=CARTESIAN_POINT('Ctrl Pts',(-1.87714511114424,0.546952271375196,
16.2942225416935));
#275063=CARTESIAN_POINT('Ctrl Pts',(-1.85563416057608,0.612158363581769,
16.2903149254472));
#275064=CARTESIAN_POINT('Ctrl Pts',(-1.83413669216254,0.677323587365809,
16.2864097583295));
#275065=CARTESIAN_POINT('Ctrl Pts',(-1.80918705990762,0.741401661179688,
16.2825045912118));
#275066=CARTESIAN_POINT('Ctrl Pts',(-1.78092360280814,0.804006915990707,
16.2785994240941));
#275067=CARTESIAN_POINT('Ctrl Pts',(-1.75266816614954,0.866594405043498,
16.2746953651623));
#275068=CARTESIAN_POINT('Ctrl Pts',(-1.72110097375604,0.927709456691211,
16.2707913062304));
#275069=CARTESIAN_POINT('Ctrl Pts',(-1.68640827532238,0.986986893998192,
16.2668872472985));
#275070=CARTESIAN_POINT('Ctrl Pts',(-1.65171352313379,1.04626784043922,
16.2629829572523));
#275071=CARTESIAN_POINT('Ctrl Pts',(-1.61389314823192,1.1037105333433,16.2590786672061));
#275072=CARTESIAN_POINT('Ctrl Pts',(-1.57317815826722,1.15897648049948,
16.2551743771598));
#275073=CARTESIAN_POINT('Ctrl Pts',(-1.53241980035068,1.21430129469546,
16.2512659284226));
#275074=CARTESIAN_POINT('Ctrl Pts',(-1.48876096651499,1.26744433919756,
16.2473574796854));
#275075=CARTESIAN_POINT('Ctrl Pts',(-1.44247400641579,1.31809891162036,
16.2434490309482));
#275076=CARTESIAN_POINT('Ctrl Pts',(-1.39615934040257,1.36878380427214,
16.2395382427368));
#275077=CARTESIAN_POINT('Ctrl Pts',(-1.3472137678834,1.41697691526967,16.2356274545255));
#275078=CARTESIAN_POINT('Ctrl Pts',(-1.2959456716492,1.4624092505635,16.2317166663141));
#275079=CARTESIAN_POINT('Ctrl Pts',(-1.24458905193016,1.50792003286317,
16.2277991254315));
#275080=CARTESIAN_POINT('Ctrl Pts',(-1.19090228930025,1.55066021915519,
16.2238815845489));
#275081=CARTESIAN_POINT('Ctrl Pts',(-1.13522520038532,1.59040238443298,
16.2199640436663));
#275082=CARTESIAN_POINT('Ctrl Pts',(-1.10894817510018,1.60915885863526,
16.218115144544));
#275083=CARTESIAN_POINT('Ctrl Pts',(-1.08222821521553,1.62724819735638,
16.2162662454217));
#275084=CARTESIAN_POINT('Ctrl Pts',(-1.05510293232958,1.6446500546285,16.2144173462994));
#275085=CARTESIAN_POINT('Ctrl Pts',(-0.997620063192867,1.68152740954919,
16.2104992295099));
#275086=CARTESIAN_POINT('Ctrl Pts',(-0.938087542964199,1.71546057626014,
16.2065811127204));
#275087=CARTESIAN_POINT('Ctrl Pts',(-0.876839237282497,1.74621560866975,
16.2026629959309));
#275088=CARTESIAN_POINT('Ctrl Pts',(-0.815683161283005,1.77692432915555,
16.1987507791685));
#275089=CARTESIAN_POINT('Ctrl Pts',(-0.75281686356938,1.80446419438366,
16.1948385624062));
#275090=CARTESIAN_POINT('Ctrl Pts',(-0.688602075615101,1.82864517647863,
16.1909263456438));
#275091=CARTESIAN_POINT('Ctrl Pts',(-0.624462800213449,1.85279772325924,
16.1870187294024));
#275092=CARTESIAN_POINT('Ctrl Pts',(-0.558978642019656,1.87359905881964,
16.183111113161));
#275093=CARTESIAN_POINT('Ctrl Pts',(-0.492533099124756,1.89090643509047,
16.1792034969195));
#275094=CARTESIAN_POINT('Ctrl Pts',(-0.426129201488483,1.90820296382919,
16.1752983298068));
#275095=CARTESIAN_POINT('Ctrl Pts',(-0.358765589358424,1.92200975357006,
16.1713931626941));
#275096=CARTESIAN_POINT('Ctrl Pts',(-0.290841290289802,1.9322337705005,
16.1674879955814));
#275097=CARTESIAN_POINT('Ctrl Pts',(-0.222936266387693,1.94245488611827,
16.1635839366546));
#275098=CARTESIAN_POINT('Ctrl Pts',(-0.15447135757717,1.94909517406813,
16.1596798777277));
#275099=CARTESIAN_POINT('Ctrl Pts',(-0.0858543711445922,1.95211296470142,
16.1557758188009));
#275100=CARTESIAN_POINT('Ctrl Pts',(-0.0172333226914123,1.9551309339833,
16.1518715287597));
#275101=CARTESIAN_POINT('Ctrl Pts',(0.0515393297417269,1.95452596114806,
16.1479672387185));
#275102=CARTESIAN_POINT('Ctrl Pts',(0.120053911615658,1.9503084520931,16.1440629486773));
#275103=CARTESIAN_POINT('Ctrl Pts',(0.188641472436451,1.94608645071897,
16.1401544999452));
#275104=CARTESIAN_POINT('Ctrl Pts',(0.256969922217087,1.93824426413374,
16.136246051213));
#275105=CARTESIAN_POINT('Ctrl Pts',(0.324633860893539,1.92684427402978,
16.1323376024808));
#275106=CARTESIAN_POINT('Ctrl Pts',(0.392338301068817,1.91543746025143,
16.1284268142745));
#275107=CARTESIAN_POINT('Ctrl Pts',(0.459376958409542,1.90046871188476,
16.1245160260683));
#275108=CARTESIAN_POINT('Ctrl Pts',(0.525356559333032,1.88205113787212,
16.120605237862));
#275109=CARTESIAN_POINT('Ctrl Pts',(0.591450085771083,1.86360176264264,
16.1166876969844));
#275110=CARTESIAN_POINT('Ctrl Pts',(0.656480440214814,1.84169183348761,
16.1127701561068));
#275111=CARTESIAN_POINT('Ctrl Pts',(0.720072213984936,1.8164834176636,16.1088526152292));
#275112=CARTESIAN_POINT('Ctrl Pts',(0.750084607277191,1.8045862044687,16.1070037160621));
#275113=CARTESIAN_POINT('Ctrl Pts',(0.779776899876457,1.79195496374141,
16.105154816895));
#275114=CARTESIAN_POINT('Ctrl Pts',(0.809111594666034,1.77861025167882,
16.103305917728));
#275115=CARTESIAN_POINT('Ctrl Pts',(0.871276564085345,1.75033064545719,
16.0993878009381));
#275116=CARTESIAN_POINT('Ctrl Pts',(0.93208036016985,1.71873192474972,16.0954696841482));
#275117=CARTESIAN_POINT('Ctrl Pts',(0.991145325020365,1.68396761984614,
16.0915515673583));
#275118=CARTESIAN_POINT('Ctrl Pts',(1.05012134793391,1.64925566415877,16.0876393505956));
#275119=CARTESIAN_POINT('Ctrl Pts',(1.10736331569261,1.61138783225709,16.0837271338329));
#275120=CARTESIAN_POINT('Ctrl Pts',(1.16251534446752,1.5705648900563,16.0798149170701));
#275121=CARTESIAN_POINT('Ctrl Pts',(1.21760251792454,1.5297899530686,16.0759073008283));
#275122=CARTESIAN_POINT('Ctrl Pts',(1.27060423981632,1.486067098487,16.0719996845865));
#275123=CARTESIAN_POINT('Ctrl Pts',(1.32119253330485,1.43964102815234,16.0680920683447));
#275124=CARTESIAN_POINT('Ctrl Pts',(1.37174912018855,1.39324405571689,16.0641869012316));
#275125=CARTESIAN_POINT('Ctrl Pts',(1.41989491766924,1.34414756024183,16.0602817341186));
#275126=CARTESIAN_POINT('Ctrl Pts',(1.46533528483458,1.29263626090975,16.0563765670055));
#275127=CARTESIAN_POINT('Ctrl Pts',(1.51076275719404,1.24113957915776,16.0524725080783));
#275128=CARTESIAN_POINT('Ctrl Pts',(1.55348599807477,1.18722982260129,16.0485684491511));
#275129=CARTESIAN_POINT('Ctrl Pts',(1.5932487504838,1.13122695295057,16.0446643902239));
#275130=CARTESIAN_POINT('Ctrl Pts',(1.63301385678685,1.07522076801575,16.0407601001824));
#275131=CARTESIAN_POINT('Ctrl Pts',(1.66981784400191,1.01712162653524,16.0368558101408));
#275132=CARTESIAN_POINT('Ctrl Pts',(1.70344718695854,0.957279312031251,
16.0329515200993));
#275133=CARTESIAN_POINT('Ctrl Pts',(1.73711235052379,0.897373255927272,
16.0290430713668));
#275134=CARTESIAN_POINT('Ctrl Pts',(1.76759587996122,0.83572075091901,16.0251346226343));
#275135=CARTESIAN_POINT('Ctrl Pts',(1.79473023028621,0.772696189001096,
16.0212261739018));
#275136=CARTESIAN_POINT('Ctrl Pts',(1.82188082237713,0.709633902569045,
16.0173153856952));
#275137=CARTESIAN_POINT('Ctrl Pts',(1.84567807517417,0.645198386229305,
16.0134045974886));
#275138=CARTESIAN_POINT('Ctrl Pts',(1.86600363512424,0.5797813671576,16.009493809282));
#275139=CARTESIAN_POINT('Ctrl Pts',(1.88636429076809,0.514251393969258,
16.0055762684041));
#275140=CARTESIAN_POINT('Ctrl Pts',(1.90324116860687,0.447737012140573,
16.0016587275262));
#275141=CARTESIAN_POINT('Ctrl Pts',(1.9165667339101,0.380641503870971,15.9977411866483));
#275142=CARTESIAN_POINT('Ctrl Pts',(1.92285578801716,0.34897550905233,15.9958922874844));
#275143=CARTESIAN_POINT('Ctrl Pts',(1.92835457016774,0.317180165470872,
15.9940433883205));
#275144=CARTESIAN_POINT('Ctrl Pts',(1.93306000430126,0.285298124373133,
15.9921944891566));
#275145=CARTESIAN_POINT('Ctrl Pts',(1.94303158136038,0.217734915413521,
15.9882763723656));
#275146=CARTESIAN_POINT('Ctrl Pts',(1.94947651482669,0.149514364227127,
15.9843582555746));
#275147=CARTESIAN_POINT('Ctrl Pts',(1.95231887838287,0.0810370107410566,
15.9804401387836));
#275148=CARTESIAN_POINT('Ctrl Pts',(1.95515696181598,0.0126627726711564,
15.9765279220198));
#275149=CARTESIAN_POINT('Ctrl Pts',(1.95440322154275,-0.0559670127300859,
15.9726157052559));
#275150=CARTESIAN_POINT('Ctrl Pts',(1.95003322385718,-0.124444468953685,
15.9687034884921));
#275151=CARTESIAN_POINT('Ctrl Pts',(1.94566836501407,-0.192841399995072,
15.9647958722491));
#275152=CARTESIAN_POINT('Ctrl Pts',(1.93769572544993,-0.261085869055538,
15.9608882560061));
#275153=CARTESIAN_POINT('Ctrl Pts',(1.92614291961,-0.328769605097942,15.9569806397632));
#275154=CARTESIAN_POINT('Ctrl Pts',(1.91459735458058,-0.396410919834754,
15.9530754726489));
#275155=CARTESIAN_POINT('Ctrl Pts',(1.89947615702947,-0.463491714927154,
15.9491703055347));
#275156=CARTESIAN_POINT('Ctrl Pts',(1.88085864327038,-0.529610011267826,
15.9452651384205));
#275157=CARTESIAN_POINT('Ctrl Pts',(1.86224641268212,-0.595709544939138,
15.9413610794921));
#275158=CARTESIAN_POINT('Ctrl Pts',(1.84013996875894,-0.660846648827569,
15.9374570205637));
#275159=CARTESIAN_POINT('Ctrl Pts',(1.81466905746596,-0.724632466755111,
15.9335529616353));
#275160=CARTESIAN_POINT('Ctrl Pts',(1.78919663833397,-0.788422060705574,
15.9296486715926));
#275161=CARTESIAN_POINT('Ctrl Pts',(1.76035954120025,-0.85085975402567,
15.9257443815498));
#275162=CARTESIAN_POINT('Ctrl Pts',(1.72833574705956,-0.911576406800913,
15.9218400915071));
#275163=CARTESIAN_POINT('Ctrl Pts',(1.6962778424755,-0.972357732485841,
15.9179316427734));
#275164=CARTESIAN_POINT('Ctrl Pts',(1.66102669674379,-1.03141392325265,
15.9140231940397));
#275165=CARTESIAN_POINT('Ctrl Pts',(1.62280590891998,-1.08840111263009,
15.910114745306));
#275166=CARTESIAN_POINT('Ctrl Pts',(1.58456224333848,-1.14542241274107,
15.9062039570982));
#275167=CARTESIAN_POINT('Ctrl Pts',(1.54334569323334,-1.20037185319889,
15.9022931688904));
#275168=CARTESIAN_POINT('Ctrl Pts',(1.49942110819802,-1.2529374845898,15.8983823806825));
#275169=CARTESIAN_POINT('Ctrl Pts',(1.45542067955548,-1.30559387989111,
15.8944648398034));
#275170=CARTESIAN_POINT('Ctrl Pts',(1.40870321831996,-1.35585789101151,
15.8905472989243));
#275171=CARTESIAN_POINT('Ctrl Pts',(1.35957085206292,-1.40345398863693,
15.8866297580452));
#275172=CARTESIAN_POINT('Ctrl Pts',(1.33638263445959,-1.42591715808889,
15.8847808588918));
#275173=CARTESIAN_POINT('Ctrl Pts',(1.31265700314292,-1.44778665477442,
15.8829319597385));
#275174=CARTESIAN_POINT('Ctrl Pts',(1.28842811743316,-1.46903675454621,
15.8810830605851));
#275175=CARTESIAN_POINT('Ctrl Pts',(1.23708318402424,-1.51406915804942,
15.8771649437949));
#275176=CARTESIAN_POINT('Ctrl Pts',(1.18327270622517,-1.55649572105797,
15.8732468270046));
#275177=CARTESIAN_POINT('Ctrl Pts',(1.12729195521896,-1.59603535289749,
15.8693287102144));
#275178=CARTESIAN_POINT('Ctrl Pts',(1.07139550184042,-1.63551544467898,
15.8654164934513));
#275179=CARTESIAN_POINT('Ctrl Pts',(1.01333565974962,-1.67211695152243,
15.8615042766881));
#275180=CARTESIAN_POINT('Ctrl Pts',(0.95344180006052,-1.70559805754385,
15.857592059925));
#275181=CARTESIAN_POINT('Ctrl Pts',(0.893618371784101,-1.73903979188998,
15.8536844436828));
#275182=CARTESIAN_POINT('Ctrl Pts',(0.831965636444704,-1.76936817401605,
15.8497768274406));
#275183=CARTESIAN_POINT('Ctrl Pts',(0.768841534976206,-1.79638489586598,
15.8458692111984));
#275184=CARTESIAN_POINT('Ctrl Pts',(0.705756997027155,-1.82338468477627,
15.8419640440849));
#275185=CARTESIAN_POINT('Ctrl Pts',(0.641203373469786,-1.847076737653,15.8380588769714));
#275186=CARTESIAN_POINT('Ctrl Pts',(0.575561370375906,-1.86730959107776,
15.8341537098579));
#275187=CARTESIAN_POINT('Ctrl Pts',(0.509937994791741,-1.88753670293987,
15.8302496509303));
#275188=CARTESIAN_POINT('Ctrl Pts',(0.443227322636232,-1.90430641923978,
15.8263455920027));
#275189=CARTESIAN_POINT('Ctrl Pts',(0.375826396658372,-1.91751675861641,
15.822441533075));
#275190=CARTESIAN_POINT('Ctrl Pts',(0.308421480648792,-1.93072788002492,
15.8185372430331));
#275191=CARTESIAN_POINT('Ctrl Pts',(0.240326712879047,-1.9403791140884,
15.8146329529911));
#275192=CARTESIAN_POINT('Ctrl Pts',(0.171948743514836,-1.94641969513352,
15.8107286629492));
#275193=CARTESIAN_POINT('Ctrl Pts',(0.103497940718056,-1.95246671035995,
15.8068202142162));
#275194=CARTESIAN_POINT('Ctrl Pts',(0.034763825229422,-1.95489535393298,
15.8029117654833));
#275195=CARTESIAN_POINT('Ctrl Pts',(-0.0338434333726768,-1.95370689255516,
15.7990033167503));
#275196=CARTESIAN_POINT('Ctrl Pts',(-0.102491758115139,-1.95251771980186,
15.7950925285433));
#275197=CARTESIAN_POINT('Ctrl Pts',(-0.171012584112308,-1.94770716763265,
15.7911817403363));
#275198=CARTESIAN_POINT('Ctrl Pts',(-0.239000172764327,-1.93932847073894,
15.7872709521292));
#275199=CARTESIAN_POINT('Ctrl Pts',(-0.307105154078534,-1.93093530653504,
15.7833534112509));
#275200=CARTESIAN_POINT('Ctrl Pts',(-0.374674576343085,-1.9189617869472,
15.7794358703725));
#275201=CARTESIAN_POINT('Ctrl Pts',(-0.441313069903809,-1.90351222069418,
15.7755183294942));
#275202=CARTESIAN_POINT('Ctrl Pts',(-0.472763374726625,-1.89622073581697,
15.773669430334));
#275203=CARTESIAN_POINT('Ctrl Pts',(-0.504006548632445,-1.88815571513218,
15.7718205311738));
#275204=CARTESIAN_POINT('Ctrl Pts',(-0.53500244970063,-1.87933189692889,
15.7699716320137));
#275205=CARTESIAN_POINT('Ctrl Pts',(-0.600687784533275,-1.86063279694431,
15.7660535152233));
#275206=CARTESIAN_POINT('Ctrl Pts',(-0.665521807765686,-1.83844878915834,
15.7621353984329));
#275207=CARTESIAN_POINT('Ctrl Pts',(-0.729108197939647,-1.81287540545323,
15.7582172816425));
#275208=CARTESIAN_POINT('Ctrl Pts',(-0.792598837668159,-1.78734053097744,
15.7543050648793));
#275209=CARTESIAN_POINT('Ctrl Pts',(-0.854845120261035,-1.75842659194378,
15.7503928481161));
#275210=CARTESIAN_POINT('Ctrl Pts',(-0.915465215454334,-1.72627907340996,
15.7464806313529));
#275211=CARTESIAN_POINT('Ctrl Pts',(-0.976014025227648,-1.69416935833641,
15.7425730151105));
#275212=CARTESIAN_POINT('Ctrl Pts',(-1.03494001294859,-1.65883384491755,
15.7386653988682));
#275213=CARTESIAN_POINT('Ctrl Pts',(-1.09188239574313,-1.62046562254996,
15.7347577826259));
#275214=CARTESIAN_POINT('Ctrl Pts',(-1.1487890894583,-1.58212144776287,
15.7308526155123));
#275215=CARTESIAN_POINT('Ctrl Pts',(-1.20371423743605,-1.54074860880089,
15.7269474483987));
#275216=CARTESIAN_POINT('Ctrl Pts',(-1.25632405649873,-1.49658473367283,
15.7230422812852));
#275217=CARTESIAN_POINT('Ctrl Pts',(-1.30891894624984,-1.45243339111499,
15.7191382223574));
#275218=CARTESIAN_POINT('Ctrl Pts',(-1.35919943484673,-1.40549290080089,
15.7152341634297));
#275219=CARTESIAN_POINT('Ctrl Pts',(-1.40686444203506,-1.35604146018378,
15.7113301045019));
#275220=CARTESIAN_POINT('Ctrl Pts',(-1.4545322709189,-1.30658709211705,
15.7074258144599));
#275221=CARTESIAN_POINT('Ctrl Pts',(-1.49958397148951,-1.2546218345644,
15.7035215244178));
#275222=CARTESIAN_POINT('Ctrl Pts',(-1.54175627363209,-1.20045974223049,
15.6996172343758));
#275223=CARTESIAN_POINT('Ctrl Pts',(-1.58397349599608,-1.14623995863819,
15.6957087856427));
#275224=CARTESIAN_POINT('Ctrl Pts',(-1.6233048963418,-1.08981905924165,
15.6918003369097));
#275225=CARTESIAN_POINT('Ctrl Pts',(-1.65952900374366,-1.03154228499543,
15.6878918881766));
#275226=CARTESIAN_POINT('Ctrl Pts',(-1.69577479375325,-0.973230628110908,
15.6839810999695));
#275227=CARTESIAN_POINT('Ctrl Pts',(-1.7289093519144,-0.91306131647089,
15.6800703117623));
#275228=CARTESIAN_POINT('Ctrl Pts',(-1.75875726583993,-0.851404063800066,
15.6761595235552));
#275229=CARTESIAN_POINT('Ctrl Pts',(-1.78865671749675,-0.7896403489179,
15.6722419826767));
#275230=CARTESIAN_POINT('Ctrl Pts',(-1.81525800800206,-0.726384018482055,
15.6683244417983));
#275231=CARTESIAN_POINT('Ctrl Pts',(-1.83843425416253,-0.662023785918493,
15.6644069009198));
#275232=CARTESIAN_POINT('Ctrl Pts',(-1.84937237666568,-0.631648715545271,
15.6625580017606));
#275233=CARTESIAN_POINT('Ctrl Pts',(-1.85954833023355,-0.601027963721518,
15.6607091026014));
#275234=CARTESIAN_POINT('Ctrl Pts',(-1.86895271668084,-0.570203246931559,
15.6588602034422));
#275235=CARTESIAN_POINT('Ctrl Pts',(-1.8933156493855,-0.490348967760566,
15.6540704592047));
#275236=CARTESIAN_POINT('Ctrl Pts',(-1.91257560688055,-0.408869779193623,
15.6492807149672));
#275237=CARTESIAN_POINT('Ctrl Pts',(-1.92655338481555,-0.32635571920184,
15.6444909707297));
#275238=CARTESIAN_POINT('Ctrl Pts',(-1.94033383030346,-0.245006558341653,
15.6397688461063));
#275239=CARTESIAN_POINT('Ctrl Pts',(-1.94898014136491,-0.162651520851779,
15.635046721483));
#275240=CARTESIAN_POINT('Ctrl Pts',(-1.95236668761014,-0.079876887208999,
15.6303245968597));
#275241=CARTESIAN_POINT('Ctrl Pts',(-1.95343165143404,-0.0538468306315289,
15.6288396350338));
#275242=CARTESIAN_POINT('Ctrl Pts',(-1.95397682314485,-0.0277754378755728,
15.6273546732079));
#275243=CARTESIAN_POINT('Ctrl Pts',(-1.95399927660164,-0.00168138046293059,
15.625869711382));
#275244=CARTESIAN_POINT('',(-1.95392498394666,0.000982598694633225,14.9258696453069));
#275245=CARTESIAN_POINT('Ctrl Pts',(-1.9527894730371,-0.0016800012556531,
15.6258696921242));
#275246=CARTESIAN_POINT('Ctrl Pts',(-1.94903578034424,0.455625916679805,
15.5998293863731));
#275247=CARTESIAN_POINT('Ctrl Pts',(-1.56072621450247,1.56910039980144,
15.5367519377649));
#275248=CARTESIAN_POINT('Ctrl Pts',(0.294214790414482,2.29052272133908,
15.4366373462993));
#275249=CARTESIAN_POINT('Ctrl Pts',(2.08372643567803,0.995560556227894,
15.325525917728));
#275250=CARTESIAN_POINT('Ctrl Pts',(1.96681121926772,-1.21025216695624,
15.2144144891566));
#275251=CARTESIAN_POINT('Ctrl Pts',(0.0504363060114985,-2.30879034537602,
15.1033030605851));
#275252=CARTESIAN_POINT('Ctrl Pts',(-1.64838339262918,-1.4312106179003,
15.0071214615743));
#275253=CARTESIAN_POINT('Ctrl Pts',(-1.94951755043896,-0.388009868955187,
14.9479770054207));
#275254=CARTESIAN_POINT('Ctrl Pts',(-1.9512855068604,0.000980447537236029,
14.9258696921242));
#275255=CARTESIAN_POINT('',(-1.95399967130156,0.00113338140505696,14.2258696921744));
#275256=CARTESIAN_POINT('Ctrl Pts',(-1.95399975291197,0.000982659630874597,
14.9258696439807));
#275257=CARTESIAN_POINT('Ctrl Pts',(-1.95396157458776,0.0768995221230205,
14.9215610769975));
#275258=CARTESIAN_POINT('Ctrl Pts',(-1.94949495136225,0.15266488028038,
14.9172525100143));
#275259=CARTESIAN_POINT('Ctrl Pts',(-1.94067744149054,0.22778733083678,
14.9129439430311));
#275260=CARTESIAN_POINT('Ctrl Pts',(-1.93182839971281,0.303178423457082,
14.9086199683726));
#275261=CARTESIAN_POINT('Ctrl Pts',(-1.91859743506083,0.377921711246782,
14.9042959937141));
#275262=CARTESIAN_POINT('Ctrl Pts',(-1.90111289227954,0.45153712007822,
14.8999720190555));
#275263=CARTESIAN_POINT('Ctrl Pts',(-1.88354470861175,0.525504683274326,
14.8956273597798));
#275264=CARTESIAN_POINT('Ctrl Pts',(-1.86168229836676,0.598333268948949,
14.8912827005041));
#275265=CARTESIAN_POINT('Ctrl Pts',(-1.8357040846616,0.669556953183755,
14.8869380412285));
#275266=CARTESIAN_POINT('Ctrl Pts',(-1.82402874165582,0.70156688862484,
14.884985428633));
#275267=CARTESIAN_POINT('Ctrl Pts',(-1.81152269757046,0.733252964852512,
14.8830328160376));
#275268=CARTESIAN_POINT('Ctrl Pts',(-1.79820517487775,0.76457448887789,
14.8810802034422));
#275269=CARTESIAN_POINT('Ctrl Pts',(-1.77148220412985,0.827424328868625,
14.8771620866518));
#275270=CARTESIAN_POINT('Ctrl Pts',(-1.74140725560317,0.888996061353628,
14.8732439698614));
#275271=CARTESIAN_POINT('Ctrl Pts',(-1.70812440854876,0.948908322716141,
14.869325853071));
#275272=CARTESIAN_POINT('Ctrl Pts',(-1.67489167988323,1.00873036625537,
14.8654136363077));
#275273=CARTESIAN_POINT('Ctrl Pts',(-1.63846087658321,1.06689747154796,
14.8615014195444));
#275274=CARTESIAN_POINT('Ctrl Pts',(-1.59902384104076,1.12304886616,14.8575892027811));
#275275=CARTESIAN_POINT('Ctrl Pts',(-1.55963318097214,1.179134230263,14.8536815865387));
#275276=CARTESIAN_POINT('Ctrl Pts',(-1.5172435908701,1.23320819061896,14.8497739702964));
#275277=CARTESIAN_POINT('Ctrl Pts',(-1.47209153029668,1.28493677915638,
14.845866354054));
#275278=CARTESIAN_POINT('Ctrl Pts',(-1.42696776912689,1.33663294640034,
14.8419611869404));
#275279=CARTESIAN_POINT('Ctrl Pts',(-1.37908529476368,1.38598628806162,
14.8380560198267));
#275280=CARTESIAN_POINT('Ctrl Pts',(-1.32872140174712,1.43269516525295,
14.8341508527131));
#275281=CARTESIAN_POINT('Ctrl Pts',(-1.27837180070615,1.47939078766803,
14.8302467937853));
#275282=CARTESIAN_POINT('Ctrl Pts',(-1.22554253937853,1.5234431010258,14.8263427348575));
#275283=CARTESIAN_POINT('Ctrl Pts',(-1.17054709964035,1.56458796094166,
14.8224386759297));
#275284=CARTESIAN_POINT('Ctrl Pts',(-1.11554840425626,1.60573525657028,
14.8185343858876));
#275285=CARTESIAN_POINT('Ctrl Pts',(-1.05838367125969,1.64397446443823,
14.8146300958455));
#275286=CARTESIAN_POINT('Ctrl Pts',(-0.999397259087691,1.67908341619111,
14.8107258058034));
#275287=CARTESIAN_POINT('Ctrl Pts',(-0.940348016987983,1.71422976457178,
14.8068173570702));
#275288=CARTESIAN_POINT('Ctrl Pts',(-0.879473646804447,1.7462389507024,
14.8029089083371));
#275289=CARTESIAN_POINT('Ctrl Pts',(-0.817144252694092,1.77493415942367,
14.799000459604));
#275290=CARTESIAN_POINT('Ctrl Pts',(-0.75477755017502,1.8036465441915,14.7950896713968));
#275291=CARTESIAN_POINT('Ctrl Pts',(-0.690954547508917,1.82904082186524,
14.7911788831896));
#275292=CARTESIAN_POINT('Ctrl Pts',(-0.626063903494332,1.8509889218311,
14.7872680949824));
#275293=CARTESIAN_POINT('Ctrl Pts',(-0.561061214243252,1.8729749190946,
14.7833505541039));
#275294=CARTESIAN_POINT('Ctrl Pts',(-0.494987677728567,1.89150272979415,
14.7794330132254));
#275295=CARTESIAN_POINT('Ctrl Pts',(-0.428244769546033,1.90649479867018,
14.7755154723469));
#275296=CARTESIAN_POINT('Ctrl Pts',(-0.396745185849562,1.91357036581587,
14.7736665731882));
#275297=CARTESIAN_POINT('Ctrl Pts',(-0.365096616230716,1.91985912672413,
14.7718176740295));
#275298=CARTESIAN_POINT('Ctrl Pts',(-0.333341622120266,1.92535694429948,
14.7699687748708));
#275299=CARTESIAN_POINT('Ctrl Pts',(-0.266047646124195,1.93700771024388,
14.7660506580804));
#275300=CARTESIAN_POINT('Ctrl Pts',(-0.198008720544545,1.94514929338545,
14.76213254129));
#275301=CARTESIAN_POINT('Ctrl Pts',(-0.129623370609614,1.94969581776025,
14.7582144244996));
#275302=CARTESIAN_POINT('Ctrl Pts',(-0.0613409975491255,1.95423549583141,
14.7543022077363));
#275303=CARTESIAN_POINT('Ctrl Pts',(0.0072862777138335,1.95519082675997,
14.750389990973));
#275304=CARTESIAN_POINT('Ctrl Pts',(0.075851313510783,1.95252722855244,
14.7464777742098));
#275305=CARTESIAN_POINT('Ctrl Pts',(0.144335721137273,1.94986676256892,
14.7425701579674));
#275306=CARTESIAN_POINT('Ctrl Pts',(0.212757545471486,1.94359583820583,
14.738662541725));
#275307=CARTESIAN_POINT('Ctrl Pts',(0.280707954473607,1.93373189566063,
14.7347549254826));
#275308=CARTESIAN_POINT('Ctrl Pts',(0.348615775030661,1.9238741354178,14.730849758369));
#275309=CARTESIAN_POINT('Ctrl Pts',(0.416052280675558,1.91042789465421,
14.7269445912553));
#275310=CARTESIAN_POINT('Ctrl Pts',(0.482613642004295,1.89346245607124,
14.7230394241417));
#275311=CARTESIAN_POINT('Ctrl Pts',(0.549156114933165,1.87650183184276,
14.7191353652139));
#275312=CARTESIAN_POINT('Ctrl Pts',(0.614823460133153,1.85602411373327,
14.7152313062861));
#275313=CARTESIAN_POINT('Ctrl Pts',(0.679223711395073,1.83214932521307,
14.7113272473583));
#275314=CARTESIAN_POINT('Ctrl Pts',(0.743627775053325,1.80827312334192,
14.7074229573162));
#275315=CARTESIAN_POINT('Ctrl Pts',(0.806764135539207,1.78099962518855,
14.7035186672741));
#275316=CARTESIAN_POINT('Ctrl Pts',(0.868259335773061,1.75049756522051,
14.6996143772319));
#275317=CARTESIAN_POINT('Ctrl Pts',(0.92982003819369,1.71996301569845,14.6957059284988));
#275318=CARTESIAN_POINT('Ctrl Pts',(0.989735650203325,1.68619326030272,
14.6917974797657));
#275319=CARTESIAN_POINT('Ctrl Pts',(1.04765684446948,1.6494032667108,14.6878890310326));
#275320=CARTESIAN_POINT('Ctrl Pts',(1.10561270853501,1.6125912517895,14.6839782428254));
#275321=CARTESIAN_POINT('Ctrl Pts',(1.16157137821388,1.57275568607684,14.6800674546182));
#275322=CARTESIAN_POINT('Ctrl Pts',(1.21521440622377,1.53015356971325,14.676156666411));
#275323=CARTESIAN_POINT('Ctrl Pts',(1.26895005846096,1.48747789321975,14.6722391255325));
#275324=CARTESIAN_POINT('Ctrl Pts',(1.32036172060979,1.44202645768731,14.668321584654));
#275325=CARTESIAN_POINT('Ctrl Pts',(1.36916642599834,1.39409443651387,14.6644040437755));
#275326=CARTESIAN_POINT('Ctrl Pts',(1.39220000280892,1.37147272652516,14.6625551446168));
#275327=CARTESIAN_POINT('Ctrl Pts',(1.41465347216608,1.34829898736798,14.6607062454581));
#275328=CARTESIAN_POINT('Ctrl Pts',(1.43650026735261,1.32460672725752,14.6588573462994));
#275329=CARTESIAN_POINT('Ctrl Pts',(1.48279716496029,1.27439899055916,14.6549392295089));
#275330=CARTESIAN_POINT('Ctrl Pts',(1.52655042044952,1.22166159012838,14.6510211127185));
#275331=CARTESIAN_POINT('Ctrl Pts',(1.56747167823192,1.16668270662628,14.6471029959281));
#275332=CARTESIAN_POINT('Ctrl Pts',(1.60833131545921,1.1117866121073,14.6431907791648));
#275333=CARTESIAN_POINT('Ctrl Pts',(1.64636712720353,1.05465612469319,14.6392785624015));
#275334=CARTESIAN_POINT('Ctrl Pts',(1.68132917142388,0.995614492320737,
14.6353663456382));
#275335=CARTESIAN_POINT('Ctrl Pts',(1.71625010247877,0.936642289195202,
14.6314587293958));
#275336=CARTESIAN_POINT('Ctrl Pts',(1.74810419513703,0.875763825691861,
14.6275511131535));
#275337=CARTESIAN_POINT('Ctrl Pts',(1.77668429032641,0.813331994026637,
14.6236434969111));
#275338=CARTESIAN_POINT('Ctrl Pts',(1.80524647271982,0.750939291995364,
14.6197383297974));
#275339=CARTESIAN_POINT('Ctrl Pts',(1.83053852388676,0.68699559932706,14.6158331626838));
#275340=CARTESIAN_POINT('Ctrl Pts',(1.8523995480318,0.621877732718885,14.6119279955702));
#275341=CARTESIAN_POINT('Ctrl Pts',(1.87425436858127,0.556778344883991,
14.6080239366424));
#275342=CARTESIAN_POINT('Ctrl Pts',(1.89267993847419,0.490505910654328,
14.6041198777146));
#275343=CARTESIAN_POINT('Ctrl Pts',(1.90756442185842,0.423454810410668,
14.6002158187868));
#275344=CARTESIAN_POINT('Ctrl Pts',(1.92244978638131,0.356399740844437,
14.5963115287446));
#275345=CARTESIAN_POINT('Ctrl Pts',(1.9337935441209,0.288566394492564,14.5924072387025));
#275346=CARTESIAN_POINT('Ctrl Pts',(1.94153481981558,0.220360031411555,
14.5885029486604));
#275347=CARTESIAN_POINT('Ctrl Pts',(1.94928434120234,0.152081017686014,
14.5845944999273));
#275348=CARTESIAN_POINT('Ctrl Pts',(1.95342366706846,0.0834286839793453,
14.5806860511942));
#275349=CARTESIAN_POINT('Ctrl Pts',(1.95394385076509,0.0148131042422796,
14.5767776024611));
#275350=CARTESIAN_POINT('Ctrl Pts',(1.95446434582726,-0.0538435466158792,
14.5728668142538));
#275351=CARTESIAN_POINT('Ctrl Pts',(1.95136140959826,-0.122462908276107,
14.5689560260466));
#275352=CARTESIAN_POINT('Ctrl Pts',(1.94467815763461,-0.190638042422939,
14.5650452378394));
#275353=CARTESIAN_POINT('Ctrl Pts',(1.93798336584796,-0.258930893062583,
14.5611276969609));
#275354=CARTESIAN_POINT('Ctrl Pts',(1.92769599364402,-0.326777499241707,
14.5572101560824));
#275355=CARTESIAN_POINT('Ctrl Pts',(1.91391047295192,-0.393780016665343,
14.5532926152039));
#275356=CARTESIAN_POINT('Ctrl Pts',(1.90740434106983,-0.425402123985535,
14.5514437160453));
#275357=CARTESIAN_POINT('Ctrl Pts',(1.90011975577961,-0.456836425151338,
14.5495948168866));
#275358=CARTESIAN_POINT('Ctrl Pts',(1.89207045129286,-0.488042423713781,
14.547745917728));
#275359=CARTESIAN_POINT('Ctrl Pts',(1.87501267130884,-0.55417298922247,
14.5438278009376));
#275360=CARTESIAN_POINT('Ctrl Pts',(1.85444986686256,-0.61953927903166,
14.5399096841471));
#275361=CARTESIAN_POINT('Ctrl Pts',(1.83046767206848,-0.683742715875045,
14.5359915673567));
#275362=CARTESIAN_POINT('Ctrl Pts',(1.80652159043993,-0.74784947310416,
14.5320793505934));
#275363=CARTESIAN_POINT('Ctrl Pts',(1.77916650819632,-0.81079639552836,
14.5281671338301));
#275364=CARTESIAN_POINT('Ctrl Pts',(1.74853835796165,-0.872198148780866,
14.5242549170668));
#275365=CARTESIAN_POINT('Ctrl Pts',(1.71794622450565,-0.933527697432714,
14.5203473008244));
#275366=CARTESIAN_POINT('Ctrl Pts',(1.68408888559597,-0.993315247470937,
14.5164396845821));
#275367=CARTESIAN_POINT('Ctrl Pts',(1.64715038750284,-1.05119532007579,
14.5125320683397));
#275368=CARTESIAN_POINT('Ctrl Pts',(1.61023504089945,-1.10903911589691,
14.508626901226));
#275369=CARTESIAN_POINT('Ctrl Pts',(1.57024262990491,-1.16497739212295,
14.5047217341124));
#275370=CARTESIAN_POINT('Ctrl Pts',(1.52740239786812,-1.21867055227683,
14.5008165669987));
#275371=CARTESIAN_POINT('Ctrl Pts',(1.48457432278571,-1.27234847569489,
14.4969125080709));
#275372=CARTESIAN_POINT('Ctrl Pts',(1.43890033758603,-1.3237821634938,14.4930084491431));
#275373=CARTESIAN_POINT('Ctrl Pts',(1.39065105676619,-1.37266370182761,
14.4891043902153));
#275374=CARTESIAN_POINT('Ctrl Pts',(1.34239891966273,-1.42154813387372,
14.4852001001732));
#275375=CARTESIAN_POINT('Ctrl Pts',(1.29157153162983,-1.46787976823632,
14.481295810131));
#275376=CARTESIAN_POINT('Ctrl Pts',(1.23847629474704,-1.51138759666396,
14.4773915200889));
#275377=CARTESIAN_POINT('Ctrl Pts',(1.18532450297689,-1.55494176786131,
14.4734830713558));
#275378=CARTESIAN_POINT('Ctrl Pts',(1.12990042271788,-1.59566581811973,
14.4695746226227));
#275379=CARTESIAN_POINT('Ctrl Pts',(1.07254367340351,-1.63332974890011,
14.4656661738895));
#275380=CARTESIAN_POINT('Ctrl Pts',(1.01515259214869,-1.67101622412111,
14.4617553856823));
#275381=CARTESIAN_POINT('Ctrl Pts',(0.955826964408324,-1.7056386864992,
14.4578445974751));
#275382=CARTESIAN_POINT('Ctrl Pts',(0.894932021626566,-1.73701257239762,
14.4539338092679));
#275383=CARTESIAN_POINT('Ctrl Pts',(0.833931932897054,-1.7684406308893,
14.4500162683894));
#275384=CARTESIAN_POINT('Ctrl Pts',(0.771357569288752,-1.79660871594869,
14.4460987275109));
#275385=CARTESIAN_POINT('Ctrl Pts',(0.707594364402169,-1.8213803050067,
14.4421811866323));
#275386=CARTESIAN_POINT('Ctrl Pts',(0.677501063650518,-1.83307135599676,
14.4403322874737));
#275387=CARTESIAN_POINT('Ctrl Pts',(0.647143180102627,-1.84400659166273,
14.4384833883152));
#275388=CARTESIAN_POINT('Ctrl Pts',(0.616562183300354,-1.85417557801949,
14.4366344891566));
#275389=CARTESIAN_POINT('Ctrl Pts',(0.551756097753758,-1.87572530721959,
14.4327163723661));
#275390=CARTESIAN_POINT('Ctrl Pts',(0.485690395251855,-1.89391606649548,
14.4287982555757));
#275391=CARTESIAN_POINT('Ctrl Pts',(0.418746351910798,-1.90860354520298,
14.4248801387853));
#275392=CARTESIAN_POINT('Ctrl Pts',(0.351903115078058,-1.92326890702942,
14.420967922022));
#275393=CARTESIAN_POINT('Ctrl Pts',(0.284184638953922,-1.93444135343305,
14.4170557052587));
#275394=CARTESIAN_POINT('Ctrl Pts',(0.215988364403192,-1.94202601075331,
14.4131434884954));
#275395=CARTESIAN_POINT('Ctrl Pts',(0.147872284382886,-1.94960174899352,
14.4092358722531));
#275396=CARTESIAN_POINT('Ctrl Pts',(0.0792800083515805,-1.95359802306459,
14.4053282560107));
#275397=CARTESIAN_POINT('Ctrl Pts',(0.0106184017329989,-1.95397114859576,
14.4014206397683));
#275398=CARTESIAN_POINT('Ctrl Pts',(-0.0580001706919385,-1.95434404026761,
14.3975154726547));
#275399=CARTESIAN_POINT('Ctrl Pts',(-0.126687496737633,-1.95109828535075,
14.393610305541));
#275400=CARTESIAN_POINT('Ctrl Pts',(-0.195033931461197,-1.94424220856836,
14.3897051384274));
#275401=CARTESIAN_POINT('Ctrl Pts',(-0.263360971226991,-1.93738807736398,
14.3858010794996));
#275402=CARTESIAN_POINT('Ctrl Pts',(-0.331346822514729,-1.92692570720796,
14.3818970205718));
#275403=CARTESIAN_POINT('Ctrl Pts',(-0.398586008999103,-1.91291536494173,
14.377992961644));
#275404=CARTESIAN_POINT('Ctrl Pts',(-0.465829175940538,-1.89890419328466,
14.3740886716018));
#275405=CARTESIAN_POINT('Ctrl Pts',(-0.53232510931066,-1.88134473537189,
14.3701843815597));
#275406=CARTESIAN_POINT('Ctrl Pts',(-0.597679375619929,-1.86034818352871,
14.3662800915176));
#275407=CARTESIAN_POINT('Ctrl Pts',(-0.663103254636134,-1.8393292670123,
14.3623716427845));
#275408=CARTESIAN_POINT('Ctrl Pts',(-0.727382570513591,-1.81486610098012,
14.3584631940514));
#275409=CARTESIAN_POINT('Ctrl Pts',(-0.790139859719754,-1.7871191907878,
14.3545547453182));
#275410=CARTESIAN_POINT('Ctrl Pts',(-0.852934713459206,-1.75935567217048,
14.350643957111));
#275411=CARTESIAN_POINT('Ctrl Pts',(-0.914205288582151,-1.72830471997885,
14.3467331689038));
#275412=CARTESIAN_POINT('Ctrl Pts',(-0.97359839248268,-1.69417300478881,
14.3428223806966));
#275413=CARTESIAN_POINT('Ctrl Pts',(-1.03309404913903,-1.65998235512281,
14.3389048398181));
#275414=CARTESIAN_POINT('Ctrl Pts',(-1.09070535174908,-1.62270059271197,
14.3349872989396));
#275415=CARTESIAN_POINT('Ctrl Pts',(-1.1461085029673,-1.58257742288523,
14.3310697580611));
#275416=CARTESIAN_POINT('Ctrl Pts',(-1.17225624279953,-1.56364113166703,
14.3292208589024));
#275417=CARTESIAN_POINT('Ctrl Pts',(-1.19791262477217,-1.54407252066101,
14.3273719597438));
#275418=CARTESIAN_POINT('Ctrl Pts',(-1.22304638500535,-1.5239007645268,
14.3255230605851));
#275419=CARTESIAN_POINT('Ctrl Pts',(-1.27563331533746,-1.48169574925391,
14.3216546409637));
#275420=CARTESIAN_POINT('Ctrl Pts',(-1.3261501296571,-1.43667130044735,
14.3177862213423));
#275421=CARTESIAN_POINT('Ctrl Pts',(-1.37427307974457,-1.38906065464737,
14.3139178017208));
#275422=CARTESIAN_POINT('Ctrl Pts',(-1.42231339471332,-1.34153176425434,
14.31005602482));
#275423=CARTESIAN_POINT('Ctrl Pts',(-1.46796764949847,-1.29142584504702,
14.3061942479193));
#275424=CARTESIAN_POINT('Ctrl Pts',(-1.51094458999001,-1.23901672546416,
14.3023324710185));
#275425=CARTESIAN_POINT('Ctrl Pts',(-1.55388041591974,-1.18665774388466,
14.2984743885469));
#275426=CARTESIAN_POINT('Ctrl Pts',(-1.59414368403146,-1.13200031688669,
14.2946163060754));
#275427=CARTESIAN_POINT('Ctrl Pts',(-1.6314805829482,-1.07535441016579,
14.2907582236038));
#275428=CARTESIAN_POINT('Ctrl Pts',(-1.66879534981622,-1.01874208121924,
14.2869024280728));
#275429=CARTESIAN_POINT('Ctrl Pts',(-1.70318690899608,-0.960144030741889,
14.2830466325418));
#275430=CARTESIAN_POINT('Ctrl Pts',(-1.73444351762022,-0.899900930205772,
14.2791908370109));
#275431=CARTESIAN_POINT('Ctrl Pts',(-1.76569297032403,-0.839671621787436,
14.2753359242297));
#275432=CARTESIAN_POINT('Ctrl Pts',(-1.79380866506376,-0.777798459862591,
14.2714810114485));
#275433=CARTESIAN_POINT('Ctrl Pts',(-1.81862474501653,-0.71464679164854,
14.2676260986674));
#275434=CARTESIAN_POINT('Ctrl Pts',(-1.84345890682138,-0.651449108950134,
14.2637683770638));
#275435=CARTESIAN_POINT('Ctrl Pts',(-1.8649884655503,-0.586971530388544,
14.2599106554601));
#275436=CARTESIAN_POINT('Ctrl Pts',(-1.88309618852626,-0.521598259926026,
14.2560529338565));
#275437=CARTESIAN_POINT('Ctrl Pts',(-1.90121085946659,-0.45619990562752,
14.2521937320385));
#275438=CARTESIAN_POINT('Ctrl Pts',(-1.91590096983881,-0.389905669032521,
14.2483345302205));
#275439=CARTESIAN_POINT('Ctrl Pts',(-1.9271002332678,-0.323110957627873,
14.2444753284025));
#275440=CARTESIAN_POINT('Ctrl Pts',(-1.9383168977339,-0.256212462857527,
14.2406101302871));
#275441=CARTESIAN_POINT('Ctrl Pts',(-1.94603182977727,-0.18881244354424,
14.2367449321717));
#275442=CARTESIAN_POINT('Ctrl Pts',(-1.9502306389416,-0.121311396552158,
14.2328797340563));
#275443=CARTESIAN_POINT('Ctrl Pts',(-1.95276900197994,-0.080504073325935,
14.230543053429));
#275444=CARTESIAN_POINT('Ctrl Pts',(-1.95402333266491,-0.0396598555490369,
14.2282063728017));
#275445=CARTESIAN_POINT('Ctrl Pts',(-1.95399967130156,0.00113338140508406,
14.2258696921744));
#275446=CARTESIAN_POINT('',(-1.95399924704828,-0.00171538181413171,13.5258696921242));
#275447=CARTESIAN_POINT('Ctrl Pts',(-1.95399967130105,0.00113338228141676,
14.2258696921242));
#275448=CARTESIAN_POINT('Ctrl Pts',(-1.95396099627773,0.0678107815027306,
14.2220503387541));
#275449=CARTESIAN_POINT('Ctrl Pts',(-1.95050967149899,0.134387737031145,
14.2182309853839));
#275450=CARTESIAN_POINT('Ctrl Pts',(-1.94367482159854,0.200609540859539,
14.2144116320137));
#275451=CARTESIAN_POINT('Ctrl Pts',(-1.93666323153074,0.268543752840517,
14.2104935152232));
#275452=CARTESIAN_POINT('Ctrl Pts',(-1.92607185784042,0.336244591636888,
14.2065753984326));
#275453=CARTESIAN_POINT('Ctrl Pts',(-1.91192597679905,0.403305168874657,
14.2026572816421));
#275454=CARTESIAN_POINT('Ctrl Pts',(-1.89780139708343,0.470264764123595,
14.1987450648787));
#275455=CARTESIAN_POINT('Ctrl Pts',(-1.88013303352604,0.536585533846818,
14.1948328481153));
#275456=CARTESIAN_POINT('Ctrl Pts',(-1.85899787281899,0.601866188495818,
14.1909206313519));
#275457=CARTESIAN_POINT('Ctrl Pts',(-1.83788756573183,0.667070077200144,
14.1870130151094));
#275458=CARTESIAN_POINT('Ctrl Pts',(-1.81331870874471,0.731235814195912,
14.1831053988669));
#275459=CARTESIAN_POINT('Ctrl Pts',(-1.78541882401548,0.793974573176728,
14.1791977826244));
#275460=CARTESIAN_POINT('Ctrl Pts',(-1.75753642575506,0.856674010154522,
14.1752926155107));
#275461=CARTESIAN_POINT('Ctrl Pts',(-1.72632734059869,0.917947794828203,
14.1713874483969));
#275462=CARTESIAN_POINT('Ctrl Pts',(-1.69196764037068,0.977425958289674,
14.1674822812832));
#275463=CARTESIAN_POINT('Ctrl Pts',(-1.65761769054058,1.03688724338034,
14.1635782223553));
#275464=CARTESIAN_POINT('Ctrl Pts',(-1.62011914644008,1.09455349308656,
14.1596741634274));
#275465=CARTESIAN_POINT('Ctrl Pts',(-1.57969371079616,1.15007990160295,
14.1557701044995));
#275466=CARTESIAN_POINT('Ctrl Pts',(-1.53926588202827,1.20560959719782,
14.1518658144572));
#275467=CARTESIAN_POINT('Ctrl Pts',(-1.4959111093021,1.25899880396326,14.147961524415));
#275468=CARTESIAN_POINT('Ctrl Pts',(-1.44989297226855,1.3099337269367,14.1440572343728));
#275469=CARTESIAN_POINT('Ctrl Pts',(-1.40382581858658,1.36092290371902,
14.1401487856396));
#275470=CARTESIAN_POINT('Ctrl Pts',(-1.35508996939058,1.40945221388702,
14.1362403369064));
#275471=CARTESIAN_POINT('Ctrl Pts',(-1.30398697371899,1.45524361272304,
14.1323318881732));
#275472=CARTESIAN_POINT('Ctrl Pts',(-1.25285338940657,1.50106242084561,
14.1284210999659));
#275473=CARTESIAN_POINT('Ctrl Pts',(-1.19935022191233,1.54413974755261,
14.1245103117586));
#275474=CARTESIAN_POINT('Ctrl Pts',(-1.14381111758975,1.58423865856067,
14.1205995235513));
#275475=CARTESIAN_POINT('Ctrl Pts',(-1.08817611512694,1.62440680746943,
14.1166819826727));
#275476=CARTESIAN_POINT('Ctrl Pts',(-1.03049857285806,1.66158601019015,
14.1127644417941));
#275477=CARTESIAN_POINT('Ctrl Pts',(-0.971139273420767,1.69558382618489,
14.1088469009154));
#275478=CARTESIAN_POINT('Ctrl Pts',(-0.943124413555305,1.71162923204131,
14.1069980017577));
#275479=CARTESIAN_POINT('Ctrl Pts',(-0.914735283688362,1.72696669522707,
14.1051491026));
#275480=CARTESIAN_POINT('Ctrl Pts',(-0.886011335217463,1.74157971791881,
14.1033002034423));
#275481=CARTESIAN_POINT('Ctrl Pts',(-0.825140635849454,1.77254707994524,
14.0993820866519));
#275482=CARTESIAN_POINT('Ctrl Pts',(-0.762523786706094,1.80038071020465,
14.0954639698615));
#275483=CARTESIAN_POINT('Ctrl Pts',(-0.698516298684525,1.82488108666622,
14.0915458530711));
#275484=CARTESIAN_POINT('Ctrl Pts',(-0.634605195211164,1.84934456966752,
14.0876336363079));
#275485=CARTESIAN_POINT('Ctrl Pts',(-0.569308064526748,1.87048458602418,
14.0837214195446));
#275486=CARTESIAN_POINT('Ctrl Pts',(-0.503003769532962,1.88814808948759,
14.0798092027813));
#275487=CARTESIAN_POINT('Ctrl Pts',(-0.436777444220597,1.90579082178168,
14.075901586539));
#275488=CARTESIAN_POINT('Ctrl Pts',(-0.369546779812551,1.91996503431085,
14.0719939702966));
#275489=CARTESIAN_POINT('Ctrl Pts',(-0.301707587451943,1.93056689386147,
14.0680863540542));
#275490=CARTESIAN_POINT('Ctrl Pts',(-0.233910913830512,1.94116210861452,
14.0641811869406));
#275491=CARTESIAN_POINT('Ctrl Pts',(-0.165506953722486,1.94818933607535,
14.060276019827));
#275492=CARTESIAN_POINT('Ctrl Pts',(-0.0969020178623522,1.95159575704965,
14.0563708527133));
#275493=CARTESIAN_POINT('Ctrl Pts',(-0.0283165503158982,1.95500121136942,
14.0524667937856));
#275494=CARTESIAN_POINT('Ctrl Pts',(0.0404692887207486,1.95478787456847,
14.0485627348578));
#275495=CARTESIAN_POINT('Ctrl Pts',(0.10904556944404,1.9509549107513,14.04465867593));
#275496=CARTESIAN_POINT('Ctrl Pts',(0.177625909778235,1.94712172002855,
14.0407543858879));
#275497=CARTESIAN_POINT('Ctrl Pts',(0.245996176201372,1.93966850688678,
14.0368500958457));
#275498=CARTESIAN_POINT('Ctrl Pts',(0.31374976880134,1.9286464379396,14.0329458058036));
#275499=CARTESIAN_POINT('Ctrl Pts',(0.381575529773145,1.91761262873276,
14.0290373570705));
#275500=CARTESIAN_POINT('Ctrl Pts',(0.448782819611164,1.90300245643445,
14.0251289083374));
#275501=CARTESIAN_POINT('Ctrl Pts',(0.514974469532562,1.88491837906305,
14.0212204596043));
#275502=CARTESIAN_POINT('Ctrl Pts',(0.581205739687136,1.86682347713351,
14.0173096713971));
#275503=CARTESIAN_POINT('Ctrl Pts',(0.646419692976838,1.84525068630374,
14.0133988831899));
#275504=CARTESIAN_POINT('Ctrl Pts',(0.710236280311381,1.82035173143254,
14.0094880949827));
#275505=CARTESIAN_POINT('Ctrl Pts',(0.774163058332594,1.79540978408792,
14.0055705541042));
#275506=CARTESIAN_POINT('Ctrl Pts',(0.836687206903627,1.76713041276687,
14.0016530132257));
#275507=CARTESIAN_POINT('Ctrl Pts',(0.897451330277916,1.7357122773612,13.9977354723472));
#275508=CARTESIAN_POINT('Ctrl Pts',(0.926129202462533,1.72088436211435,
13.9958865731884));
#275509=CARTESIAN_POINT('Ctrl Pts',(0.954415441251867,1.70535795982813,
13.9940376740296));
#275510=CARTESIAN_POINT('Ctrl Pts',(0.982274783907155,1.68915725996727,
13.9921887748708));
#275511=CARTESIAN_POINT('Ctrl Pts',(1.04131324347289,1.65482535287576,13.9882706580804));
#275512=CARTESIAN_POINT('Ctrl Pts',(1.09866664513048,1.61732644504668,13.98435254129));
#275513=CARTESIAN_POINT('Ctrl Pts',(1.15397450463527,1.57685092594442,13.9804344244996));
#275514=CARTESIAN_POINT('Ctrl Pts',(1.2091990797742,1.53643635618954,13.9765222077363));
#275515=CARTESIAN_POINT('Ctrl Pts',(1.26238383220613,1.49305435904853,13.972609990973));
#275516=CARTESIAN_POINT('Ctrl Pts',(1.31319464913323,1.44694015546182,13.9686977742097));
#275517=CARTESIAN_POINT('Ctrl Pts',(1.3639457157348,1.40088017927868,13.9647901579674));
#275518=CARTESIAN_POINT('Ctrl Pts',(1.41232802847653,1.35209470652972,13.960882541725));
#275519=CARTESIAN_POINT('Ctrl Pts',(1.45803961969731,1.30085989537418,13.9569749254826));
#275520=CARTESIAN_POINT('Ctrl Pts',(1.5037225608243,1.2496571960333,13.953069758369));
#275521=CARTESIAN_POINT('Ctrl Pts',(1.54673777417703,1.19600856972771,13.9491645912554));
#275522=CARTESIAN_POINT('Ctrl Pts',(1.58682044878298,1.14022667190528,13.9452594241417));
#275523=CARTESIAN_POINT('Ctrl Pts',(1.62689174895831,1.08446060354863,13.9413553652139));
#275524=CARTESIAN_POINT('Ctrl Pts',(1.66403187551092,1.02656286469612,13.9374513062861));
#275525=CARTESIAN_POINT('Ctrl Pts',(1.69801772136349,0.966877354133167,
13.9335472473583));
#275526=CARTESIAN_POINT('Ctrl Pts',(1.73200557912613,0.907188310279321,
13.9296429573162));
#275527=CARTESIAN_POINT('Ctrl Pts',(1.76283854430515,0.845711713307905,
13.9257386672741));
#275528=CARTESIAN_POINT('Ctrl Pts',(1.79033899997154,0.78281687844661,13.921834377232));
#275529=CARTESIAN_POINT('Ctrl Pts',(1.81786874800509,0.719855050564654,
13.9179259284989));
#275530=CARTESIAN_POINT('Ctrl Pts',(1.84205870507964,0.655472421551075,
13.9140174797658));
#275531=CARTESIAN_POINT('Ctrl Pts',(1.8627794572565,0.590058212063163,13.9101090310327));
#275532=CARTESIAN_POINT('Ctrl Pts',(1.88351261222184,0.52460484769339,13.9061982428255));
#275533=CARTESIAN_POINT('Ctrl Pts',(1.90077230594726,0.458119150130883,
13.9022874546183));
#275534=CARTESIAN_POINT('Ctrl Pts',(1.91447979817761,0.391002688443205,
13.8983766664111));
#275535=CARTESIAN_POINT('Ctrl Pts',(1.92821095883092,0.323770338248981,
13.8944591255326));
#275536=CARTESIAN_POINT('Ctrl Pts',(1.9383776036575,0.255905536401278,13.8905415846541));
#275537=CARTESIAN_POINT('Ctrl Pts',(1.94495270955195,0.187816286851116,
13.8866240437756));
#275538=CARTESIAN_POINT('Ctrl Pts',(1.9480558571984,0.155681291935121,13.8847751446169));
#275539=CARTESIAN_POINT('Ctrl Pts',(1.95035977824699,0.123496319967377,
13.8829262454581));
#275540=CARTESIAN_POINT('Ctrl Pts',(1.9518656609298,0.0913041164628929,
13.8810773462994));
#275541=CARTESIAN_POINT('Ctrl Pts',(1.95505687024807,0.0230836229466753,
13.8771592295089));
#275542=CARTESIAN_POINT('Ctrl Pts',(1.95467349411293,-0.0454396124766511,
13.8732411127185));
#275543=CARTESIAN_POINT('Ctrl Pts',(1.95067988638708,-0.113859478502549,
13.8693229959281));
#275544=CARTESIAN_POINT('Ctrl Pts',(1.94669229236508,-0.182176315678574,
13.8654107791648));
#275545=CARTESIAN_POINT('Ctrl Pts',(1.93910528452002,-0.250389605287109,
13.8614985624015));
#275546=CARTESIAN_POINT('Ctrl Pts',(1.92793518405277,-0.318091065720813,
13.8575863456382));
#275547=CARTESIAN_POINT('Ctrl Pts',(1.91677821892126,-0.385712913494362,
13.8536787293958));
#275548=CARTESIAN_POINT('Ctrl Pts',(1.90204660892068,-0.452823644413003,
13.8497711131534));
#275549=CARTESIAN_POINT('Ctrl Pts',(1.88380850378713,-0.519019769430116,
13.845863496911));
#275550=CARTESIAN_POINT('Ctrl Pts',(1.86558182952721,-0.585174405513252,
13.8419583297973));
#275551=CARTESIAN_POINT('Ctrl Pts',(1.84385315007809,-0.650415099667435,
13.8380531626836));
#275552=CARTESIAN_POINT('Ctrl Pts',(1.81874143303448,-0.714349774104889,
13.83414799557));
#275553=CARTESIAN_POINT('Ctrl Pts',(1.79363684204934,-0.778266305528533,
13.8302439366422));
#275554=CARTESIAN_POINT('Ctrl Pts',(1.76515129901099,-0.840877095353031,
13.8263398777144));
#275555=CARTESIAN_POINT('Ctrl Pts',(1.73345264296861,-0.901808147326888,
13.8224358187865));
#275556=CARTESIAN_POINT('Ctrl Pts',(1.70175211041427,-0.962742806325828,
13.8185315287444));
#275557=CARTESIAN_POINT('Ctrl Pts',(1.66683831650622,-1.02199709487888,
13.8146272387023));
#275558=CARTESIAN_POINT('Ctrl Pts',(1.62892513120441,-1.07922144017374,
13.8107229486601));
#275559=CARTESIAN_POINT('Ctrl Pts',(1.59097156231926,-1.13650673851434,
13.806814499927));
#275560=CARTESIAN_POINT('Ctrl Pts',(1.55001249834279,-1.19175736765287,
13.8029060511939));
#275561=CARTESIAN_POINT('Ctrl Pts',(1.50630468257954,-1.24465344704418,
13.7989976024607));
#275562=CARTESIAN_POINT('Ctrl Pts',(1.46257070469682,-1.29758118835966,
13.7950868142535));
#275563=CARTESIAN_POINT('Ctrl Pts',(1.41608503347078,-1.34815121286628,
13.7911760260463));
#275564=CARTESIAN_POINT('Ctrl Pts',(1.36714227790619,-1.39607950775072,
13.787265237839));
#275565=CARTESIAN_POINT('Ctrl Pts',(1.31811501397054,-1.44409055935943,
13.7833476969605));
#275566=CARTESIAN_POINT('Ctrl Pts',(1.26662256706105,-1.48945045252723,
13.779430156082));
#275567=CARTESIAN_POINT('Ctrl Pts',(1.21299301048388,-1.53191512706065,
13.7755126152035));
#275568=CARTESIAN_POINT('Ctrl Pts',(1.18768232577094,-1.55195650083197,
13.773663716045));
#275569=CARTESIAN_POINT('Ctrl Pts',(1.16189604347026,-1.57135361705028,
13.7718148168865));
#275570=CARTESIAN_POINT('Ctrl Pts',(1.13567071565667,-1.59008428254601,
13.7699659177279));
#275571=CARTESIAN_POINT('Ctrl Pts',(1.08009499819913,-1.62977759661178,
13.7660478009375));
#275572=CARTESIAN_POINT('Ctrl Pts',(1.02232559979735,-1.66663241147189,
13.7621296841471));
#275573=CARTESIAN_POINT('Ctrl Pts',(0.96268432550937,-1.70039845019294,
13.7582115673567));
#275574=CARTESIAN_POINT('Ctrl Pts',(0.903132860983582,-1.73411364291945,
13.7542993505934));
#275575=CARTESIAN_POINT('Ctrl Pts',(0.841715539352873,-1.76474905006382,
13.7503871338302));
#275576=CARTESIAN_POINT('Ctrl Pts',(0.778784183350029,-1.79209687119972,
13.7464749170669));
#275577=CARTESIAN_POINT('Ctrl Pts',(0.715926830664457,-1.81941253301772,
13.7425673008245));
#275578=CARTESIAN_POINT('Ctrl Pts',(0.651559428515125,-1.84344809163674,
13.7386596845822));
#275579=CARTESIAN_POINT('Ctrl Pts',(0.586057893006253,-1.86404188419817,
13.7347520683398));
#275580=CARTESIAN_POINT('Ctrl Pts',(0.520597411091987,-1.88462276944065,
13.7308469012261));
#275581=CARTESIAN_POINT('Ctrl Pts',(0.454004674054457,-1.9017660205359,
13.7269417341125));
#275582=CARTESIAN_POINT('Ctrl Pts',(0.386673583144682,-1.91535885413101,
13.7230365669989));
#275583=CARTESIAN_POINT('Ctrl Pts',(0.319361599064237,-1.92894783043006,
13.7191325080711));
#275584=CARTESIAN_POINT('Ctrl Pts',(0.251312158982779,-1.93898829203193,
13.7152284491433));
#275585=CARTESIAN_POINT('Ctrl Pts',(0.182930490072227,-1.94541831897459,
13.7113243902155));
#275586=CARTESIAN_POINT('Ctrl Pts',(0.114544773071485,-1.95184872656502,
13.7074201001734));
#275587=CARTESIAN_POINT('Ctrl Pts',(0.0458272781528218,-1.95466823166777,
13.7035158101313));
#275588=CARTESIAN_POINT('Ctrl Pts',(-0.0228123100831663,-1.95386683233752,
13.6996115200892));
#275589=CARTESIAN_POINT('Ctrl Pts',(-0.0915250104175157,-1.9530645793893,
13.6957030713561));
#275590=CARTESIAN_POINT('Ctrl Pts',(-0.160159145670226,-1.94863373070259,
13.691794622623));
#275591=CARTESIAN_POINT('Ctrl Pts',(-0.228306712890433,-1.94061640847674,
13.6878861738899));
#275592=CARTESIAN_POINT('Ctrl Pts',(-0.296495071094226,-1.93259428733477,
13.6839753856827));
#275593=CARTESIAN_POINT('Ctrl Pts',(-0.364195796770205,-1.9209815033955,
13.6800645974755));
#275594=CARTESIAN_POINT('Ctrl Pts',(-0.431010473043962,-1.90587144690465,
13.6761538092683));
#275595=CARTESIAN_POINT('Ctrl Pts',(-0.497940516738045,-1.89073530021423,
13.6722362683898));
#275596=CARTESIAN_POINT('Ctrl Pts',(-0.563980984428117,-1.87208996234832,
13.6683187275113));
#275597=CARTESIAN_POINT('Ctrl Pts',(-0.628748864686283,-1.85007861053408,
13.6644011866328));
#275598=CARTESIAN_POINT('Ctrl Pts',(-0.659316326018667,-1.83969026460129,
13.662552287474));
#275599=CARTESIAN_POINT('Ctrl Pts',(-0.689600625865148,-1.82855286564416,
13.6607033883153));
#275600=CARTESIAN_POINT('Ctrl Pts',(-0.719563290249536,-1.81668507764149,
13.6588544891566));
#275601=CARTESIAN_POINT('Ctrl Pts',(-0.783059029244552,-1.79153531259394,
13.6549363723662));
#275602=CARTESIAN_POINT('Ctrl Pts',(-0.845360519085135,-1.76300278495008,
13.6510182555757));
#275603=CARTESIAN_POINT('Ctrl Pts',(-0.906082926910697,-1.73122203358233,
13.6471001387853));
#275604=CARTESIAN_POINT('Ctrl Pts',(-0.966713896968201,-1.69948913869914,
13.643187922022));
#275605=CARTESIAN_POINT('Ctrl Pts',(-1.02577007187256,-1.66451795380519,
13.6392757052587));
#275606=CARTESIAN_POINT('Ctrl Pts',(-1.0828860142905,-1.62649127881278,
13.6353634884955));
#275607=CARTESIAN_POINT('Ctrl Pts',(-1.13993479195181,-1.5885093207989,
13.6314558722531));
#275608=CARTESIAN_POINT('Ctrl Pts',(-1.19504746090461,-1.54747927987148,
13.6275482560107));
#275609=CARTESIAN_POINT('Ctrl Pts',(-1.24788426892885,-1.50362922669118,
13.6236406397683));
#275610=CARTESIAN_POINT('Ctrl Pts',(-1.30068796107453,-1.45980665687125,
13.6197354726547));
#275611=CARTESIAN_POINT('Ctrl Pts',(-1.35121824418428,-1.41316789431115,
13.615830305541));
#275612=CARTESIAN_POINT('Ctrl Pts',(-1.3991666684344,-1.36398263696507,
13.6119251384274));
#275613=CARTESIAN_POINT('Ctrl Pts',(-1.44710148615675,-1.31481133712812,
13.6080210794996));
#275614=CARTESIAN_POINT('Ctrl Pts',(-1.49245555629169,-1.26309532909577,
13.6041170205718));
#275615=CARTESIAN_POINT('Ctrl Pts',(-1.53495701085206,-1.20914142052785,
13.600212961644));
#275616=CARTESIAN_POINT('Ctrl Pts',(-1.5774609814335,-1.1551843179711,13.5963086716018));
#275617=CARTESIAN_POINT('Ctrl Pts',(-1.61711169881252,-1.09898943983908,
13.5924043815597));
#275618=CARTESIAN_POINT('Ctrl Pts',(-1.65367848921153,-1.04089550595584,
13.5885000915176));
#275619=CARTESIAN_POINT('Ctrl Pts',(-1.69028422906881,-0.982739692776438,
13.5845916427845));
#275620=CARTESIAN_POINT('Ctrl Pts',(-1.72379922382787,-0.92268120404838,
13.5806831940514));
#275621=CARTESIAN_POINT('Ctrl Pts',(-1.75403749779322,-0.86108562659895,
13.5767747453182));
#275622=CARTESIAN_POINT('Ctrl Pts',(-1.78429387143533,-0.799453179980236,
13.572863957111));
#275623=CARTESIAN_POINT('Ctrl Pts',(-1.81126942765639,-0.736282265989115,
13.5689531689038));
#275624=CARTESIAN_POINT('Ctrl Pts',(-1.83482645819514,-0.671958234049603,
13.5650423806966));
#275625=CARTESIAN_POINT('Ctrl Pts',(-1.85842416413629,-0.607523135230167,
13.5611248398181));
#275626=CARTESIAN_POINT('Ctrl Pts',(-1.87859141908748,-0.541931414528383,
13.5572072989395));
#275627=CARTESIAN_POINT('Ctrl Pts',(-1.89524069535008,-0.475582491991621,
13.553289758061));
#275628=CARTESIAN_POINT('Ctrl Pts',(-1.9030983881805,-0.444268851404427,
13.5514408589024));
#275629=CARTESIAN_POINT('Ctrl Pts',(-1.91017322836625,-0.412786680116798,
13.5495919597437));
#275630=CARTESIAN_POINT('Ctrl Pts',(-1.91646002034225,-0.381178423352868,
13.5477430605851));
#275631=CARTESIAN_POINT('Ctrl Pts',(-1.935685974682,-0.284515625598044,
13.5420888491942));
#275632=CARTESIAN_POINT('Ctrl Pts',(-1.94760342518579,-0.186354486565157,
13.5364346378032));
#275633=CARTESIAN_POINT('Ctrl Pts',(-1.95203518396287,-0.087605025946325,
13.5307804264123));
#275634=CARTESIAN_POINT('Ctrl Pts',(-1.953318191635,-0.0590167561496238,
13.5291435149829));
#275635=CARTESIAN_POINT('Ctrl Pts',(-1.95397408345252,-0.0303793484914462,
13.5275066035536));
#275636=CARTESIAN_POINT('Ctrl Pts',(-1.95399924704828,-0.00171538181413171,
13.5258696921242));
#275637=CARTESIAN_POINT('',(-1.95079785653176,-3.37693124380367E-5,12.8258696921242));
#275638=CARTESIAN_POINT('Ctrl Pts',(-1.95470780459474,-0.00170932991778109,
13.5258693111351));
#275639=CARTESIAN_POINT('Ctrl Pts',(-1.94992637237433,0.51936472124033,
13.4961234180947));
#275640=CARTESIAN_POINT('Ctrl Pts',(-1.46762209028228,1.69704725867551,
13.429340382197));
#275641=CARTESIAN_POINT('Ctrl Pts',(0.520936993743039,2.24981806562466,
13.3255202034423));
#275642=CARTESIAN_POINT('Ctrl Pts',(2.17254014841156,0.783023616121871,
13.2144087748708));
#275643=CARTESIAN_POINT('Ctrl Pts',(1.83645968680275,-1.40016873933449,
13.1032973462993));
#275644=CARTESIAN_POINT('Ctrl Pts',(-0.179820256539059,-2.3023295496518,
12.992185917728));
#275645=CARTESIAN_POINT('Ctrl Pts',(-1.72100430673717,-1.30004007511163,
12.899710033003));
#275646=CARTESIAN_POINT('Ctrl Pts',(-1.95084782093774,-0.324022277657586,
12.844271291135));
#275647=CARTESIAN_POINT('Ctrl Pts',(-1.95079785653176,-3.37693124380367E-5,
12.8258696921242));
#275648=CARTESIAN_POINT('',(-1.95399923090066,0.0017336780615255,12.1258696921242));
#275649=CARTESIAN_POINT('Ctrl Pts',(-1.95079785653176,-3.37693124380367E-5,
12.8258696921242));
#275650=CARTESIAN_POINT('Ctrl Pts',(-1.95074725691387,0.32807369838409,
12.8072341482779));
#275651=CARTESIAN_POINT('Ctrl Pts',(-1.71669518394517,1.30834496185473,
12.7515614615743));
#275652=CARTESIAN_POINT('Ctrl Pts',(-0.165312909848787,2.30341666263357,
12.6588516320137));
#275653=CARTESIAN_POINT('Ctrl Pts',(1.84524376358971,1.38857197609474,12.5477402034423));
#275654=CARTESIAN_POINT('Ctrl Pts',(2.1675642957523,-0.796694234723817,
12.4366287748709));
#275655=CARTESIAN_POINT('Ctrl Pts',(0.506753680239931,-2.25305512303262,
12.3255173462994));
#275656=CARTESIAN_POINT('Ctrl Pts',(-1.47381110597352,-1.68904181734237,
12.221931090597));
#275657=CARTESIAN_POINT('Ctrl Pts',(-1.94982291098112,-0.515331947862959,
12.1553819777518));
#275658=CARTESIAN_POINT('Ctrl Pts',(-1.95458395099462,0.00172866677834459,
12.1258700077636));
#275659=CARTESIAN_POINT('',(-1.95399970412604,-0.00107530244352288,11.4258696921242));
#275660=CARTESIAN_POINT('Ctrl Pts',(-1.95399923090066,0.0017336780615255,
12.1258696921242));
#275661=CARTESIAN_POINT('Ctrl Pts',(-1.95391274729375,0.0992078891813078,
12.1203044978164));
#275662=CARTESIAN_POINT('Ctrl Pts',(-1.94652911131939,0.19636936180308,
12.1147393035087));
#275663=CARTESIAN_POINT('Ctrl Pts',(-1.93200815213827,0.292336279088428,
12.1091741092009));
#275664=CARTESIAN_POINT('Ctrl Pts',(-1.92689436108002,0.32613258395921,
12.1072142358528));
#275665=CARTESIAN_POINT('Ctrl Pts',(-1.9208957923614,0.359781016894373,
12.1052543625046));
#275666=CARTESIAN_POINT('Ctrl Pts',(-1.91402071706402,0.39324381069478,
12.1032944891565));
#275667=CARTESIAN_POINT('Ctrl Pts',(-1.90027628404543,0.460141569353427,
12.099376372366));
#275668=CARTESIAN_POINT('Ctrl Pts',(-1.88299312449379,0.526450491574315,
12.0954582555756));
#275669=CARTESIAN_POINT('Ctrl Pts',(-1.86223692385971,0.591768231162787,
12.0915401387851));
#275670=CARTESIAN_POINT('Ctrl Pts',(-1.84151197858469,0.656987613183806,
12.0876279220218));
#275671=CARTESIAN_POINT('Ctrl Pts',(-1.81732451933111,0.721218309756002,
12.0837157052585));
#275672=CARTESIAN_POINT('Ctrl Pts',(-1.78979112696608,0.784068697139146,
12.0798034884952));
#275673=CARTESIAN_POINT('Ctrl Pts',(-1.76229011213906,0.846845176419049,
12.0758958722528));
#275674=CARTESIAN_POINT('Ctrl Pts',(-1.73145117482954,0.908244121713762,
12.0719882560104));
#275675=CARTESIAN_POINT('Ctrl Pts',(-1.69743993836622,0.967891344955244,
12.068080639768));
#275676=CARTESIAN_POINT('Ctrl Pts',(-1.66345001870875,1.02750118383764,
12.0641754726543));
#275677=CARTESIAN_POINT('Ctrl Pts',(-1.62629198708003,1.0853610522253,12.0602703055406));
#275678=CARTESIAN_POINT('Ctrl Pts',(-1.5861778963528,1.14112036224134,12.056365138427));
#275679=CARTESIAN_POINT('Ctrl Pts',(-1.54607518897126,1.19686384920143,
12.0524610794991));
#275680=CARTESIAN_POINT('Ctrl Pts',(-1.50301837487858,1.25050756201909,
12.0485570205713));
#275681=CARTESIAN_POINT('Ctrl Pts',(-1.45726240406239,1.30173049657227,
12.0446529616435));
#275682=CARTESIAN_POINT('Ctrl Pts',(-1.41150372456271,1.35295646344485,
12.0407486716013));
#275683=CARTESIAN_POINT('Ctrl Pts',(-1.36304590070439,1.40176100241345,
12.0368443815592));
#275684=CARTESIAN_POINT('Ctrl Pts',(-1.31218246172391,1.44785813778291,
12.032940091517));
#275685=CARTESIAN_POINT('Ctrl Pts',(-1.26126484507645,1.49400437394654,
12.0290316427839));
#275686=CARTESIAN_POINT('Ctrl Pts',(-1.20793686479125,1.53743712035715,
12.0251231940507));
#275687=CARTESIAN_POINT('Ctrl Pts',(-1.15252626910834,1.57790975629635,
12.0212147453176));
#275688=CARTESIAN_POINT('Ctrl Pts',(-1.09708250639116,1.61840661787844,
12.0173039571104));
#275689=CARTESIAN_POINT('Ctrl Pts',(-1.03955405934958,1.65593957391646,
12.0133931689031));
#275690=CARTESIAN_POINT('Ctrl Pts',(-0.980296518374739,1.69030610720732,
12.0094823806959));
#275691=CARTESIAN_POINT('Ctrl Pts',(-0.920936658717528,1.72473198042937,
12.0055648398173));
#275692=CARTESIAN_POINT('Ctrl Pts',(-0.859842184062017,1.75598029500031,
12.0016472989388));
#275693=CARTESIAN_POINT('Ctrl Pts',(-0.797391253547561,1.78389550948643,
11.9977297580603));
#275694=CARTESIAN_POINT('Ctrl Pts',(-0.767917285962512,1.79707020712689,
11.9958808589019));
#275695=CARTESIAN_POINT('Ctrl Pts',(-0.738141436690851,1.80950319841902,
11.9940319597435));
#275696=CARTESIAN_POINT('Ctrl Pts',(-0.708104604416077,1.82118199782579,
11.9921830605852));
#275697=CARTESIAN_POINT('Ctrl Pts',(-0.644451691635783,1.84593126543223,
11.9882649437947));
#275698=CARTESIAN_POINT('Ctrl Pts',(-0.57937350324923,1.86738843594533,
11.9843468270043));
#275699=CARTESIAN_POINT('Ctrl Pts',(-0.513243658350625,1.88539039648633,
11.9804287102139));
#275700=CARTESIAN_POINT('Ctrl Pts',(-0.447213393913931,1.90336524909219,
11.9765164934506));
#275701=CARTESIAN_POINT('Ctrl Pts',(-0.380135086678046,1.91789508961401,
11.9726042766873));
#275702=CARTESIAN_POINT('Ctrl Pts',(-0.312400961577164,1.92886537612288,
11.968692059924));
#275703=CARTESIAN_POINT('Ctrl Pts',(-0.244746487548015,1.93982276226467,
11.9647844436816));
#275704=CARTESIAN_POINT('Ctrl Pts',(-0.176438210524025,1.94722882921171,
11.9608768274393));
#275705=CARTESIAN_POINT('Ctrl Pts',(-0.107880316682717,1.95101969166701,
11.9569692111969));
#275706=CARTESIAN_POINT('Ctrl Pts',(-0.0393653920322853,1.95480817816992,
11.9530640440832));
#275707=CARTESIAN_POINT('Ctrl Pts',(0.0293983490624891,1.95498592782676,
11.9491588769696));
#275708=CARTESIAN_POINT('Ctrl Pts',(0.0980013551684196,1.95154086157199,
11.9452537098559));
#275709=CARTESIAN_POINT('Ctrl Pts',(0.166584893508266,1.94809677293829,
11.9413496509281));
#275710=CARTESIAN_POINT('Ctrl Pts',(0.235007296377531,1.94103193393072,
11.9374455920003));
#275711=CARTESIAN_POINT('Ctrl Pts',(0.302860589942995,1.93038635072345,
11.9335415330725));
#275712=CARTESIAN_POINT('Ctrl Pts',(0.370717900319621,1.91974013731393,
11.9296372430304));
#275713=CARTESIAN_POINT('Ctrl Pts',(0.438005548968938,1.90551283763362,
11.9257329529882));
#275714=CARTESIAN_POINT('Ctrl Pts',(0.504324055963543,1.8877958699437,11.9218286629461));
#275715=CARTESIAN_POINT('Ctrl Pts',(0.57071320273515,1.8700600308602,11.917920214213));
#275716=CARTESIAN_POINT('Ctrl Pts',(0.636130671593625,1.84882723287807,
11.9140117654799));
#275717=CARTESIAN_POINT('Ctrl Pts',(0.700191476562453,1.82423899096289,
11.9101033167467));
#275718=CARTESIAN_POINT('Ctrl Pts',(0.764290626307935,1.79963603130189,
11.9061925285395));
#275719=CARTESIAN_POINT('Ctrl Pts',(0.827031046681989,1.77167383075916,
11.9022817403323));
#275720=CARTESIAN_POINT('Ctrl Pts',(0.88804969428404,1.74054122056389,11.8983709521251));
#275721=CARTESIAN_POINT('Ctrl Pts',(0.949173701432201,1.70935485438076,
11.8944534112466));
#275722=CARTESIAN_POINT('Ctrl Pts',(1.00856957676314,1.67498739898236,11.8905358703681));
#275723=CARTESIAN_POINT('Ctrl Pts',(1.06590149327693,1.63767213038203,11.8866183294895));
#275724=CARTESIAN_POINT('Ctrl Pts',(1.09295952164025,1.6200610394301,11.8847694303309));
#275725=CARTESIAN_POINT('Ctrl Pts',(1.11955828035541,1.60179395133601,11.8829205311723));
#275726=CARTESIAN_POINT('Ctrl Pts',(1.14566509189828,1.5828984481658,11.8810716320136));
#275727=CARTESIAN_POINT('Ctrl Pts',(1.20098965417766,1.54285581637127,11.8771535152232));
#275728=CARTESIAN_POINT('Ctrl Pts',(1.25432203901108,1.49982980681833,11.8732353984328));
#275729=CARTESIAN_POINT('Ctrl Pts',(1.30532252235046,1.45404577391657,11.8693172816424));
#275730=CARTESIAN_POINT('Ctrl Pts',(1.3562462075105,1.40833068409416,11.8654050648791));
#275731=CARTESIAN_POINT('Ctrl Pts',(1.40484459708485,1.35986613934267,11.8614928481158));
#275732=CARTESIAN_POINT('Ctrl Pts',(1.45080867347306,1.30891947535949,11.8575806313526));
#275733=CARTESIAN_POINT('Ctrl Pts',(1.49671869899783,1.25803272144942,11.8536730151102));
#275734=CARTESIAN_POINT('Ctrl Pts',(1.54000023565451,1.20467000860407,11.8497653988678));
#275735=CARTESIAN_POINT('Ctrl Pts',(1.58038032930572,1.14913620373894,11.8458577826255));
#275736=CARTESIAN_POINT('Ctrl Pts',(1.62073511442054,1.09363720511605,11.8419526155118));
#275737=CARTESIAN_POINT('Ctrl Pts',(1.65819177523754,1.03597021070243,11.8380474483982));
#275738=CARTESIAN_POINT('Ctrl Pts',(1.69251796539022,0.976472701529003,
11.8341422812846));
#275739=CARTESIAN_POINT('Ctrl Pts',(1.7268344146543,0.916992076216168,11.8302382223568));
#275740=CARTESIAN_POINT('Ctrl Pts',(1.75802191108362,0.855682393204036,
11.826334163429));
#275741=CARTESIAN_POINT('Ctrl Pts',(1.78589271726098,0.792908066823759,
11.8224301045012));
#275742=CARTESIAN_POINT('Ctrl Pts',(1.81376517334743,0.730130024299399,
11.8185258144591));
#275743=CARTESIAN_POINT('Ctrl Pts',(1.83832035211883,0.665887616869239,
11.814621524417));
#275744=CARTESIAN_POINT('Ctrl Pts',(1.85941831203987,0.600566017062898,
11.8107172343749));
#275745=CARTESIAN_POINT('Ctrl Pts',(1.88053874464993,0.535174839344564,
11.8068087856418));
#275746=CARTESIAN_POINT('Ctrl Pts',(1.89819445783113,0.468702644149648,
11.8029003369087));
#275747=CARTESIAN_POINT('Ctrl Pts',(1.91229545626018,0.401549608350767,
11.7989918881756));
#275748=CARTESIAN_POINT('Ctrl Pts',(1.92640489510198,0.334356376863449,
11.7950810999684));
#275749=CARTESIAN_POINT('Ctrl Pts',(1.93695530903598,0.266481979822375,
11.7911703117612));
#275750=CARTESIAN_POINT('Ctrl Pts',(1.9439083545101,0.198333832882401,11.787259523554));
#275751=CARTESIAN_POINT('Ctrl Pts',(1.95087340565371,0.130068016047827,
11.7833419826755));
#275752=CARTESIAN_POINT('Ctrl Pts',(1.9542286671504,0.0615279969557309,
11.779424441797));
#275753=CARTESIAN_POINT('Ctrl Pts',(1.95398789637902,-0.00687755801797681,
11.7755069009185));
#275754=CARTESIAN_POINT('Ctrl Pts',(1.95387426364602,-0.0391618345492261,
11.7736580017598));
#275755=CARTESIAN_POINT('Ctrl Pts',(1.95296040136146,-0.0714162191886032,
11.771809102601));
#275756=CARTESIAN_POINT('Ctrl Pts',(1.95125175022806,-0.10359829743738,
11.7699602034423));
#275757=CARTESIAN_POINT('Ctrl Pts',(1.94763084171983,-0.171797333897219,
11.7660420866519));
#275758=CARTESIAN_POINT('Ctrl Pts',(1.94042297028202,-0.239941499894348,
11.7621239698614));
#275759=CARTESIAN_POINT('Ctrl Pts',(1.92963312460916,-0.307623153242896,
11.758205853071));
#275760=CARTESIAN_POINT('Ctrl Pts',(1.91885952663531,-0.375202889366135,
11.7542936363077));
#275761=CARTESIAN_POINT('Ctrl Pts',(1.90451473612943,-0.442321013241658,
11.7503814195445));
#275762=CARTESIAN_POINT('Ctrl Pts',(1.88665566681589,-0.508572900252736,
11.7464692027812));
#275763=CARTESIAN_POINT('Ctrl Pts',(1.86881759864483,-0.57474687921085,
11.7425615865388));
#275764=CARTESIAN_POINT('Ctrl Pts',(1.84747358643237,-0.640056171660605,
11.7386539702964));
#275765=CARTESIAN_POINT('Ctrl Pts',(1.8227316371679,-0.704106084952569,
11.734746354054));
#275766=CARTESIAN_POINT('Ctrl Pts',(1.79800519511173,-0.768115854465375,
11.7308411869404));
#275767=CARTESIAN_POINT('Ctrl Pts',(1.76988521746549,-0.830867352785871,
11.7269360198267));
#275768=CARTESIAN_POINT('Ctrl Pts',(1.73852913946858,-0.891982304319223,
11.7230308527131));
#275769=CARTESIAN_POINT('Ctrl Pts',(1.70718195951896,-0.953079913003496,
11.7191267937853));
#275770=CARTESIAN_POINT('Ctrl Pts',(1.67260072667862,-1.01254145939989,
11.7152227348575));
#275771=CARTESIAN_POINT('Ctrl Pts',(1.634989703211,-1.07001152815939,11.7113186759296));
#275772=CARTESIAN_POINT('Ctrl Pts',(1.59737645322832,-1.12748499905906,
11.7074143858875));
#275773=CARTESIAN_POINT('Ctrl Pts',(1.55673332802689,-1.18296634809468,
11.7035100958454));
#275774=CARTESIAN_POINT('Ctrl Pts',(1.51330795868977,-1.23612904753759,
11.6996058058033));
#275775=CARTESIAN_POINT('Ctrl Pts',(1.46983633441501,-1.28934837372624,
11.6956973570702));
#275776=CARTESIAN_POINT('Ctrl Pts',(1.42357686347721,-1.34024373982725,
11.691788908337));
#275777=CARTESIAN_POINT('Ctrl Pts',(1.37481687903088,-1.38852243378773,
11.6878804596039));
#275778=CARTESIAN_POINT('Ctrl Pts',(1.32602770839632,-1.43683002585114,
11.6839696713967));
#275779=CARTESIAN_POINT('Ctrl Pts',(1.27473541283795,-1.48251750142439,
11.6800588831895));
#275780=CARTESIAN_POINT('Ctrl Pts',(1.22126142963808,-1.52533161000431,
11.6761480949823));
#275781=CARTESIAN_POINT('Ctrl Pts',(1.16769511409685,-1.5682196447564,11.6722305541038));
#275782=CARTESIAN_POINT('Ctrl Pts',(1.11193999188157,-1.60822412380125,
11.6683130132252));
#275783=CARTESIAN_POINT('Ctrl Pts',(1.05434681795526,-1.64513488427777,
11.6643954723467));
#275784=CARTESIAN_POINT('Ctrl Pts',(1.02716548810646,-1.66255506599524,
11.6625465731881));
#275785=CARTESIAN_POINT('Ctrl Pts',(0.999575108630041,-1.67928681524516,
11.6606976740295));
#275786=CARTESIAN_POINT('Ctrl Pts',(0.971614260689926,-1.69531169064098,
11.6588487748708));
#275787=CARTESIAN_POINT('Ctrl Pts',(0.91236069497888,-1.72927099721534,
11.6549306580804));
#275788=CARTESIAN_POINT('Ctrl Pts',(0.851207137213693,-1.76018738676486,
11.65101254129));
#275789=CARTESIAN_POINT('Ctrl Pts',(0.788498724613717,-1.7878438861608,
11.6470944244995));
#275790=CARTESIAN_POINT('Ctrl Pts',(0.725884740372109,-1.81545873950435,
11.6431822077362));
#275791=CARTESIAN_POINT('Ctrl Pts',(0.661720994481132,-1.83982324812798,
11.639269990973));
#275792=CARTESIAN_POINT('Ctrl Pts',(0.596378260925824,-1.86076569451801,
11.6353577742097));
#275793=CARTESIAN_POINT('Ctrl Pts',(0.531112366316169,-1.88168351390803,
11.6314501579673));
#275794=CARTESIAN_POINT('Ctrl Pts',(0.46467070367683,-1.89918711363325,
11.6275425417249));
#275795=CARTESIAN_POINT('Ctrl Pts',(0.397443424205221,-1.91315308445405,
11.6236349254825));
#275796=CARTESIAN_POINT('Ctrl Pts',(0.330258279951637,-1.92711030199447,
11.6197297583688));
#275797=CARTESIAN_POINT('Ctrl Pts',(0.262288976130544,-1.9375341890993,
11.6158245912552));
#275798=CARTESIAN_POINT('Ctrl Pts',(0.193938690156597,-1.944351764589,11.6119194241415));
#275799=CARTESIAN_POINT('Ctrl Pts',(0.12560780023328,-1.95116740542638,
11.6080153652137));
#275800=CARTESIAN_POINT('Ctrl Pts',(0.0568966320012735,-1.95437871743335,
11.6041113062859));
#275801=CARTESIAN_POINT('Ctrl Pts',(-0.011785434644376,-1.95396445810313,
11.6002072473581));
#275802=CARTESIAN_POINT('Ctrl Pts',(-0.0804715671632938,-1.95355017424939,
11.596302957316));
#275803=CARTESIAN_POINT('Ctrl Pts',(-0.149128102821917,-1.94950989847778,
11.5923986672738));
#275804=CARTESIAN_POINT('Ctrl Pts',(-0.217346398632557,-1.9418744920827,
11.5884943772317));
#275805=CARTESIAN_POINT('Ctrl Pts',(-0.285637357798015,-1.9342309527632,
11.5845859284986));
#275806=CARTESIAN_POINT('Ctrl Pts',(-0.353488655770739,-1.92298469536685,
11.5806774797655));
#275807=CARTESIAN_POINT('Ctrl Pts',(-0.420498515544062,-1.90821827850622,
11.5767690310323));
#275808=CARTESIAN_POINT('Ctrl Pts',(-0.487548485305181,-1.89344302293436,
11.5728582428251));
#275809=CARTESIAN_POINT('Ctrl Pts',(-0.553755540325949,-1.87514354552687,
11.5689474546179));
#275810=CARTESIAN_POINT('Ctrl Pts',(-0.618732549399968,-1.85345246292237,
11.5650366664107));
#275811=CARTESIAN_POINT('Ctrl Pts',(-0.683821752835107,-1.83172392680641,
11.5611191255322));
#275812=CARTESIAN_POINT('Ctrl Pts',(-0.747676213911406,-1.80659227748625,
11.5572015846537));
#275813=CARTESIAN_POINT('Ctrl Pts',(-0.80992909009743,-1.77823813619379,
11.5532840437751));
#275814=CARTESIAN_POINT('Ctrl Pts',(-0.839309585150223,-1.76485628528171,
11.5514351446165));
#275815=CARTESIAN_POINT('Ctrl Pts',(-0.868333705387705,-1.75075731663089,
11.549586245458));
#275816=CARTESIAN_POINT('Ctrl Pts',(-0.896965027564618,-1.73596363421761,
11.5477373462994));
#275817=CARTESIAN_POINT('Ctrl Pts',(-0.957639436783788,-1.70461342499374,
11.5438192295089));
#275818=CARTESIAN_POINT('Ctrl Pts',(-1.01678854115817,-1.67001625427391,
11.5399011127185));
#275819=CARTESIAN_POINT('Ctrl Pts',(-1.07404282521682,-1.632344329362,11.5359829959281));
#275820=CARTESIAN_POINT('Ctrl Pts',(-1.13121089392045,-1.59472913205456,
11.5320707791648));
#275821=CARTESIAN_POINT('Ctrl Pts',(-1.18648939745831,-1.55404863778721,
11.5281585624015));
#275822=CARTESIAN_POINT('Ctrl Pts',(-1.23953292724915,-1.51052114260779,
11.5242463456382));
#275823=CARTESIAN_POINT('Ctrl Pts',(-1.2925140811846,-1.46704483302548,
11.5203387293958));
#275824=CARTESIAN_POINT('Ctrl Pts',(-1.34326510255321,-1.42072848205026,
11.5164311131535));
#275825=CARTESIAN_POINT('Ctrl Pts',(-1.39147065006314,-1.37183287247859,
11.5125234969111));
#275826=CARTESIAN_POINT('Ctrl Pts',(-1.43964598437286,-1.32296790860887,
11.5086183297974));
#275827=CARTESIAN_POINT('Ctrl Pts',(-1.48527866502574,-1.27152724239304,
11.5047131626838));
#275828=CARTESIAN_POINT('Ctrl Pts',(-1.52808864439131,-1.21780995844275,
11.5008079955701));
#275829=CARTESIAN_POINT('Ctrl Pts',(-1.57088647538741,-1.16410791807403,
11.4969039366423));
#275830=CARTESIAN_POINT('Ctrl Pts',(-1.61086288882351,-1.10813092696698,
11.4929998777145));
#275831=CARTESIAN_POINT('Ctrl Pts',(-1.64777793385773,-1.05021135048691,
11.4890958187867));
#275832=CARTESIAN_POINT('Ctrl Pts',(-1.68469516420617,-0.9922883452565,
11.4851915287446));
#275833=CARTESIAN_POINT('Ctrl Pts',(-1.71855040414558,-0.932422942513319,
11.4812872387025));
#275834=CARTESIAN_POINT('Ctrl Pts',(-1.74914787126292,-0.870975157198189,
11.4773829486603));
#275835=CARTESIAN_POINT('Ctrl Pts',(-1.77977792955806,-0.809461920200752,
11.4734744999272));
#275836=CARTESIAN_POINT('Ctrl Pts',(-1.80714307022,-0.746363378073689,11.4695660511941));
#275837=CARTESIAN_POINT('Ctrl Pts',(-1.83109466309896,-0.682061826208244,
11.465657602461));
#275838=CARTESIAN_POINT('Ctrl Pts',(-1.85506059264569,-0.617721785462693,
11.4617468142538));
#275839=CARTESIAN_POINT('Ctrl Pts',(-1.87560876081767,-0.552177771299046,
11.4578360260465));
#275840=CARTESIAN_POINT('Ctrl Pts',(-1.89264053357121,-0.485826934909212,
11.4539252378393));
#275841=CARTESIAN_POINT('Ctrl Pts',(-1.90970171470921,-0.419361532001062,
11.4500076969608));
#275842=CARTESIAN_POINT('Ctrl Pts',(-1.92323428537703,-0.352087008383132,
11.4460901560823));
#275843=CARTESIAN_POINT('Ctrl Pts',(-1.93319094420419,-0.284409516800858,
11.4421726152038));
#275844=CARTESIAN_POINT('Ctrl Pts',(-1.93789002934436,-0.252468852714836,
11.4403237160452));
#275845=CARTESIAN_POINT('Ctrl Pts',(-1.94179336691381,-0.220438485429623,
11.4384748168865));
#275846=CARTESIAN_POINT('Ctrl Pts',(-1.94490001565959,-0.188361166611744,
11.4366259177279));
#275847=CARTESIAN_POINT('Ctrl Pts',(-1.95092446803442,-0.126156425958906,
11.4330405091934));
#275848=CARTESIAN_POINT('Ctrl Pts',(-1.95396526428295,-0.0636581075121945,
11.4294551006588));
#275849=CARTESIAN_POINT('Ctrl Pts',(-1.95399970412604,-0.00107530244352288,
11.4258696921242));
#275850=CARTESIAN_POINT('',(-1.95134965453372,-0.00103648843533824,10.7258696921242));
#275851=CARTESIAN_POINT('Ctrl Pts',(-1.95645396550645,-0.00105959575216067,
11.4258687161274));
#275852=CARTESIAN_POINT('Ctrl Pts',(-1.95257275277448,0.583565857793029,
11.3924173071372));
#275853=CARTESIAN_POINT('Ctrl Pts',(-1.36384586590087,1.82225161540351,
11.3219287552896));
#275854=CARTESIAN_POINT('Ctrl Pts',(0.742476273254284,2.18672944451667,
11.214403060585));
#275855=CARTESIAN_POINT('Ctrl Pts',(2.2397387517957,0.562696191178322,11.1032916320137));
#275856=CARTESIAN_POINT('Ctrl Pts',(1.68783678799721,-1.57615470590446,
10.9921802034423));
#275857=CARTESIAN_POINT('Ctrl Pts',(-0.408287745359925,-2.2729623395146,
10.8810687748709));
#275858=CARTESIAN_POINT('Ctrl Pts',(-1.7845049539434,-1.16824013984896,
10.7922986044314));
#275859=CARTESIAN_POINT('Ctrl Pts',(-1.95259451044093,-0.259597370141399,
10.7405655768493));
#275860=CARTESIAN_POINT('Ctrl Pts',(-1.95134965453372,-0.00103648843533824,
10.7258696921242));
#275861=CARTESIAN_POINT('',(-1.95399929751496,0.00165689801507491,10.0258696714934));
#275862=CARTESIAN_POINT('Ctrl Pts',(-1.95134965453372,-0.00103648843533824,
10.7258696921242));
#275863=CARTESIAN_POINT('Ctrl Pts',(-1.94945717594664,0.392037865993335,
10.7035284339921));
#275864=CARTESIAN_POINT('Ctrl Pts',(-1.64348006051442,1.43945790588366,
10.6441500330031));
#275865=CARTESIAN_POINT('Ctrl Pts',(0.0649797842751265,2.30842680358238,
10.5477344891565));
#275866=CARTESIAN_POINT('Ctrl Pts',(1.97439630915861,1.19783800834803,10.4366230605851));
#275867=CARTESIAN_POINT('Ctrl Pts',(2.07741344546512,-1.0086674657501,10.3255116320137));
#275868=CARTESIAN_POINT('Ctrl Pts',(0.279779552238291,-2.29233070956424,
10.2144002034423));
#275869=CARTESIAN_POINT('Ctrl Pts',(-1.56625610044506,-1.56095036901687,
10.1145195568125));
#275870=CARTESIAN_POINT('Ctrl Pts',(-1.94902830395309,-0.451607116338367,
10.0516760530398));
#275871=CARTESIAN_POINT('Ctrl Pts',(-1.95267873247834,0.00165541588313972,
10.0258696921242));
#275872=CARTESIAN_POINT('',(-1.95399999960791,3.91444967126425E-5,9.32586969217706));
#275873=CARTESIAN_POINT('Ctrl Pts',(-1.95399929751496,0.00165689801507491,
10.0258696714934));
#275874=CARTESIAN_POINT('Ctrl Pts',(-1.95392948695817,0.0839853079092353,
10.0211854615976));
#275875=CARTESIAN_POINT('Ctrl Pts',(-1.94865267969109,0.166088006905242,
10.0165012517017));
#275876=CARTESIAN_POINT('Ctrl Pts',(-1.93827701010705,0.247382764335887,
10.0118170418058));
#275877=CARTESIAN_POINT('Ctrl Pts',(-1.92775896101606,0.329793084226128,
10.007068553119));
#275878=CARTESIAN_POINT('Ctrl Pts',(-1.91200123245361,0.411373120614258,
10.0023200644323));
#275879=CARTESIAN_POINT('Ctrl Pts',(-1.8911653299869,0.491538090747332,
9.99757157574553));
#275880=CARTESIAN_POINT('Ctrl Pts',(-1.88327554679925,0.521893590568139,
9.99577349926348));
#275881=CARTESIAN_POINT('Ctrl Pts',(-1.87465811584151,0.552046411622639,
9.99397542278144));
#275882=CARTESIAN_POINT('Ctrl Pts',(-1.86532357338296,0.581965606012771,
9.99217734629939));
#275883=CARTESIAN_POINT('Ctrl Pts',(-1.84498304398784,0.647161329924655,
9.98825922950897));
#275884=CARTESIAN_POINT('Ctrl Pts',(-1.82118005276578,0.711418612616846,
9.98434111271855));
#275885=CARTESIAN_POINT('Ctrl Pts',(-1.7940200408267,0.774343653110278,
9.98042299592813));
#275886=CARTESIAN_POINT('Ctrl Pts',(-1.76690092731312,0.837173939040036,
9.97651077916485));
#275887=CARTESIAN_POINT('Ctrl Pts',(-1.73643501904436,0.898675516260269,
9.97259856240157));
#275888=CARTESIAN_POINT('Ctrl Pts',(-1.70277733117232,0.95847032319508,
9.96868634563829));
#275889=CARTESIAN_POINT('Ctrl Pts',(-1.66915922262466,1.0181948151971,9.9647787293959));
#275890=CARTESIAN_POINT('Ctrl Pts',(-1.63235702878227,1.0762160963446,9.96087111315351));
#275891=CARTESIAN_POINT('Ctrl Pts',(-1.59257282631954,1.13217833969238,
9.95696349691113));
#275892=CARTESIAN_POINT('Ctrl Pts',(-1.55281355891379,1.18810550827076,
9.95305832979748));
#275893=CARTESIAN_POINT('Ctrl Pts',(-1.51007627474735,1.24197579902889,
9.94915316268384));
#275894=CARTESIAN_POINT('Ctrl Pts',(-1.46460689797784,1.29346149320176,
9.94524799557019));
#275895=CARTESIAN_POINT('Ctrl Pts',(-1.41915042424628,1.34493257706077,
9.94134393664239));
#275896=CARTESIAN_POINT('Ctrl Pts',(-1.37096372246039,1.39402003916266,
9.93743987771458));
#275897=CARTESIAN_POINT('Ctrl Pts',(-1.32033245331152,1.4404298708137,9.93353581878677));
#275898=CARTESIAN_POINT('Ctrl Pts',(-1.26969818686899,1.48684244985577,
9.92963152874465));
#275899=CARTESIAN_POINT('Ctrl Pts',(-1.21661943008506,1.53057675327101,
9.92572723870252));
#275900=CARTESIAN_POINT('Ctrl Pts',(-1.16141674139082,1.57137746987066,
9.9218229486604));
#275901=CARTESIAN_POINT('Ctrl Pts',(-1.10615525303724,1.6122216457346,9.91791449992728));
#275902=CARTESIAN_POINT('Ctrl Pts',(-1.04876571419292,1.65012570585005,
9.91400605119417));
#275903=CARTESIAN_POINT('Ctrl Pts',(-0.98959881145575,1.68487690718502,
9.91009760246104));
#275904=CARTESIAN_POINT('Ctrl Pts',(-0.930396493277447,1.71964890949263,
9.90618681425383));
#275905=CARTESIAN_POINT('Ctrl Pts',(-0.869415130643365,1.7512640707161,
9.90227602604662));
#275906=CARTESIAN_POINT('Ctrl Pts',(-0.807028720130453,1.77955630562357,
9.89836523783941));
#275907=CARTESIAN_POINT('Ctrl Pts',(-0.74453458838551,1.80789739210586,
9.8944476969609));
#275908=CARTESIAN_POINT('Ctrl Pts',(-0.68063102453977,1.83290392174707,
9.89053015608238));
#275909=CARTESIAN_POINT('Ctrl Pts',(-0.615709801840668,1.85445879973574,
9.88661261520387));
#275910=CARTESIAN_POINT('Ctrl Pts',(-0.585069969928584,1.86463171101191,
9.88476371604523));
#275911=CARTESIAN_POINT('Ctrl Pts',(-0.554203648136369,1.87403653167203,
9.88291481688659));
#275912=CARTESIAN_POINT('Ctrl Pts',(-0.523152775522914,1.88266491268698,
9.88106591772794));
#275913=CARTESIAN_POINT('Ctrl Pts',(-0.457350947026457,1.90094984962951,
9.87714780093752));
#275914=CARTESIAN_POINT('Ctrl Pts',(-0.390458897492729,1.91581707799529,
9.87322968414709));
#275915=CARTESIAN_POINT('Ctrl Pts',(-0.322864636989375,1.92714151690573,
9.86931156735667));
#275916=CARTESIAN_POINT('Ctrl Pts',(-0.255372162112371,1.93844890310935,
9.86539935059339));
#275917=CARTESIAN_POINT('Ctrl Pts',(-0.187180056070632,1.9462240070194,
9.8614871338301));
#275918=CARTESIAN_POINT('Ctrl Pts',(-0.118690003493383,1.95039193063106,
9.85757491706682));
#275919=CARTESIAN_POINT('Ctrl Pts',(-0.0502804909110705,1.95455495302664,
9.85366730082444));
#275920=CARTESIAN_POINT('Ctrl Pts',(0.0184257837265425,1.95511918970179,
9.84975968458205));
#275921=CARTESIAN_POINT('Ctrl Pts',(0.0870202805502169,1.95206133888589,
9.84585206833967));
#275922=CARTESIAN_POINT('Ctrl Pts',(0.155571785241821,1.94900540460167,
9.84194690122602));
#275923=CARTESIAN_POINT('Ctrl Pts',(0.2240111608026,1.94233190798178,9.83804173411238));
#275924=CARTESIAN_POINT('Ctrl Pts',(0.291929689823532,1.93206963026686,
9.83413656699874));
#275925=CARTESIAN_POINT('Ctrl Pts',(0.359828945315338,1.92181026472203,
9.83023250807094));
#275926=CARTESIAN_POINT('Ctrl Pts',(0.427207161550223,1.90796421324135,
9.82632844914314));
#275927=CARTESIAN_POINT('Ctrl Pts',(0.493662379692254,1.89061192603786,
9.82242439021533));
#275928=CARTESIAN_POINT('Ctrl Pts',(0.560121531881548,1.8732586116055,9.81852010017321));
#275929=CARTESIAN_POINT('Ctrl Pts',(0.625657102224863,1.85239877611429,
9.81461581013109));
#275930=CARTESIAN_POINT('Ctrl Pts',(0.689880705298606,1.82816317993135,
9.81071152008897));
#275931=CARTESIAN_POINT('Ctrl Pts',(0.754172716742869,1.80390176897683,
9.80680307135586));
#275932=CARTESIAN_POINT('Ctrl Pts',(0.817149510945161,1.77625759537737,
9.80289462262275));
#275933=CARTESIAN_POINT('Ctrl Pts',(0.878442115050694,1.74540982308032,
9.79898617388963));
#275934=CARTESIAN_POINT('Ctrl Pts',(0.93977140697515,1.71454358628007,9.79507538568242));
#275935=CARTESIAN_POINT('Ctrl Pts',(0.999414075337499,1.68047017848876,
9.79116459747521));
#275936=CARTESIAN_POINT('Ctrl Pts',(1.05702769443046,1.64341365857991,9.78725380926801));
#275937=CARTESIAN_POINT('Ctrl Pts',(1.11474079368233,1.60629315399962,9.7833362683895));
#275938=CARTESIAN_POINT('Ctrl Pts',(1.17041745233701,1.56617954436482,9.77941872751099));
#275939=CARTESIAN_POINT('Ctrl Pts',(1.22374675336249,1.52333840089285,9.77550118663248));
#275940=CARTESIAN_POINT('Ctrl Pts',(1.24891573126341,1.50311935109166,9.77365228747383));
#275941=CARTESIAN_POINT('Ctrl Pts',(1.27356237264419,1.48229332071419,9.77180338831518));
#275942=CARTESIAN_POINT('Ctrl Pts',(1.29765691031169,1.46089101000736,9.76995448915654));
#275943=CARTESIAN_POINT('Ctrl Pts',(1.34871713831335,1.41553604700562,9.76603637236611));
#275944=CARTESIAN_POINT('Ctrl Pts',(1.39749788996994,1.36741101154671,9.76211825557569));
#275945=CARTESIAN_POINT('Ctrl Pts',(1.44368358142382,1.3167739808818,9.75820013878526));
#275946=CARTESIAN_POINT('Ctrl Pts',(1.48979972496789,1.26621320109742,9.75428792202198));
#275947=CARTESIAN_POINT('Ctrl Pts',(1.53332823495643,1.21314829381023,9.7503757052587));
#275948=CARTESIAN_POINT('Ctrl Pts',(1.57398826347465,1.15787604968928,9.74646348849542));
#275949=CARTESIAN_POINT('Ctrl Pts',(1.61460047835618,1.10266880225171,9.74255587225303));
#275950=CARTESIAN_POINT('Ctrl Pts',(1.652350620811,1.04525976740311,9.73864825601065));
#275951=CARTESIAN_POINT('Ctrl Pts',(1.68699746590993,0.985979487623083,
9.73474063976826));
#275952=CARTESIAN_POINT('Ctrl Pts',(1.72162259583039,0.926736362217474,
9.73083547265462));
#275953=CARTESIAN_POINT('Ctrl Pts',(1.75314803904495,0.865624742091583,
9.72693030554098));
#275954=CARTESIAN_POINT('Ctrl Pts',(1.78137622546144,0.803003576181791,
9.72302513842733));
#275955=CARTESIAN_POINT('Ctrl Pts',(1.80959640144573,0.740400180545905,
9.71912107949953));
#275956=CARTESIAN_POINT('Ctrl Pts',(1.83452097606573,0.676288537729521,
9.71521702057172));
#275957=CARTESIAN_POINT('Ctrl Pts',(1.8559994494078,0.611049951966226,9.71131296164392));
#275958=CARTESIAN_POINT('Ctrl Pts',(1.87747919424264,0.545807504178463,
9.7074086716018));
#275959=CARTESIAN_POINT('Ctrl Pts',(1.89551228139774,0.479438449005124,
9.70350438155968));
#275960=CARTESIAN_POINT('Ctrl Pts',(1.90999783704255,0.412339984106304,
9.69960009151755));
#275961=CARTESIAN_POINT('Ctrl Pts',(1.92449882211221,0.345170048651036,
9.69569164278444));
#275962=CARTESIAN_POINT('Ctrl Pts',(1.93544463058594,0.277269634669579,
9.69178319405132));
#275963=CARTESIAN_POINT('Ctrl Pts',(1.94278558114032,0.209045893796705,
9.6878747453182));
#275964=CARTESIAN_POINT('Ctrl Pts',(1.95013092575609,0.14078131634512,9.68396395711099));
#275965=CARTESIAN_POINT('Ctrl Pts',(1.95386709136618,0.072193518053941,
9.68005316890378));
#275966=CARTESIAN_POINT('Ctrl Pts',(1.95399651261058,0.00369170769181413,
9.67614238069657));
#275967=CARTESIAN_POINT('Ctrl Pts',(1.95412615732378,-0.0649283832276949,
9.67222483981805));
#275968=CARTESIAN_POINT('Ctrl Pts',(1.95063665321014,-0.133461698906467,
9.66830729893954));
#275969=CARTESIAN_POINT('Ctrl Pts',(1.94358240125738,-0.201502976460919,
9.66438975806103));
#275970=CARTESIAN_POINT('Ctrl Pts',(1.94025311870366,-0.233615330798652,
9.66254085890239));
#275971=CARTESIAN_POINT('Ctrl Pts',(1.93613056531544,-0.265618221702319,
9.66069195974374));
#275972=CARTESIAN_POINT('Ctrl Pts',(1.93122438013529,-0.297469987681229,
9.6588430605851));
#275973=CARTESIAN_POINT('Ctrl Pts',(1.92082737906498,-0.364969038942825,
9.65492494379468));
#275974=CARTESIAN_POINT('Ctrl Pts',(1.90686672512084,-0.432056153290937,
9.65100682700425));
#275975=CARTESIAN_POINT('Ctrl Pts',(1.88938799219554,-0.498326213385671,
9.64708871021382));
#275976=CARTESIAN_POINT('Ctrl Pts',(1.87193557931229,-0.564496481877911,
9.64317649345054));
#275977=CARTESIAN_POINT('Ctrl Pts',(1.85097572581657,-0.629851666130271,
9.63926427668725));
#275978=CARTESIAN_POINT('Ctrl Pts',(1.82660537170836,-0.693994824221443,
9.63535205992397));
#275979=CARTESIAN_POINT('Ctrl Pts',(1.80226367560408,-0.758062553992272,
9.63144444368158));
#275980=CARTESIAN_POINT('Ctrl Pts',(1.77451961774217,-0.820920630569309,
9.6275368274392));
#275981=CARTESIAN_POINT('Ctrl Pts',(1.74351998777852,-0.88218708458966,
9.62362921119681));
#275982=CARTESIAN_POINT('Ctrl Pts',(1.71253978707301,-0.943415139385506,
9.61972404408316));
#275983=CARTESIAN_POINT('Ctrl Pts',(1.6783082834547,-1.00305311255965,9.61581887696952));
#275984=CARTESIAN_POINT('Ctrl Pts',(1.64101981344774,-1.06074029426243,
9.61191370985587));
#275985=CARTESIAN_POINT('Ctrl Pts',(1.60374192494811,-1.11841110582891,
9.60800965092807));
#275986=CARTESIAN_POINT('Ctrl Pts',(1.56340905906781,-1.17413181198458,
9.60410559200026));
#275987=CARTESIAN_POINT('Ctrl Pts',(1.52025986903153,-1.22756911439325,
9.60020153307246));
#275988=CARTESIAN_POINT('Ctrl Pts',(1.47710812462923,-1.28100958020845,
9.59629724303034));
#275989=CARTESIAN_POINT('Ctrl Pts',(1.4311400360793,-1.33216599282712,9.59239295298821));
#275990=CARTESIAN_POINT('Ctrl Pts',(1.38263453184847,-1.3807381183049,9.58848866294609));
#275991=CARTESIAN_POINT('Ctrl Pts',(1.33407736152685,-1.42936198083572,
9.58458021421297));
#275992=CARTESIAN_POINT('Ctrl Pts',(1.28297772990803,-1.47539571401498,
9.58067176547986));
#275993=CARTESIAN_POINT('Ctrl Pts',(1.22965070125184,-1.51857668654265,
9.57676331674674));
#275994=CARTESIAN_POINT('Ctrl Pts',(1.17629175271886,-1.56178350583804,
9.57285252853952));
#275995=CARTESIAN_POINT('Ctrl Pts',(1.12070315185605,-1.60213387711285,
9.56894174033231));
#275996=CARTESIAN_POINT('Ctrl Pts',(1.06322996616869,-1.63940783182249,
9.5650309521251));
#275997=CARTESIAN_POINT('Ctrl Pts',(1.00565754280569,-1.67674614664343,
9.56111341124659));
#275998=CARTESIAN_POINT('Ctrl Pts',(0.946194466017227,-1.71099719765996,
9.55719587036807));
#275999=CARTESIAN_POINT('Ctrl Pts',(0.885210682680147,-1.74198681030281,
9.55327832948956));
#276000=CARTESIAN_POINT('Ctrl Pts',(0.856429141096074,-1.75661248250855,
9.55142943033093));
#276001=CARTESIAN_POINT('Ctrl Pts',(0.827309167574824,-1.7705123967077,
9.5495805311723));
#276002=CARTESIAN_POINT('Ctrl Pts',(0.797890988516439,-1.78367204677437,
9.54773163201366));
#276003=CARTESIAN_POINT('Ctrl Pts',(0.73554910211656,-1.81155947678457,
9.54381351522324));
#276004=CARTESIAN_POINT('Ctrl Pts',(0.671619816017365,-1.83622984664296,
9.53989539843281));
#276005=CARTESIAN_POINT('Ctrl Pts',(0.606468165748695,-1.85750164574178,
9.53597728164239));
#276006=CARTESIAN_POINT('Ctrl Pts',(0.541414622944768,-1.87874141307668,
9.5320650648791));
#276007=CARTESIAN_POINT('Ctrl Pts',(0.475142832887637,-1.89659261499268,
9.52815284811582));
#276008=CARTESIAN_POINT('Ctrl Pts',(0.408038831897616,-1.9109213253464,
9.52424063135254));
#276009=CARTESIAN_POINT('Ctrl Pts',(0.341013740993034,-1.92523318603777,
9.52033301511015));
#276010=CARTESIAN_POINT('Ctrl Pts',(0.273158861483582,-1.93603067946743,
9.51642539886777));
#276011=CARTESIAN_POINT('Ctrl Pts',(0.204874697954479,-1.94322987784206,
9.51251778262539));
#276012=CARTESIAN_POINT('Ctrl Pts',(0.136633332053651,-1.95042456406336,
9.50861261551174));
#276013=CARTESIAN_POINT('Ctrl Pts',(0.0679637039277501,-1.95402537749045,
9.5047074483981));
#276014=CARTESIAN_POINT('Ctrl Pts',(-0.000725744151200082,-1.953999865224,
9.50080228128446));
#276015=CARTESIAN_POINT('Ctrl Pts',(-0.0693956999340427,-1.95397436019728,
9.49689822235665));
#276016=CARTESIAN_POINT('Ctrl Pts',(-0.138084972855544,-1.95032457251632,
9.49299416342885));
#276017=CARTESIAN_POINT('Ctrl Pts',(-0.206384103313727,-1.94307014847622,
9.48909010450105));
#276018=CARTESIAN_POINT('Ctrl Pts',(-0.27468727697597,-1.9358152949853,
9.48518581445893));
#276019=CARTESIAN_POINT('Ctrl Pts',(-0.342599773465787,-1.92495543598685,
9.48128152441681));
#276020=CARTESIAN_POINT('Ctrl Pts',(-0.409718057092925,-1.91056198896869,
9.47737723437469));
#276021=CARTESIAN_POINT('Ctrl Pts',(-0.476907832386587,-1.89615321063604,
9.47346878564157));
#276022=CARTESIAN_POINT('Ctrl Pts',(-0.543301224668324,-1.87820343617182,
9.46956033690846));
#276023=CARTESIAN_POINT('Ctrl Pts',(-0.60850668024895,-1.85683483920687,
9.46565188817534));
#276024=CARTESIAN_POINT('Ctrl Pts',(-0.673751165757901,-1.83545345167401,
9.46174109996814));
#276025=CARTESIAN_POINT('Ctrl Pts',(-0.737805840669606,-1.81064934657337,
9.45783031176093));
#276026=CARTESIAN_POINT('Ctrl Pts',(-0.800298711104466,-1.78259304750258,
9.45391952355373));
#276027=CARTESIAN_POINT('Ctrl Pts',(-0.862899486593402,-1.75448830424212,
9.45000198267521));
#276028=CARTESIAN_POINT('Ctrl Pts',(-0.923932638108802,-1.7231203841169,
9.4460844417967));
#276029=CARTESIAN_POINT('Ctrl Pts',(-0.983051141817712,-1.68870555532067,
9.44216690091819));
#276030=CARTESIAN_POINT('Ctrl Pts',(-1.01095235718662,-1.6724633385884,
9.44031800175954));
#276031=CARTESIAN_POINT('Ctrl Pts',(-1.03842753006701,-1.65554307417473,
9.4384691026009));
#276032=CARTESIAN_POINT('Ctrl Pts',(-1.06544265032794,-1.63797068315101,
9.43662020344225));
#276033=CARTESIAN_POINT('Ctrl Pts',(-1.1226587199488,-1.60075363068159,
9.43270436882958));
#276034=CARTESIAN_POINT('Ctrl Pts',(-1.1780364749103,-1.56046083031989,
9.42878853421692));
#276035=CARTESIAN_POINT('Ctrl Pts',(-1.23122563104289,-1.51730005123016,
9.42487269960425));
#276036=CARTESIAN_POINT('Ctrl Pts',(-1.28433467052284,-1.47420428345847,
9.42096276325326));
#276037=CARTESIAN_POINT('Ctrl Pts',(-1.33526127416141,-1.42824941800991,
9.41705282690228));
#276038=CARTESIAN_POINT('Ctrl Pts',(-1.38368371239994,-1.37968669778291,
9.41314289055129));
#276039=CARTESIAN_POINT('Ctrl Pts',(-1.43204927728936,-1.33118101566968,
9.40923754651707));
#276040=CARTESIAN_POINT('Ctrl Pts',(-1.47791617174053,-1.28007390884125,
9.40533220248285));
#276041=CARTESIAN_POINT('Ctrl Pts',(-1.52099680099037,-1.22665591401056,
9.40142685844863));
#276042=CARTESIAN_POINT('Ctrl Pts',(-1.56405051188734,-1.17327129669684,
9.39752395461621));
#276043=CARTESIAN_POINT('Ctrl Pts',(-1.60432110247687,-1.1175790381103,
9.39362105078379));
#276044=CARTESIAN_POINT('Ctrl Pts',(-1.64155990459192,-1.05990427852527,
9.38971814695136));
#276045=CARTESIAN_POINT('Ctrl Pts',(-1.67878825190776,-1.00224571113753,
9.38581633885976));
#276046=CARTESIAN_POINT('Ctrl Pts',(-1.71298623341745,-0.942606161247988,
9.38191453076817));
#276047=CARTESIAN_POINT('Ctrl Pts',(-1.74394839247643,-0.881339891516826,
9.37801272267657));
#276048=CARTESIAN_POINT('Ctrl Pts',(-1.77491251225945,-0.820069742009442,
9.37411066749727));
#276049=CARTESIAN_POINT('Ctrl Pts',(-1.80264018298136,-0.757173108918886,
9.37020861231796));
#276050=CARTESIAN_POINT('Ctrl Pts',(-1.82697265374871,-0.693027360538097,
9.36630655713865));
#276051=CARTESIAN_POINT('Ctrl Pts',(-1.8513310801166,-0.628813187481577,
9.36240033961239));
#276052=CARTESIAN_POINT('Ctrl Pts',(-1.87228690420847,-0.563347701541565,
9.35849412208613));
#276053=CARTESIAN_POINT('Ctrl Pts',(-1.88973051800933,-0.497025722980409,
9.35458790455987));
#276054=CARTESIAN_POINT('Ctrl Pts',(-1.90718467303244,-0.430663665871048,
9.35067932649597));
#276055=CARTESIAN_POINT('Ctrl Pts',(-1.92112229410764,-0.363444568437687,
9.34677074843206));
#276056=CARTESIAN_POINT('Ctrl Pts',(-1.93148500290727,-0.295773027073632,
9.34286217036815));
#276057=CARTESIAN_POINT('Ctrl Pts',(-1.94186551985346,-0.227985193266197,
9.3389468754764));
#276058=CARTESIAN_POINT('Ctrl Pts',(-1.9486588156178,-0.159743853599226,
9.33503158058464));
#276059=CARTESIAN_POINT('Ctrl Pts',(-1.95185848490155,-0.0914573940029764,
9.33111628569289));
#276060=CARTESIAN_POINT('Ctrl Pts',(-1.95328769730922,-0.060955536880899,
9.32936742118761));
#276061=CARTESIAN_POINT('Ctrl Pts',(-1.95400061029009,-0.0304446549697955,
9.32761855668234));
#276062=CARTESIAN_POINT('Ctrl Pts',(-1.95399999960791,3.91444967267211E-5,
9.32586969217706));
#276063=CARTESIAN_POINT('',(-1.9539992760325,-0.00168204175487709,8.62586971134118));
#276064=CARTESIAN_POINT('Ctrl Pts',(-1.95399999960789,3.91454175048696E-5,
9.32586969212423));
#276065=CARTESIAN_POINT('Ctrl Pts',(-1.9539999575976,0.00213614972020012,
9.32574938637309));
#276066=CARTESIAN_POINT('Ctrl Pts',(-1.95399653987704,0.00423315001500904,
9.32562908062195));
#276067=CARTESIAN_POINT('Ctrl Pts',(-1.95398974647657,0.00633013936807953,
9.32550877487081));
#276068=CARTESIAN_POINT('Ctrl Pts',(-1.95376849906167,0.0746248727085479,
9.32159065808039));
#276069=CARTESIAN_POINT('Ctrl Pts',(-1.9499620047619,0.143043374382022,
9.31767254128996));
#276070=CARTESIAN_POINT('Ctrl Pts',(-1.94255495232333,0.211178259307431,
9.31375442449954));
#276071=CARTESIAN_POINT('Ctrl Pts',(-1.93515905366417,0.279210544516802,
9.30984220773625));
#276072=CARTESIAN_POINT('Ctrl Pts',(-1.9241734100253,0.346959575514039,
9.30592999097297));
#276073=CARTESIAN_POINT('Ctrl Pts',(-1.90963472102237,0.414018396047568,
9.30201777420969));
#276074=CARTESIAN_POINT('Ctrl Pts',(-1.89511312860348,0.480998359625015,
9.2981101579673));
#276075=CARTESIAN_POINT('Ctrl Pts',(-1.87704689243386,0.547289246240515,
9.29420254172492));
#276076=CARTESIAN_POINT('Ctrl Pts',(-1.85552423648662,0.612491475704569,
9.29029492548253));
#276077=CARTESIAN_POINT('Ctrl Pts',(-1.83401507003066,0.677652839166399,
9.28638975836889));
#276078=CARTESIAN_POINT('Ctrl Pts',(-1.80905393495955,0.74172643294925,
9.28248459125525));
#276079=CARTESIAN_POINT('Ctrl Pts',(-1.78077923950232,0.804326612861677,
9.2785794241416));
#276080=CARTESIAN_POINT('Ctrl Pts',(-1.75251256767537,0.866909028455468,
9.2746753652138));
#276081=CARTESIAN_POINT('Ctrl Pts',(-1.72093440450345,0.928018412148079,
9.27077130628599));
#276082=CARTESIAN_POINT('Ctrl Pts',(-1.68623106523404,0.987289620445632,
9.26686724735819));
#276083=CARTESIAN_POINT('Ctrl Pts',(-1.65152567158002,1.04656433750806,
9.26296295731607));
#276084=CARTESIAN_POINT('Ctrl Pts',(-1.61369498527018,1.10400023995831,
9.25905866727395));
#276085=CARTESIAN_POINT('Ctrl Pts',(-1.57297007471654,1.15925887706165,
9.25515437723183));
#276086=CARTESIAN_POINT('Ctrl Pts',(-1.53220178564418,1.21457637341826,
9.25124592849871));
#276087=CARTESIAN_POINT('Ctrl Pts',(-1.48853341237372,1.26771157942995,
9.2473374797656));
#276088=CARTESIAN_POINT('Ctrl Pts',(-1.44223735961487,1.31835784160869,
9.24342903103248));
#276089=CARTESIAN_POINT('Ctrl Pts',(-1.39591359549956,1.369034419042,9.23951824282527));
#276090=CARTESIAN_POINT('Ctrl Pts',(-1.34695937224762,1.41721874256836,
9.23560745461806));
#276091=CARTESIAN_POINT('Ctrl Pts',(-1.29568312093407,1.46264187350375,
9.23169666641085));
#276092=CARTESIAN_POINT('Ctrl Pts',(-1.24431833205406,1.50814343555239,
9.22777912553234));
#276093=CARTESIAN_POINT('Ctrl Pts',(-1.19062389767963,1.55087398333843,
9.22386158465383));
#276094=CARTESIAN_POINT('Ctrl Pts',(-1.1349396752578,1.59060615286303,9.21994404377531));
#276095=CARTESIAN_POINT('Ctrl Pts',(-1.10865928274165,1.60935790991755,
9.21809514461667));
#276096=CARTESIAN_POINT('Ctrl Pts',(-1.08193607537915,1.62744245196018,
9.21624624545803));
#276097=CARTESIAN_POINT('Ctrl Pts',(-1.05480766842268,1.6448394397742,9.21439734629939));
#276098=CARTESIAN_POINT('Ctrl Pts',(-0.997318179990151,1.68170647480873,
9.21047922950896));
#276099=CARTESIAN_POINT('Ctrl Pts',(-0.937779569037563,1.7156289537267,
9.20656111271854));
#276100=CARTESIAN_POINT('Ctrl Pts',(-0.876525743196571,1.74637299037568,
9.20264299592811));
#276101=CARTESIAN_POINT('Ctrl Pts',(-0.815364155350078,1.77707073165871,
9.19873077916483));
#276102=CARTESIAN_POINT('Ctrl Pts',(-0.752492914688218,1.80459931071507,
9.19481856240154));
#276103=CARTESIAN_POINT('Ctrl Pts',(-0.68827378679257,1.82876876461028,
9.19090634563826));
#276104=CARTESIAN_POINT('Ctrl Pts',(-0.624130176553013,1.85290979674757,
9.18699872939587));
#276105=CARTESIAN_POINT('Ctrl Pts',(-0.558642285150861,1.87369937628413,
9.18309111315349));
#276106=CARTESIAN_POINT('Ctrl Pts',(-0.492193636297234,1.89099482399834,
9.1791834969111));
#276107=CARTESIAN_POINT('Ctrl Pts',(-0.425786634648827,1.90827943165676,
9.17527832979746));
#276108=CARTESIAN_POINT('Ctrl Pts',(-0.358420544998612,1.92207412808434,
9.17137316268381));
#276109=CARTESIAN_POINT('Ctrl Pts',(-0.290494411596948,1.93228595110324,
9.16746799557017));
#276110=CARTESIAN_POINT('Ctrl Pts',(-0.222587553882365,1.94249487626979,
9.16356393664236));
#276111=CARTESIAN_POINT('Ctrl Pts',(-0.15412145409728,1.94912287331416,
9.15965987771456));
#276112=CARTESIAN_POINT('Ctrl Pts',(-0.085503927002166,1.95212834579779,
9.15575581878675));
#276113=CARTESIAN_POINT('Ctrl Pts',(-0.0168823378544266,1.95513399620079,
9.15185152874463));
#276114=CARTESIAN_POINT('Ctrl Pts',(0.0518902048814037,1.95451667732754,
9.14794723870251));
#276115=CARTESIAN_POINT('Ctrl Pts',(0.120404028540657,1.95028686861989,
9.14404294866039));
#276116=CARTESIAN_POINT('Ctrl Pts',(0.188990830338985,1.946052554492,9.14013449992727));
#276117=CARTESIAN_POINT('Ctrl Pts',(0.257317871206661,1.93819810172526,
9.13622605119416));
#276118=CARTESIAN_POINT('Ctrl Pts',(0.324979762284765,1.92678596478834,
9.13231760246104));
#276119=CARTESIAN_POINT('Ctrl Pts',(0.392682153635994,1.91536699690633,
9.12840681425383));
#276120=CARTESIAN_POINT('Ctrl Pts',(0.459718122725694,1.90038621401291,
9.12449602604662));
#276121=CARTESIAN_POINT('Ctrl Pts',(0.52569441628263,1.88195679564895,9.12058523783941));
#276122=CARTESIAN_POINT('Ctrl Pts',(0.591784629643076,1.86349555561685,
9.1166676969609));
#276123=CARTESIAN_POINT('Ctrl Pts',(0.656811049788291,1.84157395257368,
9.11275015608239));
#276124=CARTESIAN_POINT('Ctrl Pts',(0.720398297139112,1.81635412116665,
9.10883261520387));
#276125=CARTESIAN_POINT('Ctrl Pts',(0.750408554025555,1.80445152039857,
9.10698371604523));
#276126=CARTESIAN_POINT('Ctrl Pts',(0.780098578454699,1.791814949581,9.10513481688659));
#276127=CARTESIAN_POINT('Ctrl Pts',(0.809430877001208,1.77846497164185,
9.10328591772795));
#276128=CARTESIAN_POINT('Ctrl Pts',(0.871590768685767,1.75017420604185,
9.09936780093752));
#276129=CARTESIAN_POINT('Ctrl Pts',(0.932388891210524,1.71856457036587,
9.0954496841471));
#276130=CARTESIAN_POINT('Ctrl Pts',(0.991447614244024,1.68378966269835,
9.09153156735667));
#276131=CARTESIAN_POINT('Ctrl Pts',(1.05041740473991,1.6490671202129,9.08761935059339));
#276132=CARTESIAN_POINT('Ctrl Pts',(1.10765257356635,1.6111890128601,9.0837071338301));
#276133=CARTESIAN_POINT('Ctrl Pts',(1.16279727294156,1.57035617044022,9.07979491706682));
#276134=CARTESIAN_POINT('Ctrl Pts',(1.217877125618,1.52957134487531,9.07588730082444));
#276135=CARTESIAN_POINT('Ctrl Pts',(1.27087099755288,1.48583897614279,9.07197968458206));
#276136=CARTESIAN_POINT('Ctrl Pts',(1.32145095584223,1.43940382495798,9.06807206833967));
#276137=CARTESIAN_POINT('Ctrl Pts',(1.37199921275103,1.39299777736377,9.06416690122603));
#276138=CARTESIAN_POINT('Ctrl Pts',(1.42013619567741,1.34389263955688,9.06026173411238));
#276139=CARTESIAN_POINT('Ctrl Pts',(1.46556731482643,1.29237318360931,9.05635656699874));
#276140=CARTESIAN_POINT('Ctrl Pts',(1.51098554179404,1.24086834755629,9.05245250807093));
#276141=CARTESIAN_POINT('Ctrl Pts',(1.5536991041313,1.18695092219986,9.04854844914313));
#276142=CARTESIAN_POINT('Ctrl Pts',(1.59345180228874,1.13094091524835,9.04464439021532));
#276143=CARTESIAN_POINT('Ctrl Pts',(1.63320685374508,1.07492759259013,9.0407401001732));
#276144=CARTESIAN_POINT('Ctrl Pts',(1.67000041043341,1.0168218449986,9.03683581013108));
#276145=CARTESIAN_POINT('Ctrl Pts',(1.70361900997975,0.956973494322396,
9.03293152008896));
#276146=CARTESIAN_POINT('Ctrl Pts',(1.73727341869132,0.897061395616624,
9.02902307135584));
#276147=CARTESIAN_POINT('Ctrl Pts',(1.76774587980351,0.835403419200247,
9.02511462262273));
#276148=CARTESIAN_POINT('Ctrl Pts',(1.79486891554512,0.772373987139582,
9.02120617388961));
#276149=CARTESIAN_POINT('Ctrl Pts',(1.82200818628015,0.709306827649563,
9.0172953856824));
#276150=CARTESIAN_POINT('Ctrl Pts',(1.84579387125264,0.644867040264066,
9.01338459747519));
#276151=CARTESIAN_POINT('Ctrl Pts',(1.86610768723412,0.579446373399391,
9.00947380926798));
#276152=CARTESIAN_POINT('Ctrl Pts',(1.88645657863134,0.513912746119507,
9.00555626838946));
#276153=CARTESIAN_POINT('Ctrl Pts',(1.90332151555797,0.447395335621599,
9.00163872751095));
#276154=CARTESIAN_POINT('Ctrl Pts',(1.9166350356817,0.380297436222503,8.99772118663244));
#276155=CARTESIAN_POINT('Ctrl Pts',(1.92291840499899,0.348630312995853,
8.9958722874738));
#276156=CARTESIAN_POINT('Ctrl Pts',(1.92841147915643,0.316833982878587,
8.99402338831516));
#276157=CARTESIAN_POINT('Ctrl Pts',(1.93311118975024,0.284951097668394,
8.99217448915653));
#276158=CARTESIAN_POINT('Ctrl Pts',(1.94307063772863,0.217386099715046,
8.9882563723661));
#276159=CARTESIAN_POINT('Ctrl Pts',(1.94950332416642,0.149164392646867,
8.98433825557568));
#276160=CARTESIAN_POINT('Ctrl Pts',(1.9523333946522,0.080686530014642,8.98042013878525));
#276161=CARTESIAN_POINT('Ctrl Pts',(1.9551592035262,0.0123117835654661,
8.97650792202197));
#276162=CARTESIAN_POINT('Ctrl Pts',(1.95439314287712,-0.0563178654085932,
8.97259570525868));
#276163=CARTESIAN_POINT('Ctrl Pts',(1.95001085222104,-0.124794536018906,
8.9686834884954));
#276164=CARTESIAN_POINT('Ctrl Pts',(1.9456337148632,-0.193190682370652,
8.96477587225301));
#276165=CARTESIAN_POINT('Ctrl Pts',(1.93764882421341,-0.261433719077107,
8.96086825601063));
#276166=CARTESIAN_POINT('Ctrl Pts',(1.92608386800902,-0.32911538006514,
8.95696063976824));
#276167=CARTESIAN_POINT('Ctrl Pts',(1.91452616023048,-0.396754621048032,
8.9530554726546));
#276168=CARTESIAN_POINT('Ctrl Pts',(1.89939292061308,-0.463832700500047,
8.94915030554095));
#276169=CARTESIAN_POINT('Ctrl Pts',(1.88076353763226,-0.529947653559265,
8.94524513842731));
#276170=CARTESIAN_POINT('Ctrl Pts',(1.86213944119049,-0.596043844897758,
8.9413410794995));
#276171=CARTESIAN_POINT('Ctrl Pts',(1.84002130424594,-0.661176979189807,
8.93743702057169));
#276172=CARTESIAN_POINT('Ctrl Pts',(1.81453894256888,-0.724958223555688,
8.93353296164389));
#276173=CARTESIAN_POINT('Ctrl Pts',(1.78905507237499,-0.788743243673656,
8.92962867160177));
#276174=CARTESIAN_POINT('Ctrl Pts',(1.760206766927,-0.851175759158179,8.92572438155965));
#276175=CARTESIAN_POINT('Ctrl Pts',(1.72817207348456,-0.911886662051858,
8.92182009151753));
#276176=CARTESIAN_POINT('Ctrl Pts',(1.69610325798926,-0.972662231730667,
8.91791164278441));
#276177=CARTESIAN_POINT('Ctrl Pts',(1.66084151109396,-1.03171209327063,
8.91400319405129));
#276178=CARTESIAN_POINT('Ctrl Pts',(1.62261049358127,-1.08869242034652,
8.91009474531818));
#276179=CARTESIAN_POINT('Ctrl Pts',(1.58435659218775,-1.14570685404836,
8.90618395711097));
#276180=CARTESIAN_POINT('Ctrl Pts',(1.54313017825848,-1.20064889444029,
8.90227316890376));
#276181=CARTESIAN_POINT('Ctrl Pts',(1.49919615738359,-1.25320663965935,
8.89836238069655));
#276182=CARTESIAN_POINT('Ctrl Pts',(1.45518627660879,-1.30585513517196,
8.89444483981803));
#276183=CARTESIAN_POINT('Ctrl Pts',(1.40845979276512,-1.35611075878259,
8.89052729893952));
#276184=CARTESIAN_POINT('Ctrl Pts',(1.359318882882,-1.40369803541946,8.88660975806101));
#276185=CARTESIAN_POINT('Ctrl Pts',(1.33612663301012,-1.42615704183813,
8.88476085890236));
#276186=CARTESIAN_POINT('Ctrl Pts',(1.3123970760063,-1.44802227902029,8.88291195974372));
#276187=CARTESIAN_POINT('Ctrl Pts',(1.28816437580854,-1.46926802895108,
8.88106306058508));
#276188=CARTESIAN_POINT('Ctrl Pts',(1.2368113590264,-1.51429121430976,8.87714494379466));
#276189=CARTESIAN_POINT('Ctrl Pts',(1.18299326569307,-1.55670811660198,
8.87322682700423));
#276190=CARTESIAN_POINT('Ctrl Pts',(1.12700541744814,-1.59623769816483,
8.86930871021381));
#276191=CARTESIAN_POINT('Ctrl Pts',(1.07110187751812,-1.6357077548037,8.86539649345053));
#276192=CARTESIAN_POINT('Ctrl Pts',(1.01303546567295,-1.67229883817997,
8.86148427668724));
#276193=CARTESIAN_POINT('Ctrl Pts',(0.953135596431997,-1.70576919154211,
8.85757205992396));
#276194=CARTESIAN_POINT('Ctrl Pts',(0.893306165670571,-1.73920018587343,
8.85366444368157));
#276195=CARTESIAN_POINT('Ctrl Pts',(0.831647986783256,-1.7695174996381,
8.84975682743919));
#276196=CARTESIAN_POINT('Ctrl Pts',(0.768519036298377,-1.79652288904066,
8.84584921119681));
#276197=CARTESIAN_POINT('Ctrl Pts',(0.705429652372076,-1.8235113526063,
8.84194404408317));
#276198=CARTESIAN_POINT('Ctrl Pts',(0.640871776664479,-1.84719181646173,
8.83803887696952));
#276199=CARTESIAN_POINT('Ctrl Pts',(0.575226142431937,-1.86741288553519,
8.83413370985588));
#276200=CARTESIAN_POINT('Ctrl Pts',(0.509599136739551,-1.88762821639009,
8.83022965092808));
#276201=CARTESIAN_POINT('Ctrl Pts',(0.442885455163538,-1.90438595654717,
8.82632559200028));
#276202=CARTESIAN_POINT('Ctrl Pts',(0.375482158754177,-1.91758419592395,
8.82242153307247));
#276203=CARTESIAN_POINT('Ctrl Pts',(0.308074872172716,-1.93078321661632,
8.81851724303035));
#276204=CARTESIAN_POINT('Ctrl Pts',(0.239978372911714,-1.94042222617882,
8.81461295298823));
#276205=CARTESIAN_POINT('Ctrl Pts',(0.171599320243784,-1.94645053194061,
8.8107086629461));
#276206=CARTESIAN_POINT('Ctrl Pts',(0.103147432989423,-1.95248525880856,
8.80680021421299));
#276207=CARTESIAN_POINT('Ctrl Pts',(0.0344128826163948,-1.95490156322096,
8.80289176547987));
#276208=CARTESIAN_POINT('Ctrl Pts',(-0.034194161530893,-1.95370078551379,
8.79898331674676));
#276209=CARTESIAN_POINT('Ctrl Pts',(-0.102842271690139,-1.95249928905897,
8.79507252853955));
#276210=CARTESIAN_POINT('Ctrl Pts',(-0.171362232997545,-1.94767643613482,
8.79116174033234));
#276211=CARTESIAN_POINT('Ctrl Pts',(-0.239348316416433,-1.93928553426993,
8.78725095212513));
#276212=CARTESIAN_POINT('Ctrl Pts',(-0.307451789898405,-1.93088014402081,
8.78333341124662));
#276213=CARTESIAN_POINT('Ctrl Pts',(-0.375019061595339,-1.91889449458849,
8.77941587036811));
#276214=CARTESIAN_POINT('Ctrl Pts',(-0.441654780584861,-1.90343296566665,
8.7754983294896));
#276215=CARTESIAN_POINT('Ctrl Pts',(-0.473103775910238,-1.89613583496618,
8.77364943033096));
#276216=CARTESIAN_POINT('Ctrl Pts',(-0.504345501457461,-1.88806520565594,
8.77180053117231));
#276217=CARTESIAN_POINT('Ctrl Pts',(-0.535339817952452,-1.87923582323098,
8.76995163201367));
#276218=CARTESIAN_POINT('Ctrl Pts',(-0.601021794873224,-1.86052493174368,
8.76603351522324));
#276219=CARTESIAN_POINT('Ctrl Pts',(-0.665851834598212,-1.83832928533814,
8.76211539843282));
#276220=CARTESIAN_POINT('Ctrl Pts',(-0.729433632825423,-1.81274448704254,
8.75819728164239));
#276221=CARTESIAN_POINT('Ctrl Pts',(-0.792919687521939,-1.7871982151647,
8.75428506487911));
#276222=CARTESIAN_POINT('Ctrl Pts',(-0.85516077849453,-1.75827310216983,
8.75037284811583));
#276223=CARTESIAN_POINT('Ctrl Pts',(-0.915775101602816,-1.72611470165929,
8.74646063135254));
#276224=CARTESIAN_POINT('Ctrl Pts',(-0.976318146078768,-1.69399411740553,
8.74255301511016));
#276225=CARTESIAN_POINT('Ctrl Pts',(-1.03523778943443,-1.6586480261867,
8.73864539886777));
#276226=CARTESIAN_POINT('Ctrl Pts',(-1.09217328346492,-1.62026958216386,
8.73473778262538));
#276227=CARTESIAN_POINT('Ctrl Pts',(-1.14907309273361,-1.58191519212802,
8.73083261551174));
#276228=CARTESIAN_POINT('Ctrl Pts',(-1.2039908125922,-1.54053249369231,
8.7269274483981));
#276229=CARTESIAN_POINT('Ctrl Pts',(-1.25659270252728,-1.49635917478231,
8.72302228128445));
#276230=CARTESIAN_POINT('Ctrl Pts',(-1.3091796654009,-1.45219839112241,
8.71911822235665));
#276231=CARTESIAN_POINT('Ctrl Pts',(-1.35945172645085,-1.40524887523147,
8.71521416342884));
#276232=CARTESIAN_POINT('Ctrl Pts',(-1.40710785536954,-1.35578887860807,
8.71131010450104));
#276233=CARTESIAN_POINT('Ctrl Pts',(-1.45476680545818,-1.30632595402851,
8.70740581445891));
#276234=CARTESIAN_POINT('Ctrl Pts',(-1.49980917652182,-1.25435260964972,
8.70350152441679));
#276235=CARTESIAN_POINT('Ctrl Pts',(-1.54197175482886,-1.20018294743343,
8.69959723437466));
#276236=CARTESIAN_POINT('Ctrl Pts',(-1.58417924299986,-1.14595558589565,
8.69568878564155));
#276237=CARTESIAN_POINT('Ctrl Pts',(-1.62350051405559,-1.08952762665063,
8.69178033690843));
#276238=CARTESIAN_POINT('Ctrl Pts',(-1.65971415905155,-1.03124435040576,
8.68787188817532));
#276239=CARTESIAN_POINT('Ctrl Pts',(-1.69594948039281,-0.972926187630654,
8.6839610999681));
#276240=CARTESIAN_POINT('Ctrl Pts',(-1.72907323645024,-0.912750928657007,
8.6800503117609));
#276241=CARTESIAN_POINT('Ctrl Pts',(-1.75891008121036,-0.851088318693526,
8.67613952355368));
#276242=CARTESIAN_POINT('Ctrl Pts',(-1.78879844458889,-0.789319237268361,
8.67222198267517));
#276243=CARTESIAN_POINT('Ctrl Pts',(-1.81538837891523,-0.726058132398077,
8.66830444179666));
#276244=CARTESIAN_POINT('Ctrl Pts',(-1.83855307077977,-0.661693740280396,
8.66438690091814));
#276245=CARTESIAN_POINT('Ctrl Pts',(-1.849485740183,-0.631316706798713,
8.66253800175951));
#276246=CARTESIAN_POINT('Ctrl Pts',(-1.85965619655906,-0.600694128694863,
8.66068910260087));
#276247=CARTESIAN_POINT('Ctrl Pts',(-1.86905504921175,-0.569867724139624,
8.65884020344224));
#276248=CARTESIAN_POINT('Ctrl Pts',(-1.89340905280269,-0.489991339757814,
8.65404939562637));
#276249=CARTESIAN_POINT('Ctrl Pts',(-1.91265750479486,-0.408490306856713,
8.6492585878105));
#276250=CARTESIAN_POINT('Ctrl Pts',(-1.92662122241073,-0.32595500511049,
8.64446777999463));
#276251=CARTESIAN_POINT('Ctrl Pts',(-1.94038744774897,-0.24458702034784,
8.63974472974686));
#276252=CARTESIAN_POINT('Ctrl Pts',(-1.94901732302756,-0.162213796102582,
8.63502167949909));
#276253=CARTESIAN_POINT('Ctrl Pts',(-1.9523852493591,-0.0794218992784852,
8.63029862925131));
#276254=CARTESIAN_POINT('Ctrl Pts',(-1.95343797789026,-0.0535432477417661,
8.62882232328127));
#276255=CARTESIAN_POINT('Ctrl Pts',(-1.95397694480636,-0.0276238470575762,
8.62734601731123));
#276256=CARTESIAN_POINT('Ctrl Pts',(-1.9539992760325,-0.00168204175487709,
8.62586971134118));
#276257=CARTESIAN_POINT('',(-1.95392409726504,0.000980978241176287,7.92586964537097));
#276258=CARTESIAN_POINT('Ctrl Pts',(-1.95279265841963,-0.00168066560016861,
8.62586969212423));
#276259=CARTESIAN_POINT('Ctrl Pts',(-1.94903606971378,0.455740440167666,
8.59982271970643));
#276260=CARTESIAN_POINT('Ctrl Pts',(-1.56056803492106,1.56933253783666,
8.53673860443147));
#276261=CARTESIAN_POINT('Ctrl Pts',(0.294625979349027,2.29046986711343,
8.43661734629939));
#276262=CARTESIAN_POINT('Ctrl Pts',(2.08390512471393,0.995186470493358,
8.32550591772794));
#276263=CARTESIAN_POINT('Ctrl Pts',(1.96659392361522,-1.21060522857867,
8.21439448915653));
#276264=CARTESIAN_POINT('Ctrl Pts',(0.050021832127414,-2.30879936247667,
8.10328306058509));
#276265=CARTESIAN_POINT('Ctrl Pts',(-1.64852255647152,-1.43097552685388,
8.007108128241));
#276266=CARTESIAN_POINT('Ctrl Pts',(-1.94951932046294,-0.387895067694587,
7.94797033875404));
#276267=CARTESIAN_POINT('Ctrl Pts',(-1.95128373292697,0.000978829950653015,
7.92586969212423));
#276268=CARTESIAN_POINT('',(-1.95399967035838,0.00113500632438228,7.22586969217443));
#276269=CARTESIAN_POINT('Ctrl Pts',(-1.95399975372591,0.000981039797854494,
7.92586964403131));
#276270=CARTESIAN_POINT('Ctrl Pts',(-1.95396164266519,0.0768892786098886,
7.92156158023155));
#276271=CARTESIAN_POINT('Ctrl Pts',(-1.94949609136418,0.152646150253345,
7.9172535164318));
#276272=CARTESIAN_POINT('Ctrl Pts',(-1.9406806068828,0.227760361057462,
7.91294545263205));
#276273=CARTESIAN_POINT('Ctrl Pts',(-1.93183365313758,0.303142712418422,
7.90862201002962));
#276274=CARTESIAN_POINT('Ctrl Pts',(-1.91860579166216,0.377877515271295,
7.90429856742719));
#276275=CARTESIAN_POINT('Ctrl Pts',(-1.90112531659489,0.451484806612561,
7.89997512482476));
#276276=CARTESIAN_POINT('Ctrl Pts',(-1.88356128832724,0.525443926193005,
7.89563101702503));
#276277=CARTESIAN_POINT('Ctrl Pts',(-1.86170404067933,0.598264447757228,
7.89128690922531));
#276278=CARTESIAN_POINT('Ctrl Pts',(-1.83573194611037,0.669480561353234,
7.88694280142558));
#276279=CARTESIAN_POINT('Ctrl Pts',(-1.82400852685083,0.701626461465531,
7.88498193543113));
#276280=CARTESIAN_POINT('Ctrl Pts',(-1.81144735004282,0.733445775577763,
7.88302106943669));
#276281=CARTESIAN_POINT('Ctrl Pts',(-1.79806788981147,0.764897289594456,
7.88106020344224));
#276282=CARTESIAN_POINT('Ctrl Pts',(-1.77133363671727,0.827742331276123,
7.87714208665181));
#276283=CARTESIAN_POINT('Ctrl Pts',(-1.74124763534362,0.889308663726999,
7.87322396986138));
#276284=CARTESIAN_POINT('Ctrl Pts',(-1.70795403340147,0.949214949201517,
7.86930585307096));
#276285=CARTESIAN_POINT('Ctrl Pts',(-1.67471056604327,1.00903102585144,
7.86539363630767));
#276286=CARTESIAN_POINT('Ctrl Pts',(-1.63826932119591,1.06719159016438,
7.86148141954439));
#276287=CARTESIAN_POINT('Ctrl Pts',(-1.59882220601409,1.12333590415167,
7.8575692027811));
#276288=CARTESIAN_POINT('Ctrl Pts',(-1.55942147815914,1.17941419595628,
7.85366158653872));
#276289=CARTESIAN_POINT('Ctrl Pts',(-1.51702218140544,1.23348054567958,
7.84975397029633));
#276290=CARTESIAN_POINT('Ctrl Pts',(-1.47186083526503,1.28520102770459,
7.84584635405395));
#276291=CARTESIAN_POINT('Ctrl Pts',(-1.42672779434805,1.33688909351695,
7.8419411869403));
#276292=CARTESIAN_POINT('Ctrl Pts',(-1.37883646086518,1.38623383854134,
7.83803601982666));
#276293=CARTESIAN_POINT('Ctrl Pts',(-1.32846418350209,1.43293367367514,
7.83413085271301));
#276294=CARTESIAN_POINT('Ctrl Pts',(-1.27810620049383,1.47962025659862,
7.83022679378521));
#276295=CARTESIAN_POINT('Ctrl Pts',(-1.2252690317646,1.5236630853598,7.8263227348574));
#276296=CARTESIAN_POINT('Ctrl Pts',(-1.17026620660454,1.56479807185446,
7.82241867592959));
#276297=CARTESIAN_POINT('Ctrl Pts',(-1.11526012536134,1.60593549347741,
7.81851438588747));
#276298=CARTESIAN_POINT('Ctrl Pts',(-1.05808852859925,1.64416443854038,
7.81461009584535));
#276299=CARTESIAN_POINT('Ctrl Pts',(-0.999095814633345,1.67926280051162,
7.81070580580322));
#276300=CARTESIAN_POINT('Ctrl Pts',(-0.940040264027335,1.71439854783084,
7.8067973570701));
#276301=CARTESIAN_POINT('Ctrl Pts',(-0.879160148548953,1.74639680530431,
7.80288890833698));
#276302=CARTESIAN_POINT('Ctrl Pts',(-0.816825604091032,1.77508082421655,
7.79898045960386));
#276303=CARTESIAN_POINT('Ctrl Pts',(-0.754453748141543,1.80378201247749,
7.79506967139665));
#276304=CARTESIAN_POINT('Ctrl Pts',(-0.690626187733681,1.8291648322634,
7.79115888318944));
#276305=CARTESIAN_POINT('Ctrl Pts',(-0.625731604650915,1.85110128273441,
7.78724809498223));
#276306=CARTESIAN_POINT('Ctrl Pts',(-0.56072496953018,1.87307561038815,
7.78333055410371));
#276307=CARTESIAN_POINT('Ctrl Pts',(-0.494648107975295,1.89159155929559,
7.7794130132252));
#276308=CARTESIAN_POINT('Ctrl Pts',(-0.42790250949824,1.90657164627116,
7.77549547234669));
#276309=CARTESIAN_POINT('Ctrl Pts',(-0.396401656107539,1.91364155851053,
7.77364657318806));
#276310=CARTESIAN_POINT('Ctrl Pts',(-0.364751958044,1.91992463777932,7.77179767402944));
#276311=CARTESIAN_POINT('Ctrl Pts',(-0.332995977480395,1.92541675462272,
7.76994877487081));
#276312=CARTESIAN_POINT('Ctrl Pts',(-0.265699911027953,1.93705543979314,
7.76603065808039));
#276313=CARTESIAN_POINT('Ctrl Pts',(-0.197659524970958,1.94518480848424,
7.76211254128997));
#276314=CARTESIAN_POINT('Ctrl Pts',(-0.129273359947703,1.94971905627653,
7.75819442449954));
#276315=CARTESIAN_POINT('Ctrl Pts',(-0.0609901730262491,1.95424647625166,
7.75428220773626));
#276316=CARTESIAN_POINT('Ctrl Pts',(0.00763727263162475,1.95518948722522,
7.75036999097297));
#276317=CARTESIAN_POINT('Ctrl Pts',(0.0762018291558524,1.95251358029421,
7.74645777420969));
#276318=CARTESIAN_POINT('Ctrl Pts',(0.144685758073215,1.94984082006147,
7.74255015796731));
#276319=CARTESIAN_POINT('Ctrl Pts',(0.213106455551338,1.94355761274228,
7.73864254172492));
#276320=CARTESIAN_POINT('Ctrl Pts',(0.281055092687847,1.93368147192712,
7.73473492548254));
#276321=CARTESIAN_POINT('Ctrl Pts',(0.348961142489828,1.9238115210597,7.73082975836889));
#276322=CARTESIAN_POINT('Ctrl Pts',(0.416395233184727,1.91035317433958,
7.72692459125525));
#276323=CARTESIAN_POINT('Ctrl Pts',(0.482953547812651,1.89337578696232,
7.7230194241416));
#276324=CARTESIAN_POINT('Ctrl Pts',(0.549492974905274,1.87640321733029,
7.7191153652138));
#276325=CARTESIAN_POINT('Ctrl Pts',(0.615156642895896,1.8559137109765,7.71521130628599));
#276326=CARTESIAN_POINT('Ctrl Pts',(0.67955260712821,1.83202736173488,7.71130724735818));
#276327=CARTESIAN_POINT('Ctrl Pts',(0.74395238350307,1.80813959845793,7.70740295731606));
#276328=CARTESIAN_POINT('Ctrl Pts',(0.807083846844779,1.78085476653105,
7.70349866727394));
#276329=CARTESIAN_POINT('Ctrl Pts',(0.868573570370838,1.75034166746189,
7.69959437723182));
#276330=CARTESIAN_POINT('Ctrl Pts',(0.930128790250098,1.71979606708032,
7.69568592849871));
#276331=CARTESIAN_POINT('Ctrl Pts',(0.990038338962065,1.68601555620313,
7.69177747976559));
#276332=CARTESIAN_POINT('Ctrl Pts',(1.04795292777079,1.64921516521545,7.68786903103247));
#276333=CARTESIAN_POINT('Ctrl Pts',(1.10590218242506,1.61239274667485,7.68395824282526));
#276334=CARTESIAN_POINT('Ctrl Pts',(1.16185369993829,1.57254713592708,7.68004745461805));
#276335=CARTESIAN_POINT('Ctrl Pts',(1.21548907916982,1.52993539027598,7.67613666641084));
#276336=CARTESIAN_POINT('Ctrl Pts',(1.26921706942169,1.48725006786827,7.67221912553233));
#276337=CARTESIAN_POINT('Ctrl Pts',(1.32062057131954,1.44178940366806,7.66830158465381));
#276338=CARTESIAN_POINT('Ctrl Pts',(1.36941667118543,1.3938486218666,7.6643840437753));
#276339=CARTESIAN_POINT('Ctrl Pts',(1.39244618658421,1.37122277726507,7.66253514461666));
#276340=CARTESIAN_POINT('Ctrl Pts',(1.41489549543891,1.34804500764465,7.66068624545802));
#276341=CARTESIAN_POINT('Ctrl Pts',(1.43673803704815,1.32434882598923,7.65883734629937));
#276342=CARTESIAN_POINT('Ctrl Pts',(1.48302592063803,1.2741327789003,7.65491922950895));
#276343=CARTESIAN_POINT('Ctrl Pts',(1.52676970802628,1.22138752475329,7.65100111271853));
#276344=CARTESIAN_POINT('Ctrl Pts',(1.56768109536323,1.16640129597011,7.6470829959281));
#276345=CARTESIAN_POINT('Ctrl Pts',(1.6085308770083,1.11149786723083,7.64317077916482));
#276346=CARTESIAN_POINT('Ctrl Pts',(1.64655643209863,1.05436055256439,7.63925856240154));
#276347=CARTESIAN_POINT('Ctrl Pts',(1.68150787662658,0.995312644771864,
7.63534634563826));
#276348=CARTESIAN_POINT('Ctrl Pts',(1.71641822045364,0.936334173605751,
7.63143872939587));
#276349=CARTESIAN_POINT('Ctrl Pts',(1.74826138372243,0.875449992650089,
7.62753111315349));
#276350=CARTESIAN_POINT('Ctrl Pts',(1.77683027071511,0.813013031304224,
7.62362349691111));
#276351=CARTESIAN_POINT('Ctrl Pts',(1.80538125193662,0.750615202807394,
7.61971832979746));
#276352=CARTESIAN_POINT('Ctrl Pts',(1.83066182355119,0.686666970751107,
7.61581316268382));
#276353=CARTESIAN_POINT('Ctrl Pts',(1.85251115741193,0.621545180710399,
7.61190799557018));
#276354=CARTESIAN_POINT('Ctrl Pts',(1.87435429099451,0.556441870556314,
7.60800393664238));
#276355=CARTESIAN_POINT('Ctrl Pts',(1.892767963391,0.490166129643999,7.60409987771457));
#276356=CARTESIAN_POINT('Ctrl Pts',(1.90764040955008,0.423112358424593,
7.60019581878677));
#276357=CARTESIAN_POINT('Ctrl Pts',(1.92251373613521,0.356054617724526,
7.59629152874465));
#276358=CARTESIAN_POINT('Ctrl Pts',(1.9338453162782,0.288219236039119,7.59238723870253));
#276359=CARTESIAN_POINT('Ctrl Pts',(1.94157434747052,0.220011484346647,
7.58848294866041));
#276360=CARTESIAN_POINT('Ctrl Pts',(1.94931161131259,0.151731080530541,
7.5845744999273));
#276361=CARTESIAN_POINT('Ctrl Pts',(1.95343861267395,0.0830780048401049,
7.58066605119418));
#276362=CARTESIAN_POINT('Ctrl Pts',(1.95394647852218,0.0144623328255586,
7.57675760246107));
#276363=CARTESIAN_POINT('Ctrl Pts',(1.95445464836289,-0.0541944103653153,
7.57284681425386));
#276364=CARTESIAN_POINT('Ctrl Pts',(1.95133939366496,-0.122813213881998,
7.56893602604665));
#276365=CARTESIAN_POINT('Ctrl Pts',(1.94464390303761,-0.19098714715567,
7.56502523783944));
#276366=CARTESIAN_POINT('Ctrl Pts',(1.93793685145502,-0.259278794848623,
7.56110769696093));
#276367=CARTESIAN_POINT('Ctrl Pts',(1.92763729962266,-0.327123553149722,
7.55719015608242));
#276368=CARTESIAN_POINT('Ctrl Pts',(1.91383975088898,-0.394123594722792,
7.55327261520391));
#276369=CARTESIAN_POINT('Ctrl Pts',(1.90732794232431,-0.425744533555481,
7.55142371604526));
#276370=CARTESIAN_POINT('Ctrl Pts',(1.90003771407892,-0.457177526489178,
7.54957481688661));
#276371=CARTESIAN_POINT('Ctrl Pts',(1.89198280763412,-0.488382079541124,
7.54772591772796));
#276372=CARTESIAN_POINT('Ctrl Pts',(1.87491315619368,-0.554509581778629,
7.54380780093753));
#276373=CARTESIAN_POINT('Ctrl Pts',(1.85433861754993,-0.61987217910844,
7.53988968414711));
#276374=CARTESIAN_POINT('Ctrl Pts',(1.83034489736836,-0.684071309643672,
7.53597156735668));
#276375=CARTESIAN_POINT('Ctrl Pts',(1.80638730770762,-0.748173767049212,
7.5320593505934));
#276376=CARTESIAN_POINT('Ctrl Pts',(1.77902092569981,-0.811115777686176,
7.52814713383011));
#276377=CARTESIAN_POINT('Ctrl Pts',(1.74838175314181,-0.872512031596563,
7.52423491706683));
#276378=CARTESIAN_POINT('Ctrl Pts',(1.71777861032403,-0.933836087373181,
7.52032730082445));
#276379=CARTESIAN_POINT('Ctrl Pts',(1.68391053892414,-0.993617558392718,
7.51641968458206));
#276380=CARTESIAN_POINT('Ctrl Pts',(1.64696165082001,-1.05149099888122,
7.51251206833968));
#276381=CARTESIAN_POINT('Ctrl Pts',(1.61003592071762,-1.10932816674273,
7.50860690122603));
#276382=CARTESIAN_POINT('Ctrl Pts',(1.57003346835176,-1.16525926264657,
7.50470173411239));
#276383=CARTESIAN_POINT('Ctrl Pts',(1.52718359803182,-1.21894473127479,
7.50079656699874));
#276384=CARTESIAN_POINT('Ctrl Pts',(1.48434588740137,-1.27261496534984,
7.49689250807094));
#276385=CARTESIAN_POINT('Ctrl Pts',(1.43866266958375,-1.32404045294532,
7.49298844914313));
#276386=CARTESIAN_POINT('Ctrl Pts',(1.39040461434827,-1.37291332880086,
7.48908439021533));
#276387=CARTESIAN_POINT('Ctrl Pts',(1.34214370230976,-1.42178909785585,
7.4851801001732));
#276388=CARTESIAN_POINT('Ctrl Pts',(1.29130799766047,-1.46811160696053,
7.48127581013109));
#276389=CARTESIAN_POINT('Ctrl Pts',(1.23820495112629,-1.51160990305249,
7.47737152008897));
#276390=CARTESIAN_POINT('Ctrl Pts',(1.18504534138621,-1.55515453176072,
7.47346307135585));
#276391=CARTESIAN_POINT('Ctrl Pts',(1.12961395125601,-1.59586863165535,
7.46955462262273));
#276392=CARTESIAN_POINT('Ctrl Pts',(1.07225044145295,-1.63352226516933,
7.46564617388961));
#276393=CARTESIAN_POINT('Ctrl Pts',(1.01485259566282,-1.67119843696031,
7.4617353856824));
#276394=CARTESIAN_POINT('Ctrl Pts',(0.955520753468631,-1.70581024866879,
7.45782459747519));
#276395=CARTESIAN_POINT('Ctrl Pts',(0.894620179441413,-1.73717320222717,
7.45391380926798));
#276396=CARTESIAN_POINT('Ctrl Pts',(0.833614449743095,-1.7685903095022,
7.44999626838946));
#276397=CARTESIAN_POINT('Ctrl Pts',(0.771035030420414,-1.7967471607843,
7.44607872751095));
#276398=CARTESIAN_POINT('Ctrl Pts',(0.707267379576142,-1.82150730269947,
7.44216118663244));
#276399=CARTESIAN_POINT('Ctrl Pts',(0.677171980536121,-1.83319295116478,
7.4403122874738));
#276400=CARTESIAN_POINT('Ctrl Pts',(0.646812134387758,-1.84412273682034,
7.43846338831516));
#276401=CARTESIAN_POINT('Ctrl Pts',(0.616229312545353,-1.8542862331258,
7.43661448915652));
#276402=CARTESIAN_POINT('Ctrl Pts',(0.551419359444688,-1.87582432801744,
7.43269637236609));
#276403=CARTESIAN_POINT('Ctrl Pts',(0.485350392409882,-1.89400322691309,
7.42877825557567));
#276404=CARTESIAN_POINT('Ctrl Pts',(0.41840371345753,-1.90867868761742,
7.42486013878524));
#276405=CARTESIAN_POINT('Ctrl Pts',(0.351557844982249,-1.92333204953779,
7.42094792202196));
#276406=CARTESIAN_POINT('Ctrl Pts',(0.283837364276381,-1.93449233896904,
7.41703570525867));
#276407=CARTESIAN_POINT('Ctrl Pts',(0.215639729230009,-1.94206475360056,
7.41312348849539));
#276408=CARTESIAN_POINT('Ctrl Pts',(0.147522290313935,-1.94962826354866,
7.409215872253));
#276409=CARTESIAN_POINT('Ctrl Pts',(0.0789292979784414,-1.95361222389878,
7.40530825601062));
#276410=CARTESIAN_POINT('Ctrl Pts',(0.0102676254828897,-1.95397302332119,
7.40140063976823));
#276411=CARTESIAN_POINT('Ctrl Pts',(-0.0583510127776918,-1.95433359660976,
7.39749547265459));
#276412=CARTESIAN_POINT('Ctrl Pts',(-0.127037755040009,-1.95107551102531,
7.39359030554095));
#276413=CARTESIAN_POINT('Ctrl Pts',(-0.195382957862223,-1.94420716483018,
7.3896851384273));
#276414=CARTESIAN_POINT('Ctrl Pts',(-0.263708766076322,-1.93734076769479,
7.3857810794995));
#276415=CARTESIAN_POINT('Ctrl Pts',(-0.331692738068321,-1.92686619291591,
7.38187702057169));
#276416=CARTESIAN_POINT('Ctrl Pts',(-0.398929408338525,-1.91284378012494,
7.37797296164389));
#276417=CARTESIAN_POINT('Ctrl Pts',(-0.466170058916744,-1.89882053722859,
7.37406867160176));
#276418=CARTESIAN_POINT('Ctrl Pts',(-0.532662838948834,-1.88124914227677,
7.37016438155964));
#276419=CARTESIAN_POINT('Ctrl Pts',(-0.598013334912811,-1.86024085840153,
7.36626009151752));
#276420=CARTESIAN_POINT('Ctrl Pts',(-0.663433439567792,-1.83921019735655,
7.3623516427844));
#276421=CARTESIAN_POINT('Ctrl Pts',(-0.727708362792241,-1.81473549232277,
7.35844319405129));
#276422=CARTESIAN_POINT('Ctrl Pts',(-0.790460669873548,-1.78697731641537,
7.35453474531817));
#276423=CARTESIAN_POINT('Ctrl Pts',(-0.853250538505934,-1.75920252533968,
7.35062395711096));
#276424=CARTESIAN_POINT('Ctrl Pts',(-0.914515538387683,-1.72814057438052,
7.34671316890375));
#276425=CARTESIAN_POINT('Ctrl Pts',(-0.973902514019989,-1.69399819751544,
7.34280238069653));
#276426=CARTESIAN_POINT('Ctrl Pts',(-1.03339203182661,-1.6597968677651,
7.33888483981802));
#276427=CARTESIAN_POINT('Ctrl Pts',(-1.09099664070203,-1.62250476359817,
7.33496729893951));
#276428=CARTESIAN_POINT('Ctrl Pts',(-1.14639258813295,-1.58237164846753,
7.33104975806099));
#276429=CARTESIAN_POINT('Ctrl Pts',(-1.17253692810868,-1.56343066352329,
7.32920085890236));
#276430=CARTESIAN_POINT('Ctrl Pts',(-1.19818979671896,-1.54385744700979,
7.32735195974373));
#276431=CARTESIAN_POINT('Ctrl Pts',(-1.22331993532184,-1.52368117919864,
7.3255030605851));
#276432=CARTESIAN_POINT('Ctrl Pts',(-1.27589864383253,-1.48146724155033,
7.32163468837022));
#276433=CARTESIAN_POINT('Ctrl Pts',(-1.32640679421288,-1.43643430037098,
7.31776631615534));
#276434=CARTESIAN_POINT('Ctrl Pts',(-1.37452068432708,-1.38881564232155,
7.31389794394046));
#276435=CARTESIAN_POINT('Ctrl Pts',(-1.42255195296738,-1.34127875533041,
7.31003621451862));
#276436=CARTESIAN_POINT('Ctrl Pts',(-1.46819676697969,-1.29116531828427,
7.30617448509677));
#276437=CARTESIAN_POINT('Ctrl Pts',(-1.51116392529286,-1.2387492041949,
7.30231275567492));
#276438=CARTESIAN_POINT('Ctrl Pts',(-1.55408997821229,-1.1863832350323,
7.29845472065398));
#276439=CARTESIAN_POINT('Ctrl Pts',(-1.59434313263755,-1.13171934287596,
7.29459668563303));
#276440=CARTESIAN_POINT('Ctrl Pts',(-1.63166963652991,-1.0750675314725,
7.29073865061208));
#276441=CARTESIAN_POINT('Ctrl Pts',(-1.66897401501377,-1.01844930061738,
7.28688290245414));
#276442=CARTESIAN_POINT('Ctrl Pts',(-1.70335490479476,-0.959845908057318,
7.2830271542962));
#276443=CARTESIAN_POINT('Ctrl Pts',(-1.73460062779139,-0.899598055837012,
7.27917140613825));
#276444=CARTESIAN_POINT('Ctrl Pts',(-1.76583919829406,-0.839363995021011,
7.275316540604));
#276445=CARTESIAN_POINT('Ctrl Pts',(-1.79394379459118,-0.777486670783983,
7.27146167506975));
#276446=CARTESIAN_POINT('Ctrl Pts',(-1.81874862909382,-0.714331452596999,
7.2676068095355));
#276447=CARTESIAN_POINT('Ctrl Pts',(-1.84357152823297,-0.651130240309164,
7.26374913661526));
#276448=CARTESIAN_POINT('Ctrl Pts',(-1.86508967956487,-0.586649746365874,
7.25989146369503));
#276449=CARTESIAN_POINT('Ctrl Pts',(-1.88318592322611,-0.521274187508859,
7.2560337907748));
#276450=CARTESIAN_POINT('Ctrl Pts',(-1.90128911181104,-0.455873539010295,
7.25217463736809));
#276451=CARTESIAN_POINT('Ctrl Pts',(-1.91596766743185,-0.389577635578429,
7.24831548396138));
#276452=CARTESIAN_POINT('Ctrl Pts',(-1.92715537849078,-0.322781887896566,
7.24445633055467));
#276453=CARTESIAN_POINT('Ctrl Pts',(-1.93836046069429,-0.255882426543101,
7.24059118504543));
#276454=CARTESIAN_POINT('Ctrl Pts',(-1.9460638204368,-0.188482074251308,
7.23672603953618));
#276455=CARTESIAN_POINT('Ctrl Pts',(-1.95025114287136,-0.120981319752049,
7.23286089402694));
#276456=CARTESIAN_POINT('Ctrl Pts',(-1.9527757926585,-0.0802832918018328,
7.23053049340943));
#276457=CARTESIAN_POINT('Ctrl Pts',(-1.95402330207662,-0.0395487931071784,
7.22820009279193));
#276458=CARTESIAN_POINT('Ctrl Pts',(-1.95399967035838,0.00113500632439505,
7.22586969217443));
#276459=CARTESIAN_POINT('',(-1.95399924754167,-0.00171481969227626,6.52586969212423));
#276460=CARTESIAN_POINT('Ctrl Pts',(-1.95399967035787,0.00113500720075899,
7.22586969212423));
#276461=CARTESIAN_POINT('Ctrl Pts',(-1.95396087209433,0.0679291157453965,
7.22204367208738));
#276462=CARTESIAN_POINT('Ctrl Pts',(-1.95049746579392,0.134622301780259,
7.21821765205052));
#276463=CARTESIAN_POINT('Ctrl Pts',(-1.94363877693846,0.200958465313502,
7.21439163201366));
#276464=CARTESIAN_POINT('Ctrl Pts',(-1.93661499146268,0.26889141748018,
7.21047351522322));
#276465=CARTESIAN_POINT('Ctrl Pts',(-1.92601146431731,0.33659035382485,
7.20655539843279));
#276466=CARTESIAN_POINT('Ctrl Pts',(-1.91185354481783,0.40364839051768,
7.20263728164236));
#276467=CARTESIAN_POINT('Ctrl Pts',(-1.89771694477201,0.470605449047257,
7.19872506487907));
#276468=CARTESIAN_POINT('Ctrl Pts',(-1.88003667562339,0.536923045882934,
7.19481284811578));
#276469=CARTESIAN_POINT('Ctrl Pts',(-1.85888979610215,0.602199905303309,
7.19090063135249));
#276470=CARTESIAN_POINT('Ctrl Pts',(-1.83776778398139,0.667400003241948,
7.1869930151101));
#276471=CARTESIAN_POINT('Ctrl Pts',(-1.81318740838512,0.731561328611459,
7.18308539886771));
#276472=CARTESIAN_POINT('Ctrl Pts',(-1.78527626127104,0.794295078004447,
7.17917778262532));
#276473=CARTESIAN_POINT('Ctrl Pts',(-1.75738260768456,0.856989508534178,
7.17527261551167));
#276474=CARTESIAN_POINT('Ctrl Pts',(-1.7261625231884,0.918257689577472,
7.17136744839802));
#276475=CARTESIAN_POINT('Ctrl Pts',(-1.69179214602062,0.977729683840544,
7.16746228128437));
#276476=CARTESIAN_POINT('Ctrl Pts',(-1.65743152228059,1.03718480148352,
7.16355822235656));
#276477=CARTESIAN_POINT('Ctrl Pts',(-1.61992262656499,1.09484431853679,
7.15965416342875));
#276478=CARTESIAN_POINT('Ctrl Pts',(-1.57948722349662,1.15036346900054,
7.15575010450094));
#276479=CARTESIAN_POINT('Ctrl Pts',(-1.53904942671422,1.20588590611308,
7.15184581445881));
#276480=CARTESIAN_POINT('Ctrl Pts',(-1.49568507028046,1.25926732898709,
7.14794152441668));
#276481=CARTESIAN_POINT('Ctrl Pts',(-1.4496577901743,1.31019398998277,7.14403723437455));
#276482=CARTESIAN_POINT('Ctrl Pts',(-1.40358148368096,1.36117489598693,
7.14012878564143));
#276483=CARTESIAN_POINT('Ctrl Pts',(-1.35483692331089,1.40969545633347,
7.13622033690831));
#276484=CARTESIAN_POINT('Ctrl Pts',(-1.30372570801213,1.45547768044318,
7.13231188817518));
#276485=CARTESIAN_POINT('Ctrl Pts',(-1.25258389915257,1.50128730834772,
7.12840109996797));
#276486=CARTESIAN_POINT('Ctrl Pts',(-1.19907299929902,1.54435502949446,
7.12449031176075));
#276487=CARTESIAN_POINT('Ctrl Pts',(-1.14352669733391,1.5844439694999,7.12057952355354));
#276488=CARTESIAN_POINT('Ctrl Pts',(-1.08788448480055,1.62460213018936,
7.11666198267502));
#276489=CARTESIAN_POINT('Ctrl Pts',(-1.03020026906842,1.66177097806323,
7.1127444417965));
#276490=CARTESIAN_POINT('Ctrl Pts',(-0.970834867316236,1.69575813735422,
7.10882690091799));
#276491=CARTESIAN_POINT('Ctrl Pts',(-0.942817127424808,1.71179851374448,
7.10697800175941));
#276492=CARTESIAN_POINT('Ctrl Pts',(-0.914425244627133,1.72713088028601,
7.10512910260083));
#276493=CARTESIAN_POINT('Ctrl Pts',(-0.885698673281844,1.74173874623802,
7.10328020344225));
#276494=CARTESIAN_POINT('Ctrl Pts',(-0.824822415646611,1.77269518028322,
7.09936208665183));
#276495=CARTESIAN_POINT('Ctrl Pts',(-0.762200570830366,1.8005175691438,
7.0954439698614));
#276496=CARTESIAN_POINT('Ctrl Pts',(-0.698188685542636,1.82500645461331,
7.09152585307098));
#276497=CARTESIAN_POINT('Ctrl Pts',(-0.634273191424624,1.84945846392608,
7.0876136363077));
#276498=CARTESIAN_POINT('Ctrl Pts',(-0.568972266745221,1.8705867578287,
7.08370141954441));
#276499=CARTESIAN_POINT('Ctrl Pts',(-0.502664801874807,1.88823835808834,
7.07978920278113));
#276500=CARTESIAN_POINT('Ctrl Pts',(-0.436435310413426,1.90586920117608,
7.07588158653875));
#276501=CARTESIAN_POINT('Ctrl Pts',(-0.369202102539755,1.92003134425622,
7.07197397029636));
#276502=CARTESIAN_POINT('Ctrl Pts',(-0.301361008030636,1.93062102517267,
7.06806635405398));
#276503=CARTESIAN_POINT('Ctrl Pts',(-0.233562433452862,1.9412040689246,
7.06416118694033));
#276504=CARTESIAN_POINT('Ctrl Pts',(-0.165157212921858,1.94821901642196,
7.06025601982669));
#276505=CARTESIAN_POINT('Ctrl Pts',(-0.0965516666476493,1.95161312141202,
7.05635085271304));
#276506=CARTESIAN_POINT('Ctrl Pts',(-0.0279655888603678,1.9550062632425,
7.05244679378524));
#276507=CARTESIAN_POINT('Ctrl Pts',(0.0408202107700112,1.95478057803995,
7.04854273485744));
#276508=CARTESIAN_POINT('Ctrl Pts',(0.109395802296484,1.9509353034993,7.04463867592963));
#276509=CARTESIAN_POINT('Ctrl Pts',(0.177975453393033,1.94708980132429,
7.04073438588751));
#276510=CARTESIAN_POINT('Ctrl Pts',(0.246344380716998,1.93962431450095,
7.03683009584539));
#276511=CARTESIAN_POINT('Ctrl Pts',(0.314095993548228,1.92859008263471,
7.03292580580327));
#276512=CARTESIAN_POINT('Ctrl Pts',(0.381919772642543,1.91754409755336,
7.02901735707015));
#276513=CARTESIAN_POINT('Ctrl Pts',(0.44912443858583,1.90292186046582,7.02510890833704));
#276514=CARTESIAN_POINT('Ctrl Pts',(0.51531284099487,1.88482590068839,7.02120045960392));
#276515=CARTESIAN_POINT('Ctrl Pts',(0.581540861693244,1.86671910924039,
7.01728967139671));
#276516=CARTESIAN_POINT('Ctrl Pts',(0.646750941193973,1.84513461157647,
7.0133788831895));
#276517=CARTESIAN_POINT('Ctrl Pts',(0.710563057650473,1.82022420077924,
7.00946809498229));
#276518=CARTESIAN_POINT('Ctrl Pts',(0.774485357073851,1.7952707777279,7.00555055410378));
#276519=CARTESIAN_POINT('Ctrl Pts',(0.837004427936686,1.76698018255334,
7.00163301322526));
#276520=CARTESIAN_POINT('Ctrl Pts',(0.89776291016151,1.73555113930369,6.99771547234675));
#276521=CARTESIAN_POINT('Ctrl Pts',(0.926438119980652,1.72071807605725,
6.9958665731881));
#276522=CARTESIAN_POINT('Ctrl Pts',(0.95472157101878,1.70518659608866,6.99401767402945));
#276523=CARTESIAN_POINT('Ctrl Pts',(0.982578004880193,1.68898089519262,
6.9921687748708));
#276524=CARTESIAN_POINT('Ctrl Pts',(1.04161030024528,1.65463839009477,6.98825065808037));
#276525=CARTESIAN_POINT('Ctrl Pts',(1.0989569691907,1.61712918681125,6.98433254128995));
#276526=CARTESIAN_POINT('Ctrl Pts',(1.15425756165627,1.57664373951737,6.98041442449952));
#276527=CARTESIAN_POINT('Ctrl Pts',(1.20947488069895,1.53621925652104,6.97650220773624));
#276528=CARTESIAN_POINT('Ctrl Pts',(1.26265184435615,1.4928277123745,6.97258999097296));
#276529=CARTESIAN_POINT('Ctrl Pts',(1.31345438206221,1.44670438799417,6.96867777420967));
#276530=CARTESIAN_POINT('Ctrl Pts',(1.36419717917855,1.40063530174292,6.96477015796729));
#276531=CARTESIAN_POINT('Ctrl Pts',(1.4125707331932,1.35184114420746,6.96086254172491));
#276532=CARTESIAN_POINT('Ctrl Pts',(1.45827312602572,1.30059812775168,6.95695492548252));
#276533=CARTESIAN_POINT('Ctrl Pts',(1.50394687452962,1.24938722825329,6.95304975836888));
#276534=CARTESIAN_POINT('Ctrl Pts',(1.54695245621044,1.19573088073896,6.94914459125524));
#276535=CARTESIAN_POINT('Ctrl Pts',(1.5870251162277,1.13994178819028,6.9452394241416));
#276536=CARTESIAN_POINT('Ctrl Pts',(1.62708640465622,1.08416852714908,6.9413353652138));
#276537=CARTESIAN_POINT('Ctrl Pts',(1.66421613683263,1.02626412184942,6.93743130628599));
#276538=CARTESIAN_POINT('Ctrl Pts',(1.69819126741979,0.966572511123276,
6.93352724735819));
#276539=CARTESIAN_POINT('Ctrl Pts',(1.7321684092827,0.906877366745105,6.92962295731607));
#276540=CARTESIAN_POINT('Ctrl Pts',(1.76299033771203,0.845395235643157,
6.92571866727396));
#276541=CARTESIAN_POINT('Ctrl Pts',(1.79047950208093,0.78249546492489,6.92181437723184));
#276542=CARTESIAN_POINT('Ctrl Pts',(1.81799794678996,0.71952869592848,6.91790592849873));
#276543=CARTESIAN_POINT('Ctrl Pts',(1.84217634553217,0.65514172538121,6.91399747976561));
#276544=CARTESIAN_POINT('Ctrl Pts',(1.86288535424368,0.589723797166438,
6.91008903103249));
#276545=CARTESIAN_POINT('Ctrl Pts',(1.8836067587144,0.524266711843878,6.90617824282529));
#276546=CARTESIAN_POINT('Ctrl Pts',(1.90085451667714,0.457777916899523,
6.90226745461808));
#276547=CARTESIAN_POINT('Ctrl Pts',(1.91454995996751,0.390658995529884,
6.89835666641087));
#276548=CARTESIAN_POINT('Ctrl Pts',(1.9282690508762,0.323424181406629,6.89443912553236));
#276549=CARTESIAN_POINT('Ctrl Pts',(1.93842351247812,0.255557555540475,
6.89052158465385));
#276550=CARTESIAN_POINT('Ctrl Pts',(1.94498639491301,0.187467126727044,
6.88660404377534));
#276551=CARTESIAN_POINT('Ctrl Pts',(1.94808377364842,0.155331575254947,
6.88475514461669));
#276552=CARTESIAN_POINT('Ctrl Pts',(1.95038191682708,0.123146190208738,
6.88290624545804));
#276553=CARTESIAN_POINT('Ctrl Pts',(1.95188202035471,0.0909537168894154,
6.88105734629938));
#276554=CARTESIAN_POINT('Ctrl Pts',(1.95506098270725,0.022732651588192,
6.87713922950896));
#276555=CARTESIAN_POINT('Ctrl Pts',(1.95466530531591,-0.0457905139071906,
6.87322111271853));
#276556=CARTESIAN_POINT('Ctrl Pts',(1.9506594149489,-0.114209661899562,
6.86930299592811));
#276557=CARTESIAN_POINT('Ctrl Pts',(1.94665955678132,-0.182525782123295,
6.86539077916482));
#276558=CARTESIAN_POINT('Ctrl Pts',(1.93906030343754,-0.250737708615958,
6.86147856240154));
#276559=CARTESIAN_POINT('Ctrl Pts',(1.92787804941269,-0.31843716270677,
6.85756634563826));
#276560=CARTESIAN_POINT('Ctrl Pts',(1.91670894501538,-0.386057006496763,
6.85365872939587));
#276561=CARTESIAN_POINT('Ctrl Pts',(1.90196528756213,-0.453165091721353,
6.84975111315348));
#276562=CARTESIAN_POINT('Ctrl Pts',(1.88371529922209,-0.519357941574634,
6.8458434969111));
#276563=CARTESIAN_POINT('Ctrl Pts',(1.86547674920357,-0.585509304546669,
6.84193832979745));
#276564=CARTESIAN_POINT('Ctrl Pts',(1.84373635812278,-0.650746096925991,
6.83803316268381));
#276565=CARTESIAN_POINT('Ctrl Pts',(1.81861316395814,-0.71467626228816,
6.83412799557017));
#276566=CARTESIAN_POINT('Ctrl Pts',(1.79349709910888,-0.778588285916091,
6.83022393664236));
#276567=CARTESIAN_POINT('Ctrl Pts',(1.76500031666709,-0.84119396101884,
6.82631987771455));
#276568=CARTESIAN_POINT('Ctrl Pts',(1.7332907228189,-0.902119321481338,
6.82241581878675));
#276569=CARTESIAN_POINT('Ctrl Pts',(1.70157925181126,-0.963048288631953,
6.81851152874463));
#276570=CARTESIAN_POINT('Ctrl Pts',(1.66665482116111,-1.02229630852045,
6.81460723870251));
#276571=CARTESIAN_POINT('Ctrl Pts',(1.62873136358012,-1.07951384673401,
6.81070294866039));
#276572=CARTESIAN_POINT('Ctrl Pts',(1.59076751147415,-1.13679233074269,
6.80679449992727));
#276573=CARTESIAN_POINT('Ctrl Pts',(1.54979852958826,-1.19203560603691,
6.80288605119415));
#276574=CARTESIAN_POINT('Ctrl Pts',(1.50608121864768,-1.24492383816711,
6.79897760246103));
#276575=CARTESIAN_POINT('Ctrl Pts',(1.46233773990412,-1.29784372752434,
6.79506681425382));
#276576=CARTESIAN_POINT('Ctrl Pts',(1.41584299111794,-1.34840540612791,
6.79115602604661));
#276577=CARTESIAN_POINT('Ctrl Pts',(1.36689163227498,-1.39632491405712,
6.7872452378394));
#276578=CARTESIAN_POINT('Ctrl Pts',(1.31785575020588,-1.44432716353839,
6.78332769696088));
#276579=CARTESIAN_POINT('Ctrl Pts',(1.26635516113751,-1.48967781207289,
6.77941015608237));
#276580=CARTESIAN_POINT('Ctrl Pts',(1.21271798218434,-1.53213285836664,
6.77549261520385));
#276581=CARTESIAN_POINT('Ctrl Pts',(1.18740370005856,-1.55216968805304,
6.77364371604522));
#276582=CARTESIAN_POINT('Ctrl Pts',(1.16161393600949,-1.57156217481763,
6.77179481688659));
#276583=CARTESIAN_POINT('Ctrl Pts',(1.13538524609547,-1.59028813205304,
6.76994591772795));
#276584=CARTESIAN_POINT('Ctrl Pts',(1.07980240380627,-1.62997146854989,
6.76602780093753));
#276585=CARTESIAN_POINT('Ctrl Pts',(1.02202639017435,-1.66681591207812,
6.7621096841471));
#276586=CARTESIAN_POINT('Ctrl Pts',(0.962379055182175,-1.70057124347869,
6.75819156735668));
#276587=CARTESIAN_POINT('Ctrl Pts',(0.902821539078585,-1.73427574500814,
6.7542793505934));
#276588=CARTESIAN_POINT('Ctrl Pts',(0.841398718781946,-1.76490012604718,
6.75036713383011));
#276589=CARTESIAN_POINT('Ctrl Pts',(0.77846245432362,-1.7922366493319,6.74645491706683));
#276590=CARTESIAN_POINT('Ctrl Pts',(0.715600198954619,-1.81954102658427,
6.74254730082445));
#276591=CARTESIAN_POINT('Ctrl Pts',(0.651228482988933,-1.84356502960705,
6.73863968458206));
#276592=CARTESIAN_POINT('Ctrl Pts',(0.585723251546375,-1.86414706302854,
6.73473206833968));
#276593=CARTESIAN_POINT('Ctrl Pts',(0.520259076014899,-1.8847161965012,
6.73082690122604));
#276594=CARTESIAN_POINT('Ctrl Pts',(0.45366326250104,-1.90184749262005,
6.72692173411239));
#276595=CARTESIAN_POINT('Ctrl Pts',(0.38632973249629,-1.91542823874698,
6.72301656699875));
#276596=CARTESIAN_POINT('Ctrl Pts',(0.319015310012996,-1.92900513100796,
6.71911250807095));
#276597=CARTESIAN_POINT('Ctrl Pts',(0.250964068568436,-1.93903337624113,
6.71520844914314));
#276598=CARTESIAN_POINT('Ctrl Pts',(0.182581246443851,-1.94545112723168,
6.71130439021534));
#276599=CARTESIAN_POINT('Ctrl Pts',(0.114194376160842,-1.95186925814327,
6.70740010017322));
#276600=CARTESIAN_POINT('Ctrl Pts',(0.0454763761929554,-1.95467642706471,
6.7034958101311));
#276601=CARTESIAN_POINT('Ctrl Pts',(-0.0231630670702663,-1.95386270559727,
6.69959152008898));
#276602=CARTESIAN_POINT('Ctrl Pts',(-0.0918756222774577,-1.95304811738682,
6.69568307135586));
#276603=CARTESIAN_POINT('Ctrl Pts',(-0.160508961000291,-1.94860494760029,
6.69177462262275));
#276604=CARTESIAN_POINT('Ctrl Pts',(-0.228655087856236,-1.94057539168089,
6.68786617388963));
#276605=CARTESIAN_POINT('Ctrl Pts',(-0.296842004833592,-1.93254102952267,
6.68395538568242));
#276606=CARTESIAN_POINT('Ctrl Pts',(-0.364540644696712,-1.92091609216458,
6.68004459747521));
#276607=CARTESIAN_POINT('Ctrl Pts',(-0.431352607342982,-1.90579404137446,
6.676133809268));
#276608=CARTESIAN_POINT('Ctrl Pts',(-0.498279932724058,-1.89064587967447,
6.67221626838949));
#276609=CARTESIAN_POINT('Ctrl Pts',(-0.564317052146925,-1.87198868655183,
6.66829872751097));
#276610=CARTESIAN_POINT('Ctrl Pts',(-0.629080979892976,-1.84996570798945,
6.66438118663246));
#276611=CARTESIAN_POINT('Ctrl Pts',(-0.65964657582003,-1.83957187476661,
6.66253228747381));
#276612=CARTESIAN_POINT('Ctrl Pts',(-0.689928875796084,-1.8284290393646,
6.66068338831517));
#276613=CARTESIAN_POINT('Ctrl Pts',(-0.71988940919612,-1.81655587266873,
6.65883448915652));
#276614=CARTESIAN_POINT('Ctrl Pts',(-0.783380632292711,-1.79139470929808,
6.6549163723661));
#276615=CARTESIAN_POINT('Ctrl Pts',(-0.845676998981992,-1.76285099777674,
6.65099825557567));
#276616=CARTESIAN_POINT('Ctrl Pts',(-0.906393700561943,-1.73105934605999,
6.64708013878525));
#276617=CARTESIAN_POINT('Ctrl Pts',(-0.967018972966463,-1.6993155672419,
6.64316792202197));
#276618=CARTESIAN_POINT('Ctrl Pts',(-1.02606886890676,-1.66433378117181,
6.63925570525869));
#276619=CARTESIAN_POINT('Ctrl Pts',(-1.0831779838716,-1.62629685336222,
6.63534348849541));
#276620=CARTESIAN_POINT('Ctrl Pts',(-1.14021994210852,-1.5883046545878,
6.63143587225302));
#276621=CARTESIAN_POINT('Ctrl Pts',(-1.19532524447755,-1.54726472051837,
6.62752825601064));
#276622=CARTESIAN_POINT('Ctrl Pts',(-1.2481541797073,-1.50340518280309,
6.62362063976826));
#276623=CARTESIAN_POINT('Ctrl Pts',(-1.30095000399279,-1.45957313439273,
6.61971547265461));
#276624=CARTESIAN_POINT('Ctrl Pts',(-1.35147191371725,-1.412925301409,6.61581030554097));
#276625=CARTESIAN_POINT('Ctrl Pts',(-1.39941150747801,-1.36373143717454,
6.61190513842733));
#276626=CARTESIAN_POINT('Ctrl Pts',(-1.44733749721686,-1.31455153289164,
6.60800107949952));
#276627=CARTESIAN_POINT('Ctrl Pts',(-1.49268228258494,-1.26282738374907,
6.60409702057172));
#276628=CARTESIAN_POINT('Ctrl Pts',(-1.53517405067746,-1.20886584620733,
6.60019296164392));
#276629=CARTESIAN_POINT('Ctrl Pts',(-1.57766833421764,-1.15490111422513,
6.5962886716018));
#276630=CARTESIAN_POINT('Ctrl Pts',(-1.61730896287684,-1.09869911891853,
6.59238438155968));
#276631=CARTESIAN_POINT('Ctrl Pts',(-1.65386532368805,-1.04059862151659,
6.58848009151756));
#276632=CARTESIAN_POINT('Ctrl Pts',(-1.69046062284836,-0.982436237827272,
6.58457164278445));
#276633=CARTESIAN_POINT('Ctrl Pts',(-1.72396483539274,-0.922371733469224,
6.58066319405133));
#276634=CARTESIAN_POINT('Ctrl Pts',(-1.75419205125869,-0.860770728650109,
6.57675474531821));
#276635=CARTESIAN_POINT('Ctrl Pts',(-1.78443736018233,-0.799132851413129,
6.572843957111));
#276636=CARTESIAN_POINT('Ctrl Pts',(-1.81140157555279,-0.7359570957995,
6.56893316890379));
#276637=CARTESIAN_POINT('Ctrl Pts',(-1.83494705828878,-0.671628835948359,
6.56502238069658));
#276638=CARTESIAN_POINT('Ctrl Pts',(-1.85853319648786,-0.607189501916973,
6.56110483981807));
#276639=CARTESIAN_POINT('Ctrl Pts',(-1.87868867611599,-0.541594161854998,
6.55718729893955));
#276640=CARTESIAN_POINT('Ctrl Pts',(-1.89532604117965,-0.475242251516302,
6.55326975806104));
#276641=CARTESIAN_POINT('Ctrl Pts',(-1.90317811247189,-0.443927200823934,
6.55142085890239));
#276642=CARTESIAN_POINT('Ctrl Pts',(-1.91024730087751,-0.412443759971224,
6.54957195974374));
#276643=CARTESIAN_POINT('Ctrl Pts',(-1.91652841845126,-0.380834375114328,
6.54772306058509));
#276644=CARTESIAN_POINT('Ctrl Pts',(-1.93574599944975,-0.284122936955839,
6.54206620590562));
#276645=CARTESIAN_POINT('Ctrl Pts',(-1.94764796351427,-0.185913139877314,
6.53640935122614));
#276646=CARTESIAN_POINT('Ctrl Pts',(-1.95205706279423,-0.0871161500250206,
6.53075249654666));
#276647=CARTESIAN_POINT('Ctrl Pts',(-1.9533256576043,-0.0586900836973724,
6.52912489507252));
#276648=CARTESIAN_POINT('Ctrl Pts',(-1.95397423542428,-0.0302155762360542,
6.52749729359838));
#276649=CARTESIAN_POINT('Ctrl Pts',(-1.95399924754167,-0.00171481969227626,
6.52586969212423));
#276650=CARTESIAN_POINT('',(-1.95079791861852,-3.56937016110504E-5,5.82586969212423));
#276651=CARTESIAN_POINT('Ctrl Pts',(-1.95471132575424,-0.00170873845395426,
6.52586930929363));
#276652=CARTESIAN_POINT('Ctrl Pts',(-1.94992942299147,0.519479667493671,
6.49611675020031));
#276653=CARTESIAN_POINT('Ctrl Pts',(-1.4674451005583,1.69727522902121,6.42932704824985));
#276654=CARTESIAN_POINT('Ctrl Pts',(0.521340871742519,2.24972451098197,
6.32550020344223));
#276655=CARTESIAN_POINT('Ctrl Pts',(2.17268068147358,0.782633590011064,
6.21438877487081));
#276656=CARTESIAN_POINT('Ctrl Pts',(1.83620829950793,-1.40049839724295,
6.10327734629938));
#276657=CARTESIAN_POINT('Ctrl Pts',(-0.180233566874121,-2.3022972312962,
5.99216591772794));
#276658=CARTESIAN_POINT('Ctrl Pts',(-1.72112656933261,-1.29980337605498,
5.89969669966956));
#276659=CARTESIAN_POINT('Ctrl Pts',(-1.95085071127348,-0.323906799394953,
5.84426462446833));
#276660=CARTESIAN_POINT('Ctrl Pts',(-1.95079791861852,-3.56937016110504E-5,
5.82586969212423));
#276661=CARTESIAN_POINT('',(-1.9539992304742,0.00173415865262049,5.12586969212423));
#276662=CARTESIAN_POINT('Ctrl Pts',(-1.95079791861852,-3.56937016110504E-5,
5.82586969212423));
#276663=CARTESIAN_POINT('Ctrl Pts',(-1.95074441628598,0.328189124878196,
5.80722748161118));
#276664=CARTESIAN_POINT('Ctrl Pts',(-1.71657185386281,1.30858158663414,
5.75154812824101));
#276665=CARTESIAN_POINT('Ctrl Pts',(-0.164899398794644,2.30344630242157,
5.65883163201366));
#276666=CARTESIAN_POINT('Ctrl Pts',(1.84549300971326,1.3882406963353,5.54772020344223));
#276667=CARTESIAN_POINT('Ctrl Pts',(2.167421238611,-0.797083342116639,5.43660877487082));
#276668=CARTESIAN_POINT('Ctrl Pts',(0.506349204565716,-2.25314605893584,
5.32549734629937));
#276669=CARTESIAN_POINT('Ctrl Pts',(-1.47398685042411,-1.68881353075032,
5.22191775663669));
#276670=CARTESIAN_POINT('Ctrl Pts',(-1.94982006439799,-0.51521705165863,
5.15537530983116));
#276671=CARTESIAN_POINT('Ctrl Pts',(-1.95458041427723,0.00172917730281742,
5.12587000588275));
#276672=CARTESIAN_POINT('',(-1.95399970505248,-0.00107361763076356,4.42586969212423));
#276673=CARTESIAN_POINT('Ctrl Pts',(-1.9539992304742,0.00173415865262049,
5.12586969212423));
#276674=CARTESIAN_POINT('Ctrl Pts',(-1.9539127601795,0.0991663567078893,
5.12030693244776));
#276675=CARTESIAN_POINT('Ctrl Pts',(-1.94653542196257,0.196286002198207,
5.11474417277129));
#276676=CARTESIAN_POINT('Ctrl Pts',(-1.93202691376388,0.292212259311616,
5.10918141309482));
#276677=CARTESIAN_POINT('Ctrl Pts',(-1.92689153376234,0.326165976375911,
5.10721243844872));
#276678=CARTESIAN_POINT('Ctrl Pts',(-1.92086312817625,0.359970460063155,
5.10524346380262));
#276679=CARTESIAN_POINT('Ctrl Pts',(-1.91395009125867,0.393587408552323,
5.10327448915652));
#276680=CARTESIAN_POINT('Ctrl Pts',(-1.9001936490042,0.460482698737512,
5.0993563723661));
#276681=CARTESIAN_POINT('Ctrl Pts',(-1.88289858598141,0.52678851722377,
5.09543825557568));
#276682=CARTESIAN_POINT('Ctrl Pts',(-1.86213065986891,0.592102529614751,
5.09152013878526));
#276683=CARTESIAN_POINT('Ctrl Pts',(-1.84139400677205,0.657318190050875,
5.08760792202197));
#276684=CARTESIAN_POINT('Ctrl Pts',(-1.81719501724086,0.721544543465094,
5.08369570525869));
#276685=CARTESIAN_POINT('Ctrl Pts',(-1.78965034244472,0.784389987052042,
5.07978348849541));
#276686=CARTESIAN_POINT('Ctrl Pts',(-1.76213805845403,0.847161528349269,
5.07587587225303));
#276687=CARTESIAN_POINT('Ctrl Pts',(-1.73128809932901,0.908554936461109,
5.07196825601064));
#276688=CARTESIAN_POINT('Ctrl Pts',(-1.69726615556976,0.968196053058186,
5.06806063976826));
#276689=CARTESIAN_POINT('Ctrl Pts',(-1.66326553532723,1.02779978912358,
5.06415547265462));
#276690=CARTESIAN_POINT('Ctrl Pts',(-1.6260971173185,1.08565298598435,5.06025030554098));
#276691=CARTESIAN_POINT('Ctrl Pts',(-1.58597301735029,1.1414050938369,5.05634513842733));
#276692=CARTESIAN_POINT('Ctrl Pts',(-1.54586030356815,1.19714138067728,
5.05244107949953));
#276693=CARTESIAN_POINT('Ctrl Pts',(-1.50279386007308,1.25077736308912,
5.04853702057173));
#276694=CARTESIAN_POINT('Ctrl Pts',(-1.45702869447512,1.30199208272406,
5.04463296164393));
#276695=CARTESIAN_POINT('Ctrl Pts',(-1.41126081964942,1.353209834192,5.04072867160181));
#276696=CARTESIAN_POINT('Ctrl Pts',(-1.36279423520233,1.40200567324579,
5.0368243815597));
#276697=CARTESIAN_POINT('Ctrl Pts',(-1.31192252170383,1.44809367688913,
5.03292009151758));
#276698=CARTESIAN_POINT('Ctrl Pts',(-1.2609966217246,1.49423077159996,5.02901164278447));
#276699=CARTESIAN_POINT('Ctrl Pts',(-1.20766084527101,1.53765394389409,
5.02510319405135));
#276700=CARTESIAN_POINT('Ctrl Pts',(-1.15224298485108,1.57811663189432,
5.02119474531824));
#276701=CARTESIAN_POINT('Ctrl Pts',(-1.09679195304843,1.61860353958292,
5.01728395711103));
#276702=CARTESIAN_POINT('Ctrl Pts',(-1.03925676903407,1.65612616753363,
5.01337316890382));
#276703=CARTESIAN_POINT('Ctrl Pts',(-0.979993059549189,1.69048206238204,
5.00946238069661));
#276704=CARTESIAN_POINT('Ctrl Pts',(-0.920627020730927,1.72489727879246,
5.0055448398181));
#276705=CARTESIAN_POINT('Ctrl Pts',(-0.859526937376322,1.75613462520569,
5.00162729893959));
#276706=CARTESIAN_POINT('Ctrl Pts',(-0.797070996541357,1.78403862807748,
4.99770975806108));
#276707=CARTESIAN_POINT('Ctrl Pts',(-0.767594664310405,1.79720803435375,
4.99586085890241));
#276708=CARTESIAN_POINT('Ctrl Pts',(-0.737816583548416,1.80963568009972,
4.99401195974375));
#276709=CARTESIAN_POINT('Ctrl Pts',(-0.707777655179647,1.82130908712069,
4.99216306058509));
#276710=CARTESIAN_POINT('Ctrl Pts',(-0.644120300446923,1.8460469273842,
4.98824494379466));
#276711=CARTESIAN_POINT('Ctrl Pts',(-0.57903826112679,1.86749241474253,
4.98432682700424));
#276712=CARTESIAN_POINT('Ctrl Pts',(-0.512905185589397,1.88548250339151,
4.98040871021381));
#276713=CARTESIAN_POINT('Ctrl Pts',(-0.446871695378696,1.90344550198243,
4.97649649345053));
#276714=CARTESIAN_POINT('Ctrl Pts',(-0.379790780832813,1.91796330040063,
4.97258427668724));
#276715=CARTESIAN_POINT('Ctrl Pts',(-0.312054687442142,1.92892142713108,
4.96867205992396));
#276716=CARTESIAN_POINT('Ctrl Pts',(-0.244398247437811,1.93986666779357,
4.96476444368157));
#276717=CARTESIAN_POINT('Ctrl Pts',(-0.176088641980505,1.94726047194811,
4.96085682743919));
#276718=CARTESIAN_POINT('Ctrl Pts',(-0.107530068709893,1.95103902685806,
4.9569492111968));
#276719=CARTESIAN_POINT('Ctrl Pts',(-0.0390144650559959,1.95481521352946,
4.95304404408316));
#276720=CARTESIAN_POINT('Ctrl Pts',(0.029749306840273,1.95498061874556,
4.94913887696951));
#276721=CARTESIAN_POINT('Ctrl Pts',(0.0983516933838985,1.95152323696351,
4.94523370985587));
#276722=CARTESIAN_POINT('Ctrl Pts',(0.166934612337252,1.94806683629734,
4.94132965092806));
#276723=CARTESIAN_POINT('Ctrl Pts',(0.235355745827034,1.94098971424263,
4.93742559200026));
#276724=CARTESIAN_POINT('Ctrl Pts',(0.303207127208492,1.93033195021218,
4.93352153307245));
#276725=CARTESIAN_POINT('Ctrl Pts',(0.371062525287945,1.91967355525841,
4.92961724303033));
#276726=CARTESIAN_POINT('Ctrl Pts',(0.438347618774167,1.90543417635696,
4.92571295298821));
#276727=CARTESIAN_POINT('Ctrl Pts',(0.504662944157557,1.88770530348204,
4.92180866294609));
#276728=CARTESIAN_POINT('Ctrl Pts',(0.571048905929022,1.86995754653263,
4.91790021421297));
#276729=CARTESIAN_POINT('Ctrl Pts',(0.636462562030419,1.84871300517614,
4.91399176547985));
#276730=CARTESIAN_POINT('Ctrl Pts',(0.700518951896146,1.82411326348841,
4.91008331674673));
#276731=CARTESIAN_POINT('Ctrl Pts',(0.764613683895754,1.79949879717146,
4.90617252853952));
#276732=CARTESIAN_POINT('Ctrl Pts',(0.827349083496318,1.77152533394545,
4.90226174033231));
#276733=CARTESIAN_POINT('Ctrl Pts',(0.888362141202018,1.74038177020991,
4.8983509521251));
#276734=CARTESIAN_POINT('Ctrl Pts',(0.949480548801892,1.70918443157326,
4.89443341124659));
#276735=CARTESIAN_POINT('Ctrl Pts',(1.00887025354459,1.67480631400611,4.89051587036808));
#276736=CARTESIAN_POINT('Ctrl Pts',(1.06619547031322,1.63748075380555,4.88659832948956));
#276737=CARTESIAN_POINT('Ctrl Pts',(1.0932503367049,1.61986480569153,4.88474943033093));
#276738=CARTESIAN_POINT('Ctrl Pts',(1.11984581569148,1.60159294289382,4.88290053117229));
#276739=CARTESIAN_POINT('Ctrl Pts',(1.1459492347009,1.58269275334426,4.88105163201366));
#276740=CARTESIAN_POINT('Ctrl Pts',(1.20126660765259,1.54264019035267,4.87713351522323));
#276741=CARTESIAN_POINT('Ctrl Pts',(1.25459126761568,1.49960460728557,4.87321539843281));
#276742=CARTESIAN_POINT('Ctrl Pts',(1.3055835310031,1.45381141953607,4.86929728164238));
#276743=CARTESIAN_POINT('Ctrl Pts',(1.35649900858906,1.40808718865157,4.86538506487909));
#276744=CARTESIAN_POINT('Ctrl Pts',(1.40508869704579,1.35961392031835,4.86147284811581));
#276745=CARTESIAN_POINT('Ctrl Pts',(1.45104362676979,1.30865900570422,4.85756063135253));
#276746=CARTESIAN_POINT('Ctrl Pts',(1.49694451638626,1.25776401086545,4.85365301511014));
#276747=CARTESIAN_POINT('Ctrl Pts',(1.54021647269384,1.2043935289965,4.84974539886775));
#276748=CARTESIAN_POINT('Ctrl Pts',(1.58058659628917,1.14885247600856,4.84583778262537));
#276749=CARTESIAN_POINT('Ctrl Pts',(1.62093141759691,1.0933462338057,4.84193261551172));
#276750=CARTESIAN_POINT('Ctrl Pts',(1.6583777254558,1.0356725161171,4.83802744839808));
#276751=CARTESIAN_POINT('Ctrl Pts',(1.69269323408757,0.976168845678951,
4.83412228128443));
#276752=CARTESIAN_POINT('Ctrl Pts',(1.72699900486188,0.916682060849792,
4.83021822235663));
#276753=CARTESIAN_POINT('Ctrl Pts',(1.75817549450015,0.8553667800591,4.82631416342882));
#276754=CARTESIAN_POINT('Ctrl Pts',(1.78603503100773,0.792587451334697,
4.82241010450102));
#276755=CARTESIAN_POINT('Ctrl Pts',(1.81389621675724,0.729804406170085,
4.81850581445889));
#276756=CARTESIAN_POINT('Ctrl Pts',(1.83843986236296,0.665557591639494,
4.81460152441677));
#276757=CARTESIAN_POINT('Ctrl Pts',(1.85952609543786,0.600232205388584,
4.81069723437465));
#276758=CARTESIAN_POINT('Ctrl Pts',(1.88063478871081,0.534837237192506,
4.80678878564153));
#276759=CARTESIAN_POINT('Ctrl Pts',(1.8982785685469,0.468361873522238,4.80288033690841));
#276760=CARTESIAN_POINT('Ctrl Pts',(1.91236751146388,0.401206307399874,
4.79897188817529));
#276761=CARTESIAN_POINT('Ctrl Pts',(1.92646488757756,0.334010544074505,
4.79506109996808));
#276762=CARTESIAN_POINT('Ctrl Pts',(1.93700311655821,0.266134254121011,
4.79115031176087));
#276763=CARTESIAN_POINT('Ctrl Pts',(1.94394392799346,0.197984860071106,
4.78723952355366));
#276764=CARTESIAN_POINT('Ctrl Pts',(1.95089672397394,0.129717793973247,
4.78332198267515));
#276765=CARTESIAN_POINT('Ctrl Pts',(1.95423968114099,0.0611771736502074,
4.77940444179663));
#276766=CARTESIAN_POINT('Ctrl Pts',(1.95398663023682,-0.00722833699840476,
4.77548690091812));
#276767=CARTESIAN_POINT('Ctrl Pts',(1.95386720184582,-0.0395125926082593,
4.77363800175949));
#276768=CARTESIAN_POINT('Ctrl Pts',(1.95294754928242,-0.0717668126698533,
4.77178910260086));
#276769=CARTESIAN_POINT('Ctrl Pts',(1.95123312086349,-0.103948583661862,
4.76994020344222));
#276770=CARTESIAN_POINT('Ctrl Pts',(1.94759996935126,-0.172146968998725,
4.7660220866518));
#276771=CARTESIAN_POINT('Ctrl Pts',(1.94037986481757,-0.240289839943688,
4.76210396986138));
#276772=CARTESIAN_POINT('Ctrl Pts',(1.92957786913664,-0.307969555213016,
4.75818585307095));
#276773=CARTESIAN_POINT('Ctrl Pts',(1.9187921394506,-0.375547356175459,
4.75427363630767));
#276774=CARTESIAN_POINT('Ctrl Pts',(1.90443530015851,-0.442662903798645,
4.75036141954439));
#276775=CARTESIAN_POINT('Ctrl Pts',(1.88656433762187,-0.508911583689494,
4.7464492027811));
#276776=CARTESIAN_POINT('Ctrl Pts',(1.86871439021339,-0.575082359298746,
4.74254158653872));
#276777=CARTESIAN_POINT('Ctrl Pts',(1.84735865404818,-0.640387819027977,
4.73863397029634));
#276778=CARTESIAN_POINT('Ctrl Pts',(1.82260520696893,-0.704433289623483,
4.73472635405396));
#276779=CARTESIAN_POINT('Ctrl Pts',(1.79786727430432,-0.768438619224335,
4.73082118694031));
#276780=CARTESIAN_POINT('Ctrl Pts',(1.76973603198864,-0.831185068447074,
4.72691601982667));
#276781=CARTESIAN_POINT('Ctrl Pts',(1.73836898316663,-0.892294389965669,
4.72301085271303));
#276782=CARTESIAN_POINT('Ctrl Pts',(1.70701083550515,-0.953386370232826,
4.71910679378522));
#276783=CARTESIAN_POINT('Ctrl Pts',(1.6724189287103,-1.01284170766265,4.71520273485742));
#276784=CARTESIAN_POINT('Ctrl Pts',(1.63479758884621,-1.07030502358095,
4.71129867592962));
#276785=CARTESIAN_POINT('Ctrl Pts',(1.59717402185634,-1.12777174123966,
4.7073943858875));
#276786=CARTESIAN_POINT('Ctrl Pts',(1.55652093732143,-1.18324579314449,
4.70349009584538));
#276787=CARTESIAN_POINT('Ctrl Pts',(1.51308602493867,-1.2364006960267,4.69958580580326));
#276788=CARTESIAN_POINT('Ctrl Pts',(1.46960484745339,-1.28961221735006,
4.69567735707014));
#276789=CARTESIAN_POINT('Ctrl Pts',(1.42333624054634,-1.34049927815017,
4.69176890833703));
#276790=CARTESIAN_POINT('Ctrl Pts',(1.37456758991495,-1.38876921796079,
4.68786045960391));
#276791=CARTESIAN_POINT('Ctrl Pts',(1.32576974790802,-1.43706805063437,
4.6839496713967));
#276792=CARTESIAN_POINT('Ctrl Pts',(1.27446925137984,-1.48274631750008,
4.68003888318949));
#276793=CARTESIAN_POINT('Ctrl Pts',(1.22098758307095,-1.52555082576313,
4.67612809498229));
#276794=CARTESIAN_POINT('Ctrl Pts',(1.16741356915097,-1.5684292436217,4.67221055410378));
#276795=CARTESIAN_POINT('Ctrl Pts',(1.11165126624692,-1.60842371288584,
4.66829301322526));
#276796=CARTESIAN_POINT('Ctrl Pts',(1.05405146704452,-1.64532413366524,
4.66437547234675));
#276797=CARTESIAN_POINT('Ctrl Pts',(1.02686701036971,-1.66273943552134,
4.6625265731881));
#276798=CARTESIAN_POINT('Ctrl Pts',(0.999273627660957,-1.67946623148854,
4.66067767402945));
#276799=CARTESIAN_POINT('Ctrl Pts',(0.971309903392171,-1.69548608710667,
4.6588287748708));
#276800=CARTESIAN_POINT('Ctrl Pts',(0.912050242275597,-1.72943475595857,
4.65491065808038));
#276801=CARTESIAN_POINT('Ctrl Pts',(0.850891135398688,-1.7603401667489,
4.65099254128995));
#276802=CARTESIAN_POINT('Ctrl Pts',(0.788177758926153,-1.78798540831131,
4.64707442449953));
#276803=CARTESIAN_POINT('Ctrl Pts',(0.725558818286718,-1.81558902077374,
4.64316220773625));
#276804=CARTESIAN_POINT('Ctrl Pts',(0.661390699523402,-1.83994201035609,
4.63924999097297));
#276805=CARTESIAN_POINT('Ctrl Pts',(0.596044207441925,-1.86087272610862,
4.63533777420968));
#276806=CARTESIAN_POINT('Ctrl Pts',(0.530774558725907,-1.88177882865563,
4.6314301579673));
#276807=CARTESIAN_POINT('Ctrl Pts',(0.464329754918427,-1.89927050051948,
4.62752254172491));
#276808=CARTESIAN_POINT('Ctrl Pts',(0.397099969364987,-1.91322440250231,
4.62361492548253));
#276809=CARTESIAN_POINT('Ctrl Pts',(0.329912320600278,-1.92716955876902,
4.61970975836889));
#276810=CARTESIAN_POINT('Ctrl Pts',(0.261941146582688,-1.93758124388507,
4.61580459125524));
#276811=CARTESIAN_POINT('Ctrl Pts',(0.193589637821925,-1.94438654905036,
4.6118994241416));
#276812=CARTESIAN_POINT('Ctrl Pts',(0.125257525458772,-1.95118992304534,
4.6079953652138));
#276813=CARTESIAN_POINT('Ctrl Pts',(0.0565457818406509,-1.95438890000059,
4.60409130628599));
#276814=CARTESIAN_POINT('Ctrl Pts',(-0.0121362093305447,-1.95396231090139,
4.60018724735819));
#276815=CARTESIAN_POINT('Ctrl Pts',(-0.0808222663705408,-1.95353569654876,
4.59628295731607));
#276816=CARTESIAN_POINT('Ctrl Pts',(-0.149478075614179,-1.94948309564992,
4.59237866727395));
#276817=CARTESIAN_POINT('Ctrl Pts',(-0.217694999620562,-1.94183544285817,
4.58847437723183));
#276818=CARTESIAN_POINT('Ctrl Pts',(-0.285984585520565,-1.93417964409764,
4.58456592849871));
#276819=CARTESIAN_POINT('Ctrl Pts',(-0.353833863476488,-1.92292120624612,
4.58065747976559));
#276820=CARTESIAN_POINT('Ctrl Pts',(-0.420841071309029,-1.90814276004168,
4.57674903103248));
#276821=CARTESIAN_POINT('Ctrl Pts',(-0.487888387541988,-1.89335546792562,
4.57283824282527));
#276822=CARTESIAN_POINT('Ctrl Pts',(-0.554092156381364,-1.87504410535043,
4.56892745461806));
#276823=CARTESIAN_POINT('Ctrl Pts',(-0.619065270434279,-1.85334135845023,
4.56501666641085));
#276824=CARTESIAN_POINT('Ctrl Pts',(-0.684150572122884,-1.83160113789806,
4.56109912553233));
#276825=CARTESIAN_POINT('Ctrl Pts',(-0.748000520547101,-1.80645802585699,
4.55718158465382));
#276826=CARTESIAN_POINT('Ctrl Pts',(-0.810248305606452,-1.77809270941137,
4.55326404377531));
#276827=CARTESIAN_POINT('Ctrl Pts',(-0.839626397882392,-1.76470558434048,
4.55141514461666));
#276828=CARTESIAN_POINT('Ctrl Pts',(-0.868647986612071,-1.75060140551863,
4.54956624545802));
#276829=CARTESIAN_POINT('Ctrl Pts',(-0.897276652572764,-1.73580258346041,
4.54771734629938));
#276830=CARTESIAN_POINT('Ctrl Pts',(-0.957945432837846,-1.7044414824973,
4.54379922950895));
#276831=CARTESIAN_POINT('Ctrl Pts',(-1.01708832538956,-1.66983369391263,
4.53988111271852));
#276832=CARTESIAN_POINT('Ctrl Pts',(-1.07433584567749,-1.63215149134277,
4.5359629959281));
#276833=CARTESIAN_POINT('Ctrl Pts',(-1.13149716079555,-1.59452603185379,
4.53205077916481));
#276834=CARTESIAN_POINT('Ctrl Pts',(-1.18676836049747,-1.55383561466824,
4.52813856240153));
#276835=CARTESIAN_POINT('Ctrl Pts',(-1.23980407539598,-1.51029859783803,
4.52422634563824));
#276836=CARTESIAN_POINT('Ctrl Pts',(-1.29277742362883,-1.46681277780186,
4.52031872939586));
#276837=CARTESIAN_POINT('Ctrl Pts',(-1.34352012948776,-1.42048731677101,
4.51641111315347));
#276838=CARTESIAN_POINT('Ctrl Pts',(-1.39171689850161,-1.37158305414767,
4.51250349691109));
#276839=CARTESIAN_POINT('Ctrl Pts',(-1.43988345981725,-1.32270944264964,
4.50859832979745));
#276840=CARTESIAN_POINT('Ctrl Pts',(-1.48550690512802,-1.27126058530313,
4.5046931626838));
#276841=CARTESIAN_POINT('Ctrl Pts',(-1.52830724049951,-1.217535616989,4.50078799557016));
#276842=CARTESIAN_POINT('Ctrl Pts',(-1.57109543023826,-1.16382589443704,
4.49688393664235));
#276843=CARTESIAN_POINT('Ctrl Pts',(-1.61106179406427,-1.10784172768312,
4.49297987771455));
#276844=CARTESIAN_POINT('Ctrl Pts',(-1.64796644080564,-1.04991552516305,
4.48907581878674));
#276845=CARTESIAN_POINT('Ctrl Pts',(-1.68487327224562,-0.991985893500431,
4.48517152874462));
#276846=CARTESIAN_POINT('Ctrl Pts',(-1.71871776462754,-0.932114414043584,
4.4812672387025));
#276847=CARTESIAN_POINT('Ctrl Pts',(-1.74930420017124,-0.870661136874301,
4.47736294866038));
#276848=CARTESIAN_POINT('Ctrl Pts',(-1.77992321514238,-0.809142402172982,
4.47345449992727));
#276849=CARTESIAN_POINT('Ctrl Pts',(-1.80727702793962,-0.746038948484227,
4.46954605119415));
#276850=CARTESIAN_POINT('Ctrl Pts',(-1.83121707704509,-0.681733097875147,
4.46563760246103));
#276851=CARTESIAN_POINT('Ctrl Pts',(-1.85517145590862,-0.617388755812789,
4.46172681425382));
#276852=CARTESIAN_POINT('Ctrl Pts',(-1.87570785731568,-0.551841053906824,
4.4578160260466));
#276853=CARTESIAN_POINT('Ctrl Pts',(-1.89272771852057,-0.485487161049503,
4.45390523783939));
#276854=CARTESIAN_POINT('Ctrl Pts',(-1.9097769675425,-0.419018696396381,
4.44998769696088));
#276855=CARTESIAN_POINT('Ctrl Pts',(-1.92329746089811,-0.351741744501189,
4.44607015608236));
#276856=CARTESIAN_POINT('Ctrl Pts',(-1.93324197013006,-0.28406246659434,
4.44215261520385));
#276857=CARTESIAN_POINT('Ctrl Pts',(-1.93793532121998,-0.252120959444919,
4.44030371604521));
#276858=CARTESIAN_POINT('Ctrl Pts',(-1.94183290864853,-0.22008989195002,
4.43845481688658));
#276859=CARTESIAN_POINT('Ctrl Pts',(-1.94493379883751,-0.188012015944455,
4.43660591772794));
#276860=CARTESIAN_POINT('Ctrl Pts',(-1.95093590311411,-0.125921859562347,
4.43302717586003));
#276861=CARTESIAN_POINT('Ctrl Pts',(-1.95396538326698,-0.0635397665011596,
4.42944843399213));
#276862=CARTESIAN_POINT('Ctrl Pts',(-1.95399970505248,-0.00107361763076356,
4.42586969212423));
#276863=CARTESIAN_POINT('',(-1.95135153623783,-0.00103806439304008,3.72586969212423));
#276864=CARTESIAN_POINT('Ctrl Pts',(-1.9564564746551,-0.00105791454139017,
4.42586871637248));
#276865=CARTESIAN_POINT('Ctrl Pts',(-1.95257935738576,0.583682076751817,
4.39241064063383));
#276866=CARTESIAN_POINT('Ctrl Pts',(-1.36364931315002,1.82247384836932,
4.32191542203802));
#276867=CARTESIAN_POINT('Ctrl Pts',(0.742868822040285,2.18659612025236,
4.21438306058509));
#276868=CARTESIAN_POINT('Ctrl Pts',(2.2398397306889,0.562294105152547,4.10327163201366));
#276869=CARTESIAN_POINT('Ctrl Pts',(1.68755381017009,-1.57645768025738,
3.99216020344222));
#276870=CARTESIAN_POINT('Ctrl Pts',(-0.408695780024086,-2.27288900724468,
3.8810487748708));
#276871=CARTESIAN_POINT('Ctrl Pts',(-1.78461130773358,-1.16800275096967,
3.79228527109813));
#276872=CARTESIAN_POINT('Ctrl Pts',(-1.95259779099517,-0.2594810280554,
3.74055891018261));
#276873=CARTESIAN_POINT('Ctrl Pts',(-1.95135153623783,-0.00103806439304008,
3.72586969212423));
#276874=CARTESIAN_POINT('',(-1.95399929813707,0.00165616419005204,3.02586967145614));
#276875=CARTESIAN_POINT('Ctrl Pts',(-1.95135153623783,-0.00103806439304008,
3.72586969212423));
#276876=CARTESIAN_POINT('Ctrl Pts',(-1.94945550559233,0.392152634644927,
3.70352176732547));
#276877=CARTESIAN_POINT('Ctrl Pts',(-1.64333976564086,1.43969285576572,
3.64413669966957));
#276878=CARTESIAN_POINT('Ctrl Pts',(0.0653941910371889,2.30841510124345,
3.54771448915652));
#276879=CARTESIAN_POINT('Ctrl Pts',(1.97461131271872,1.19748354624812,3.43660306058508));
#276880=CARTESIAN_POINT('Ctrl Pts',(2.0772323364324,-1.00904038587818,3.32549163201366));
#276881=CARTESIAN_POINT('Ctrl Pts',(0.279368029483037,-2.2923808985465,
3.21438020344223));
#276882=CARTESIAN_POINT('Ctrl Pts',(-1.56641308901667,-1.56071800928074,
3.11450622347908));
#276883=CARTESIAN_POINT('Ctrl Pts',(-1.94902816663213,-0.451492593907781,
3.05166938637309));
#276884=CARTESIAN_POINT('Ctrl Pts',(-1.9526756070676,0.00165467924746206,
3.02586969212423));
#276885=CARTESIAN_POINT('',(-1.95399999956327,4.13126301758459E-5,2.32586969217956));
#276886=CARTESIAN_POINT('Ctrl Pts',(-1.95399929813707,0.00165616419005204,
3.02586967145614));
#276887=CARTESIAN_POINT('Ctrl Pts',(-1.95392953159649,0.0839691209373926,
3.02118636728134));
#276888=CARTESIAN_POINT('Ctrl Pts',(-1.94865472071711,0.166056497020639,
3.01650306310655));
#276889=CARTESIAN_POINT('Ctrl Pts',(-1.93828293935986,0.247336303413968,
3.01181975893175));
#276890=CARTESIAN_POINT('Ctrl Pts',(-1.92776906934288,0.329729605971204,
3.00707229563226));
#276891=CARTESIAN_POINT('Ctrl Pts',(-1.912017700784,0.411293043825035,3.00232483233277));
#276892=CARTESIAN_POINT('Ctrl Pts',(-1.89119027174125,0.491442118739601,
2.99757736903329));
#276893=CARTESIAN_POINT('Ctrl Pts',(-1.88326427479092,0.521943306478164,
2.99577069478865));
#276894=CARTESIAN_POINT('Ctrl Pts',(-1.87460364264371,0.552239885614248,
2.99396402054401));
#276895=CARTESIAN_POINT('Ctrl Pts',(-1.86521906910856,0.582300458727094,
2.99215734629938));
#276896=CARTESIAN_POINT('Ctrl Pts',(-1.84486683613545,0.647492530056354,
2.98823922950956));
#276897=CARTESIAN_POINT('Ctrl Pts',(-1.82105230986066,0.711745538601787,
2.98432111271974));
#276898=CARTESIAN_POINT('Ctrl Pts',(-1.79388100208733,0.774665702319497,
2.98040299592992));
#276899=CARTESIAN_POINT('Ctrl Pts',(-1.76675060974911,0.837491118817201,
2.97649077916723));
#276900=CARTESIAN_POINT('Ctrl Pts',(-1.73627366123969,0.898987225812118,
2.97257856240455));
#276901=CARTESIAN_POINT('Ctrl Pts',(-1.70260523957784,0.958775989562772,
2.96866634564187));
#276902=CARTESIAN_POINT('Ctrl Pts',(-1.66897640986261,1.01849444548712,
2.96475872940008));
#276903=CARTESIAN_POINT('Ctrl Pts',(-1.63216380066439,1.07650911897933,
2.96085111315828));
#276904=CARTESIAN_POINT('Ctrl Pts',(-1.59236955253217,1.13246421937671,
2.95694349691649));
#276905=CARTESIAN_POINT('Ctrl Pts',(-1.55260024575307,1.18838424948169,
2.95303832980343));
#276906=CARTESIAN_POINT('Ctrl Pts',(-1.50985329151177,1.24224686718789,
2.94913316269037));
#276907=CARTESIAN_POINT('Ctrl Pts',(-1.46437467279383,1.29372439788386,
2.94522799557731));
#276908=CARTESIAN_POINT('Ctrl Pts',(-1.41890895973643,1.34518732058261,
2.94132393665009));
#276909=CARTESIAN_POINT('Ctrl Pts',(-1.37071344657607,1.39426613143396,
2.93741987772286));
#276910=CARTESIAN_POINT('Ctrl Pts',(-1.32007384677977,1.4406668730307,2.93351581879564));
#276911=CARTESIAN_POINT('Ctrl Pts',(-1.26943124919653,1.48707036148046,
2.92961152875409));
#276912=CARTESIAN_POINT('Ctrl Pts',(-1.21634464211473,1.53079513551345,
2.92570723871255));
#276913=CARTESIAN_POINT('Ctrl Pts',(-1.16113462979361,1.57158594149161,
2.921802948671));
#276914=CARTESIAN_POINT('Ctrl Pts',(-1.1058658100121,1.61242019617782,2.91789449993844));
#276915=CARTESIAN_POINT('Ctrl Pts',(-1.04846946758296,1.65031395313702,
2.91398605120588));
#276916=CARTESIAN_POINT('Ctrl Pts',(-0.989296327289874,1.68505453229584,
2.91007760247332));
#276917=CARTESIAN_POINT('Ctrl Pts',(-0.930087767821911,1.71981590606929,
2.90616681426667));
#276918=CARTESIAN_POINT('Ctrl Pts',(-0.869100730642009,1.75142011943706,
2.90225602606001));
#276919=CARTESIAN_POINT('Ctrl Pts',(-0.806709242136566,1.77970115430975,
2.89834523785335));
#276920=CARTESIAN_POINT('Ctrl Pts',(-0.74421002363075,1.80803102141854,
2.89442769697537));
#276921=CARTESIAN_POINT('Ctrl Pts',(-0.680301971665396,1.83302607872028,
2.8905101560974));
#276922=CARTESIAN_POINT('Ctrl Pts',(-0.615376880502353,1.85456930173644,
2.88659261521942));
#276923=CARTESIAN_POINT('Ctrl Pts',(-0.584735222763013,1.86473671243142,
2.88474371605559));
#276924=CARTESIAN_POINT('Ctrl Pts',(-0.553867213033213,1.87413599185907,
2.88289481689176));
#276925=CARTESIAN_POINT('Ctrl Pts',(-0.522814791870344,1.88275879851923,
2.88104591772793));
#276926=CARTESIAN_POINT('Ctrl Pts',(-0.457009681946909,1.9010319224455,
2.87712780093843));
#276927=CARTESIAN_POINT('Ctrl Pts',(-0.390114964549388,1.91588714213598,
2.87320968414892));
#276928=CARTESIAN_POINT('Ctrl Pts',(-0.322518672193423,1.92719944636942,
2.86929156735941));
#276929=CARTESIAN_POINT('Ctrl Pts',(-0.255024168523623,1.93849471616879,
2.86537935059706));
#276930=CARTESIAN_POINT('Ctrl Pts',(-0.186830667813991,1.94625757813585,
2.8614671338347));
#276931=CARTESIAN_POINT('Ctrl Pts',(-0.118339868132747,1.95041320637713,
2.85755491707235));
#276932=CARTESIAN_POINT('Ctrl Pts',(-0.0499296093251734,1.95456394786091,
2.8536473008309));
#276933=CARTESIAN_POINT('Ctrl Pts',(0.0187767654808092,1.95511585040939,
2.84973968458946));
#276934=CARTESIAN_POINT('Ctrl Pts',(0.0873707122396018,1.95204568559313,
2.84583206834801));
#276935=CARTESIAN_POINT('Ctrl Pts',(0.155921667210954,1.94897744502645,
2.84192690123531));
#276936=CARTESIAN_POINT('Ctrl Pts',(0.224359843630586,1.94229166231341,
2.83802173412261));
#276937=CARTESIAN_POINT('Ctrl Pts',(0.292276529263017,1.93201719206687,
2.83411656700991));
#276938=CARTESIAN_POINT('Ctrl Pts',(0.360173941889366,1.92174563745035,
2.83021250808306));
#276939=CARTESIAN_POINT('Ctrl Pts',(0.427549671387565,1.90788749049407,
2.8263084491562));
#276940=CARTESIAN_POINT('Ctrl Pts',(0.494001773370695,1.89052327356915,
2.82240439022935));
#276941=CARTESIAN_POINT('Ctrl Pts',(0.560457809216534,1.87315802870916,
2.81850010018818));
#276942=CARTESIAN_POINT('Ctrl Pts',(0.625989633742968,1.85228642864929,
2.81459581014701));
#276943=CARTESIAN_POINT('Ctrl Pts',(0.690208885006844,1.82803930347726,
2.81069152010585));
#276944=CARTESIAN_POINT('Ctrl Pts',(0.754496540005923,1.80376635125341,
2.80678307137368));
#276945=CARTESIAN_POINT('Ctrl Pts',(0.817468370513111,1.77611087254772,
2.80287462264151));
#276946=CARTESIAN_POINT('Ctrl Pts',(0.878755435843135,1.7452520975424,2.79896617390935));
#276947=CARTESIAN_POINT('Ctrl Pts',(0.940079185676753,1.714374851448,2.79505538570309));
#276948=CARTESIAN_POINT('Ctrl Pts',(0.999715736226602,1.68029073719743,
2.79114459749683));
#276949=CARTESIAN_POINT('Ctrl Pts',(1.05732270201401,1.6432238751326,2.78723380929057));
#276950=CARTESIAN_POINT('Ctrl Pts',(1.11502913647236,1.60609301053865,2.783316268413));
#276951=CARTESIAN_POINT('Ctrl Pts',(1.17069859304666,1.56596940652051,2.77939872753543));
#276952=CARTESIAN_POINT('Ctrl Pts',(1.22402020238525,1.52311869010684,2.77548118665786));
#276953=CARTESIAN_POINT('Ctrl Pts',(1.24918555028494,1.50289512221988,2.77363228749075));
#276954=CARTESIAN_POINT('Ctrl Pts',(1.27382845270328,1.48206466753042,2.77178338832364));
#276955=CARTESIAN_POINT('Ctrl Pts',(1.2979191479585,1.46065803162913,2.76993448915652));
#276956=CARTESIAN_POINT('Ctrl Pts',(1.3489712330856,1.41529390300022,2.76601637236201));
#276957=CARTESIAN_POINT('Ctrl Pts',(1.39774334461602,1.36716011116494,2.7620982555675));
#276958=CARTESIAN_POINT('Ctrl Pts',(1.44391994502689,1.31651479002461,2.75818013877299));
#276959=CARTESIAN_POINT('Ctrl Pts',(1.49002701121773,1.26594573224868,2.75426792200561));
#276960=CARTESIAN_POINT('Ctrl Pts',(1.53354599434848,1.21287301153751,2.75035570523823));
#276961=CARTESIAN_POINT('Ctrl Pts',(1.57419609978841,1.15759346897387,2.74644348847085));
#276962=CARTESIAN_POINT('Ctrl Pts',(1.61479840326056,1.10237893167612,2.74253587222438));
#276963=CARTESIAN_POINT('Ctrl Pts',(1.65253823908165,1.04496312079801,2.73862825597791));
#276964=CARTESIAN_POINT('Ctrl Pts',(1.68717444166508,0.985676622119112,
2.73472063973143));
#276965=CARTESIAN_POINT('Ctrl Pts',(1.72178893574027,0.926427281712436,
2.73081547261371));
#276966=CARTESIAN_POINT('Ctrl Pts',(1.75330340772147,0.865310003067912,
2.72691030549598));
#276967=CARTESIAN_POINT('Ctrl Pts',(1.78152035195789,0.802683770584543,
2.72300513837825));
#276968=CARTESIAN_POINT('Ctrl Pts',(1.80972928895227,0.740075309813019,
2.71910107944638));
#276969=CARTESIAN_POINT('Ctrl Pts',(1.83464235386879,0.675959193508858,
2.7151970205145));
#276970=CARTESIAN_POINT('Ctrl Pts',(1.85610911524766,0.610716752917867,
2.71129296158262));
#276971=CARTESIAN_POINT('Ctrl Pts',(1.87757714742586,0.545470450074506,
2.70738867153645));
#276972=CARTESIAN_POINT('Ctrl Pts',(1.8955983197249,0.479098158605541,2.70348438149028));
#276973=CARTESIAN_POINT('Ctrl Pts',(1.91007182962046,0.411997094274172,
2.6995800914441));
#276974=CARTESIAN_POINT('Ctrl Pts',(1.92456075611001,0.344824556618577,
2.69567164270699));
#276975=CARTESIAN_POINT('Ctrl Pts',(1.93549437491877,0.27692217867235,2.69176319396987));
#276976=CARTESIAN_POINT('Ctrl Pts',(1.94282307781572,0.208697120983155,
2.68785474523276));
#276977=CARTESIAN_POINT('Ctrl Pts',(1.95015616744294,0.140431225927526,
2.68394395702157));
#276978=CARTESIAN_POINT('Ctrl Pts',(1.95388002009114,0.0718427579564729,
2.68003316881039));
#276979=CARTESIAN_POINT('Ctrl Pts',(1.95399714386114,0.00334092539568565,
2.67612238059921));
#276980=CARTESIAN_POINT('Ctrl Pts',(1.95411446986615,-0.0652791877592747,
2.6722048397168));
#276981=CARTESIAN_POINT('Ctrl Pts',(1.95061266267349,-0.133811875965454,
2.6682872988344));
#276982=CARTESIAN_POINT('Ctrl Pts',(1.94354619602246,-0.20185188611111,
2.664369757952));
#276983=CARTESIAN_POINT('Ctrl Pts',(1.94021114876168,-0.233963641627143,
2.66252085882969));
#276984=CARTESIAN_POINT('Ctrl Pts',(1.93608285036119,-0.265965791307287,
2.66067195970739));
#276985=CARTESIAN_POINT('Ctrl Pts',(1.9311709473418,-0.297816675394412,
2.65882306058509));
#276986=CARTESIAN_POINT('Ctrl Pts',(1.92076182905302,-0.365313859022907,
2.65490494379978));
#276987=CARTESIAN_POINT('Ctrl Pts',(1.90678913190683,-0.432398466001827,
2.65098682701447));
#276988=CARTESIAN_POINT('Ctrl Pts',(1.88929850252114,-0.498665387179999,
2.64706871022916));
#276989=CARTESIAN_POINT('Ctrl Pts',(1.87183421109152,-0.564832521482559,
2.64315649347098));
#276990=CARTESIAN_POINT('Ctrl Pts',(1.85086262543722,-0.630183941907614,
2.63924427671279));
#276991=CARTESIAN_POINT('Ctrl Pts',(1.82648075681501,-0.694322723943613,
2.63533205995461));
#276992=CARTESIAN_POINT('Ctrl Pts',(1.80212755973679,-0.75838608280596,
2.63142444371727));
#276993=CARTESIAN_POINT('Ctrl Pts',(1.77437221811931,-0.821239177707652,
2.62751682747993));
#276994=CARTESIAN_POINT('Ctrl Pts',(1.74336159018658,-0.882500065644257,
2.62360921124259));
#276995=CARTESIAN_POINT('Ctrl Pts',(1.71237039840481,-0.943722557845439,
2.61970404413396));
#276996=CARTESIAN_POINT('Ctrl Pts',(1.67812818921998,-1.00335438478286,
2.61579887702533));
#276997=CARTESIAN_POINT('Ctrl Pts',(1.64082936390711,-1.06103487150056,
2.6118937099167));
#276998=CARTESIAN_POINT('Ctrl Pts',(1.60354112303974,-1.11869898998244,
2.60798965099386));
#276999=CARTESIAN_POINT('Ctrl Pts',(1.56319825492906,-1.17441245466215,
2.60408559207103));
#277000=CARTESIAN_POINT('Ctrl Pts',(1.52003947262901,-1.22784201005248,
2.6001815331482));
#277001=CARTESIAN_POINT('Ctrl Pts',(1.47687813539453,-1.28127472839143,
2.596277243111));
#277002=CARTESIAN_POINT('Ctrl Pts',(1.43090086409557,-1.33242288798782,
2.5923729530738));
#277003=CARTESIAN_POINT('Ctrl Pts',(1.38238664109173,-1.38098630497595,
2.5884686630366));
#277004=CARTESIAN_POINT('Ctrl Pts',(1.33382074270884,-1.42960144974257,
2.58456021430829));
#277005=CARTESIAN_POINT('Ctrl Pts',(1.28271284805352,-1.47562600878443,
2.58065176557999));
#277006=CARTESIAN_POINT('Ctrl Pts',(1.22937806852749,-1.51879740736664,
2.57674331685169));
#277007=CARTESIAN_POINT('Ctrl Pts',(1.17601136448446,-1.56199464698654,
2.57283252864924));
#277008=CARTESIAN_POINT('Ctrl Pts',(1.12041552094019,-1.60233503837291,
2.56892174044679));
#277009=CARTESIAN_POINT('Ctrl Pts',(1.06293564488252,-1.63959867493182,
2.56501095224434));
#277010=CARTESIAN_POINT('Ctrl Pts',(1.00535651959502,-1.67692665378725,
2.56109341137045));
#277011=CARTESIAN_POINT('Ctrl Pts',(0.945887295140474,-1.71116702948653,
2.55717587049657));
#277012=CARTESIAN_POINT('Ctrl Pts',(0.88489794965692,-1.74214569387666,
2.55325832962268));
#277013=CARTESIAN_POINT('Ctrl Pts',(0.856113782270623,-1.75676619937872,
2.55140943041967));
#277014=CARTESIAN_POINT('Ctrl Pts',(0.826991313224014,-1.77066088609606,
2.54956053121666));
#277015=CARTESIAN_POINT('Ctrl Pts',(0.797570771523595,-1.78381525512348,
2.54771163201366));
#277016=CARTESIAN_POINT('Ctrl Pts',(0.735223879866186,-1.81169149305702,
2.54379351522746));
#277017=CARTESIAN_POINT('Ctrl Pts',(0.671290166061522,-1.83635038593064,
2.53987539844126));
#277018=CARTESIAN_POINT('Ctrl Pts',(0.606134698217115,-1.85761048867012,
2.53595728165506));
#277019=CARTESIAN_POINT('Ctrl Pts',(0.541077343587392,-1.87883857725802,
2.53204506489608));
#277020=CARTESIAN_POINT('Ctrl Pts',(0.474802350038025,-1.89667788179146,
2.52813284813709));
#277021=CARTESIAN_POINT('Ctrl Pts',(0.40769577792443,-1.91099454542984,
2.52422063137811));
#277022=CARTESIAN_POINT('Ctrl Pts',(0.340668118921272,-1.92529437357173,
2.5203130151401));
#277023=CARTESIAN_POINT('Ctrl Pts',(0.272811302223436,-1.93607968555399,
2.5164053989021));
#277024=CARTESIAN_POINT('Ctrl Pts',(0.204525847475429,-1.94326662548258,
2.5124977826641));
#277025=CARTESIAN_POINT('Ctrl Pts',(0.1362831911659,-1.95044906094082,2.50859261555489));
#277026=CARTESIAN_POINT('Ctrl Pts',(0.0676129178068932,-1.95403754678965,
2.50468744844568));
#277027=CARTESIAN_POINT('Ctrl Pts',(-0.00107652451106434,-1.95399970345314,
2.50078228133647));
#277028=CARTESIAN_POINT('Ctrl Pts',(-0.0697464745338006,-1.95396187085561,
2.49687822241314));
#277029=CARTESIAN_POINT('Ctrl Pts',(-0.138435091067868,-1.95029975220233,
2.49297416348981));
#277030=CARTESIAN_POINT('Ctrl Pts',(-0.206732918045551,-1.9430330672936,
2.48907010456648));
#277031=CARTESIAN_POINT('Ctrl Pts',(-0.275034788149518,-1.9357659522083,
2.48516581452887));
#277032=CARTESIAN_POINT('Ctrl Pts',(-0.342945333921737,-1.92489390181521,
2.48126152449125));
#277033=CARTESIAN_POINT('Ctrl Pts',(-0.410061032500004,-1.91048840604308,
2.47735723445364));
#277034=CARTESIAN_POINT('Ctrl Pts',(-0.477248219990985,-1.89606756612268,
2.47344878572506));
#277035=CARTESIAN_POINT('Ctrl Pts',(-0.543638388808918,-1.87810587310111,
2.46954033699648));
#277036=CARTESIAN_POINT('Ctrl Pts',(-0.608840007204148,-1.85672557089831,
2.46563188826789));
#277037=CARTESIAN_POINT('Ctrl Pts',(-0.674080653230671,-1.83533247112128,
2.46172110006523));
#277038=CARTESIAN_POINT('Ctrl Pts',(-0.738130874239155,-1.81051686743246,
2.45781031186258));
#277039=CARTESIAN_POINT('Ctrl Pts',(-0.800618706968965,-1.78244935020644,
2.45389952365992));
#277040=CARTESIAN_POINT('Ctrl Pts',(-0.863214436054704,-1.75433336942045,
2.44998198278594));
#277041=CARTESIAN_POINT('Ctrl Pts',(-0.924241955393526,-1.72295449324751,
2.44606444191196));
#277042=CARTESIAN_POINT('Ctrl Pts',(-0.983354279983066,-1.68852905217499,
2.44214690103798));
#277043=CARTESIAN_POINT('Ctrl Pts',(-1.01125257972668,-1.67228182656653,
2.4402980018394));
#277044=CARTESIAN_POINT('Ctrl Pts',(-1.03872471524778,-1.65535662974093,
2.43844910264081));
#277045=CARTESIAN_POINT('Ctrl Pts',(-1.06573668106705,-1.63777938887635,
2.43660020344223));
#277046=CARTESIAN_POINT('Ctrl Pts',(-1.12294424235479,-1.60055325395682,
2.43268449382947));
#277047=CARTESIAN_POINT('Ctrl Pts',(-1.17831309400748,-1.56025187137137,
2.42876878421671));
#277048=CARTESIAN_POINT('Ctrl Pts',(-1.23149300216491,-1.517083051655,2.42485307460396));
#277049=CARTESIAN_POINT('Ctrl Pts',(-1.28459280640327,-1.47397925633903,
2.42094326315269));
#277050=CARTESIAN_POINT('Ctrl Pts',(-1.33550983127716,-1.42801690352454,
2.41703345170141));
#277051=CARTESIAN_POINT('Ctrl Pts',(-1.38392240404207,-1.37944727321867,
2.41312364025014));
#277052=CARTESIAN_POINT('Ctrl Pts',(-1.43227811874202,-1.33093468543372,
2.40921842067037));
#277053=CARTESIAN_POINT('Ctrl Pts',(-1.47813487660824,-1.27982124855245,
2.40531320109061));
#277054=CARTESIAN_POINT('Ctrl Pts',(-1.52120514589974,-1.22639753101845,
2.40140798151084));
#277055=CARTESIAN_POINT('Ctrl Pts',(-1.56424850782029,-1.17300718898474,
2.3975052016463));
#277056=CARTESIAN_POINT('Ctrl Pts',(-1.60450852579453,-1.11730981187041,
2.39360242178176));
#277057=CARTESIAN_POINT('Ctrl Pts',(-1.64173660049825,-1.05963056514261,
2.38969964191722));
#277058=CARTESIAN_POINT('Ctrl Pts',(-1.67895422954386,-1.00196750237533,
2.38579795711614));
#277059=CARTESIAN_POINT('Ctrl Pts',(-1.71314133713107,-0.942324087565681,
2.38189627231505));
#277060=CARTESIAN_POINT('Ctrl Pts',(-1.74409254061705,-0.881054600898244,
2.37799458751397));
#277061=CARTESIAN_POINT('Ctrl Pts',(-1.77504571108668,-0.819781220486312,
2.37409265475645));
#277062=CARTESIAN_POINT('Ctrl Pts',(-1.80276234945153,-0.7568820039011,
2.37019072199893));
#277063=CARTESIAN_POINT('Ctrl Pts',(-1.82708378310748,-0.692734328228109,
2.3662887892414));
#277064=CARTESIAN_POINT('Ctrl Pts',(-1.85143116240428,-0.628518221040039,
2.36238269397655));
#277065=CARTESIAN_POINT('Ctrl Pts',(-1.87237593424198,-0.563051458451526,
2.35847659871169));
#277066=CARTESIAN_POINT('Ctrl Pts',(-1.88980857233421,-0.496728859572438,
2.35457050344684));
#277067=CARTESIAN_POINT('Ctrl Pts',(-1.9072517504597,-0.430366161059865,
2.35066204649847));
#277068=CARTESIAN_POINT('Ctrl Pts',(-1.92117846918179,-0.363147078863803,
2.3467535895501));
#277069=CARTESIAN_POINT('Ctrl Pts',(-1.93153043378067,-0.2954761976523,
2.34284513260173));
#277070=CARTESIAN_POINT('Ctrl Pts',(-1.94190018322113,-0.227689056779093,
2.3389299608615));
#277071=CARTESIAN_POINT('Ctrl Pts',(-1.94868287364594,-0.159449057639085,
2.33501478912126));
#277072=CARTESIAN_POINT('Ctrl Pts',(-1.9518721839828,-0.0911645621620376,
2.33109961738103));
#277073=CARTESIAN_POINT('Ctrl Pts',(-1.95329228809852,-0.0607595269588351,
2.32935630898054));
#277074=CARTESIAN_POINT('Ctrl Pts',(-1.95400064202245,-0.0303456469757893,
2.32761300058005));
#277075=CARTESIAN_POINT('Ctrl Pts',(-1.95399999956327,4.13126301756066E-5,
2.32586969217956));
#277076=CARTESIAN_POINT('',(-1.95399927547201,-0.00168269273987639,1.62586971130023));
#277077=CARTESIAN_POINT('Ctrl Pts',(-1.95399999956325,4.13135945347792E-5,
2.32586969212423));
#277078=CARTESIAN_POINT('Ctrl Pts',(-1.95399995276918,0.00225452253103485,
2.32574271970642));
#277079=CARTESIAN_POINT('Ctrl Pts',(-1.95399614577176,0.0044677267577048,
2.32561574728861));
#277080=CARTESIAN_POINT('Ctrl Pts',(-1.95398857860865,0.00668091812061876,
2.3254887748708));
#277081=CARTESIAN_POINT('Ctrl Pts',(-1.95375507097746,0.0749756099772388,
2.32157065812134));
#277082=CARTESIAN_POINT('Ctrl Pts',(-1.94993629437008,0.143393426555683,
2.31765254137188));
#277083=CARTESIAN_POINT('Ctrl Pts',(-1.94251701066304,0.211526980039711,
2.31373442462242));
#277084=CARTESIAN_POINT('Ctrl Pts',(-1.93510889915362,0.279557935813039,
2.30982220790001));
#277085=CARTESIAN_POINT('Ctrl Pts',(-1.92411109363811,0.347304992968974,
2.30590999117761));
#277086=CARTESIAN_POINT('Ctrl Pts',(-1.90956036678483,0.414361201857249,
2.3019977744552));
#277087=CARTESIAN_POINT('Ctrl Pts',(-1.89502675067027,0.481338556865477,
2.29809015825336));
#277088=CARTESIAN_POINT('Ctrl Pts',(-1.87694861462697,0.547626198615865,
2.29418254205152));
#277089=CARTESIAN_POINT('Ctrl Pts',(-1.85541425435577,0.612824562769333,
2.29027492584969));
#277090=CARTESIAN_POINT('Ctrl Pts',(-1.83389339091051,0.67798206334657,
2.28636975877636));
#277091=CARTESIAN_POINT('Ctrl Pts',(-1.80892075423999,0.742051174598245,
2.28246459170303));
#277092=CARTESIAN_POINT('Ctrl Pts',(-1.78063482179842,0.804646277191972,
2.2785594246297));
#277093=CARTESIAN_POINT('Ctrl Pts',(-1.75235691617392,0.867223616912274,
2.27465536574193));
#277094=CARTESIAN_POINT('Ctrl Pts',(-1.72076778375044,0.928327330315059,
2.27075130685415));
#277095=CARTESIAN_POINT('Ctrl Pts',(-1.68605380531961,0.987592307365376,
2.26684724796638));
#277096=CARTESIAN_POINT('Ctrl Pts',(-1.65133777187124,1.046860792817,2.26294295796394));
#277097=CARTESIAN_POINT('Ctrl Pts',(-1.61349677597143,1.10428990267778,
2.25903866796151));
#277098=CARTESIAN_POINT('Ctrl Pts',(-1.57276194678371,1.15954122770565,
2.25513437795907));
#277099=CARTESIAN_POINT('Ctrl Pts',(-1.53198372850369,1.21485140420998,
2.25122592926485));
#277100=CARTESIAN_POINT('Ctrl Pts',(-1.48830581788254,1.26797876983067,
2.24731748057063));
#277101=CARTESIAN_POINT('Ctrl Pts',(-1.44200067467252,1.31861671999259,
2.24340903187641));
#277102=CARTESIAN_POINT('Ctrl Pts',(-1.39566781465987,1.36928498043913,
2.23949824370771));
#277103=CARTESIAN_POINT('Ctrl Pts',(-1.34670494300387,1.41746051485351,
2.23558745553901));
#277104=CARTESIAN_POINT('Ctrl Pts',(-1.29542053905071,1.46287443993173,
2.2316766673703));
#277105=CARTESIAN_POINT('Ctrl Pts',(-1.24404758344009,1.50836678024006,
2.2277591265293));
#277106=CARTESIAN_POINT('Ctrl Pts',(-1.19034547986167,1.55108768817199,
2.22384158568829));
#277107=CARTESIAN_POINT('Ctrl Pts',(-1.13465412656932,1.59080986074993,
2.21992404484728));
#277108=CARTESIAN_POINT('Ctrl Pts',(-1.1083703632788,1.60955690350795,2.21807514533131));
#277109=CARTESIAN_POINT('Ctrl Pts',(-1.0816439047551,1.6276366515146,2.21622624581534));
#277110=CARTESIAN_POINT('Ctrl Pts',(-1.05451236992383,1.64502877229476,
2.21437734629937));
#277111=CARTESIAN_POINT('Ctrl Pts',(-0.997016264336595,1.68188548604064,
2.21045922952302));
#277112=CARTESIAN_POINT('Ctrl Pts',(-0.937471564875764,1.71579727589714,
2.20654111274667));
#277113=CARTESIAN_POINT('Ctrl Pts',(-0.876212221149488,1.74653031565681,
2.20262299597032));
#277114=CARTESIAN_POINT('Ctrl Pts',(-0.815045123734695,1.77721707660601,
2.1987107792216));
#277115=CARTESIAN_POINT('Ctrl Pts',(-0.752168942461889,1.80473436849974,
2.19479856247288));
#277116=CARTESIAN_POINT('Ctrl Pts',(-0.687945477004168,1.82889229334849,
2.19088634572416));
#277117=CARTESIAN_POINT('Ctrl Pts',(-0.623797534314021,1.8530218099927,
2.18697872949698));
#277118=CARTESIAN_POINT('Ctrl Pts',(-0.558305912133177,1.8737996328006,
2.18307111326981));
#277119=CARTESIAN_POINT('Ctrl Pts',(-0.49185415977605,1.89108315140054,
2.17916349704263));
#277120=CARTESIAN_POINT('Ctrl Pts',(-0.425444056576054,1.9083558374196,
2.17525832994458));
#277121=CARTESIAN_POINT('Ctrl Pts',(-0.358075491891942,1.92213844012248,
2.17135316284652));
#277122=CARTESIAN_POINT('Ctrl Pts',(-0.290147526652456,1.93233806896657,
2.16744799574847));
#277123=CARTESIAN_POINT('Ctrl Pts',(-0.222238837626192,1.94253480341776,
2.16354393683662));
#277124=CARTESIAN_POINT('Ctrl Pts',(-0.153771549376384,1.94915050944118,
2.15963987792477));
#277125=CARTESIAN_POINT('Ctrl Pts',(-0.0851534841210611,1.95214366380706,
2.15573581901292));
#277126=CARTESIAN_POINT('Ctrl Pts',(-0.0165313567871024,1.95513699536284,
2.15183152898708));
#277127=CARTESIAN_POINT('Ctrl Pts',(0.0522410737505755,1.95450733063121,
2.14792723896125));
#277128=CARTESIAN_POINT('Ctrl Pts',(0.120754136718002,1.9502652225955,2.14402294893542));
#277129=CARTESIAN_POINT('Ctrl Pts',(0.189340177007754,1.94601859603921,
2.14011450021897));
#277130=CARTESIAN_POINT('Ctrl Pts',(0.257665806500161,1.93815187756227,
2.13620605150253));
#277131=CARTESIAN_POINT('Ctrl Pts',(0.325325647557145,1.92672759440496,
2.13229760278608));
#277132=CARTESIAN_POINT('Ctrl Pts',(0.393025987656144,1.9152964730329,2.12838681459579));
#277133=CARTESIAN_POINT('Ctrl Pts',(0.460059266106312,1.9003036563682,2.1244760264055));
#277134=CARTESIAN_POINT('Ctrl Pts',(0.526032249962911,1.88186239454402,
2.1205652382152));
#277135=CARTESIAN_POINT('Ctrl Pts',(0.592119147905457,1.86338929060264,
2.1166476973538));
#277136=CARTESIAN_POINT('Ctrl Pts',(0.657141631466861,1.84145601470102,
2.1127301564924));
#277137=CARTESIAN_POINT('Ctrl Pts',(0.72072435018235,1.81622476886927,2.108812615631));
#277138=CARTESIAN_POINT('Ctrl Pts',(0.750732472203038,1.80431678004858,
2.10696371632998));
#277139=CARTESIAN_POINT('Ctrl Pts',(0.780420229962298,1.79167487856341,
2.10511481702896));
#277140=CARTESIAN_POINT('Ctrl Pts',(0.809750133717947,1.778319634077,2.10326591772794));
#277141=CARTESIAN_POINT('Ctrl Pts',(0.871904948480085,1.75001770870858,
2.09934780076015));
#277142=CARTESIAN_POINT('Ctrl Pts',(0.932697398100167,1.71839715751514,
2.09542968379236));
#277143=CARTESIAN_POINT('Ctrl Pts',(0.991749879805991,1.68361164640329,
2.09151156682456));
#277144=CARTESIAN_POINT('Ctrl Pts',(1.05071343838672,1.6488785164322,2.08759934988324));
#277145=CARTESIAN_POINT('Ctrl Pts',(1.10794180861744,1.61099013280824,2.08368713294192));
#277146=CARTESIAN_POINT('Ctrl Pts',(1.16307917875715,1.57014738924141,2.0797749160006));
#277147=CARTESIAN_POINT('Ctrl Pts',(1.21815171082154,1.52935267416916,2.07586729958006));
#277148=CARTESIAN_POINT('Ctrl Pts',(1.27113773279588,1.48561079024756,2.07195968315951));
#277149=CARTESIAN_POINT('Ctrl Pts',(1.32170935570517,1.43916655708832,2.06805206673896));
#277150=CARTESIAN_POINT('Ctrl Pts',(1.37224928245928,1.39275143321084,2.06414689944718));
#277151=CARTESIAN_POINT('Ctrl Pts',(1.42037745047451,1.3436376518615,2.0602417321554));
#277152=CARTESIAN_POINT('Ctrl Pts',(1.4657993210686,1.29211003802108,2.05633656486362));
#277153=CARTESIAN_POINT('Ctrl Pts',(1.51120830210297,1.24059704639342,2.05243250575797));
#277154=CARTESIAN_POINT('Ctrl Pts',(1.55391218517407,1.18667195089701,2.04852844665232));
#277155=CARTESIAN_POINT('Ctrl Pts',(1.59365482817077,1.13065480525578,2.04462438754667));
#277156=CARTESIAN_POINT('Ctrl Pts',(1.63339982386536,1.07463434349338,2.04072009732726));
#277157=CARTESIAN_POINT('Ctrl Pts',(1.67018294892636,1.01652198836168,2.03681580710785));
#277158=CARTESIAN_POINT('Ctrl Pts',(1.70379080376997,0.956667600051811,
2.03291151688845));
#277159=CARTESIAN_POINT('Ctrl Pts',(1.73743445631471,0.896749457315643,
2.02900306798009));
#277160=CARTESIAN_POINT('Ctrl Pts',(1.76789584759997,0.835086008032117,
2.02509461907174));
#277161=CARTESIAN_POINT('Ctrl Pts',(1.79500756706025,0.772051704354332,
2.02118617016338));
#277162=CARTESIAN_POINT('Ctrl Pts',(1.82213551473332,0.70897967034763,2.01727538178185));
#277163=CARTESIAN_POINT('Ctrl Pts',(1.84590962998046,0.644535610442962,
2.01336459340032));
#277164=CARTESIAN_POINT('Ctrl Pts',(1.86621169988821,0.579111294312565,
2.00945380501878));
#277165=CARTESIAN_POINT('Ctrl Pts',(1.88654882491167,0.513574011524938,
2.00553626396918));
#277166=CARTESIAN_POINT('Ctrl Pts',(1.90340181860026,0.447053570943978,
2.00161872291957));
#277167=CARTESIAN_POINT('Ctrl Pts',(1.9167032910083,0.379953279019851,1.99770118186997));
#277168=CARTESIAN_POINT('Ctrl Pts',(1.92298096869351,0.348285055205146,
1.99585228429881));
#277169=CARTESIAN_POINT('Ctrl Pts',(1.92846832939046,0.31648776660826,1.99400338672766));
#277170=CARTESIAN_POINT('Ctrl Pts',(1.93316231235789,0.284604065464821,
1.99215448915651));
#277171=CARTESIAN_POINT('Ctrl Pts',(1.94310963030885,0.217037285839111,
1.9882363726813));
#277172=CARTESIAN_POINT('Ctrl Pts',(1.94953006943767,0.148814430209601,
1.9843182562061));
#277173=CARTESIAN_POINT('Ctrl Pts',(1.95234784722165,0.0803360656803328,
1.98040013973089));
#277174=CARTESIAN_POINT('Ctrl Pts',(1.95516138190453,0.0119608180915343,
1.97648792328245));
#277175=CARTESIAN_POINT('Ctrl Pts',(1.95438300189478,-0.0566686872867476,
1.97257570683401));
#277176=CARTESIAN_POINT('Ctrl Pts',(1.94998841991117,-0.125144565252865,
1.96866349038556));
#277177=CARTESIAN_POINT('Ctrl Pts',(1.94559900567774,-0.193539919922068,
1.96475587445596));
#277178=CARTESIAN_POINT('Ctrl Pts',(1.93760186620457,-0.261781517418771,
1.96084825852636));
#277179=CARTESIAN_POINT('Ctrl Pts',(1.92602476249998,-0.329461096697164,
1.95694064259676));
#277180=CARTESIAN_POINT('Ctrl Pts',(1.91445491483107,-0.39709825729692,
1.95303547579444));
#277181=CARTESIAN_POINT('Ctrl Pts',(1.89930963660505,-0.464173614679122,
1.94913030899212));
#277182=CARTESIAN_POINT('Ctrl Pts',(1.88066838843659,-0.530285218288522,
1.94522514218981));
#277183=CARTESIAN_POINT('Ctrl Pts',(1.86203243016553,-0.596378061158479,
1.94132108357142));
#277184=CARTESIAN_POINT('Ctrl Pts',(1.83990260479671,-0.661507219978381,
1.93741702495304));
#277185=CARTESIAN_POINT('Ctrl Pts',(1.81440879788158,-0.725283885226974,
1.93351296633465));
#277186=CARTESIAN_POINT('Ctrl Pts',(1.78891348175653,-0.789064325995465,
1.92960867659959));
#277187=CARTESIAN_POINT('Ctrl Pts',(1.76005397366994,-0.851491658445897,
1.92570438686453));
#277188=CARTESIAN_POINT('Ctrl Pts',(1.72800838712072,-0.91219680663794,
1.92180009712947));
#277189=CARTESIAN_POINT('Ctrl Pts',(1.69592866686687,-0.972966615578026,
1.91789164869778));
#277190=CARTESIAN_POINT('Ctrl Pts',(1.6606563254714,-1.03201014353248,1.9139832002661));
#277191=CARTESIAN_POINT('Ctrl Pts',(1.62241508541658,-1.08898360438196,
1.91007475183441));
#277192=CARTESIAN_POINT('Ctrl Pts',(1.58415095533317,-1.14599116779049,
1.90616396392586));
#277193=CARTESIAN_POINT('Ctrl Pts',(1.5429146851814,-1.20092580466354,1.90225317601731));
#277194=CARTESIAN_POINT('Ctrl Pts',(1.49897123651761,-1.25347566075009,
1.89834238810876));
#277195=CARTESIAN_POINT('Ctrl Pts',(1.45495191158654,-1.30611625361418,
1.89442484752154));
#277196=CARTESIAN_POINT('Ctrl Pts',(1.40821641355045,-1.3563634873396,1.89050730693432));
#277197=CARTESIAN_POINT('Ctrl Pts',(1.35906696886309,-1.403941941159,1.8865897663471));
#277198=CARTESIAN_POINT('Ctrl Pts',(1.33587065457882,-1.42639681882801,
1.88474086442643));
#277199=CARTESIAN_POINT('Ctrl Pts',(1.31213713815235,-1.44825782905257,
1.88289196250575));
#277200=CARTESIAN_POINT('Ctrl Pts',(1.28790058829699,-1.46949925983794,
1.88104306058508));
#277201=CARTESIAN_POINT('Ctrl Pts',(1.23653949008005,-1.51451322508245,
1.87712494378595));
#277202=CARTESIAN_POINT('Ctrl Pts',(1.18271378322824,-1.55692046485142,
1.87320682698681));
#277203=CARTESIAN_POINT('Ctrl Pts',(1.12671883981177,-1.59643999449188,
1.86928871018768));
#277204=CARTESIAN_POINT('Ctrl Pts',(1.07080821544005,-1.6359000143126,1.8653764934189));
#277205=CARTESIAN_POINT('Ctrl Pts',(1.01273523600505,-1.67248067271155,
1.86146427665012));
#277206=CARTESIAN_POINT('Ctrl Pts',(0.952829359406696,-1.70594027206483,
1.85755205988134));
#277207=CARTESIAN_POINT('Ctrl Pts',(0.892993928424069,-1.73936052499314,
1.85364444363817));
#277208=CARTESIAN_POINT('Ctrl Pts',(0.831330308286831,-1.76966676917587,
1.84973682739499));
#277209=CARTESIAN_POINT('Ctrl Pts',(0.768196511093922,-1.79666082507053,
1.84582921115182));
#277210=CARTESIAN_POINT('Ctrl Pts',(0.705102283544324,-1.82363796221152,
1.84192404404029));
#277211=CARTESIAN_POINT('Ctrl Pts',(0.640540158052951,-1.84730683613038,
1.83801887692877));
#277212=CARTESIAN_POINT('Ctrl Pts',(0.574890895038697,-1.8675161200915,
1.83411370981725));
#277213=CARTESIAN_POINT('Ctrl Pts',(0.509260261642748,-1.88771966916346,
1.83020965089444));
#277214=CARTESIAN_POINT('Ctrl Pts',(0.442543573042965,-1.9044654325612,
1.82630559197164));
#277215=CARTESIAN_POINT('Ctrl Pts',(0.375137908571045,-1.91765157146781,
1.82240153304883));
#277216=CARTESIAN_POINT('Ctrl Pts',(0.307728253836181,-1.93083849096402,
1.81849724301456));
#277217=CARTESIAN_POINT('Ctrl Pts',(0.239630025475597,-1.9404652756969,
1.8145929529803));
#277218=CARTESIAN_POINT('Ctrl Pts',(0.171249891851364,-1.9464813059829,
1.81068866294603));
#277219=CARTESIAN_POINT('Ctrl Pts',(0.102796922562699,-1.95250374429328,
1.80678021422497));
#277220=CARTESIAN_POINT('Ctrl Pts',(0.0340619396847903,-1.95490770949013,
1.80287176550391));
#277221=CARTESIAN_POINT('Ctrl Pts',(-0.0345448876872097,-1.95369461552585,
1.79896331678284));
#277222=CARTESIAN_POINT('Ctrl Pts',(-0.103192780899194,-1.95248079544254,
1.7950525285901));
#277223=CARTESIAN_POINT('Ctrl Pts',(-0.171711875212067,-1.94764564196821,
1.79114174039736));
#277224=CARTESIAN_POINT('Ctrl Pts',(-0.239696451164668,-1.93924253545013,
1.78723095220461));
#277225=CARTESIAN_POINT('Ctrl Pts',(-0.307798414516753,-1.93082491948182,
1.78331341134409));
#277226=CARTESIAN_POINT('Ctrl Pts',(-0.375363533421236,-1.91882714065102,
1.77939587048356));
#277227=CARTESIAN_POINT('Ctrl Pts',(-0.441996475697194,-1.90335364960673,
1.77547832962303));
#277228=CARTESIAN_POINT('Ctrl Pts',(-0.473444161442377,-1.89605087312529,
1.77362943041991));
#277229=CARTESIAN_POINT('Ctrl Pts',(-0.504684438554311,-1.88797463520856,
1.77178053121678));
#277230=CARTESIAN_POINT('Ctrl Pts',(-0.53567717040266,-1.87913968855681,
1.76993163201366));
#277231=CARTESIAN_POINT('Ctrl Pts',(-0.601355806447537,-1.86041700065518,
1.76601351410009));
#277232=CARTESIAN_POINT('Ctrl Pts',(-0.666181878691961,-1.8382097089528,
1.76209539618651));
#277233=CARTESIAN_POINT('Ctrl Pts',(-0.729759099842181,-1.81261348781187,
1.75817727827294));
#277234=CARTESIAN_POINT('Ctrl Pts',(-0.793240584466634,-1.78705581024427,
1.75426506038126));
#277235=CARTESIAN_POINT('Ctrl Pts',(-0.855476497621202,-1.75811951341578,
1.75035284248957));
#277236=CARTESIAN_POINT('Ctrl Pts',(-0.916085061160763,-1.72595021965238,
1.74644062459789));
#277237=CARTESIAN_POINT('Ctrl Pts',(-0.976622352896508,-1.693818754926,
1.74253300722484));
#277238=CARTESIAN_POINT('Ctrl Pts',(-1.03553566315849,-1.65846207320843,
1.7386253898518));
#277239=CARTESIAN_POINT('Ctrl Pts',(-1.09246427829761,-1.62007339359786,
1.73471777247875));
#277240=CARTESIAN_POINT('Ctrl Pts',(-1.1493572130075,-1.58170877437524,
1.7308126042337));
#277241=CARTESIAN_POINT('Ctrl Pts',(-1.20426751323631,-1.54031620129325,
1.72690743598865));
#277242=CARTESIAN_POINT('Ctrl Pts',(-1.25686148103153,-1.49613342235886,
1.7230022677436));
#277243=CARTESIAN_POINT('Ctrl Pts',(-1.30944052400483,-1.45196318136628,
1.71909820768534));
#277244=CARTESIAN_POINT('Ctrl Pts',(-1.35970416298529,-1.40500462259933,
1.71519414762709));
#277245=CARTESIAN_POINT('Ctrl Pts',(-1.40735141751415,-1.35553605175993,
1.71129008756883));
#277246=CARTESIAN_POINT('Ctrl Pts',(-1.45500149265431,-1.30606455249137,
1.70738579639892));
#277247=CARTESIAN_POINT('Ctrl Pts',(-1.50003453646376,-1.25408310220287,
1.70348150522901));
#277248=CARTESIAN_POINT('Ctrl Pts',(-1.54218739149781,-1.19990585026708,
1.6995772140591));
#277249=CARTESIAN_POINT('Ctrl Pts',(-1.58438514589974,-1.14567089110451,
1.69566876420989));
#277250=CARTESIAN_POINT('Ctrl Pts',(-1.6236962864148,-1.08923585159076,
1.69176031436068));
#277251=CARTESIAN_POINT('Ctrl Pts',(-1.65989946598296,-1.03094605233712,
1.68785186451148));
#277252=CARTESIAN_POINT('Ctrl Pts',(-1.69612431557922,-0.97262136273397,
1.68394107519322));
#277253=CARTESIAN_POINT('Ctrl Pts',(-1.72923726469211,-0.912440134903767,
1.68003028587496));
#277254=CARTESIAN_POINT('Ctrl Pts',(-1.7590630335812,-0.850772145693606,
1.6761194965567));
#277255=CARTESIAN_POINT('Ctrl Pts',(-1.78894030180151,-0.788997676070033,
1.67220195458656));
#277256=CARTESIAN_POINT('Ctrl Pts',(-1.81551887123367,-0.725731774693214,
1.66828441261642));
#277257=CARTESIAN_POINT('Ctrl Pts',(-1.83867199814743,-0.661363200691231,
1.66436687064629));
#277258=CARTESIAN_POINT('Ctrl Pts',(-1.84959914674408,-0.63098436781505,
1.66251798157827));
#277259=CARTESIAN_POINT('Ctrl Pts',(-1.85976404653653,-0.600360129903417,
1.66066909251025));
#277260=CARTESIAN_POINT('Ctrl Pts',(-1.86915731446041,-0.569532206112297,
1.65882020344223));
#277261=CARTESIAN_POINT('Ctrl Pts',(-1.8935023589502,-0.489633795643859,
1.65402833686476));
#277262=CARTESIAN_POINT('Ctrl Pts',(-1.9127392853033,-0.408111000000661,
1.6492364702873));
#277263=CARTESIAN_POINT('Ctrl Pts',(-1.92668893233299,-0.325554539248911,
1.64444460370984));
#277264=CARTESIAN_POINT('Ctrl Pts',(-1.94044092837958,-0.244167811723697,
1.63972063255209));
#277265=CARTESIAN_POINT('Ctrl Pts',(-1.9490543683818,-0.161776482890145,
1.63499666139434));
#277266=CARTESIAN_POINT('Ctrl Pts',(-1.95240368494034,-0.0789674048668311,
1.63027269023658));
#277267=CARTESIAN_POINT('Ctrl Pts',(-1.9534442621557,-0.0532399950175315,
1.62880503059113));
#277268=CARTESIAN_POINT('Ctrl Pts',(-1.95397706656825,-0.0274724170513964,
1.62733737094568));
#277269=CARTESIAN_POINT('Ctrl Pts',(-1.95399927547201,-0.00168269273987639,
1.62586971130023));
#277270=CARTESIAN_POINT('',(-1.95128155810217,0.000979544143981243,0.92586969212423));
#277271=CARTESIAN_POINT('Ctrl Pts',(-1.95279584397335,-0.00168131964740442,
1.62586969212423));
#277272=CARTESIAN_POINT('Ctrl Pts',(-1.94903635596163,0.455855006369031,
1.59981605303975));
#277273=CARTESIAN_POINT('Ctrl Pts',(-1.5604097983178,1.56956480808681,1.53672527109813));
#277274=CARTESIAN_POINT('Ctrl Pts',(0.295037094833478,2.29041656967945,
1.43659734629937));
#277275=CARTESIAN_POINT('Ctrl Pts',(2.08408386827561,0.994813055513272,
1.32548591772794));
#277276=CARTESIAN_POINT('Ctrl Pts',(1.96637633306231,-1.2109595884189,1.21437448915651));
#277277=CARTESIAN_POINT('Ctrl Pts',(0.0496077971367581,-2.30880576088663,
1.10326306058507));
#277278=CARTESIAN_POINT('Ctrl Pts',(-1.64866235520027,-1.43074427962715,
1.00709479490765));
#277279=CARTESIAN_POINT('Ctrl Pts',(-1.94952086313801,-0.387778936703525,
0.94796367208737));
#277280=CARTESIAN_POINT('Ctrl Pts',(-1.95128155810217,0.000979544143981243,
0.92586969212423));
#277281=CARTESIAN_POINT('Ctrl Pts',(-1.95128155810217,0.000979544143981243,
0.92586969212423));
#277282=CARTESIAN_POINT('Ctrl Pts',(-1.95247239613589,0.26391457510812,
0.910926529230228));
#277283=CARTESIAN_POINT('Ctrl Pts',(-1.78053982253993,1.17704879552172,
0.858946223479081));
#277284=CARTESIAN_POINT('Ctrl Pts',(-0.393146886163405,2.27561306770598,
0.769928774870794));
#277285=CARTESIAN_POINT('Ctrl Pts',(1.69830019267039,1.56491440632532,0.658817346299364));
#277286=CARTESIAN_POINT('Ctrl Pts',(2.23593132308835,-0.577660774765208,
0.547705917727936));
#277287=CARTESIAN_POINT('Ctrl Pts',(0.727920063175579,-2.19150414145949,
0.436594489156507));
#277288=CARTESIAN_POINT('Ctrl Pts',(-1.37114873684965,-1.8142179137927,
0.329316074498916));
#277289=CARTESIAN_POINT('Ctrl Pts',(-1.95230321089235,-0.579086516543689,
0.259074802698467));
#277290=CARTESIAN_POINT('Ctrl Pts',(-1.95633516444562,0.00125643977877596,
0.225870673755162));
#277291=CARTESIAN_POINT('Origin',(0.,0.,-1.29405622560371));
#277292=CARTESIAN_POINT('',(-1.5554991203045,0.00165430708296759,19.3559437744328));
#277293=CARTESIAN_POINT('Ctrl Pts',(1.43457668357356,0.601306900797836,
19.0501843444911));
#277294=CARTESIAN_POINT('Ctrl Pts',(1.41216525140568,0.65477530102884,19.0543252140175));
#277295=CARTESIAN_POINT('Ctrl Pts',(1.38675571510824,0.707000646875421,
19.0584660835438));
#277296=CARTESIAN_POINT('Ctrl Pts',(1.35851806141379,0.757633768263079,
19.0626069530701));
#277297=CARTESIAN_POINT('Ctrl Pts',(1.33025588857326,0.808310855091825,
19.0667514181709));
#277298=CARTESIAN_POINT('Ctrl Pts',(1.29916094303211,0.857392499965521,
19.0708958832716));
#277299=CARTESIAN_POINT('Ctrl Pts',(1.26544878283799,0.904554933662872,
19.0750403483724));
#277300=CARTESIAN_POINT('Ctrl Pts',(1.23172305766809,0.951736344407892,
19.0791864811078));
#277301=CARTESIAN_POINT('Ctrl Pts',(1.19537834213245,0.996996597851846,
19.0833326138433));
#277302=CARTESIAN_POINT('Ctrl Pts',(1.15667116469418,1.04004426192591,19.0874787465787));
#277303=CARTESIAN_POINT('Ctrl Pts',(1.11789124042643,1.08317283040286,19.0916326716161));
#277304=CARTESIAN_POINT('Ctrl Pts',(1.07674034965028,1.12408013174388,19.0957865966534));
#277305=CARTESIAN_POINT('Ctrl Pts',(1.03351196134665,1.16251162392185,19.0999405216907));
#277306=CARTESIAN_POINT('Ctrl Pts',(0.994573128000671,1.19712955736511,
19.1036822525557));
#277307=CARTESIAN_POINT('Ctrl Pts',(0.953949324318807,1.229739010674,19.1074239834207));
#277308=CARTESIAN_POINT('Ctrl Pts',(0.911875475596432,1.26018386238111,
19.1111657142858));
#277309=CARTESIAN_POINT('Ctrl Pts',(0.865165552439733,1.29398340121437,
19.1153197426546));
#277310=CARTESIAN_POINT('Ctrl Pts',(0.816478836708566,1.32525119701336,
19.1194737710234));
#277311=CARTESIAN_POINT('Ctrl Pts',(0.766120348130251,1.3537502953576,19.1236277993922));
#277312=CARTESIAN_POINT('Ctrl Pts',(0.715849438396,1.38219983069547,19.1277746034575));
#277313=CARTESIAN_POINT('Ctrl Pts',(0.663912975180353,1.40788997309079,
19.1319214075229));
#277314=CARTESIAN_POINT('Ctrl Pts',(0.610645586257866,1.4306265124007,19.1360682115882));
#277315=CARTESIAN_POINT('Ctrl Pts',(0.557429987971653,1.45334094550527,
19.140210983813));
#277316=CARTESIAN_POINT('Ctrl Pts',(0.502886503168866,1.47310726328047,
19.1443537560377));
#277317=CARTESIAN_POINT('Ctrl Pts',(0.447373486568487,1.48977757182593,
19.1484965282625));
#277318=CARTESIAN_POINT('Ctrl Pts',(0.391893291858678,1.50643802410566,
19.1526368510866));
#277319=CARTESIAN_POINT('Ctrl Pts',(0.335445197875963,1.52000594727083,
19.1567771739108));
#277320=CARTESIAN_POINT('Ctrl Pts',(0.278404563902768,1.53038268050776,
19.1609174967349));
#277321=CARTESIAN_POINT('Ctrl Pts',(0.22137592216974,1.54075723213715,19.1650569490964));
#277322=CARTESIAN_POINT('Ctrl Pts',(0.163755498144067,1.54794183323517,
19.1691964014578));
#277323=CARTESIAN_POINT('Ctrl Pts',(0.10592858108544,1.55188897338348,19.1733358538192));
#277324=CARTESIAN_POINT('Ctrl Pts',(0.0480488391534791,1.55583971924327,
19.1774790875693));
#277325=CARTESIAN_POINT('Ctrl Pts',(-0.0100372538376572,1.55654705787194,
19.1816223213193));
#277326=CARTESIAN_POINT('Ctrl Pts',(-0.0679408912885707,1.55401553573023,
19.1857655550694));
#277327=CARTESIAN_POINT('Ctrl Pts',(-0.12586890829889,1.55148294772466,
19.1899105332731));
#277328=CARTESIAN_POINT('Ctrl Pts',(-0.183613799011935,1.54570883074677,
19.1940555114768));
#277329=CARTESIAN_POINT('Ctrl Pts',(-0.240791598067284,1.53674970515703,
19.1982004896806));
#277330=CARTESIAN_POINT('Ctrl Pts',(-0.298080326888325,1.52777319810596,
19.2023535094926));
#277331=CARTESIAN_POINT('Ctrl Pts',(-0.354799255932419,1.51559944214355,
19.2065065293045));
#277332=CARTESIAN_POINT('Ctrl Pts',(-0.410575232362685,1.50033603854947,
19.2106595491165));
#277333=CARTESIAN_POINT('Ctrl Pts',(-0.462584185204256,1.48610350173825,
19.2145320803634));
#277334=CARTESIAN_POINT('Ctrl Pts',(-0.513773077525469,1.46918519379234,
19.2184046116103));
#277335=CARTESIAN_POINT('Ctrl Pts',(-0.563855216483735,1.4497060201448,
19.2222771428572));
#277336=CARTESIAN_POINT('Ctrl Pts',(-0.616912826678665,1.42906955325644,
19.2263797482498));
#277337=CARTESIAN_POINT('Ctrl Pts',(-0.668961426240364,1.40546750481788,
19.2304823536425));
#277338=CARTESIAN_POINT('Ctrl Pts',(-0.719642355782659,1.37901962631559,
19.2345849590351));
#277339=CARTESIAN_POINT('Ctrl Pts',(-0.77049884857814,1.35248013000692,
19.2387017762182));
#277340=CARTESIAN_POINT('Ctrl Pts',(-0.819977650252828,1.32307518099454,
19.2428185934012));
#277341=CARTESIAN_POINT('Ctrl Pts',(-0.867733843715434,1.29097568779231,
19.2469354105843));
#277342=CARTESIAN_POINT('Ctrl Pts',(-0.915193225731834,1.25907569744635,
19.2510266411707));
#277343=CARTESIAN_POINT('Ctrl Pts',(-0.960950890138361,1.22451483889158,
19.255117871757));
#277344=CARTESIAN_POINT('Ctrl Pts',(-1.00469287591273,1.18750683159728,
19.2592091023434));
#277345=CARTESIAN_POINT('Ctrl Pts',(-1.04840932105716,1.15052043301146,
19.2632979440897));
#277346=CARTESIAN_POINT('Ctrl Pts',(-1.09011201223326,1.11109005909351,
19.2673867858361));
#277347=CARTESIAN_POINT('Ctrl Pts',(-1.1295188048071,1.06947067261666,19.2714756275824));
#277348=CARTESIAN_POINT('Ctrl Pts',(-1.16891852586963,1.02785875469899,
19.27556373559));
#277349=CARTESIAN_POINT('Ctrl Pts',(-1.20602279940129,0.984058990653992,
19.2796518435976));
#277350=CARTESIAN_POINT('Ctrl Pts',(-1.24058691992718,0.938362586693218,
19.2837399516052));
#277351=CARTESIAN_POINT('Ctrl Pts',(-1.27556766726258,0.892115370309084,
19.2878773365905));
#277352=CARTESIAN_POINT('Ctrl Pts',(-1.30794624959268,0.843925907830145,
19.2920147215758));
#277353=CARTESIAN_POINT('Ctrl Pts',(-1.33751322872518,0.794127579791279,
19.2961521065611));
#277354=CARTESIAN_POINT('Ctrl Pts',(-1.36677378652093,0.744845343375333,
19.3002466132045));
#277355=CARTESIAN_POINT('Ctrl Pts',(-1.39328056462831,0.693987948459924,
19.304341119848));
#277356=CARTESIAN_POINT('Ctrl Pts',(-1.41687753982944,0.641902085311207,
19.3084356264915));
#277357=CARTESIAN_POINT('Ctrl Pts',(-1.44084518209379,0.588998044673036,
19.3125944506477));
#277358=CARTESIAN_POINT('Ctrl Pts',(-1.46181059972095,0.53482713688006,
19.3167532748039));
#277359=CARTESIAN_POINT('Ctrl Pts',(-1.47966264316261,0.479769436739197,
19.32091209896));
#277360=CARTESIAN_POINT('Ctrl Pts',(-1.49751468660427,0.424711736598334,
19.3250709231162));
#277361=CARTESIAN_POINT('Ctrl Pts',(-1.51225329463471,0.36876781285147,
19.3292297472724));
#277362=CARTESIAN_POINT('Ctrl Pts',(-1.52382169500351,0.312326258640937,
19.3333885714286));
#277363=CARTESIAN_POINT('Ctrl Pts',(-1.54270018455889,0.220219203414235,
19.3401753626783));
#277364=CARTESIAN_POINT('Ctrl Pts',(-1.55321832214834,0.126427694770151,
19.346962153928));
#277365=CARTESIAN_POINT('Ctrl Pts',(-1.55516758360058,0.0321564444232205,
19.3537489451776));
#277366=CARTESIAN_POINT('Ctrl Pts',(-1.55537771215927,0.021994091939033,
19.3544805549172));
#277367=CARTESIAN_POINT('Ctrl Pts',(-1.55548830227265,0.0118261996198327,
19.3552121646567));
#277368=CARTESIAN_POINT('Ctrl Pts',(-1.55549912030396,0.00165430758992738,
19.3559437743963));
#277369=CARTESIAN_POINT('Ctrl Pts',(-1.5554991203045,0.00165430708298941,
19.3559437744328));
#277370=CARTESIAN_POINT('Ctrl Pts',(-1.55556084030585,-0.056379300333557,
19.3601178211375));
#277371=CARTESIAN_POINT('Ctrl Pts',(-1.55237061563408,-0.114519110625628,
19.3642918678422));
#277372=CARTESIAN_POINT('Ctrl Pts',(-1.54591951792332,-0.172374865057931,
19.3684659145469));
#277373=CARTESIAN_POINT('Ctrl Pts',(-1.53947673878304,-0.230156015571265,
19.372634578896));
#277374=CARTESIAN_POINT('Ctrl Pts',(-1.52978148020292,-0.287653331891395,
19.3768032432451));
#277375=CARTESIAN_POINT('Ctrl Pts',(-1.51687679201396,-0.344477935214204,
19.3809719075943));
#277376=CARTESIAN_POINT('Ctrl Pts',(-1.5039840172698,-0.401250078782456,
19.3851367234852));
#277377=CARTESIAN_POINT('Ctrl Pts',(-1.48788780344455,-0.457350244605693,
19.3893015393762));
#277378=CARTESIAN_POINT('Ctrl Pts',(-1.46868254079216,-0.512398130726777,
19.3934663552672));
#277379=CARTESIAN_POINT('Ctrl Pts',(-1.44907153883229,-0.568608984082246,
19.3977191589949));
#277380=CARTESIAN_POINT('Ctrl Pts',(-1.4262186995935,-0.62372204056427,
19.4019719627227));
#277381=CARTESIAN_POINT('Ctrl Pts',(-1.40027824131161,-0.67734857858363,
19.4062247664504));
#277382=CARTESIAN_POINT('Ctrl Pts',(-1.37488544150799,-0.729842945849225,
19.4103877844082));
#277383=CARTESIAN_POINT('Ctrl Pts',(-1.34653441421956,-0.7809125017701,
19.4145508023661));
#277384=CARTESIAN_POINT('Ctrl Pts',(-1.31541745783214,-0.830215129728687,
19.418713820324));
#277385=CARTESIAN_POINT('Ctrl Pts',(-1.28329383035402,-0.881112757199572,
19.4230115169366));
#277386=CARTESIAN_POINT('Ctrl Pts',(-1.2482224869797,-0.9301266417569,19.4273092135493));
#277387=CARTESIAN_POINT('Ctrl Pts',(-1.21046337906679,-0.976912820029617,
19.431606910162));
#277388=CARTESIAN_POINT('Ctrl Pts',(-1.17270427115388,-1.02369899830233,
19.4359046067747));
#277389=CARTESIAN_POINT('Ctrl Pts',(-1.1322578120547,-1.06825703820874,
19.4402023033873));
#277390=CARTESIAN_POINT('Ctrl Pts',(-1.08942750315405,-1.11028283125136,
19.4445));
#277391=CARTESIAN_POINT('Ctrl Pts',(1.43457668357355,0.601306900797844,
19.188224604057));
#277392=CARTESIAN_POINT('Ctrl Pts',(1.41216743227266,0.654770097993729,
19.1923698776825));
#277393=CARTESIAN_POINT('Ctrl Pts',(1.38678365308771,0.706935688811212,
19.196515151308));
#277394=CARTESIAN_POINT('Ctrl Pts',(1.35861269545265,0.757464054430887,
19.2006604249335));
#277395=CARTESIAN_POINT('Ctrl Pts',(1.33038896676601,0.808087071962046,
19.2048134636641));
#277396=CARTESIAN_POINT('Ctrl Pts',(1.29936790941001,0.857066299073572,
19.2089665023947));
#277397=CARTESIAN_POINT('Ctrl Pts',(1.26578076354097,0.904090321068441,
19.2131195411254));
#277398=CARTESIAN_POINT('Ctrl Pts',(1.24133295867943,0.938318716598623,
19.2161425035666));
#277399=CARTESIAN_POINT('Ctrl Pts',(1.21552649144371,0.971511806329961,
19.2191654660078));
#277400=CARTESIAN_POINT('Ctrl Pts',(1.18846325072905,1.00356133428233,19.222188428449));
#277401=CARTESIAN_POINT('Ctrl Pts',(1.1517364653547,1.04705487398317,19.2262908082764));
#277402=CARTESIAN_POINT('Ctrl Pts',(1.11253187745988,1.08863250047883,19.2303931881038));
#277403=CARTESIAN_POINT('Ctrl Pts',(1.07107902497437,1.12799378201298,19.2344955679313));
#277404=CARTESIAN_POINT('Ctrl Pts',(1.0294613286051,1.16751158996519,19.2386142615268));
#277405=CARTESIAN_POINT('Ctrl Pts',(0.985577740531738,1.20479492777059,
19.2427329551224));
#277406=CARTESIAN_POINT('Ctrl Pts',(0.939702167676443,1.2395725416708,19.2468516487179));
#277407=CARTESIAN_POINT('Ctrl Pts',(0.894135131767176,1.27411625813681,
19.2509426419696));
#277408=CARTESIAN_POINT('Ctrl Pts',(0.846603236937218,1.30618750689656,
19.2550336352213));
#277409=CARTESIAN_POINT('Ctrl Pts',(0.797410439026016,1.33555862534459,
19.2591246284729));
#277410=CARTESIAN_POINT('Ctrl Pts',(0.748246399707,1.36491257314868,19.2632132300898));
#277411=CARTESIAN_POINT('Ctrl Pts',(0.697423837101224,1.39156924397987,
19.2673018317067));
#277412=CARTESIAN_POINT('Ctrl Pts',(0.645275403958348,1.41534444678544,
19.2713904333236));
#277413=CARTESIAN_POINT('Ctrl Pts',(0.593136361375232,1.43911536830298,
19.275478298691));
#277414=CARTESIAN_POINT('Ctrl Pts',(0.539672406972039,1.4600056302342,19.2795661640584));
#277415=CARTESIAN_POINT('Ctrl Pts',(0.485238336597361,1.47787821104996,
19.2836540294258));
#277416=CARTESIAN_POINT('Ctrl Pts',(0.430098739008545,1.49598244075887,
19.287794878159));
#277417=CARTESIAN_POINT('Ctrl Pts',(0.373964217362291,1.51098999177411,
19.2919357268923));
#277418=CARTESIAN_POINT('Ctrl Pts',(0.317219060538567,1.5228106637501,19.2960765756255));
#277419=CARTESIAN_POINT('Ctrl Pts',(0.261112250559756,1.53449836070086,
19.3001708424498));
#277420=CARTESIAN_POINT('Ctrl Pts',(0.2044090212878,1.54307051340458,19.3042651092742));
#277421=CARTESIAN_POINT('Ctrl Pts',(0.147487896314991,1.54849203111949,
19.3083593760985));
#277422=CARTESIAN_POINT('Ctrl Pts',(0.0895953539540989,1.55400607259568,
19.3125235157862));
#277423=CARTESIAN_POINT('Ctrl Pts',(0.0314779830049255,1.55626090059159,
19.3166876554739));
#277424=CARTESIAN_POINT('Ctrl Pts',(-0.0264670923239539,1.55527481270157,
19.3208517951615));
#277425=CARTESIAN_POINT('Ctrl Pts',(-0.0844121676528332,1.55428872481156,
19.3250159348492));
#277426=CARTESIAN_POINT('Ctrl Pts',(-0.142184385757248,1.55006184865992,
19.3291800745368));
#277427=CARTESIAN_POINT('Ctrl Pts',(-0.199396272421212,1.54266696877341,
19.3333442142245));
#277428=CARTESIAN_POINT('Ctrl Pts',(-0.257983830795176,1.53509427746251,
19.3376084815167));
#277429=CARTESIAN_POINT('Ctrl Pts',(-0.316239637736243,1.52416678472547,
19.341872748809));
#277430=CARTESIAN_POINT('Ctrl Pts',(-0.373762636432102,1.50992772727946,
19.3461370161012));
#277431=CARTESIAN_POINT('Ctrl Pts',(-0.431161723190074,1.49571934259465,
19.3503920976132));
#277432=CARTESIAN_POINT('Ctrl Pts',(-0.487830672928362,1.47821369472334,
19.3546471791252));
#277433=CARTESIAN_POINT('Ctrl Pts',(-0.543377082667122,1.45750526449552,
19.3589022606373));
#277434=CARTESIAN_POINT('Ctrl Pts',(-0.59885268524449,1.43682323210635,
19.3631519180319));
#277435=CARTESIAN_POINT('Ctrl Pts',(-0.653208136621592,1.41294669183088,
19.3674015754266));
#277436=CARTESIAN_POINT('Ctrl Pts',(-0.706065742672148,1.38601999156752,
19.3716512328213));
#277437=CARTESIAN_POINT('Ctrl Pts',(-0.75887202062975,1.35911943884049,
19.3758967635287));
#277438=CARTESIAN_POINT('Ctrl Pts',(-0.810182910949864,1.32917482829704,
19.3801422942362));
#277439=CARTESIAN_POINT('Ctrl Pts',(-0.859641922762942,1.29637803692767,
19.3843878249436));
#277440=CARTESIAN_POINT('Ctrl Pts',(-0.909067905774261,1.26360314730443,
19.3886305204793));
#277441=CARTESIAN_POINT('Ctrl Pts',(-0.956644063784778,1.22798012937832,
19.392873216015));
#277442=CARTESIAN_POINT('Ctrl Pts',(-1.00204122892994,1.18974519352867,
19.3971159115506));
#277443=CARTESIAN_POINT('Ctrl Pts',(-1.04743549440577,1.15151269987273,
19.4013583360911));
#277444=CARTESIAN_POINT('Ctrl Pts',(-1.0906506639901,1.11066892264387,19.4056007606316));
#277445=CARTESIAN_POINT('Ctrl Pts',(-1.13139026211381,1.06749066731005,
19.4098431851721));
#277446=CARTESIAN_POINT('Ctrl Pts',(-1.17212552180437,1.02431701010636,
19.4140851579292));
#277447=CARTESIAN_POINT('Ctrl Pts',(-1.21038540545579,0.978809726755231,
19.4183271306862));
#277448=CARTESIAN_POINT('Ctrl Pts',(-1.24591151176093,0.931281243696875,
19.4225691034433));
#277449=CARTESIAN_POINT('Ctrl Pts',(-1.28146386078651,0.883717651902334,
19.4268142096961));
#277450=CARTESIAN_POINT('Ctrl Pts',(-1.31427811083376,0.834130270116786,
19.431059315949));
#277451=CARTESIAN_POINT('Ctrl Pts',(-1.34413794171349,0.782862340163462,
19.4353044222019));
#277452=CARTESIAN_POINT('Ctrl Pts',(-1.36569832846932,0.745844166737887,
19.4383696148012));
#277453=CARTESIAN_POINT('Ctrl Pts',(-1.38571928238916,0.707950473050287,
19.4414348074006));
#277454=CARTESIAN_POINT('Ctrl Pts',(-1.40413430885519,0.669318379170746,
19.4445));
#277455=CARTESIAN_POINT('Origin',(0.,0.,19.5));
#277456=CARTESIAN_POINT('Ctrl Pts',(-1.47185199869187,1.28247177392349,
19.0478006871829));
#277457=CARTESIAN_POINT('Ctrl Pts',(-1.51144177862091,1.22242094713282,
19.057401752771));
#277458=CARTESIAN_POINT('Ctrl Pts',(-1.54765772157622,1.16040792388231,
19.0669290794631));
#277459=CARTESIAN_POINT('Ctrl Pts',(-1.58029338748837,1.09674732240684,
19.0764143170251));
#277460=CARTESIAN_POINT('Ctrl Pts',(-1.61209525197559,1.03471317158705,
19.0856572183462));
#277461=CARTESIAN_POINT('Ctrl Pts',(-1.64049721800471,0.971114777397238,
19.0948602908743));
#277462=CARTESIAN_POINT('Ctrl Pts',(-1.66529723976271,0.906247628640641,
19.1040834245205));
#277463=CARTESIAN_POINT('Ctrl Pts',(-1.68190479772454,0.862808758170836,
19.110259779046));
#277464=CARTESIAN_POINT('Ctrl Pts',(-1.69689691388732,0.818801033375964,
19.1164457635402));
#277465=CARTESIAN_POINT('Ctrl Pts',(-1.71021021312761,0.774313234575083,
19.1226667961376));
#277466=CARTESIAN_POINT('Ctrl Pts',(-1.7216141158004,0.736205886539485,
19.1279956067491));
#277467=CARTESIAN_POINT('Ctrl Pts',(-1.73178621748778,0.697746318117437,
19.133350240274));
#277468=CARTESIAN_POINT('Ctrl Pts',(-1.74068496568679,0.658989750956657,
19.1387499787417));
#277469=CARTESIAN_POINT('Ctrl Pts',(-1.7432210526171,0.647944374546164,
19.1402888700384));
#277470=CARTESIAN_POINT('Ctrl Pts',(-1.74565316923663,0.636876891220236,
19.1418311622824));
#277471=CARTESIAN_POINT('Ctrl Pts',(-1.74797838874301,0.625799357894018,
19.1433758366721));
#277472=CARTESIAN_POINT('Ctrl Pts',(-1.76164806252324,0.560675929141002,
19.1524567836303));
#277473=CARTESIAN_POINT('Ctrl Pts',(-1.77165033127344,0.495102739838834,
19.1616335477411));
#277474=CARTESIAN_POINT('Ctrl Pts',(-1.77788723803438,0.429303598977395,
19.171015415248));
#277475=CARTESIAN_POINT('Ctrl Pts',(-1.77990435472474,0.40802309081357,
19.174049663195));
#277476=CARTESIAN_POINT('Ctrl Pts',(-1.78152735810959,0.386718695885184,
19.1771054696483));
#277477=CARTESIAN_POINT('Ctrl Pts',(-1.782752068437,0.365397267570637,19.1801867951176));
#277478=CARTESIAN_POINT('Ctrl Pts',(-1.78664149044997,0.297684902631543,
19.1899724357224));
#277479=CARTESIAN_POINT('Ctrl Pts',(-1.78651848057804,0.229795248329717,
19.2000151467373));
#277480=CARTESIAN_POINT('Ctrl Pts',(-1.78241468021328,0.161998904792477,
19.2102386367469));
#277481=CARTESIAN_POINT('Ctrl Pts',(-1.77917700700339,0.108511311418388,
19.2183044091465));
#277482=CARTESIAN_POINT('Ctrl Pts',(-1.77345979502346,0.0550827527395637,
19.2264826262492));
#277483=CARTESIAN_POINT('Ctrl Pts',(-1.76525906565932,0.00187739191350949,
19.2347399360171));
#277484=CARTESIAN_POINT('Ctrl Pts',(1.13606316703866,-1.59291762710367,
-0.2315727930662));
#277485=CARTESIAN_POINT('Ctrl Pts',(1.66580206489195,-1.21512977859719,
-0.19452378898432));
#277486=CARTESIAN_POINT('Ctrl Pts',(2.30945033465884,0.103704944516998,
-0.120437642045298));
#277487=CARTESIAN_POINT('Ctrl Pts',(1.16340190037011,2.00012615618488,-0.00931435224913369));
#277488=CARTESIAN_POINT('Ctrl Pts',(-1.04789748215315,2.06050089268765,
0.101797076322295));
#277489=CARTESIAN_POINT('Ctrl Pts',(-2.29995644073094,0.238662326668711,
0.212908504893725));
#277490=CARTESIAN_POINT('Ctrl Pts',(-1.4480231663316,-1.80307307028203,
0.324019933465153));
#277491=CARTESIAN_POINT('Ctrl Pts',(0.72886412800377,-2.19434637934446,
0.435131362036582));
#277492=CARTESIAN_POINT('Ctrl Pts',(2.23883118012918,-0.578409963100118,
0.546242790608011));
#277493=CARTESIAN_POINT('Ctrl Pts',(1.70050277721327,1.56694399820618,0.657354219179439));
#277494=CARTESIAN_POINT('Ctrl Pts',(-0.393656772023556,2.27856438938052,
0.768465647750868));
#277495=CARTESIAN_POINT('Ctrl Pts',(-2.12764424093886,0.905559934895846,
0.879577076322298));
#277496=CARTESIAN_POINT('Ctrl Pts',(-1.91502951955452,-1.29598480721124,
0.990688504893724));
#277497=CARTESIAN_POINT('Ctrl Pts',(0.0496721352129712,-2.31180013131849,
1.10179993346515));
#277498=CARTESIAN_POINT('Ctrl Pts',(1.96892659486843,-1.2125301239951,1.21291136203658));
#277499=CARTESIAN_POINT('Ctrl Pts',(2.08678678907498,0.996103263138911,
1.32402279060801));
#277500=CARTESIAN_POINT('Ctrl Pts',(0.295419738695494,2.29338709053012,
1.43513421917944));
#277501=CARTESIAN_POINT('Ctrl Pts',(-1.76623022736053,1.49242425224886,
1.54624564775086));
#277502=CARTESIAN_POINT('Ctrl Pts',(-2.21193462336081,-0.673976513940082,
1.6573570763223));
#277503=CARTESIAN_POINT('Ctrl Pts',(-0.633912852843943,-2.22374754587002,
1.76846850489372));
#277504=CARTESIAN_POINT('Ctrl Pts',(1.52408352559897,-1.73898487447381,
1.87957993346515));
#277505=CARTESIAN_POINT('Ctrl Pts',(2.28767721897072,0.336796477013934,
1.99069136203658));
#277506=CARTESIAN_POINT('Ctrl Pts',(0.95824696965368,2.1044385505715,2.10180279060801));
#277507=CARTESIAN_POINT('Ctrl Pts',(-1.24789517519063,1.94670402200824,
2.21291421917944));
#277508=CARTESIAN_POINT('Ctrl Pts',(-2.31232272803813,0.00790610348200404,
2.32402564775087));
#277509=CARTESIAN_POINT('Ctrl Pts',(-1.26117786751997,-1.93812519847901,
2.4351370763223));
#277510=CARTESIAN_POINT('Ctrl Pts',(0.943834084851752,-2.11094199967052,
2.54624850489373));
#277511=CARTESIAN_POINT('Ctrl Pts',(2.28532066231724,-0.352432083948816,
2.65735993346515));
#277512=CARTESIAN_POINT('Ctrl Pts',(1.53593934849974,1.72852226495878,2.76847136203658));
#277513=CARTESIAN_POINT('Ctrl Pts',(-0.618691705176725,2.22803040322512,
2.87958279060801));
#277514=CARTESIAN_POINT('Ctrl Pts',(-2.20727413292089,0.689086210494794,
2.99069421917944));
#277515=CARTESIAN_POINT('Ctrl Pts',(-1.77639439610933,-1.48031140398554,
3.10180564775087));
#277516=CARTESIAN_POINT('Ctrl Pts',(0.279730351589628,-2.29535396700367,
3.21291707632229));
#277517=CARTESIAN_POINT('Ctrl Pts',(2.07992637124202,-1.01034904542294,
3.32402850489373));
#277518=CARTESIAN_POINT('Ctrl Pts',(1.97717225475611,1.19903660427677,3.43513993346515));
#277519=CARTESIAN_POINT('Ctrl Pts',(0.0654790030363215,2.31140896501537,
3.54625136203659));
#277520=CARTESIAN_POINT('Ctrl Pts',(-1.90612179130951,1.30904492668386,
3.65736279060801));
#277521=CARTESIAN_POINT('Ctrl Pts',(-2.13378839047699,-0.890980363446882,
3.76847421917944));
#277522=CARTESIAN_POINT('Ctrl Pts',(-0.409225831785102,-2.27583679599057,
3.87958564775087));
#277523=CARTESIAN_POINT('Ctrl Pts',(1.68974245735601,-1.57850224301131,
3.9906970763223));
#277524=CARTESIAN_POINT('Ctrl Pts',(2.24274465667945,0.563023363919505,
4.10180850489373));
#277525=CARTESIAN_POINT('Ctrl Pts',(0.743832274433361,2.18943199275407,
4.21291993346515));
#277526=CARTESIAN_POINT('Ctrl Pts',(-1.43562137478499,1.8127024498367,4.32403136203659));
#277527=CARTESIAN_POINT('Ctrl Pts',(-2.30160742805521,-0.222490787460244,
4.43514279060801));
#277528=CARTESIAN_POINT('Ctrl Pts',(-1.06182462858958,-2.0541244756597,
4.54625421917945));
#277529=CARTESIAN_POINT('Ctrl Pts',(1.14943454112788,-2.00641449831427,
4.65736564775087));
#277530=CARTESIAN_POINT('Ctrl Pts',(2.30906195754891,-0.123011298603022,
4.7684770763223));
#277531=CARTESIAN_POINT('Ctrl Pts',(1.35610028081068,1.87293644627061,4.87958850489373));
#277532=CARTESIAN_POINT('Ctrl Pts',(-0.837574168101038,2.15531167498194,
4.99069993346516));
#277533=CARTESIAN_POINT('Ctrl Pts',(-2.26494174228494,0.465765828972943,
5.10181136203659));
#277534=CARTESIAN_POINT('Ctrl Pts',(-1.6200863491512,-1.64991488407055,
5.21292279060802));
#277535=CARTESIAN_POINT('Ctrl Pts',(0.507005906446861,-2.25606824236582,
5.32403421917943));
#277536=CARTESIAN_POINT('Ctrl Pts',(2.17023224254229,-0.798117107205096,
5.43514564775089));
#277537=CARTESIAN_POINT('Ctrl Pts',(1.84788649373611,1.39004115394159,5.54625707632229));
#277538=CARTESIAN_POINT('Ctrl Pts',(-0.16511326255594,2.30643372198547,
5.65736850489374));
#277539=CARTESIAN_POINT('Ctrl Pts',(-2.02704887071144,1.11264180180822,
5.76847993346515));
#277540=CARTESIAN_POINT('Ctrl Pts',(-2.0344126162256,-1.09911974339729,
5.87959136203659));
#277541=CARTESIAN_POINT('Ctrl Pts',(-0.180467318050853,-2.30528316058985,
5.99070279060801));
#277542=CARTESIAN_POINT('Ctrl Pts',(1.83858974186744,-1.40231475228758,
6.10181421917945));
#277543=CARTESIAN_POINT('Ctrl Pts',(2.17549850655909,0.783648614713761,
6.21292564775089));
#277544=CARTESIAN_POINT('Ctrl Pts',(0.522017016837799,2.25264225688753,
6.3240370763223));
#277545=CARTESIAN_POINT('Ctrl Pts',(-1.60906424131313,1.66066588172064,
6.43514850489373));
#277546=CARTESIAN_POINT('Ctrl Pts',(-2.26799289858753,-0.450674067747575,
6.54625993346516));
#277547=CARTESIAN_POINT('Ctrl Pts',(-0.851907048237055,-2.14968678754548,
6.65737136203658));
#277548=CARTESIAN_POINT('Ctrl Pts',(1.34359900459318,-1.88192471109761,
6.76848279060803));
#277549=CARTESIAN_POINT('Ctrl Pts',(2.30982985612209,0.107633355195401,
6.87959421917944));
#277550=CARTESIAN_POINT('Ctrl Pts',(1.16276905467301,1.99871634527724,6.99070564775088));
#277551=CARTESIAN_POINT('Ctrl Pts',(-1.04812340999086,2.06114924758318,
7.10181707632231));
#277552=CARTESIAN_POINT('Ctrl Pts',(-2.30007491727047,0.237811434390506,
7.21292850489373));
#277553=CARTESIAN_POINT('Ctrl Pts',(-1.44765968471916,-1.80310297560135,
7.32403993346517));
#277554=CARTESIAN_POINT('Ctrl Pts',(0.729237141124034,-2.19433636787728,
7.43515136203658));
#277555=CARTESIAN_POINT('Ctrl Pts',(2.23894596639031,-0.577944515475454,
7.54626279060803));
#277556=CARTESIAN_POINT('Ctrl Pts',(1.700215678403,1.5672158595089,7.65737421917944));
#277557=CARTESIAN_POINT('Ctrl Pts',(-0.39406277773538,2.27851123117423,
7.76848564775089));
#277558=CARTESIAN_POINT('Ctrl Pts',(-2.12780836746792,0.905168743780466,
7.8795970763223));
#277559=CARTESIAN_POINT('Ctrl Pts',(-1.91479599570453,-1.2963237243133,
7.99070850489374));
#277560=CARTESIAN_POINT('Ctrl Pts',(0.0500867071799966,-2.31179372461027,
8.10181993346516));
#277561=CARTESIAN_POINT('Ctrl Pts',(1.96914446762206,-1.21217530457315,
8.2129313620366));
#277562=CARTESIAN_POINT('Ctrl Pts',(2.08660781369462,0.996477162413753,
8.32404279060801));
#277563=CARTESIAN_POINT('Ctrl Pts',(0.295008090021127,2.29344045708749,
8.43515421917946));
#277564=CARTESIAN_POINT('Ctrl Pts',(-1.76649815189665,1.49210696088762,
8.54626564775088));
#277565=CARTESIAN_POINT('Ctrl Pts',(-2.21181357806678,-0.674373486476905,
8.65737707632231));
#277566=CARTESIAN_POINT('Ctrl Pts',(-0.633513645693009,-2.22386136350815,
8.76848850489374));
#277567=CARTESIAN_POINT('Ctrl Pts',(1.52439568775516,-1.73871121539405,
8.87959993346515));
#277568=CARTESIAN_POINT('Ctrl Pts',(2.28761671798039,0.337207139604478,
8.99071136203661));
#277569=CARTESIAN_POINT('Ctrl Pts',(0.957869167637863,2.10461054855105,
9.10182279060801));
#277570=CARTESIAN_POINT('Ctrl Pts',(-1.24824462727842,1.94647996492492,
9.21293421917946));
#277571=CARTESIAN_POINT('Ctrl Pts',(-2.31232410970608,0.0074909983048494,
9.32404564775087));
#277572=CARTESIAN_POINT('Ctrl Pts',(-1.26082991597317,-1.93835157450104,
9.43515707632232));
#277573=CARTESIAN_POINT('Ctrl Pts',(0.944213025165924,-2.11077252836269,
9.54626850489372));
#277574=CARTESIAN_POINT('Ctrl Pts',(2.2853838938978,-0.352021818778507,
9.65737993346518));
#277575=CARTESIAN_POINT('Ctrl Pts',(1.53562902018864,1.72879796845614,9.7684913620366));
#277576=CARTESIAN_POINT('Ctrl Pts',(-0.619091670303133,2.22791929996239,
9.87960279060802));
#277577=CARTESIAN_POINT('Ctrl Pts',(-2.20739780181248,0.688689950512571,
9.99071421917945));
#277578=CARTESIAN_POINT('Ctrl Pts',(-1.77612862260868,-1.480630277731,10.1018256477509));
#277579=CARTESIAN_POINT('Ctrl Pts',(0.280142408063027,-2.29530371292957,
10.2129370763223));
#277580=CARTESIAN_POINT('Ctrl Pts',(2.08010771516136,-1.00997564164182,
10.3240485048938));
#277581=CARTESIAN_POINT('Ctrl Pts',(1.9769569723504,1.19939152609093,10.4351599334652));
#277582=CARTESIAN_POINT('Ctrl Pts',(0.0650640588157258,2.31142068253143,
10.5462713620366));
#277583=CARTESIAN_POINT('Ctrl Pts',(-1.9063567597894,1.30870271940912,10.6573827906081));
#277584=CARTESIAN_POINT('Ctrl Pts',(-2.13362840767391,-0.891363405884791,
10.7684942191795));
#277585=CARTESIAN_POINT('Ctrl Pts',(-0.408817267926587,-2.27591022336749,
10.8796056477509));
#277586=CARTESIAN_POINT('Ctrl Pts',(1.6900258021868,-1.57819887572082,10.9907170763223));
#277587=CARTESIAN_POINT('Ctrl Pts',(2.24264354682321,0.563425971424641,
11.1018285048938));
#277588=CARTESIAN_POINT('Ctrl Pts',(0.743439216537086,2.18956548993136,
11.2129399334652));
#277589=CARTESIAN_POINT('Ctrl Pts',(-1.43594676723325,1.81244469848213,
11.3240513620366));
#277590=CARTESIAN_POINT('Ctrl Pts',(-2.30156744951535,-0.222903967472517,
11.435162790608));
#277591=CARTESIAN_POINT('Ctrl Pts',(-1.06145585591785,-2.05431506087097,
11.5462742191795));
#277592=CARTESIAN_POINT('Ctrl Pts',(1.14979471329312,-2.00620811997828,
11.6573856477509));
#277593=CARTESIAN_POINT('Ctrl Pts',(2.3090840032781,-0.122596774789466,
11.7684970763223));
#277594=CARTESIAN_POINT('Ctrl Pts',(1.35576403019591,1.87317986264281,11.8796085048938));
#277595=CARTESIAN_POINT('Ctrl Pts',(-0.837961075250009,2.15516127928966,
11.9907199334652));
#277596=CARTESIAN_POINT('Ctrl Pts',(-2.26502531987419,0.465359220078858,
12.1018313620366));
#277597=CARTESIAN_POINT('Ctrl Pts',(-1.61979013101972,-1.65020569470438,
12.212942790608));
#277598=CARTESIAN_POINT('Ctrl Pts',(0.507410906699071,-2.25597718852529,
12.3240542191795));
#277599=CARTESIAN_POINT('Ctrl Pts',(2.17037548521933,-0.797727495165182,
12.4351656477509));
#277600=CARTESIAN_POINT('Ctrl Pts',(1.84763692435666,1.39037286334906,12.5462770763223));
#277601=CARTESIAN_POINT('Ctrl Pts',(-0.165527309906998,2.30640404375699,
12.6573885048938));
#277602=CARTESIAN_POINT('Ctrl Pts',(-2.02724857903657,1.11227788891887,
12.7684999334652));
#277603=CARTESIAN_POINT('Ctrl Pts',(-2.03421526992979,-1.09948494258363,
12.8796113620366));
#277604=CARTESIAN_POINT('Ctrl Pts',(-0.180053471679505,-2.30531552086038,
12.9907227906081));
#277605=CARTESIAN_POINT('Ctrl Pts',(1.83884145519558,-1.40198466683405,
13.1018342191795));
#277606=CARTESIAN_POINT('Ctrl Pts',(2.17535779123418,0.784039146663179,
13.2129456477509));
#277607=CARTESIAN_POINT('Ctrl Pts',(0.521612615035739,2.25273593286457,
13.3240570763224));
#277608=CARTESIAN_POINT('Ctrl Pts',(-1.60936233742585,1.66037699642546,
13.4351685048938));
#277609=CARTESIAN_POINT('Ctrl Pts',(-2.26791195722282,-0.451081209616796,
13.5462799334652));
#277610=CARTESIAN_POINT('Ctrl Pts',(-0.851521123641821,-2.14983968690118,
13.6573913620366));
#277611=CARTESIAN_POINT('Ctrl Pts',(1.34393682527549,-1.88168347844478,
13.7685027906081));
#277612=CARTESIAN_POINT('Ctrl Pts',(2.30981049660767,0.108048013145282,
13.8796142191795));
#277613=CARTESIAN_POINT('Ctrl Pts',(1.16241022721892,1.99892505288228,13.9907256477509));
#277614=CARTESIAN_POINT('Ctrl Pts',(-1.04849340974778,2.06096105569685,
14.1018370763224));
#277615=CARTESIAN_POINT('Ctrl Pts',(-2.30011757201657,0.237398522076775,
14.2129485048938));
#277616=CARTESIAN_POINT('Ctrl Pts',(-1.4473359691043,-1.80336282980451,
14.3240599334652));
#277617=CARTESIAN_POINT('Ctrl Pts',(0.729631055715192,-2.19420542017367,
14.4351713620366));
#277618=CARTESIAN_POINT('Ctrl Pts',(2.23904968266907,-0.577542571524482,
14.5462827906081));
#277619=CARTESIAN_POINT('Ctrl Pts',(1.69993430507442,1.5675210562588,14.6573942191795));
#277620=CARTESIAN_POINT('Ctrl Pts',(-0.394471808763476,2.27844045247504,
14.7685056477509));
#277621=CARTESIAN_POINT('Ctrl Pts',(-2.12797082869335,0.904786745931656,
14.8796170763224));
#277622=CARTESIAN_POINT('Ctrl Pts',(-1.91456324936044,-1.29666744679644,
14.9907285048938));
#277623=CARTESIAN_POINT('Ctrl Pts',(0.0505017186100073,-2.31178469581453,
15.1018399334652));
#277624=CARTESIAN_POINT('Ctrl Pts',(1.96936204509281,-1.21182178505348,
15.2129513620366));
#277625=CARTESIAN_POINT('Ctrl Pts',(2.0864288929107,0.996851733312993,15.3240627906081));
#277626=CARTESIAN_POINT('Ctrl Pts',(0.294596367801226,2.2934933798619,15.4351742191795));
#277627=CARTESIAN_POINT('Ctrl Pts',(-1.76676598584593,1.49178981583561,
15.5462856477509));
#277628=CARTESIAN_POINT('Ctrl Pts',(-2.21169247918187,-0.674770539446852,
15.6573970763223));
#277629=CARTESIAN_POINT('Ctrl Pts',(-0.633114408827972,-2.22397505578959,
15.7685085048938));
#277630=CARTESIAN_POINT('Ctrl Pts',(1.5247077958973,-1.73843752848017,15.8796199334652));
#277631=CARTESIAN_POINT('Ctrl Pts',(2.28755614583539,0.337617806115804,
15.9907313620366));
#277632=CARTESIAN_POINT('Ctrl Pts',(0.957491333401296,2.10478247099586,
16.1018427906081));
#277633=CARTESIAN_POINT('Ctrl Pts',(-1.24859403842671,1.94625584904281,
16.2129542191795));
#277634=CARTESIAN_POINT('Ctrl Pts',(-2.31232541723185,0.00707589104983105,
16.3240656477509));
#277635=CARTESIAN_POINT('Ctrl Pts',(-1.26048192358796,-1.93857788752706,
16.4351770763223));
#277636=CARTESIAN_POINT('Ctrl Pts',(0.944591934930056,-2.11060298847667,
16.5462885048938));
#277637=CARTESIAN_POINT('Ctrl Pts',(2.28544705191438,-0.351611544136238,
16.6573999334652));
#277638=CARTESIAN_POINT('Ctrl Pts',(1.535318642296,1.72907362023293,16.7685113620367));
#277639=CARTESIAN_POINT('Ctrl Pts',(-0.619491615341388,2.22780811707463,
16.879622790608));
#277640=CARTESIAN_POINT('Ctrl Pts',(-2.20752139980484,0.688293683343328,
16.9907342191795));
#277641=CARTESIAN_POINT('Ctrl Pts',(-1.77586279142397,-1.4809491323765,
17.1018456477509));
#277642=CARTESIAN_POINT('Ctrl Pts',(0.28055445466867,-2.2952533304037,17.2129570763224));
#277643=CARTESIAN_POINT('Ctrl Pts',(2.08028899363887,-1.00960230898613,
17.3240685048938));
#277644=CARTESIAN_POINT('Ctrl Pts',(1.97674162320076,1.19974660651667,17.4351799334652));
#277645=CARTESIAN_POINT('Ctrl Pts',(0.0646491182662103,2.31143195022664,
17.5462913620366));
#277646=CARTESIAN_POINT('Ctrl Pts',(-1.90659167780665,1.30836118408193,
17.6574027906081));
#277647=CARTESIAN_POINT('Ctrl Pts',(-2.13346833523032,-0.891747778323729,
17.7685142191795));
#277648=CARTESIAN_POINT('Ctrl Pts',(-0.408408730619048,-2.2759809922174,
17.8796256477509));
#277649=CARTESIAN_POINT('Ctrl Pts',(1.69030916813735,-1.57790037625904,
17.9907370763224));
#277650=CARTESIAN_POINT('Ctrl Pts',(2.24254222088181,0.56383791930961,18.1018485048938));
#277651=CARTESIAN_POINT('Ctrl Pts',(0.743046408301969,2.18968111053243,
18.2129599334652));
#277652=CARTESIAN_POINT('Ctrl Pts',(-1.43627263399722,1.81222076736117,
18.3240713620366));
#277653=CARTESIAN_POINT('Ctrl Pts',(-2.3015264063899,-0.223381600007984,
18.4351827906081));
#277654=CARTESIAN_POINT('Ctrl Pts',(-1.06108893265441,-2.05438293086541,
18.5462942191795));
#277655=CARTESIAN_POINT('Ctrl Pts',(1.15015842546083,-2.00623507679203,
18.6574056477509));
#277656=CARTESIAN_POINT('Ctrl Pts',(2.30909922726198,-0.121737808789031,
18.7685170763224));
#277657=CARTESIAN_POINT('Ctrl Pts',(1.3554400697113,1.87257450567142,18.8796285048938));
#277658=CARTESIAN_POINT('Ctrl Pts',(-0.838367091757206,2.15665232290657,
18.9907399334652));
#277659=CARTESIAN_POINT('Ctrl Pts',(-2.26513615382795,0.461567928622731,
19.101853497924));
#277660=CARTESIAN_POINT('Ctrl Pts',(-1.83454523104888,-0.941064438844653,
19.1759299195257));
#277661=CARTESIAN_POINT('Ctrl Pts',(-1.37022001648085,-1.39661133546032,
19.2129691982704));
#277662=CARTESIAN_POINT('Ctrl Pts',(1.05790751410524,-1.48333259624667,
-0.153861392747535));
#277663=CARTESIAN_POINT('Ctrl Pts',(1.55120293711735,-1.13153472508212,
-0.116812388665656));
#277664=CARTESIAN_POINT('Ctrl Pts',(2.15057131801661,0.0965705457561521,
-0.0427262417266339));
#277665=CARTESIAN_POINT('Ctrl Pts',(1.08336547476853,1.8625271474138,0.0683970480695312));
#277666=CARTESIAN_POINT('Ctrl Pts',(-0.975807202051508,1.91874839396202,
0.17950847664096));
#277667=CARTESIAN_POINT('Ctrl Pts',(-2.14173055808719,0.222243512545894,
0.290619905212389));
#277668=CARTESIAN_POINT('Ctrl Pts',(-1.3484061737991,-1.67903036105319,
0.401731333783817));
#277669=CARTESIAN_POINT('Ctrl Pts',(0.678721800115099,-2.04338595829077,
0.512842762355246));
#277670=CARTESIAN_POINT('Ctrl Pts',(2.08481041986917,-0.538618154298584,
0.623954190926675));
#277671=CARTESIAN_POINT('Ctrl Pts',(1.58351640821179,1.45914582743268,0.735065619498103));
#277672=CARTESIAN_POINT('Ctrl Pts',(-0.36657508947119,2.12181017643735,
0.846177048069534));
#277673=CARTESIAN_POINT('Ctrl Pts',(-1.98127260449714,0.843261789831782,
0.957288476640961));
#277674=CARTESIAN_POINT('Ctrl Pts',(-1.7832847479344,-1.20682731866822,
1.06839990521239));
#277675=CARTESIAN_POINT('Ctrl Pts',(0.0462549324791658,-2.15275946002753,
1.17951133378381));
#277676=CARTESIAN_POINT('Ctrl Pts',(1.83347396506348,-1.12911391414712,
1.29062276235524));
#277677=CARTESIAN_POINT('Ctrl Pts',(1.94322594777237,0.927576174876139,
1.40173419092667));
#277678=CARTESIAN_POINT('Ctrl Pts',(0.275096289051986,2.13561314741684,
1.5128456194981));
#277679=CARTESIAN_POINT('Ctrl Pts',(-1.64472212758652,1.38975267968814,
1.62395704806953));
#277680=CARTESIAN_POINT('Ctrl Pts',(-2.05976421615942,-0.627610188512866,
1.73506847664096));
#277681=CARTESIAN_POINT('Ctrl Pts',(-0.590302713589067,-2.07076446671643,
1.84617990521239));
#277682=CARTESIAN_POINT('Ctrl Pts',(1.41923394810694,-1.6193511232449,1.95729133378382));
#277683=CARTESIAN_POINT('Ctrl Pts',(2.13029608741303,0.313626507834027,
2.06840276235524));
#277684=CARTESIAN_POINT('Ctrl Pts',(0.892324211344424,1.95966335342563,
2.17951419092667));
#277685=CARTESIAN_POINT('Ctrl Pts',(-1.1620460208133,1.81278019776812,2.2906256194981));
#277686=CARTESIAN_POINT('Ctrl Pts',(-2.15324610461966,0.0073622017891174,
2.40173704806953));
#277687=CARTESIAN_POINT('Ctrl Pts',(-1.17441492813331,-1.80479155581837,
2.51284847664096));
#277688=CARTESIAN_POINT('Ctrl Pts',(0.87890286332936,-1.96571939667137,
2.62395990521239));
#277689=CARTESIAN_POINT('Ctrl Pts',(2.12810165046316,-0.32818646061126,
2.73507133378382));
#277690=CARTESIAN_POINT('Ctrl Pts',(1.43027414771603,1.60960829067691,2.84618276235524));
#277691=CARTESIAN_POINT('Ctrl Pts',(-0.57612870728583,2.07475268419347,
2.95729419092668));
#277692=CARTESIAN_POINT('Ctrl Pts',(-2.05542434492789,0.641680411001263,
3.0684056194981));
#277693=CARTESIAN_POINT('Ctrl Pts',(-1.65418705067002,-1.3784731368187,
3.17951704806954));
#277694=CARTESIAN_POINT('Ctrl Pts',(0.260486255919504,-2.13744471229902,
3.29062847664096));
#277695=CARTESIAN_POINT('Ctrl Pts',(1.93683749351561,-0.940841916218584,
3.4017399052124));
#277696=CARTESIAN_POINT('Ctrl Pts',(1.84115236341935,1.11654868334311,3.51285133378381));
#277697=CARTESIAN_POINT('Ctrl Pts',(0.0609743642238004,2.15239520407475,
3.62396276235526));
#277698=CARTESIAN_POINT('Ctrl Pts',(-1.77498982832302,1.21898896506789,
3.73507419092667));
#277699=CARTESIAN_POINT('Ctrl Pts',(-1.98699406625453,-0.829685222405054,
3.84618561949811));
#277700=CARTESIAN_POINT('Ctrl Pts',(-0.381073073198851,-2.11927022828449,
3.95729704806953));
#277701=CARTESIAN_POINT('Ctrl Pts',(1.57349634633365,-1.4699089208803,4.06840847664097));
#277702=CARTESIAN_POINT('Ctrl Pts',(2.08845466815477,0.524290078746098,
4.17951990521239));
#277703=CARTESIAN_POINT('Ctrl Pts',(0.692660210442579,2.03880965773632,
4.29063133378382));
#277704=CARTESIAN_POINT('Ctrl Pts',(-1.33685756554719,1.68799728585336,
4.40174276235526));
#277705=CARTESIAN_POINT('Ctrl Pts',(-2.1432679654662,-0.207184497044221,
4.51285419092667));
#277706=CARTESIAN_POINT('Ctrl Pts',(-0.988776228152036,-1.91281064359507,
4.62396561949811));
#277707=CARTESIAN_POINT('Ctrl Pts',(1.07035900230882,-1.86838288200936,
4.73507704806953));
#277708=CARTESIAN_POINT('Ctrl Pts',(2.150209659374,-0.114548716028891,4.84618847664097));
#277709=CARTESIAN_POINT('Ctrl Pts',(1.26280713834729,1.74408747456893,4.9572999052124));
#277710=CARTESIAN_POINT('Ctrl Pts',(-0.779953115075661,2.00703665285239,
5.06841133378382));
#277711=CARTESIAN_POINT('Ctrl Pts',(-2.10912470159532,0.433723391955705,
5.17952276235525));
#277712=CARTESIAN_POINT('Ctrl Pts',(-1.50863224158034,-1.53640871752064,
5.29063419092668));
#277713=CARTESIAN_POINT('Ctrl Pts',(0.472126351498558,-2.10086165556654,
5.40174561949812));
#277714=CARTESIAN_POINT('Ctrl Pts',(2.02093075750676,-0.743210509191247,
5.51285704806953));
#277715=CARTESIAN_POINT('Ctrl Pts',(1.72076083765024,1.29441304351369,5.62396847664098));
#277716=CARTESIAN_POINT('Ctrl Pts',(-0.153754268428281,2.1477622337096,
5.73507990521239));
#277717=CARTESIAN_POINT('Ctrl Pts',(-1.88759770935448,1.03609742555844,
5.84619133378383));
#277718=CARTESIAN_POINT('Ctrl Pts',(-1.89445486478159,-1.02350561938589,
5.95730276235525));
#277719=CARTESIAN_POINT('Ctrl Pts',(-0.168052039143294,-2.14669082537494,
6.0684141909267));
#277720=CARTESIAN_POINT('Ctrl Pts',(1.71210365735957,-1.30584227763736,
6.17952561949811));
#277721=CARTESIAN_POINT('Ctrl Pts',(2.02583472802201,0.72973737902694,6.29063704806955));
#277722=CARTESIAN_POINT('Ctrl Pts',(0.48610477007458,2.09767136132423,6.40174847664096));
#277723=CARTESIAN_POINT('Ctrl Pts',(-1.49836840146871,1.54642009851438,
6.51285990521241));
#277724=CARTESIAN_POINT('Ctrl Pts',(-2.11196595309689,-0.419669870932711,
6.62397133378382));
#277725=CARTESIAN_POINT('Ctrl Pts',(-0.793299962358999,-2.00179873047476,
6.73508276235527));
#277726=CARTESIAN_POINT('Ctrl Pts',(1.25116588948884,-1.75245739023484,
6.84619419092668));
#277727=CARTESIAN_POINT('Ctrl Pts',(2.1509247302382,0.10022870077407,6.95730561949813));
#277728=CARTESIAN_POINT('Ctrl Pts',(1.08277616579552,1.86121432468007,7.06841704806953));
#277729=CARTESIAN_POINT('Ctrl Pts',(-0.976017587146367,1.91935214517559,
7.17952847664098));
#277730=CARTESIAN_POINT('Ctrl Pts',(-2.14184088401364,0.221451157542293,
7.29063990521239));
#277731=CARTESIAN_POINT('Ctrl Pts',(-1.34806769796412,-1.67905820903114,
7.40175133378384));
#277732=CARTESIAN_POINT('Ctrl Pts',(0.679069151736237,-2.04337663556412,
7.51286276235525));
#277733=CARTESIAN_POINT('Ctrl Pts',(2.08491730939053,-0.538184727220017,
7.6239741909267));
#277734=CARTESIAN_POINT('Ctrl Pts',(1.58324906041151,1.45939898599225,7.7350856194981));
#277735=CARTESIAN_POINT('Ctrl Pts',(-0.366953163953109,2.12176067525863,
7.84619704806955));
#277736=CARTESIAN_POINT('Ctrl Pts',(-1.98142543991457,0.8428975107737,7.95730847664098));
#277737=CARTESIAN_POINT('Ctrl Pts',(-1.78306728939617,-1.20714291991236,
8.06841990521241));
#277738=CARTESIAN_POINT('Ctrl Pts',(0.046640983899346,-2.15275349406987,
8.17953133378384));
#277739=CARTESIAN_POINT('Ctrl Pts',(1.83367684922511,-1.12878350458582,
8.29064276235526));
#277740=CARTESIAN_POINT('Ctrl Pts',(1.94305928503282,0.927924351688705,
8.4017541909267));
#277741=CARTESIAN_POINT('Ctrl Pts',(0.274712959816065,2.13566284261309,
8.51286561949811));
#277742=CARTESIAN_POINT('Ctrl Pts',(-1.64497162021,1.38945721643843,8.62397704806956));
#277743=CARTESIAN_POINT('Ctrl Pts',(-2.05965149819634,-0.627979851258548,
8.73508847664097));
#277744=CARTESIAN_POINT('Ctrl Pts',(-0.58993096995992,-2.07087045425137,
8.84619990521242));
#277745=CARTESIAN_POINT('Ctrl Pts',(1.41952463501611,-1.61909629058667,
8.95731133378382));
#277746=CARTESIAN_POINT('Ctrl Pts',(2.13023974859831,0.314008918823931,
9.06842276235528));
#277747=CARTESIAN_POINT('Ctrl Pts',(0.891972400280589,1.95982351877582,
9.17953419092668));
#277748=CARTESIAN_POINT('Ctrl Pts',(-1.16237143228708,1.81257155472881,
9.29064561949813));
#277749=CARTESIAN_POINT('Ctrl Pts',(-2.15324739123553,0.00697565384108067,
9.40175704806954));
#277750=CARTESIAN_POINT('Ctrl Pts',(-1.17409091397056,-1.80500235826464,
9.51286847664099));
#277751=CARTESIAN_POINT('Ctrl Pts',(0.879255734382123,-1.9655615841701,
9.62397990521238));
#277752=CARTESIAN_POINT('Ctrl Pts',(2.12816053201671,-0.327804419701003,
9.73509133378385));
#277753=CARTESIAN_POINT('Ctrl Pts',(1.42998516849226,1.6098650271067,9.84620276235524));
#277754=CARTESIAN_POINT('Ctrl Pts',(-0.576501156745404,2.07464922429802,
9.95731419092671));
#277755=CARTESIAN_POINT('Ctrl Pts',(-2.05553950599769,0.641311411789866,
10.0684256194981));
#277756=CARTESIAN_POINT('Ctrl Pts',(-1.65393956110117,-1.37877007359226,
10.1795370480696));
#277757=CARTESIAN_POINT('Ctrl Pts',(0.26086996489986,-2.13739791546223,
10.290648476641));
#277758=CARTESIAN_POINT('Ctrl Pts',(1.93700636185011,-0.940494200812156,
10.4017599052124));
#277759=CARTESIAN_POINT('Ctrl Pts',(1.84095189140225,1.11687918825252,10.5128713337839));
#277760=CARTESIAN_POINT('Ctrl Pts',(0.0605879661592919,2.15240611548235,
10.6239827623553));
#277761=CARTESIAN_POINT('Ctrl Pts',(-1.7752086321076,1.21867029999906,10.7350941909267));
#277762=CARTESIAN_POINT('Ctrl Pts',(-1.98684508949477,-0.830041913375277,
10.8462056194981));
#277763=CARTESIAN_POINT('Ctrl Pts',(-0.380692616558361,-2.1193386042129,
10.9573170480696));
#277764=CARTESIAN_POINT('Ctrl Pts',(1.57376019841008,-1.46962642379259,
11.068428476641));
#277765=CARTESIAN_POINT('Ctrl Pts',(2.08836051416776,0.524664988801521,
11.1795399052124));
#277766=CARTESIAN_POINT('Ctrl Pts',(0.6922941930291,2.03893397095329,11.2906513337839));
#277767=CARTESIAN_POINT('Ctrl Pts',(-1.3371605725683,1.68775726654574,11.4017627623553));
#277768=CARTESIAN_POINT('Ctrl Pts',(-2.1432307372566,-0.207569252269409,
11.5128741909267));
#277769=CARTESIAN_POINT('Ctrl Pts',(-0.988432825257067,-1.91298811746531,
11.6239856194981));
#277770=CARTESIAN_POINT('Ctrl Pts',(1.07069439637054,-1.86819070150503,
11.7350970480696));
#277771=CARTESIAN_POINT('Ctrl Pts',(2.15023018846362,-0.11416270944945,
11.846208476641));
#277772=CARTESIAN_POINT('Ctrl Pts',(1.26249402014902,1.74431414507166,11.9573199052124));
#277773=CARTESIAN_POINT('Ctrl Pts',(-0.780313404883507,2.00689660365656,
12.0684313337839));
#277774=CARTESIAN_POINT('Ctrl Pts',(-2.10920252945054,0.433344755787544,
12.1795427623553));
#277775=CARTESIAN_POINT('Ctrl Pts',(-1.50835640182406,-1.53667952178895,
12.2906541909267));
#277776=CARTESIAN_POINT('Ctrl Pts',(0.472503489691624,-2.10077686578998,
12.4017656194981));
#277777=CARTESIAN_POINT('Ctrl Pts',(2.02106414578021,-0.742847700575875,
12.5128770480696));
#277778=CARTESIAN_POINT('Ctrl Pts',(1.72052843743741,1.29472193291777,12.623988476641));
#277779=CARTESIAN_POINT('Ctrl Pts',(-0.154139831323539,2.14773459719973,
12.7350999052125));
#277780=CARTESIAN_POINT('Ctrl Pts',(-1.88778367871244,1.03575854811633,
12.8462113337838));
#277781=CARTESIAN_POINT('Ctrl Pts',(-1.89427109495674,-1.02384569463398,
12.9573227623553));
#277782=CARTESIAN_POINT('Ctrl Pts',(-0.167666663401311,-2.14672095941532,
13.0684341909267));
#277783=CARTESIAN_POINT('Ctrl Pts',(1.71233805402778,-1.30553490046703,
13.1795456194982));
#277784=CARTESIAN_POINT('Ctrl Pts',(2.02570369323109,0.730101044266491,
13.2906570480696));
#277785=CARTESIAN_POINT('Ctrl Pts',(0.485728189161183,2.09775859284699,
13.401768476641));
#277786=CARTESIAN_POINT('Ctrl Pts',(-1.4986459900102,1.54615108713072,13.5128799052124));
#277787=CARTESIAN_POINT('Ctrl Pts',(-2.11189058010671,-0.420049003409895,
13.6239913337839));
#277788=CARTESIAN_POINT('Ctrl Pts',(-0.792940587509937,-2.00194111109406,
13.7351027623553));
#277789=CARTESIAN_POINT('Ctrl Pts',(1.25148046974159,-1.75223275322215,
13.8462141909267));
#277790=CARTESIAN_POINT('Ctrl Pts',(2.15090670256477,0.100614832261903,
13.9573256194981));
#277791=CARTESIAN_POINT('Ctrl Pts',(1.08244202393532,1.86140867421099,14.0684370480696));
#277792=CARTESIAN_POINT('Ctrl Pts',(-0.97636213270898,1.91917689998111,
14.179548476641));
#277793=CARTESIAN_POINT('Ctrl Pts',(-2.14188060431944,0.221066651599284,
14.2906599052124));
#277794=CARTESIAN_POINT('Ctrl Pts',(-1.34776625241837,-1.67930018652154,
14.4017713337838));
#277795=CARTESIAN_POINT('Ctrl Pts',(0.679435966908132,-2.04325469642938,
14.5128827623553));
#277796=CARTESIAN_POINT('Ctrl Pts',(2.08501389049079,-0.53781043506944,
14.6239941909267));
#277797=CARTESIAN_POINT('Ctrl Pts',(1.58298704420748,1.4596831866814,14.7351056194982));
#277798=CARTESIAN_POINT('Ctrl Pts',(-0.36733405562417,2.12169476579173,
14.8462170480696));
#277799=CARTESIAN_POINT('Ctrl Pts',(-1.9815767245932,0.842541792529895,
14.957328476641));
#277800=CARTESIAN_POINT('Ctrl Pts',(-1.78285055487521,-1.20746299595058,
15.0684399052124));
#277801=CARTESIAN_POINT('Ctrl Pts',(0.0470274445495869,-2.15274508641162,
15.1795513337839));
#277802=CARTESIAN_POINT('Ctrl Pts',(1.83387945841787,-1.1284543054998,15.2906627623553));
#277803=CARTESIAN_POINT('Ctrl Pts',(1.94289267313373,0.928273153921158,
15.4017741909267));
#277804=CARTESIAN_POINT('Ctrl Pts',(0.274329562094182,2.13571212455651,
15.5128856194982));
#277805=CARTESIAN_POINT('Ctrl Pts',(-1.64522102847855,1.38916188943257,
15.6239970480696));
#277806=CARTESIAN_POINT('Ctrl Pts',(-2.05953873032919,-0.628349588903945,
15.735108476641));
#277807=CARTESIAN_POINT('Ctrl Pts',(-0.589559198660854,-2.07097632505356,
15.8462199052124));
#277808=CARTESIAN_POINT('Ctrl Pts',(1.41981527162715,-1.61884143200916,
15.9573313337839));
#277809=CARTESIAN_POINT('Ctrl Pts',(2.13018334352401,0.314391333464881,
16.0684427623553));
#277810=CARTESIAN_POINT('Ctrl Pts',(0.891620559212638,1.95998361378768,
16.1795541909267));
#277811=CARTESIAN_POINT('Ctrl Pts',(-1.16269680563781,1.81236285693576,
16.2906656194981));
#277812=CARTESIAN_POINT('Ctrl Pts',(-2.15324860880986,0.00658910395812926,
16.4017770480696));
#277813=CARTESIAN_POINT('Ctrl Pts',(-1.17376686177888,-1.8052131020487,
16.512888476641));
#277814=CARTESIAN_POINT('Ctrl Pts',(0.87960857698654,-1.96540370780851,
16.6239999052125));
#277815=CARTESIAN_POINT('Ctrl Pts',(2.12821934506713,-0.327422369970407,
16.7351113337838));
#277816=CARTESIAN_POINT('Ctrl Pts',(1.42969614309794,1.61012171537405,16.8462227623553));
#277817=CARTESIAN_POINT('Ctrl Pts',(-0.576873587498792,2.07454569025536,
16.9573341909267));
#277818=CARTESIAN_POINT('Ctrl Pts',(-2.05565460104578,0.640942405885882,
17.0684456194982));
#277819=CARTESIAN_POINT('Ctrl Pts',(-1.65369201781665,-1.37906699257984,
17.1795570480696));
#277820=CARTESIAN_POINT('Ctrl Pts',(0.261253664691311,-2.13735099901054,
17.290668476641));
#277821=CARTESIAN_POINT('Ctrl Pts',(1.93717516924488,-0.940146551638089,
17.4017799052124));
#277822=CARTESIAN_POINT('Ctrl Pts',(1.84075135723286,1.11720984086182,17.5128913337839));
#277823=CARTESIAN_POINT('Ctrl Pts',(0.0602015715133129,2.15241660801462,
17.6240027623553));
#277824=CARTESIAN_POINT('Ctrl Pts',(-1.7754273889011,1.21835226065102,17.7351141909267));
#277825=CARTESIAN_POINT('Ctrl Pts',(-1.98669602926134,-0.830399842848887,
17.8462256194982));
#277826=CARTESIAN_POINT('Ctrl Pts',(-0.380312184642269,-2.11940450450811,
17.9573370480696));
#277827=CARTESIAN_POINT('Ctrl Pts',(1.57402407015333,-1.4693484596505,18.068448476641));
#277828=CARTESIAN_POINT('Ctrl Pts',(2.0882661589612,0.525048596663805,18.1795599052125));
#277829=CARTESIAN_POINT('Ctrl Pts',(0.691928408101298,2.03904163741605,
18.2906713337839));
#277830=CARTESIAN_POINT('Ctrl Pts',(-1.33746402127451,1.68754874080316,
18.4017827623553));
#277831=CARTESIAN_POINT('Ctrl Pts',(-2.14319251769972,-0.208014025995827,
18.5128941909267));
#277832=CARTESIAN_POINT('Ctrl Pts',(-0.988091144540052,-1.91305131833229,
18.6240056194981));
#277833=CARTESIAN_POINT('Ctrl Pts',(1.07103308689969,-1.86821580382033,
18.7351170480696));
#277834=CARTESIAN_POINT('Ctrl Pts',(2.15024436511102,-0.113362836156677,
18.846228476641));
#277835=CARTESIAN_POINT('Ctrl Pts',(1.26219234657939,1.74375043373295,18.9573399052124));
#277836=CARTESIAN_POINT('Ctrl Pts',(-0.780691489418133,2.00828507068194,
19.0684513337839));
#277837=CARTESIAN_POINT('Ctrl Pts',(-2.10930573856417,0.429814286852394,
19.1795648982427));
#277838=CARTESIAN_POINT('Ctrl Pts',(-1.70833738932978,-0.876323755576083,
19.2536413198444));
#277839=CARTESIAN_POINT('Ctrl Pts',(-1.27595550447344,-1.3005312283113,
19.290680598589));
#277840=CARTESIAN_POINT('Ctrl Pts',(0.979751861171807,-1.37374756538967,
-0.0761499924288698));
#277841=CARTESIAN_POINT('Ctrl Pts',(1.43660380934276,-1.04793967156705,
-0.0391009883469908));
#277842=CARTESIAN_POINT('Ctrl Pts',(1.99169230137438,0.0894361469953051,
0.0349851585920312));
#277843=CARTESIAN_POINT('Ctrl Pts',(1.00332904916694,1.72492813864273,0.146108448388196));
#277844=CARTESIAN_POINT('Ctrl Pts',(-0.903716921949864,1.77699589523638,
0.257219876959625));
#277845=CARTESIAN_POINT('Ctrl Pts',(-1.98350467544344,0.205824698423077,
0.368331305531054));
#277846=CARTESIAN_POINT('Ctrl Pts',(-1.24878918126658,-1.55498765182436,
0.479442734102483));
#277847=CARTESIAN_POINT('Ctrl Pts',(0.628579472226426,-1.89242553723708,
0.590554162673911));
#277848=CARTESIAN_POINT('Ctrl Pts',(1.93078965960915,-0.498826345497046,
0.701665591245341));
#277849=CARTESIAN_POINT('Ctrl Pts',(1.4665300392103,1.35134765665918,0.812777019816767));
#277850=CARTESIAN_POINT('Ctrl Pts',(-0.339493406918823,1.96505596349419,
0.923888448388199));
#277851=CARTESIAN_POINT('Ctrl Pts',(-1.83490096805542,0.780963644767716,
1.03499987695962));
#277852=CARTESIAN_POINT('Ctrl Pts',(-1.65153997631426,-1.11766983012519,
1.14611130553105));
#277853=CARTESIAN_POINT('Ctrl Pts',(0.0428377297453559,-1.99371878873657,
1.25722273410248));
#277854=CARTESIAN_POINT('Ctrl Pts',(1.69802133525854,-1.04569770429913,
1.36833416267391));
#277855=CARTESIAN_POINT('Ctrl Pts',(1.79966510646976,0.859049086613364,
1.47944559124534));
#277856=CARTESIAN_POINT('Ctrl Pts',(0.254772839408482,1.97783920430355,
1.59055701981676));
#277857=CARTESIAN_POINT('Ctrl Pts',(-1.5232140278125,1.28708110712742,1.7016684483882));
#277858=CARTESIAN_POINT('Ctrl Pts',(-1.907593808958,-0.581243863085647,
1.81277987695962));
#277859=CARTESIAN_POINT('Ctrl Pts',(-0.546692574334192,-1.91778138756283,
1.92389130553106));
#277860=CARTESIAN_POINT('Ctrl Pts',(1.31438437061491,-1.49971737201599,
2.03500273410248));
#277861=CARTESIAN_POINT('Ctrl Pts',(1.97291495585534,0.290456538654119,
2.14611416267391));
#277862=CARTESIAN_POINT('Ctrl Pts',(0.826401453035167,1.81488815627977,
2.25722559124534));
#277863=CARTESIAN_POINT('Ctrl Pts',(-1.07619686643597,1.67885637352799,
2.36833701981677));
#277864=CARTESIAN_POINT('Ctrl Pts',(-1.9941694812012,0.00681830009622902,
2.4794484483882));
#277865=CARTESIAN_POINT('Ctrl Pts',(-1.08765198874667,-1.67145791315773,
2.59055987695962));
#277866=CARTESIAN_POINT('Ctrl Pts',(0.813971641806969,-1.82049679367221,
2.70167130553106));
#277867=CARTESIAN_POINT('Ctrl Pts',(1.97088263860907,-0.303940837273705,
2.81278273410248));
#277868=CARTESIAN_POINT('Ctrl Pts',(1.32460894693233,1.49069431639504,2.92389416267391));
#277869=CARTESIAN_POINT('Ctrl Pts',(-0.533565709394934,1.92147496516182,
3.03500559124534));
#277870=CARTESIAN_POINT('Ctrl Pts',(-1.90357455693488,0.594274611507729,
3.14611701981677));
#277871=CARTESIAN_POINT('Ctrl Pts',(-1.5319797052307,-1.27663486965186,
3.2572284483882));
#277872=CARTESIAN_POINT('Ctrl Pts',(0.241242160249381,-1.97953545759437,
3.36833987695962));
#277873=CARTESIAN_POINT('Ctrl Pts',(1.79374861578921,-0.871334787014221,
3.47945130553106));
#277874=CARTESIAN_POINT('Ctrl Pts',(1.70513247208259,1.03406076240944,3.59056273410248));
#277875=CARTESIAN_POINT('Ctrl Pts',(0.0564697254112784,1.99338144313412,
3.70167416267392));
#277876=CARTESIAN_POINT('Ctrl Pts',(-1.64385786533654,1.12893300345194,
3.81278559124534));
#277877=CARTESIAN_POINT('Ctrl Pts',(-1.84019974203207,-0.76839008136323,
3.92389701981677));
#277878=CARTESIAN_POINT('Ctrl Pts',(-0.3529203146126,-1.9627036605784,4.0350084483882));
#277879=CARTESIAN_POINT('Ctrl Pts',(1.45725023531129,-1.36131559874929,
4.14611987695963));
#277880=CARTESIAN_POINT('Ctrl Pts',(1.93416467963008,0.485556793572691,
4.25723130553106));
#277881=CARTESIAN_POINT('Ctrl Pts',(0.641488146451795,1.88818732271859,
4.36834273410248));
#277882=CARTESIAN_POINT('Ctrl Pts',(-1.23809375630938,1.56329212187003,
4.47945416267392));
#277883=CARTESIAN_POINT('Ctrl Pts',(-1.98492850287721,-0.1918782066282,
4.59056559124534));
#277884=CARTESIAN_POINT('Ctrl Pts',(-0.915727827714486,-1.77149681153045,
4.70167701981678));
#277885=CARTESIAN_POINT('Ctrl Pts',(0.991283463489736,-1.73035126570446,
4.8127884483882));
#277886=CARTESIAN_POINT('Ctrl Pts',(1.9913573611991,-0.106086133454761,
4.92389987695964));
#277887=CARTESIAN_POINT('Ctrl Pts',(1.16951399588391,1.61523850286725,5.03501130553107));
#277888=CARTESIAN_POINT('Ctrl Pts',(-0.72233206205028,1.85876163072283,
5.14612273410249));
#277889=CARTESIAN_POINT('Ctrl Pts',(-1.95330766090571,0.401680954938468,
5.25723416267391));
#277890=CARTESIAN_POINT('Ctrl Pts',(-1.39717813400948,-1.42290255097073,
5.36834559124535));
#277891=CARTESIAN_POINT('Ctrl Pts',(0.437246796550256,-1.94565506876726,
5.47945701981677));
#277892=CARTESIAN_POINT('Ctrl Pts',(1.87162927247121,-0.688303911177398,
5.59056844838821));
#277893=CARTESIAN_POINT('Ctrl Pts',(1.59363518156437,1.1987849330858,5.70167987695963));
#277894=CARTESIAN_POINT('Ctrl Pts',(-0.142395274300623,1.98909074543372,
5.81279130553107));
#277895=CARTESIAN_POINT('Ctrl Pts',(-1.74814654799753,0.959553049308661,
5.92390273410249));
#277896=CARTESIAN_POINT('Ctrl Pts',(-1.75449711333758,-0.947891495374496,
6.03501416267391));
#277897=CARTESIAN_POINT('Ctrl Pts',(-0.155636760235733,-1.98809849016002,
6.14612559124535));
#277898=CARTESIAN_POINT('Ctrl Pts',(1.58561757285168,-1.20936980298714,
6.25723701981678));
#277899=CARTESIAN_POINT('Ctrl Pts',(1.87617094948495,0.675826143340122,
6.36834844838821));
#277900=CARTESIAN_POINT('Ctrl Pts',(0.45019252331136,1.94270046576094,6.47945987695964));
#277901=CARTESIAN_POINT('Ctrl Pts',(-1.3876725616243,1.43217431530812,6.59057130553106));
#277902=CARTESIAN_POINT('Ctrl Pts',(-1.95593900760625,-0.388665674117844,
6.7016827341025));
#277903=CARTESIAN_POINT('Ctrl Pts',(-0.734692876480939,-1.85391067340403,
6.81279416267391));
#277904=CARTESIAN_POINT('Ctrl Pts',(1.15873277438451,-1.62299006937209,
6.92390559124537));
#277905=CARTESIAN_POINT('Ctrl Pts',(1.99201960435431,0.0928240463527359,
7.03501701981677));
#277906=CARTESIAN_POINT('Ctrl Pts',(1.00278327691804,1.72371230408288,7.14612844838821));
#277907=CARTESIAN_POINT('Ctrl Pts',(-0.903911764301868,1.77755504276799,
7.25723987695964));
#277908=CARTESIAN_POINT('Ctrl Pts',(-1.98360685075681,0.205090880694083,
7.36835130553106));
#277909=CARTESIAN_POINT('Ctrl Pts',(-1.24847571120909,-1.55501344246093,
7.4794627341025));
#277910=CARTESIAN_POINT('Ctrl Pts',(0.62890116234844,-1.89241690325098,
7.59057416267391));
#277911=CARTESIAN_POINT('Ctrl Pts',(1.93088865239076,-0.49842493896458,
7.70168559124536));
#277912=CARTESIAN_POINT('Ctrl Pts',(1.46628244242002,1.35158211247559,7.81279701981678));
#277913=CARTESIAN_POINT('Ctrl Pts',(-0.33984355017084,1.96501011934303,
7.92390844838821));
#277914=CARTESIAN_POINT('Ctrl Pts',(-1.83504251236122,0.780626277766932,
8.03501987695964));
#277915=CARTESIAN_POINT('Ctrl Pts',(-1.65133858308781,-1.1179621155114,
8.14613130553108));
#277916=CARTESIAN_POINT('Ctrl Pts',(0.0431952606186986,-1.99371326352946,
8.25724273410249));
#277917=CARTESIAN_POINT('Ctrl Pts',(1.69820923082814,-1.04539170459849,
8.36835416267393));
#277918=CARTESIAN_POINT('Ctrl Pts',(1.79951075637102,0.859371540963658,
8.47946559124535));
#277919=CARTESIAN_POINT('Ctrl Pts',(0.254417829611001,1.97788522813869,
8.59057701981678));
#277920=CARTESIAN_POINT('Ctrl Pts',(-1.52344508852334,1.28680747198924,
8.70168844838821));
#277921=CARTESIAN_POINT('Ctrl Pts',(-1.90748941832589,-0.58158621604019,
8.81279987695964));
#277922=CARTESIAN_POINT('Ctrl Pts',(-0.54634829422683,-1.91787954499458,
8.92391130553106));
#277923=CARTESIAN_POINT('Ctrl Pts',(1.31465358227707,-1.49948136577929,
9.03502273410249));
#277924=CARTESIAN_POINT('Ctrl Pts',(1.97286277921622,0.290810698043381,
9.14613416267393));
#277925=CARTESIAN_POINT('Ctrl Pts',(0.826075632923317,1.81503648900058,
9.25724559124534));
#277926=CARTESIAN_POINT('Ctrl Pts',(-1.07649823729575,1.67866314453268,
9.36835701981679));
#277927=CARTESIAN_POINT('Ctrl Pts',(-1.99417067276499,0.00646030937731316,
9.47946844838821));
#277928=CARTESIAN_POINT('Ctrl Pts',(-1.08735191196796,-1.67165314202824,
9.59057987695965));
#277929=CARTESIAN_POINT('Ctrl Pts',(0.814298443598325,-1.82035063997751,
9.70169130553106));
#277930=CARTESIAN_POINT('Ctrl Pts',(1.97093717013561,-0.303587020623497,
9.81280273410251));
#277931=CARTESIAN_POINT('Ctrl Pts',(1.3243413167959,1.49093208575727,9.92391416267391));
#277932=CARTESIAN_POINT('Ctrl Pts',(-0.533910643187675,1.92137914863364,
10.0350255912454));
#277933=CARTESIAN_POINT('Ctrl Pts',(-1.9036812101829,0.59393287306716,10.1461370198168));
#277934=CARTESIAN_POINT('Ctrl Pts',(-1.53175049959366,-1.27690986945351,
10.2572484483882));
#277935=CARTESIAN_POINT('Ctrl Pts',(0.24159752173669,-1.9794921179949,10.3683598769596));
#277936=CARTESIAN_POINT('Ctrl Pts',(1.79390500853888,-0.8710127599825,10.4794713055311));
#277937=CARTESIAN_POINT('Ctrl Pts',(1.70494681045408,1.03436685041413,10.5905827341025));
#277938=CARTESIAN_POINT('Ctrl Pts',(0.0561118735028585,1.99339154843327,
10.7016941626739));
#277939=CARTESIAN_POINT('Ctrl Pts',(-1.64406050442579,1.128637880589,10.8128055912454));
#277940=CARTESIAN_POINT('Ctrl Pts',(-1.84006177131562,-0.768720420865766,
10.9239170198168));
#277941=CARTESIAN_POINT('Ctrl Pts',(-0.352567965190137,-1.96276698505831,
11.0350284483882));
#277942=CARTESIAN_POINT('Ctrl Pts',(1.45749459463335,-1.36105397186436,
11.1461398769597));
#277943=CARTESIAN_POINT('Ctrl Pts',(1.93407748151231,0.485904006178401,
11.2572513055311));
#277944=CARTESIAN_POINT('Ctrl Pts',(0.641149169521112,1.88830245197522,
11.3683627341025));
#277945=CARTESIAN_POINT('Ctrl Pts',(-1.23837437790336,1.56306983460935,
11.4794741626739));
#277946=CARTESIAN_POINT('Ctrl Pts',(-1.98489402499784,-0.192234537066302,
11.5905855912454));
#277947=CARTESIAN_POINT('Ctrl Pts',(-0.915409794596289,-1.77166117405965,
11.7016970198168));
#277948=CARTESIAN_POINT('Ctrl Pts',(0.991594079447964,-1.73017328303178,
11.8128084483882));
#277949=CARTESIAN_POINT('Ctrl Pts',(1.99137637364914,-0.105728644109437,
11.9239198769596));
#277950=CARTESIAN_POINT('Ctrl Pts',(1.16922401010214,1.61544842750052,12.0350313055311));
#277951=CARTESIAN_POINT('Ctrl Pts',(-0.722665734517006,1.85863192802346,
12.1461427341025));
#277952=CARTESIAN_POINT('Ctrl Pts',(-1.95337973902688,0.401330291496232,
12.2572541626739));
#277953=CARTESIAN_POINT('Ctrl Pts',(-1.39692267262841,-1.42315334887352,
12.3683655912453));
#277954=CARTESIAN_POINT('Ctrl Pts',(0.437596072684178,-1.94557654305468,
12.4794770198168));
#277955=CARTESIAN_POINT('Ctrl Pts',(1.87175280634107,-0.687967905986568,
12.5905884483882));
#277956=CARTESIAN_POINT('Ctrl Pts',(1.59341995051815,1.19907100248648,12.7016998769597));
#277957=CARTESIAN_POINT('Ctrl Pts',(-0.142752352740081,1.98906515064247,
12.8128113055311));
#277958=CARTESIAN_POINT('Ctrl Pts',(-1.74831877838833,0.959239207313788,
12.9239227341025));
#277959=CARTESIAN_POINT('Ctrl Pts',(-1.7543269199837,-0.948206446684336,
13.0350341626739));
#277960=CARTESIAN_POINT('Ctrl Pts',(-0.155279855123116,-1.98812639797025,
13.1461455912454));
#277961=CARTESIAN_POINT('Ctrl Pts',(1.58583465285997,-1.20908513410002,
13.2572570198168));
#277962=CARTESIAN_POINT('Ctrl Pts',(1.87604959522801,0.676162941869805,
13.3683684483882));
#277963=CARTESIAN_POINT('Ctrl Pts',(0.449843763286628,1.9427812528294,13.4794798769597));
#277964=CARTESIAN_POINT('Ctrl Pts',(-1.38792964259454,1.43192517783599,
13.5905913055311));
#277965=CARTESIAN_POINT('Ctrl Pts',(-1.95586920299061,-0.389016797202991,
13.7017027341025));
#277966=CARTESIAN_POINT('Ctrl Pts',(-0.734360051378052,-1.85404253528694,
13.8128141626739));
#277967=CARTESIAN_POINT('Ctrl Pts',(1.15902411420771,-1.62278202799953,
13.9239255912454));
#277968=CARTESIAN_POINT('Ctrl Pts',(1.99200290852187,0.0931816513785255,
14.0350370198168));
#277969=CARTESIAN_POINT('Ctrl Pts',(1.00247382065172,1.7238922955397,14.1461484483882));
#277970=CARTESIAN_POINT('Ctrl Pts',(-0.904230855670186,1.77739274426537,
14.2572598769597));
#277971=CARTESIAN_POINT('Ctrl Pts',(-1.98364363662232,0.204734781121791,
14.3683713055311));
#277972=CARTESIAN_POINT('Ctrl Pts',(-1.24819653573245,-1.55523754323857,
14.4794827341025));
#277973=CARTESIAN_POINT('Ctrl Pts',(0.629240878101075,-1.8923039726851,
14.590594162674));
#277974=CARTESIAN_POINT('Ctrl Pts',(1.9309780983125,-0.498078298614397,
14.7017055912454));
#277975=CARTESIAN_POINT('Ctrl Pts',(1.46603978334054,1.351845317104,14.8128170198168));
#277976=CARTESIAN_POINT('Ctrl Pts',(-0.340196302484868,1.96494907910841,
14.9239284483882));
#277977=CARTESIAN_POINT('Ctrl Pts',(-1.83518262049305,0.780296839128134,
15.0350398769597));
#277978=CARTESIAN_POINT('Ctrl Pts',(-1.65113786038999,-1.11825854510472,
15.1461513055311));
#277979=CARTESIAN_POINT('Ctrl Pts',(0.0435531704891701,-1.99370547700871,
15.2572627341025));
#277980=CARTESIAN_POINT('Ctrl Pts',(1.69839687174293,-1.04508682594613,
15.3683741626739));
#277981=CARTESIAN_POINT('Ctrl Pts',(1.79935645335677,0.859694574529323,
15.4794855912454));
#277982=CARTESIAN_POINT('Ctrl Pts',(0.254062756387133,1.97793086925111,
15.5905970198168));
#277983=CARTESIAN_POINT('Ctrl Pts',(-1.52367607111119,1.28653396302953,
15.7017084483882));
#277984=CARTESIAN_POINT('Ctrl Pts',(-1.90738498147651,-0.58192863836104,
15.8128198769597));
#277985=CARTESIAN_POINT('Ctrl Pts',(-0.546003988493735,-1.91797759431753,
15.9239313055311));
#277986=CARTESIAN_POINT('Ctrl Pts',(1.31492274735698,-1.49924533553815,
16.0350427341025));
#277987=CARTESIAN_POINT('Ctrl Pts',(1.97281054121263,0.291164860813958,
16.146154162674));
#277988=CARTESIAN_POINT('Ctrl Pts',(0.82574978502398,1.8151847565795,16.2572655912454));
#277989=CARTESIAN_POINT('Ctrl Pts',(-1.07679957284889,1.67846986482871,
16.3683770198168));
#277990=CARTESIAN_POINT('Ctrl Pts',(-1.99417180038787,0.00610231686643078,
16.4794884483882));
#277991=CARTESIAN_POINT('Ctrl Pts',(-1.0870517999698,-1.67184831657035,
16.5905998769597));
#277992=CARTESIAN_POINT('Ctrl Pts',(0.814625219043029,-1.82020442714035,
16.7017113055311));
#277993=CARTESIAN_POINT('Ctrl Pts',(1.97099163821986,-0.303233195804582,
16.8128227341025));
#277994=CARTESIAN_POINT('Ctrl Pts',(1.32407364389988,1.49116981051517,16.923934162674));
#277995=CARTESIAN_POINT('Ctrl Pts',(-0.5342555596562,1.92128326343608,17.0350455912454));
#277996=CARTESIAN_POINT('Ctrl Pts',(-1.90378780228672,0.593591128428439,
17.1461570198168));
#277997=CARTESIAN_POINT('Ctrl Pts',(-1.53152124420933,-1.27718485278317,
17.2572684483882));
#277998=CARTESIAN_POINT('Ctrl Pts',(0.241952874713956,-1.97944866761738,
17.3683798769597));
#277999=CARTESIAN_POINT('Ctrl Pts',(1.79406134485088,-0.870690794290049,
17.4794913055311));
#278000=CARTESIAN_POINT('Ctrl Pts',(1.70476109126497,1.03467307520697,17.5906027341025));
#278001=CARTESIAN_POINT('Ctrl Pts',(0.0557540247604131,1.9934012658026,
17.7017141626739));
#278002=CARTESIAN_POINT('Ctrl Pts',(-1.64426309999555,1.12834333722013,
17.8128255912454));
#278003=CARTESIAN_POINT('Ctrl Pts',(-1.83992372329235,-0.769051907374047,
17.9239370198168));
#278004=CARTESIAN_POINT('Ctrl Pts',(-0.35221563866549,-1.96282801679883,
18.0350484483882));
#278005=CARTESIAN_POINT('Ctrl Pts',(1.45773897216931,-1.36079654304198,
18.1461598769597));
#278006=CARTESIAN_POINT('Ctrl Pts',(1.9339900970406,0.486259274017999,18.2572713055311));
#278007=CARTESIAN_POINT('Ctrl Pts',(0.640810407900626,1.88840216429967,
18.3683827341025));
#278008=CARTESIAN_POINT('Ctrl Pts',(-1.23865540855179,1.56287671424517,
18.479494162674));
#278009=CARTESIAN_POINT('Ctrl Pts',(-1.98485862900955,-0.192646451983672,
18.5906055912454));
#278010=CARTESIAN_POINT('Ctrl Pts',(-0.915093356425693,-1.77171970579917,
18.7017170198168));
#278011=CARTESIAN_POINT('Ctrl Pts',(0.991907748338541,-1.73019653084864,
18.8128284483882));
#278012=CARTESIAN_POINT('Ctrl Pts',(1.99138950296005,-0.10498786352432,
18.9239398769597));
#278013=CARTESIAN_POINT('Ctrl Pts',(1.16894462344746,1.61492636179448,19.0350513055311));
#278014=CARTESIAN_POINT('Ctrl Pts',(-0.723015887079062,1.85991781845732,
19.1461627341025));
#278015=CARTESIAN_POINT('Ctrl Pts',(-1.95347532330039,0.398060645082057,
19.2572762985614));
#278016=CARTESIAN_POINT('Ctrl Pts',(-1.58212954761068,-0.811583072307517,
19.331352720163));
#278017=CARTESIAN_POINT('Ctrl Pts',(-1.18169099246603,-1.20445112116229,
19.3683919989077));
#278018=CARTESIAN_POINT('Ctrl Pts',(0.90159620823838,-1.26416253453268,
0.00156140788979508));
#278019=CARTESIAN_POINT('Ctrl Pts',(1.32200468156816,-0.964344618051984,
0.0386104119716742));
#278020=CARTESIAN_POINT('Ctrl Pts',(1.83281328473215,0.0823017482344568,
0.112696558910696));
#278021=CARTESIAN_POINT('Ctrl Pts',(0.923292623565352,1.58732912987166,
0.223819848706861));
#278022=CARTESIAN_POINT('Ctrl Pts',(-0.831626641848217,1.63524339651075,
0.334931277278289));
#278023=CARTESIAN_POINT('Ctrl Pts',(-1.82527879279968,0.189405884300259,
0.446042705849719));
#278024=CARTESIAN_POINT('Ctrl Pts',(-1.14917218873408,-1.43094494259553,
0.557154134421147));
#278025=CARTESIAN_POINT('Ctrl Pts',(0.578437144337754,-1.74146511618339,
0.668265562992576));
#278026=CARTESIAN_POINT('Ctrl Pts',(1.77676889934914,-0.459034536695509,
0.779376991564005));
#278027=CARTESIAN_POINT('Ctrl Pts',(1.34954367020881,1.24354948588568,0.890488420135434));
#278028=CARTESIAN_POINT('Ctrl Pts',(-0.312411724366456,1.80830175055102,
1.00159984870686));
#278029=CARTESIAN_POINT('Ctrl Pts',(-1.68852933161371,0.71866549970365,
1.11271127727829));
#278030=CARTESIAN_POINT('Ctrl Pts',(-1.51979520469414,-1.02851234158217,
1.22382270584972));
#278031=CARTESIAN_POINT('Ctrl Pts',(0.0394205270115515,-1.83467811744561,
1.33493413442115));
#278032=CARTESIAN_POINT('Ctrl Pts',(1.56256870545359,-0.962281494451149,
1.44604556299257));
#278033=CARTESIAN_POINT('Ctrl Pts',(1.65610426516714,0.790521998350591,
1.557156991564));
#278034=CARTESIAN_POINT('Ctrl Pts',(0.234449389764976,1.82006526119027,
1.66826842013543));
#278035=CARTESIAN_POINT('Ctrl Pts',(-1.40170592803849,1.1844095345667,1.77937984870686));
#278036=CARTESIAN_POINT('Ctrl Pts',(-1.75542340175659,-0.53487753765843,
1.89049127727829));
#278037=CARTESIAN_POINT('Ctrl Pts',(-0.503082435079318,-1.76479830840923,
2.00160270584972));
#278038=CARTESIAN_POINT('Ctrl Pts',(1.20953479312287,-1.38008362078707,
2.11271413442115));
#278039=CARTESIAN_POINT('Ctrl Pts',(1.81553382429765,0.267286569474214,
2.22382556299257));
#278040=CARTESIAN_POINT('Ctrl Pts',(0.760478694725908,1.6701129591339,2.33493699156401));
#278041=CARTESIAN_POINT('Ctrl Pts',(-0.990347712058639,1.54493254928788,
2.44604842013543));
#278042=CARTESIAN_POINT('Ctrl Pts',(-1.83509285778272,0.00627439840333995,
2.55715984870686));
#278043=CARTESIAN_POINT('Ctrl Pts',(-1.00088904936001,-1.53812427049709,
2.66827127727829));
#278044=CARTESIAN_POINT('Ctrl Pts',(0.749040420284577,-1.67527419067305,
2.77938270584972));
#278045=CARTESIAN_POINT('Ctrl Pts',(1.813663626755,-0.279695213936149,2.89049413442115));
#278046=CARTESIAN_POINT('Ctrl Pts',(1.21894374614861,1.37178034211317,3.00160556299258));
#278047=CARTESIAN_POINT('Ctrl Pts',(-0.491002711504038,1.76819724613016,
3.11271699156401));
#278048=CARTESIAN_POINT('Ctrl Pts',(-1.75172476894188,0.546868812014197,
3.22382842013543));
#278049=CARTESIAN_POINT('Ctrl Pts',(-1.40977235979138,-1.17479660248503,
3.33493984870686));
#278050=CARTESIAN_POINT('Ctrl Pts',(0.221998064579255,-1.82162620288972,
3.4460512772783));
#278051=CARTESIAN_POINT('Ctrl Pts',(1.65065973806281,-0.801827657809858,
3.55716270584972));
#278052=CARTESIAN_POINT('Ctrl Pts',(1.56911258074583,0.951572841475777,
3.66827413442115));
#278053=CARTESIAN_POINT('Ctrl Pts',(0.0519650865987583,1.8343676821935,
3.77938556299258));
#278054=CARTESIAN_POINT('Ctrl Pts',(-1.51272590235006,1.03887704183597,
3.89049699156401));
#278055=CARTESIAN_POINT('Ctrl Pts',(-1.69340541780961,-0.707094940321402,
4.00160842013543));
#278056=CARTESIAN_POINT('Ctrl Pts',(-0.324767556026349,-1.80613709287233,
4.11271984870687));
#278057=CARTESIAN_POINT('Ctrl Pts',(1.34100412428894,-1.25272227661828,
4.2238312772783));
#278058=CARTESIAN_POINT('Ctrl Pts',(1.77987469110539,0.446823508399282,
4.33494270584973));
#278059=CARTESIAN_POINT('Ctrl Pts',(0.59031608246101,1.73756498770084,4.44605413442115));
#278060=CARTESIAN_POINT('Ctrl Pts',(-1.13932994707157,1.43858695788669,
4.55716556299259));
#278061=CARTESIAN_POINT('Ctrl Pts',(-1.8265890402882,-0.176571916212174,
4.66827699156401));
#278062=CARTESIAN_POINT('Ctrl Pts',(-0.842679427276936,-1.63018297946582,
4.77938842013544));
#278063=CARTESIAN_POINT('Ctrl Pts',(0.912207924670662,-1.59231964939954,
4.89049984870687));
#278064=CARTESIAN_POINT('Ctrl Pts',(1.83250506302419,-0.0976235508806328,
5.0016112772783));
#278065=CARTESIAN_POINT('Ctrl Pts',(1.07622085342053,1.48638953116558,5.11272270584973));
#278066=CARTESIAN_POINT('Ctrl Pts',(-0.6647110090249,1.71048660859329,5.22383413442115));
#278067=CARTESIAN_POINT('Ctrl Pts',(-1.79749062021609,0.369638517921229,
5.33494556299259));
#278068=CARTESIAN_POINT('Ctrl Pts',(-1.28572402643862,-1.30939638442082,
5.44605699156401));
#278069=CARTESIAN_POINT('Ctrl Pts',(0.402367241601951,-1.79044848196799,
5.55716842013545));
#278070=CARTESIAN_POINT('Ctrl Pts',(1.72232778743567,-0.633397313163549,
5.66827984870687));
#278071=CARTESIAN_POINT('Ctrl Pts',(1.4665095254785,1.1031568226579,5.7793912772783));
#278072=CARTESIAN_POINT('Ctrl Pts',(-0.131036280172964,1.83041925715784,
5.89050270584972));
#278073=CARTESIAN_POINT('Ctrl Pts',(-1.60869538664057,0.883008673058882,
6.00161413442115));
#278074=CARTESIAN_POINT('Ctrl Pts',(-1.61453936189358,-0.872277371363101,
6.11272556299259));
#278075=CARTESIAN_POINT('Ctrl Pts',(-0.143221481328173,-1.8295061549451,
6.22383699156401));
#278076=CARTESIAN_POINT('Ctrl Pts',(1.4591314883438,-1.11289732833692,6.33494842013545));
#278077=CARTESIAN_POINT('Ctrl Pts',(1.72650717094787,0.621914907653302,
6.44605984870686));
#278078=CARTESIAN_POINT('Ctrl Pts',(0.414280276548138,1.78772957019764,
6.55717127727831));
#278079=CARTESIAN_POINT('Ctrl Pts',(-1.27697672177988,1.31792853210186,
6.66828270584972));
#278080=CARTESIAN_POINT('Ctrl Pts',(-1.79991206211562,-0.357661477302979,
6.77939413442117));
#278081=CARTESIAN_POINT('Ctrl Pts',(-0.67608579060288,-1.7060226163333,
6.89050556299257));
#278082=CARTESIAN_POINT('Ctrl Pts',(1.06629965928017,-1.49352274850932,
7.00161699156402));
#278083=CARTESIAN_POINT('Ctrl Pts',(1.83311447847042,0.0854193919314032,
7.11272842013543));
#278084=CARTESIAN_POINT('Ctrl Pts',(0.922790388040553,1.58621028348571,
7.22383984870687));
#278085=CARTESIAN_POINT('Ctrl Pts',(-0.83180594145737,1.63575794036039,
7.33495127727829));
#278086=CARTESIAN_POINT('Ctrl Pts',(-1.82537281749998,0.188730603845873,
7.44606270584973));
#278087=CARTESIAN_POINT('Ctrl Pts',(-1.14888372445405,-1.43096867589072,
7.55717413442116));
#278088=CARTESIAN_POINT('Ctrl Pts',(0.578733172960644,-1.74145717093782,
7.66828556299258));
#278089=CARTESIAN_POINT('Ctrl Pts',(1.77685999539097,-0.458665150709145,
7.77939699156402));
#278090=CARTESIAN_POINT('Ctrl Pts',(1.34931582442854,1.24376523895894,7.89050842013544));
#278091=CARTESIAN_POINT('Ctrl Pts',(-0.312733936388572,1.80825956342743,
8.00161984870688));
#278092=CARTESIAN_POINT('Ctrl Pts',(-1.68865958480786,0.718355044760163,
8.1127312772783));
#278093=CARTESIAN_POINT('Ctrl Pts',(-1.51960987677947,-1.02878131111046,
8.22384270584974));
#278094=CARTESIAN_POINT('Ctrl Pts',(0.0397495373380485,-1.83467303298905,
8.33495413442116));
#278095=CARTESIAN_POINT('Ctrl Pts',(1.56274161243117,-0.961999904611144,
8.44606556299259));
#278096=CARTESIAN_POINT('Ctrl Pts',(1.6559622277092,0.790818730238608,8.55717699156402));
#278097=CARTESIAN_POINT('Ctrl Pts',(0.234122699405938,1.82010761366429,
8.66828842013545));
#278098=CARTESIAN_POINT('Ctrl Pts',(-1.40191855683668,1.18415772754004,
8.77939984870686));
#278099=CARTESIAN_POINT('Ctrl Pts',(-1.75532733845545,-0.535192580821834,
8.89051127727831));
#278100=CARTESIAN_POINT('Ctrl Pts',(-0.502765618493741,-1.7648886357378,
9.00162270584972));
#278101=CARTESIAN_POINT('Ctrl Pts',(1.20978252953801,-1.3798664409719,9.11273413442116));
#278102=CARTESIAN_POINT('Ctrl Pts',(1.81548580983413,0.26761247726283,9.22384556299259));
#278103=CARTESIAN_POINT('Ctrl Pts',(0.760178865566043,1.67024945922534,
9.33495699156402));
#278104=CARTESIAN_POINT('Ctrl Pts',(-0.990625042304408,1.54475473433657,
9.44606842013544));
#278105=CARTESIAN_POINT('Ctrl Pts',(-1.83509395429444,0.00594496491354616,
9.55717984870688));
#278106=CARTESIAN_POINT('Ctrl Pts',(-1.00061290996535,-1.53830392579183,
9.6682912772783));
#278107=CARTESIAN_POINT('Ctrl Pts',(0.749341152814527,-1.67513969578493,
9.77940270584973));
#278108=CARTESIAN_POINT('Ctrl Pts',(1.81371380825452,-0.279369621545994,
9.89051413442117));
#278109=CARTESIAN_POINT('Ctrl Pts',(1.21869746509954,1.37199914440783,10.0016255629926));
#278110=CARTESIAN_POINT('Ctrl Pts',(-0.491320129629947,1.76810907296927,
10.112736991564));
#278111=CARTESIAN_POINT('Ctrl Pts',(-1.7518229143681,0.546554334344457,
10.2238484201354));
#278112=CARTESIAN_POINT('Ctrl Pts',(-1.40956143808614,-1.17504966531477,
10.3349598487069));
#278113=CARTESIAN_POINT('Ctrl Pts',(0.222325078573523,-1.82158632052756,
10.4460712772783));
#278114=CARTESIAN_POINT('Ctrl Pts',(1.65080365522765,-0.801531319152839,
10.5571827058497));
#278115=CARTESIAN_POINT('Ctrl Pts',(1.56894172950593,0.951854512575722,
10.6682941344212));
#278116=CARTESIAN_POINT('Ctrl Pts',(0.0516357808464248,1.8343769813842,
10.7794055629926));
#278117=CARTESIAN_POINT('Ctrl Pts',(-1.51291237674398,1.03860546117894,
10.890516991564));
#278118=CARTESIAN_POINT('Ctrl Pts',(-1.69327845313648,-0.70739892835625,
11.0016284201355));
#278119=CARTESIAN_POINT('Ctrl Pts',(-0.324443313821911,-1.80619536590374,
11.1127398487069));
#278120=CARTESIAN_POINT('Ctrl Pts',(1.34122899085663,-1.25248151993613,
11.2238512772783));
#278121=CARTESIAN_POINT('Ctrl Pts',(1.77979444885685,0.447143023555279,
11.3349627058497));
#278122=CARTESIAN_POINT('Ctrl Pts',(0.590004146013124,1.73767093299715,
11.4460741344212));
#278123=CARTESIAN_POINT('Ctrl Pts',(-1.13958818323841,1.43838240267295,
11.5571855629926));
#278124=CARTESIAN_POINT('Ctrl Pts',(-1.82655731273908,-0.176899821863194,
11.668296991564));
#278125=CARTESIAN_POINT('Ctrl Pts',(-0.842386763935508,-1.63033423065398,
11.7794084201354));
#278126=CARTESIAN_POINT('Ctrl Pts',(0.912493762525382,-1.59215586455853,
11.8905198487069));
#278127=CARTESIAN_POINT('Ctrl Pts',(1.83252255883466,-0.0972945787694221,
12.0016312772783));
#278128=CARTESIAN_POINT('Ctrl Pts',(1.07595400005526,1.48658270992936,12.1127427058498));
#278129=CARTESIAN_POINT('Ctrl Pts',(-0.665018064150505,1.71036725239036,
12.2238541344211));
#278130=CARTESIAN_POINT('Ctrl Pts',(-1.79755694860324,0.369315827204919,
12.3349655629926));
#278131=CARTESIAN_POINT('Ctrl Pts',(-1.28548894343276,-1.3096271759581,
12.446076991564));
#278132=CARTESIAN_POINT('Ctrl Pts',(0.402688655676732,-1.79037622031939,
12.5571884201355));
#278133=CARTESIAN_POINT('Ctrl Pts',(1.72244146690194,-0.633088111397257,
12.6682998487069));
#278134=CARTESIAN_POINT('Ctrl Pts',(1.4663114635989,1.10342007205519,12.7794112772783));
#278135=CARTESIAN_POINT('Ctrl Pts',(-0.131364874156623,1.83039570408523,
12.8905227058497));
#278136=CARTESIAN_POINT('Ctrl Pts',(-1.6088538780642,0.882719866511245,
13.0016341344212));
#278137=CARTESIAN_POINT('Ctrl Pts',(-1.61438274501066,-0.872567198734688,
13.1127455629926));
#278138=CARTESIAN_POINT('Ctrl Pts',(-0.142893046844922,-1.82953183652519,
13.223856991564));
#278139=CARTESIAN_POINT('Ctrl Pts',(1.45933125169217,-1.11263536773302,
13.3349684201355));
#278140=CARTESIAN_POINT('Ctrl Pts',(1.72639549722492,0.62222483947312,13.4460798487069));
#278141=CARTESIAN_POINT('Ctrl Pts',(0.413959337412072,1.78780391281181,
13.5571912772783));
#278142=CARTESIAN_POINT('Ctrl Pts',(-1.27721329517889,1.31769926854125,
13.6683027058497));
#278143=CARTESIAN_POINT('Ctrl Pts',(-1.7998478258745,-0.357984590996087,
13.7794141344212));
#278144=CARTESIAN_POINT('Ctrl Pts',(-0.675779515246169,-1.70614395947982,
13.8905255629926));
#278145=CARTESIAN_POINT('Ctrl Pts',(1.06656775867382,-1.49333130277691,
14.001636991564));
#278146=CARTESIAN_POINT('Ctrl Pts',(1.83309911447898,0.0857484704951466,
14.1127484201355));
#278147=CARTESIAN_POINT('Ctrl Pts',(0.922505617368107,1.58637591686842,
14.2238598487069));
#278148=CARTESIAN_POINT('Ctrl Pts',(-0.83209957863139,1.63560858854962,
14.3349712772783));
#278149=CARTESIAN_POINT('Ctrl Pts',(-1.82540666892521,0.1884029106443,14.4460827058497));
#278150=CARTESIAN_POINT('Ctrl Pts',(-1.14862681904651,-1.43117489995561,
14.5571941344212));
#278151=CARTESIAN_POINT('Ctrl Pts',(0.579045789294013,-1.74135324894081,
14.6683055629926));
#278152=CARTESIAN_POINT('Ctrl Pts',(1.77694230613423,-0.458346162159357,
14.779416991564));
#278153=CARTESIAN_POINT('Ctrl Pts',(1.34909252247358,1.24400744752661,14.8905284201355));
#278154=CARTESIAN_POINT('Ctrl Pts',(-0.313058549345564,1.8082033924251,
15.0016398487069));
#278155=CARTESIAN_POINT('Ctrl Pts',(-1.6887885163929,0.718051885726373,
15.1127512772783));
#278156=CARTESIAN_POINT('Ctrl Pts',(-1.51942516590475,-1.02905409425885,
15.2238627058497));
#278157=CARTESIAN_POINT('Ctrl Pts',(0.0400788964287514,-1.83466586760579,
15.3349741344212));
#278158=CARTESIAN_POINT('Ctrl Pts',(1.56291428506798,-0.961719346392447,
15.4460855629926));
#278159=CARTESIAN_POINT('Ctrl Pts',(1.6558202335798,0.791115995137488,15.5571969915641));
#278160=CARTESIAN_POINT('Ctrl Pts',(0.233795950680089,1.82014961394571,
15.6683084201354));
#278161=CARTESIAN_POINT('Ctrl Pts',(-1.40213111374382,1.1839060366265,15.7794198487069));
#278162=CARTESIAN_POINT('Ctrl Pts',(-1.75523123262381,-0.535507687818136,
15.8905312772783));
#278163=CARTESIAN_POINT('Ctrl Pts',(-0.502448778326618,-1.76497886358149,
16.0016427058498));
#278164=CARTESIAN_POINT('Ctrl Pts',(1.21003022308683,-1.37964923906714,
16.1127541344212));
#278165=CARTESIAN_POINT('Ctrl Pts',(1.81543773890125,0.267938388163036,
16.2238655629926));
#278166=CARTESIAN_POINT('Ctrl Pts',(0.759879010835324,1.67038589937133,
16.334976991564));
#278167=CARTESIAN_POINT('Ctrl Pts',(-0.990902340059985,1.54457687272166,
16.4460884201355));
#278168=CARTESIAN_POINT('Ctrl Pts',(-1.83509499196587,0.0056155297747307,
16.5571998487069));
#278169=CARTESIAN_POINT('Ctrl Pts',(-1.00033673816072,-1.53848353109199,
16.6683112772783));
#278170=CARTESIAN_POINT('Ctrl Pts',(0.74964186109952,-1.67500514647217,
16.7794227058498));
#278171=CARTESIAN_POINT('Ctrl Pts',(1.8137639313726,-0.279044021638752,
16.8905341344212));
#278172=CARTESIAN_POINT('Ctrl Pts',(1.21845114470182,1.37221790565629,17.0016455629926));
#278173=CARTESIAN_POINT('Ctrl Pts',(-0.491637531813608,1.76802083661681,
17.112756991564));
#278174=CARTESIAN_POINT('Ctrl Pts',(-1.75192100352765,0.546239850970993,
17.2238684201355));
#278175=CARTESIAN_POINT('Ctrl Pts',(-1.40935047060202,-1.17530271298651,
17.3349798487069));
#278176=CARTESIAN_POINT('Ctrl Pts',(0.222652084736599,-1.82154633622422,
17.4460912772783));
#278177=CARTESIAN_POINT('Ctrl Pts',(1.65094752045689,-0.801235036942007,
17.5572027058497));
#278178=CARTESIAN_POINT('Ctrl Pts',(1.56877082529708,0.952136309552117,
17.6683141344212));
#278179=CARTESIAN_POINT('Ctrl Pts',(0.051306478007515,1.83438592359057,
17.7794255629926));
#278180=CARTESIAN_POINT('Ctrl Pts',(-1.51309881109001,1.03833441378922,
17.8905369915641));
#278181=CARTESIAN_POINT('Ctrl Pts',(-1.69315141732336,-0.707703971899209,
18.0016484201354));
#278182=CARTESIAN_POINT('Ctrl Pts',(-0.324119092688714,-1.80625152908954,
18.1127598487069));
#278183=CARTESIAN_POINT('Ctrl Pts',(1.34145387418529,-1.25224462643346,
18.2238712772783));
#278184=CARTESIAN_POINT('Ctrl Pts',(1.77971403511999,0.447469951372195,
18.3349827058498));
#278185=CARTESIAN_POINT('Ctrl Pts',(0.589692407699955,1.73776269118328,
18.4460941344212));
#278186=CARTESIAN_POINT('Ctrl Pts',(-1.13984679582908,1.43820468768718,
18.5572055629926));
#278187=CARTESIAN_POINT('Ctrl Pts',(-1.82652474031938,-0.177278877971518,
18.668316991564));
#278188=CARTESIAN_POINT('Ctrl Pts',(-0.842095568311332,-1.63038809326605,
18.7794284201355));
#278189=CARTESIAN_POINT('Ctrl Pts',(0.9127824097774,-1.59217725787693,18.8905398487069));
#278190=CARTESIAN_POINT('Ctrl Pts',(1.83253464080909,-0.0966128908919654,
19.0016512772783));
#278191=CARTESIAN_POINT('Ctrl Pts',(1.07569690031554,1.48610228985601,19.1127627058498));
#278192=CARTESIAN_POINT('Ctrl Pts',(-0.665340284739988,1.71155056623269,
19.2238741344212));
#278193=CARTESIAN_POINT('Ctrl Pts',(-1.79764490803661,0.366307003311719,
19.33498769888));
#278194=CARTESIAN_POINT('Ctrl Pts',(-1.45592170589159,-0.746842389038948,
19.4090641204817));
#278195=CARTESIAN_POINT('Ctrl Pts',(-1.08742648045863,-1.10837101401327,
19.4461033992263));
#278196=CARTESIAN_POINT('Ctrl Pts',(0.863566907998541,1.75641557941956,
1.92055572834082E-15));
#278197=CARTESIAN_POINT('Ctrl Pts',(0.902606995688333,1.73244080950236,
2.43072380935166E-15));
#278198=CARTESIAN_POINT('Ctrl Pts',(0.940685126167239,1.70703143391729,
2.63212312969157E-15));
#278199=CARTESIAN_POINT('Ctrl Pts',(0.977710780925362,1.68018273146334,
2.4459601011273E-15));
#278200=CARTESIAN_POINT('Ctrl Pts',(1.03606710713796,1.63786635248171,2.04295423620313E-15));
#278201=CARTESIAN_POINT('Ctrl Pts',(1.09181123604325,1.59197570838927,-9.03406496512887E-16));
#278202=CARTESIAN_POINT('Ctrl Pts',(1.14478006703473,1.54285501782175,9.74914593498966E-16));
#278203=CARTESIAN_POINT('Ctrl Pts',(1.16983151419263,1.51962353694747,1.8632608275243E-15));
#278204=CARTESIAN_POINT('Ctrl Pts',(1.19426155983482,1.49566911335637,1.92711446182748E-16));
#278205=CARTESIAN_POINT('Ctrl Pts',(1.21804938169849,1.47102626716015,6.97358837342676E-16));
#278206=CARTESIAN_POINT('Ctrl Pts',(1.23021944053223,1.45841877035958,8.54673365253237E-16));
#278207=CARTESIAN_POINT('Ctrl Pts',(1.24222136284868,1.44563106829319,-1.63299175600747E-15));
#278208=CARTESIAN_POINT('Ctrl Pts',(1.25405211098615,1.43266770693123,-9.57567358739198E-16));
#278209=CARTESIAN_POINT('Ctrl Pts',(1.26392059005265,1.42185447189777,-4.55923984025048E-16));
#278210=CARTESIAN_POINT('Ctrl Pts',(1.27366323022463,1.41092637478828,3.63847824488057E-16));
#278211=CARTESIAN_POINT('Ctrl Pts',(1.28327753990859,1.39988788299174,4.9960036108132E-16));
#278212=CARTESIAN_POINT('Ctrl Pts',(1.33011375332078,1.34611375104404,1.52177178458909E-15));
#278213=CARTESIAN_POINT('Ctrl Pts',(1.37391850734965,1.28971037306795,-1.41152132602092E-15));
#278214=CARTESIAN_POINT('Ctrl Pts',(1.41452895199254,1.2310109768871,-7.84095011141517E-16));
#278215=CARTESIAN_POINT('Ctrl Pts',(1.45487911675909,1.17268779603001,-1.60689987954089E-16));
#278216=CARTESIAN_POINT('Ctrl Pts',(1.49207610172446,1.11209686113068,-5.01359578401628E-15));
#278217=CARTESIAN_POINT('Ctrl Pts',(1.5259112036015,1.04955135028031,-3.68455266297474E-15));
#278218=CARTESIAN_POINT('Ctrl Pts',(1.53054536577512,1.040984920022,-3.50252272906105E-15));
#278219=CARTESIAN_POINT('Ctrl Pts',(1.53511638288187,1.03238181735526,-3.52147310612354E-15));
#278220=CARTESIAN_POINT('Ctrl Pts',(1.53962364151379,1.02374284391693,-3.58046925441613E-15));
#278221=CARTESIAN_POINT('Ctrl Pts',(1.54538639912254,1.01269748043125,-3.73160264907701E-15));
#278222=CARTESIAN_POINT('Ctrl Pts',(1.5510405224455,1.00160191092775,-9.50044333076555E-16));
#278223=CARTESIAN_POINT('Ctrl Pts',(1.55658450782952,0.990459465485314,
-1.04083408558608E-15));
#278224=CARTESIAN_POINT('Ctrl Pts',(1.58754494280248,0.928234381242756,
-1.95974260143647E-15));
#278225=CARTESIAN_POINT('Ctrl Pts',(1.61508262262489,0.86453306559026,-1.88413048647842E-15));
#278226=CARTESIAN_POINT('Ctrl Pts',(1.63904429710683,0.799662226664679,
-2.2065682614425E-15));
#278227=CARTESIAN_POINT('Ctrl Pts',(1.66267977657407,0.735674487301784,
-2.52461662719312E-15));
#278228=CARTESIAN_POINT('Ctrl Pts',(1.68283613808164,0.670547857459508,
-2.36383228719471E-15));
#278229=CARTESIAN_POINT('Ctrl Pts',(1.69931635736196,0.604571550293125,
-4.16333634234434E-15));
#278230=CARTESIAN_POINT('Ctrl Pts',(1.71527817949359,0.540670575313434,
-5.9062357033828E-15));
#278231=CARTESIAN_POINT('Ctrl Pts',(1.72779149233561,0.475971746451621,
-1.53638505387586E-15));
#278232=CARTESIAN_POINT('Ctrl Pts',(1.73662900130601,0.410745883467762,
-1.76247905159244E-15));
#278233=CARTESIAN_POINT('Ctrl Pts',(1.73865871892773,0.395765408321034,
-1.81440623750726E-15));
#278234=CARTESIAN_POINT('Ctrl Pts',(1.74049433596503,0.380757194592868,
-1.77301121448585E-15));
#278235=CARTESIAN_POINT('Ctrl Pts',(1.74213272345364,0.365724650926664,
-1.70696790036118E-15));
#278236=CARTESIAN_POINT('Ctrl Pts',(1.74338727089007,0.354213919032973,
-1.74377001770268E-15));
#278237=CARTESIAN_POINT('Ctrl Pts',(1.74452611236442,0.342688540754893,
-1.34699067263872E-15));
#278238=CARTESIAN_POINT('Ctrl Pts',(1.74554673034743,0.331165227615983,
-2.02615701994091E-15));
#278239=CARTESIAN_POINT('Ctrl Pts',(1.75129561321446,0.266257320271039,
-4.77896472164434E-15));
#278240=CARTESIAN_POINT('Ctrl Pts',(1.75331133583169,0.201296883564266,
-1.89713026672775E-15));
#278241=CARTESIAN_POINT('Ctrl Pts',(1.75142675830796,0.136544317949457,
-1.45716771982052E-15));
#278242=CARTESIAN_POINT('Ctrl Pts',(1.75088407860913,0.117898280647071,
-1.2709926870932E-15));
#278243=CARTESIAN_POINT('Ctrl Pts',(1.75001766131977,0.099269521756727,
-4.72295564128628E-15));
#278244=CARTESIAN_POINT('Ctrl Pts',(1.74882271567549,0.0806644060278795,
-4.56579218877096E-15));
#278245=CARTESIAN_POINT('Ctrl Pts',(1.74456498482946,0.0143722064518782,
-3.40614148876069E-15));
#278246=CARTESIAN_POINT('Ctrl Pts',(1.73613992417247,-0.0516216682407977,
-2.7009660656099E-15));
#278247=CARTESIAN_POINT('Ctrl Pts',(1.72372303569837,-0.117012374160561,
-1.88737914186277E-15));
#278248=CARTESIAN_POINT('Ctrl Pts',(1.7117534570167,-0.180047425267717,
-1.10310112257602E-15));
#278249=CARTESIAN_POINT('Ctrl Pts',(1.69607360968479,-0.242522628982395,
-2.53169565084214E-15));
#278250=CARTESIAN_POINT('Ctrl Pts',(1.67680428334833,-0.304137057490082,
-2.4980018054066E-15));
#278251=CARTESIAN_POINT('Ctrl Pts',(1.67349444731961,-0.314720388313531,
-2.69394111988223E-15));
#278252=CARTESIAN_POINT('Ctrl Pts',(1.67008022174013,-0.325273006340074,
3.29470571676352E-16));
#278253=CARTESIAN_POINT('Ctrl Pts',(1.66656493085673,-0.335786380672971,
2.4980018054066E-16));
#278254=CARTESIAN_POINT('Ctrl Pts',(1.64601993144971,-0.397231443570826,
4.68513083847165E-17));
#278255=CARTESIAN_POINT('Ctrl Pts',(1.62200297335448,-0.457413864499819,
-2.65433772659743E-15));
#278256=CARTESIAN_POINT('Ctrl Pts',(1.59470046562981,-0.516060019276523,
-1.13797860024079E-15));
#278257=CARTESIAN_POINT('Ctrl Pts',(1.56765678382067,-0.574150212496288,
3.64005544772621E-16));
#278258=CARTESIAN_POINT('Ctrl Pts',(1.53738877393808,-0.630733917539196,
-2.58600310425349E-15));
#278259=CARTESIAN_POINT('Ctrl Pts',(1.50403879475748,-0.685513423969216,
-2.3037127760972E-15));
#278260=CARTESIAN_POINT('Ctrl Pts',(1.4709648894784,-0.739839461088768,
-2.02375927075665E-15));
#278261=CARTESIAN_POINT('Ctrl Pts',(1.43485912858928,-0.792391764160348,
-9.14736882961259E-16));
#278262=CARTESIAN_POINT('Ctrl Pts',(1.39583294870606,-0.842837370270167,
8.60422844084496E-16));
#278263=CARTESIAN_POINT('Ctrl Pts',(1.38892463177069,-0.851767125527953,
1.12372394253433E-15));
#278264=CARTESIAN_POINT('Ctrl Pts',(1.38192474839882,-0.860630742755753,
-1.42167219695244E-15));
#278265=CARTESIAN_POINT('Ctrl Pts',(1.37483385167802,-0.869426208469204,
-1.27675647831893E-15));
#278266=CARTESIAN_POINT('Ctrl Pts',(1.36805999011309,-0.877828427467431,
-1.10795478880039E-15));
#278267=CARTESIAN_POINT('Ctrl Pts',(1.36120614272911,-0.886164561590754,
8.11183197120448E-16));
#278268=CARTESIAN_POINT('Ctrl Pts',(1.35427819652575,-0.89442703186717,
5.55111512312578E-16));
#278269=CARTESIAN_POINT('Ctrl Pts',(1.31436511271567,-0.942028537268739,
-7.1629539480613E-16));
#278270=CARTESIAN_POINT('Ctrl Pts',(1.27194408914578,-0.987251877392324,
1.06778634412269E-17));
#278271=CARTESIAN_POINT('Ctrl Pts',(1.22715435283182,-1.02982897690716,
-1.38777878078145E-16));
#278272=CARTESIAN_POINT('Ctrl Pts',(1.18376706222622,-1.07107291227764,
-2.83553896506172E-16));
#278273=CARTESIAN_POINT('Ctrl Pts',(1.1381563430115,-1.10983414583466,1.71437262194897E-16));
#278274=CARTESIAN_POINT('Ctrl Pts',(1.09042633843192,-1.14582699077891,
-5.55111512312578E-16));
#278275=CARTESIAN_POINT('Ctrl Pts',(1.04308447972006,-1.18152713778282,
-1.27575190891385E-15));
#278276=CARTESIAN_POINT('Ctrl Pts',(0.993657096245488,-1.21450424181457,
5.94987629519964E-16));
#278277=CARTESIAN_POINT('Ctrl Pts',(0.942232789017055,-1.24443055068302,
9.15933995315754E-16));
#278278=CARTESIAN_POINT('Ctrl Pts',(0.929479875758739,-1.25185209200677,
9.75669572373557E-16));
#278279=CARTESIAN_POINT('Ctrl Pts',(0.916604109661386,-1.25908574890519,
1.77947334077032E-15));
#278280=CARTESIAN_POINT('Ctrl Pts',(0.903606778650208,-1.26612599672284,
5.55111512312578E-17));
#278281=CARTESIAN_POINT('Ctrl Pts',(-0.684401294465645,1.39375859696713,
-0.231689979925561));
#278282=CARTESIAN_POINT('Ctrl Pts',(-1.14800519021184,1.16611376614941,
-0.194632647470989));
#278283=CARTESIAN_POINT('Ctrl Pts',(-1.82210733642078,0.215869300640666,
-0.120523386424568));
#278284=CARTESIAN_POINT('Ctrl Pts',(-1.16801489871654,-1.41729336359585,
-0.00936219678629828));
#278285=CARTESIAN_POINT('Ctrl Pts',(0.556977146514337,-1.7482231903558,
0.101793588989252));
#278286=CARTESIAN_POINT('Ctrl Pts',(1.7712308476463,-0.480771985689559,
0.212949374764799));
#278287=CARTESIAN_POINT('Ctrl Pts',(1.36418695589471,1.22803976333708,0.324105160540349));
#278288=CARTESIAN_POINT('Ctrl Pts',(-0.292095232734673,1.81186540287904,
0.435260946315896));
#278289=CARTESIAN_POINT('Ctrl Pts',(-1.68082790602658,0.737104570480516,
0.546416732091446));
#278290=CARTESIAN_POINT('Ctrl Pts',(-1.53068522271668,-1.01270541030781,
0.657572517866994));
#278291=CARTESIAN_POINT('Ctrl Pts',(0.0209552616995192,-1.83521194377032,
0.768728303642543));
#278292=CARTESIAN_POINT('Ctrl Pts',(1.55339315684676,-0.977479777233187,
0.879884089418091));
#278293=CARTESIAN_POINT('Ctrl Pts',(1.66358198078138,0.775239234716729,
0.99103987519364));
#278294=CARTESIAN_POINT('Ctrl Pts',(0.250621806749922,1.81815076116018,
1.10219566096919));
#278295=CARTESIAN_POINT('Ctrl Pts',(-1.39180062373996,1.19640434318354,
1.21335144674473));
#278296=CARTESIAN_POINT('Ctrl Pts',(-1.75991773480115,-0.52075105178842,
1.32450723252028));
#278297=CARTESIAN_POINT('Ctrl Pts',(-0.51668649624412,-1.76111466039208,
1.43566301829583));
#278298=CARTESIAN_POINT('Ctrl Pts',(1.19961287026365,-1.38903568181859,
1.54681880407138));
#278299=CARTESIAN_POINT('Ctrl Pts',(1.81756935651455,0.254818854352526,
1.65797458984693));
#278300=CARTESIAN_POINT('Ctrl Pts',(0.771393309043584,1.66536574983418,
1.76913037562248));
#278301=CARTESIAN_POINT('Ctrl Pts',(-0.981055945000064,1.55113512014234,
1.88028616139803));
#278302=CARTESIAN_POINT('Ctrl Pts',(-1.83526878868891,0.016714169768612,
1.99144194717358));
#278303=CARTESIAN_POINT('Ctrl Pts',(-1.00914391160594,-1.53300992150868,
2.10259773294912));
#278304=CARTESIAN_POINT('Ctrl Pts',(0.740934210662865,-1.67913888064429,
2.21375351872467));
#278305=CARTESIAN_POINT('Ctrl Pts',(1.81262685979311,-0.287879739532146,
2.32490930450022));
#278306=CARTESIAN_POINT('Ctrl Pts',(1.22471232570858,1.36695668999331,2.43606509027577));
#278307=CARTESIAN_POINT('Ctrl Pts',(-0.484525859611966,1.77023319621169,
2.54722087605132));
#278308=CARTESIAN_POINT('Ctrl Pts',(-1.75014124923941,0.552717363477061,
2.65837666182686));
#278309=CARTESIAN_POINT('Ctrl Pts',(-1.41336011130569,-1.17085612758582,
2.76953244760242));
#278310=CARTESIAN_POINT('Ctrl Pts',(0.217467055686965,-1.82241569244561,
2.88068823337796));
#278311=CARTESIAN_POINT('Ctrl Pts',(1.64918546226433,-0.805405604147006,
2.99184401915352));
#278312=CARTESIAN_POINT('Ctrl Pts',(1.57094056800582,0.949018760557804,
3.10299980492906));
#278313=CARTESIAN_POINT('Ctrl Pts',(0.0543719317205851,1.8345393343365,
3.21415559070461));
#278314=CARTESIAN_POINT('Ctrl Pts',(-1.51197862623999,1.04039007585601,
3.32531137648016));
#278315=CARTESIAN_POINT('Ctrl Pts',(-1.6939898909823,-0.70632083743466,
3.43646716225571));
#278316=CARTESIAN_POINT('Ctrl Pts',(-0.325015759708903,-1.80633762959686,
3.54762294803126));
#278317=CARTESIAN_POINT('Ctrl Pts',(1.34153670982427,-1.2525055418417,3.6587787338068));
#278318=CARTESIAN_POINT('Ctrl Pts',(1.779803310452,0.448097146001531,3.76993451958235));
#278319=CARTESIAN_POINT('Ctrl Pts',(0.588515356479842,1.73843048504668,
3.8810903053579));
#278320=CARTESIAN_POINT('Ctrl Pts',(-1.14160622813708,1.43708945303688,
3.99224609113345));
#278321=CARTESIAN_POINT('Ctrl Pts',(-1.82649454585514,-0.180023748746552,
4.103401876909));
#278322=CARTESIAN_POINT('Ctrl Pts',(-0.839078688908557,-1.6323105801198,
4.21455766268455));
#278323=CARTESIAN_POINT('Ctrl Pts',(0.916581889884211,-1.59008443652773,
4.3257134484601));
#278324=CARTESIAN_POINT('Ctrl Pts',(1.83303726855532,-0.0920067836558015,
4.43686923423564));
#278325=CARTESIAN_POINT('Ctrl Pts',(1.07119807827886,1.49031055597253,4.5480250200112));
#278326=CARTESIAN_POINT('Ctrl Pts',(-0.671409996451009,1.7081274814302,
4.65918080578674));
#278327=CARTESIAN_POINT('Ctrl Pts',(-1.79928766176102,0.36201489801663,
4.77033659156229));
#278328=CARTESIAN_POINT('Ctrl Pts',(-1.27977126558102,-1.31555174126471,
4.88149237733784));
#278329=CARTESIAN_POINT('Ctrl Pts',(0.411479716340706,-1.78862386185346,
4.99264816311339));
#278330=CARTESIAN_POINT('Ctrl Pts',(1.72598758178942,-0.624065496290367,
5.10380394888895));
#278331=CARTESIAN_POINT('Ctrl Pts',(1.46021356520572,1.11187554165951,5.21495973466448));
#278332=CARTESIAN_POINT('Ctrl Pts',(-0.142504624869778,1.82980417204742,
5.32611552044004));
#278333=CARTESIAN_POINT('Ctrl Pts',(-1.61474825118621,0.87239839605682,
5.43727130621559));
#278334=CARTESIAN_POINT('Ctrl Pts',(-1.60855864176201,-0.883759001178613,
5.54842709199114));
#278335=CARTESIAN_POINT('Ctrl Pts',(-0.129602886982468,-1.83076322003618,
5.65958287776667));
#278336=CARTESIAN_POINT('Ctrl Pts',(1.46801484214636,-1.10155494615087,
5.77073866354224));
#278337=CARTESIAN_POINT('Ctrl Pts',(1.72154569482533,0.636216391473685,
5.88189444931778));
#278338=CARTESIAN_POINT('Ctrl Pts',(0.398861573927917,1.79147992480942,
5.99305023509333));
#278339=CARTESIAN_POINT('Ctrl Pts',(-1.28901272873415,1.30649801427816,
6.10420602086888));
#278340=CARTESIAN_POINT('Ctrl Pts',(-1.79669113519176,-0.374688992198572,
6.21536180664442));
#278341=CARTESIAN_POINT('Ctrl Pts',(-0.659352811222979,-1.71281777970798,
6.32651759241998));
#278342=CARTESIAN_POINT('Ctrl Pts',(1.0816765893424,-1.48272270914694,6.43767337819552));
#278343=CARTESIAN_POINT('Ctrl Pts',(1.83234317710919,0.104925485240009,
6.54882916397107));
#278344=CARTESIAN_POINT('Ctrl Pts',(0.905350693048038,1.59650587181786,
6.65998494974661));
#278345=CARTESIAN_POINT('Ctrl Pts',(-0.850563917802709,1.62635540331244,
6.77114073552217));
#278346=CARTESIAN_POINT('Ctrl Pts',(-1.82771814648395,0.167144408116774,
6.88229652129771));
#278347=CARTESIAN_POINT('Ctrl Pts',(-1.13144789469704,-1.44510087458871,
6.99345230707328));
#278348=CARTESIAN_POINT('Ctrl Pts',(0.600754844274818,-1.7342388800946,
7.1046080928488));
#278349=CARTESIAN_POINT('Ctrl Pts',(1.78291770696527,-0.435540269482793,
7.21576387862437));
#278350=CARTESIAN_POINT('Ctrl Pts',(1.33267453197674,1.26193084912447,7.3269196643999));
#278351=CARTESIAN_POINT('Ctrl Pts',(-0.337740467970948,1.8040017329388,
7.43807545017548));
#278352=CARTESIAN_POINT('Ctrl Pts',(-1.69892662525787,0.69436244004221,
7.54923123595101));
#278353=CARTESIAN_POINT('Ctrl Pts',(-1.50460740514568,-1.05102208945971,
7.66038702172655));
#278354=CARTESIAN_POINT('Ctrl Pts',(0.0673021562935621,-1.83411049173971,
7.77154280750212));
#278355=CARTESIAN_POINT('Ctrl Pts',(1.57759112478382,-0.937921702038478,
7.88269859327765));
#278356=CARTESIAN_POINT('Ctrl Pts',(1.64346722608163,0.817010619849554,
7.9938543790532));
#278357=CARTESIAN_POINT('Ctrl Pts',(0.204615536465528,1.82390333032986,
8.10501016482876));
#278358=CARTESIAN_POINT('Ctrl Pts',(-1.42157830350579,1.16086433451675,
8.21616595060431));
#278359=CARTESIAN_POINT('Ctrl Pts',(-1.74620169150925,-0.565040289467627,
8.32732173637986));
#278360=CARTESIAN_POINT('Ctrl Pts',(-0.472035537466569,-1.77360461420242,
8.43847752215539));
#278361=CARTESIAN_POINT('Ctrl Pts',(1.23431750795601,-1.35828979444915,
8.54963330793096));
#278362=CARTESIAN_POINT('Ctrl Pts',(1.81055257623992,0.300649704510773,
8.6607890937065));
#278363=CARTESIAN_POINT('Ctrl Pts',(0.729079638460007,1.68431996869195,
8.77194487948205));
#278364=CARTESIAN_POINT('Ctrl Pts',(-1.01992495213898,1.52585843647297,
8.8831006652576));
#278365=CARTESIAN_POINT('Ctrl Pts',(-1.8351053716353,-0.0296504830769352,
8.99425645103314));
#278366=CARTESIAN_POINT('Ctrl Pts',(-0.970097705763678,-1.55801197602055,
9.10541223680869));
#278367=CARTESIAN_POINT('Ctrl Pts',(0.783113238274159,-1.65988690343384,
9.21656802258424));
#278368=CARTESIAN_POINT('Ctrl Pts',(1.81932037818187,-0.242000491081359,
9.32772380835979));
#278369=CARTESIAN_POINT('Ctrl Pts',(1.18979187689078,1.3974570354169,9.43887959413534));
#278370=CARTESIAN_POINT('Ctrl Pts',(-0.52908776821942,1.75742909093711,
9.55003537991088));
#278371=CARTESIAN_POINT('Ctrl Pts',(-1.7635445687253,0.508332007915007,
9.66119116568645));
#278372=CARTESIAN_POINT('Ctrl Pts',(-1.38333301384016,-1.20618433457385,
9.77234695146198));
#278373=CARTESIAN_POINT('Ctrl Pts',(0.263432322574806,-1.81634090621069,
9.88350273723755));
#278374=CARTESIAN_POINT('Ctrl Pts',(1.66900396159649,-0.763489785345338,
9.99465852301308));
#278375=CARTESIAN_POINT('Ctrl Pts',(1.54646685326738,0.98839827392439,10.1058143087887));
#278376=CARTESIAN_POINT('Ctrl Pts',(0.00801367742611086,1.83532739780278,
10.2169700945642));
#278377=CARTESIAN_POINT('Ctrl Pts',(-1.53777667127697,1.00186515331543,
10.3281258803398));
#278378=CARTESIAN_POINT('Ctrl Pts',(-1.67560752022996,-0.748886048942189,
10.4392816661153));
#278379=CARTESIAN_POINT('Ctrl Pts',(-0.279283527308905,-1.81397122014803,
10.5504374518909));
#278380=CARTESIAN_POINT('Ctrl Pts',(1.37274722898226,-1.21821833899879,
10.6615932376664));
#278381=CARTESIAN_POINT('Ctrl Pts',(1.76791634996442,0.492912421916842,
10.7727490234419));
#278382=CARTESIAN_POINT('Ctrl Pts',(0.544414394587412,1.75274180731717,
10.8839048092175));
#278383=CARTESIAN_POINT('Ctrl Pts',(-1.17754317725016,1.40779364321019,
10.995060594993));
#278384=CARTESIAN_POINT('Ctrl Pts',(-1.82136428509877,-0.226103996245259,
11.1062163807686));
#278385=CARTESIAN_POINT('Ctrl Pts',(-0.797578388881661,-1.65298505430036,
11.2173721665441));
#278386=CARTESIAN_POINT('Ctrl Pts',(0.956455332261048,-1.56642397630427,
11.3285279523197));
#278387=CARTESIAN_POINT('Ctrl Pts',(1.83477647673596,-0.0456744629728,11.4396837380952));
#278388=CARTESIAN_POINT('Ctrl Pts',(1.0332106658487,1.51689373264178,11.5508395238708));
#278389=CARTESIAN_POINT('Ctrl Pts',(-0.714343466617656,1.69062245573992,
11.6619953096463));
#278390=CARTESIAN_POINT('Ctrl Pts',(-1.80785810902362,0.316448943415789,
11.7731510954219));
#278391=CARTESIAN_POINT('Ctrl Pts',(-1.24613174905026,-1.34745929072473,
11.8843068811974));
#278392=CARTESIAN_POINT('Ctrl Pts',(0.456529485789276,-1.77765905188718,
11.995462666973));
#278393=CARTESIAN_POINT('Ctrl Pts',(1.74120087955567,-0.580267501404289,
12.1066184527485));
#278394=CARTESIAN_POINT('Ctrl Pts',(1.43166138097717,1.14840609819434,12.2177742385241));
#278395=CARTESIAN_POINT('Ctrl Pts',(-0.188680446328495,1.8256205973106,
12.3289300242996));
#278396=CARTESIAN_POINT('Ctrl Pts',(-1.63626999315856,0.831331092670267,
12.4400858100752));
#278397=CARTESIAN_POINT('Ctrl Pts',(-1.58572140065101,-0.924109579903169,
12.5512415958507));
#278398=CARTESIAN_POINT('Ctrl Pts',(-0.0833160127418071,-1.83345284045492,
12.6623973816263));
#278399=CARTESIAN_POINT('Ctrl Pts',(1.4953719549543,-1.06412104221633,12.7735531674018));
#278400=CARTESIAN_POINT('Ctrl Pts',(1.70492538643103,0.679500038892133,
12.8847089531774));
#278401=CARTESIAN_POINT('Ctrl Pts',(0.353481087205217,1.8009836193424,12.9958647389529));
#278402=CARTESIAN_POINT('Ctrl Pts',(-1.32160387064712,1.27352035132619,
13.1070205247285));
#278403=CARTESIAN_POINT('Ctrl Pts',(-1.78665309357124,-0.419954282492473,
13.218176310504));
#278404=CARTESIAN_POINT('Ctrl Pts',(-0.615876228847231,-1.72892664589692,
13.3293320962796));
#278405=CARTESIAN_POINT('Ctrl Pts',(1.118785368473,-1.454926175255,13.4404878820551));
#278406=CARTESIAN_POINT('Ctrl Pts',(1.82910805030238,0.151177433734229,
13.5516436678307));
#278407=CARTESIAN_POINT('Ctrl Pts',(0.864733681776538,1.61886581771084,
13.6627994536062));
#278408=CARTESIAN_POINT('Ctrl Pts',(-0.891374639248479,1.60435099920687,
13.7739552393818));
#278409=CARTESIAN_POINT('Ctrl Pts',(-1.83135704640849,0.120922474012888,
13.8851110251573));
#278410=CARTESIAN_POINT('Ctrl Pts',(-1.09458326452843,-1.47322040210069,
13.9962668109329));
#278411=CARTESIAN_POINT('Ctrl Pts',(0.644370440058169,-1.71851028863102,
14.1074225967084));
#278412=CARTESIAN_POINT('Ctrl Pts',(1.79335064629233,-0.390364362607969,
14.218578382484));
#278413=CARTESIAN_POINT('Ctrl Pts',(1.30037261113015,1.29519185774694,14.3297341682595));
#278414=CARTESIAN_POINT('Ctrl Pts',(-0.383202215655351,1.79489468718037,
14.440889954035));
#278415=CARTESIAN_POINT('Ctrl Pts',(-1.71592427562836,0.651225580318193,
14.5520457398106));
#278416=CARTESIAN_POINT('Ctrl Pts',(-1.47757822808704,-1.08869346284187,
14.6632015255862));
#278417=CARTESIAN_POINT('Ctrl Pts',(0.113610752837791,-1.83182517533499,
14.7743573113617));
#278418=CARTESIAN_POINT('Ctrl Pts',(1.60077985771719,-0.897772088716452,
14.8855130971372));
#278419=CARTESIAN_POINT('Ctrl Pts',(1.62230492612552,0.858264296601231,
14.9966688829128));
#278420=CARTESIAN_POINT('Ctrl Pts',(0.158478008843229,1.82848997723926,
15.1078246686883));
#278421=CARTESIAN_POINT('Ctrl Pts',(-1.45044840319647,1.12458450363503,
15.2189804544639));
#278422=CARTESIAN_POINT('Ctrl Pts',(-1.73137144106518,-0.608969464929189,
15.3301362402394));
#278423=CARTESIAN_POINT('Ctrl Pts',(-0.427083236250261,-1.78496240449614,
15.441292026015));
#278424=CARTESIAN_POINT('Ctrl Pts',(1.26823437542981,-1.32667721964631,
15.5524478117905));
#278425=CARTESIAN_POINT('Ctrl Pts',(1.80238036177279,0.346288763393393,
15.6636035975661));
#278426=CARTESIAN_POINT('Ctrl Pts',(0.686300668452443,1.70219924469092,
15.7747593833416));
#278427=CARTESIAN_POINT('Ctrl Pts',(-1.05814305448729,1.49960799957408,
15.8859151691172));
#278428=CARTESIAN_POINT('Ctrl Pts',(-1.83377082810206,-0.0759962248318786,
15.9970709548927));
#278429=CARTESIAN_POINT('Ctrl Pts',(-0.930432399362984,-1.58201973006431,
16.1082267406683));
#278430=CARTESIAN_POINT('Ctrl Pts',(0.824792496331553,-1.6395756201318,
16.2193825264438));
#278431=CARTESIAN_POINT('Ctrl Pts',(1.82485284047757,-0.195966800714232,
16.3305383122194));
#278432=CARTESIAN_POINT('Ctrl Pts',(1.15411212440423,1.42706554861312,16.4416940979949));
#278433=CARTESIAN_POINT('Ctrl Pts',(-0.573312022371201,1.7435034273505,
16.5528498837705));
#278434=CARTESIAN_POINT('Ctrl Pts',(-1.77582242710928,0.463622243834642,
16.664005669546));
#278435=CARTESIAN_POINT('Ctrl Pts',(-1.35242309784257,-1.24074277651812,
16.7751614553216));
#278436=CARTESIAN_POINT('Ctrl Pts',(0.309229470154115,-1.80910696534636,
16.8863172410971));
#278437=CARTESIAN_POINT('Ctrl Pts',(1.68775733648514,-0.721086720278873,
16.9974730268726));
#278438=CARTESIAN_POINT('Ctrl Pts',(1.52100620597035,1.02714700757733,17.1086288126482));
#278439=CARTESIAN_POINT('Ctrl Pts',(-0.0383496797956876,1.83494419322939,
17.2197845984237));
#278440=CARTESIAN_POINT('Ctrl Pts',(-1.56259335699694,0.962700851162004,
17.3309403841993));
#278441=CARTESIAN_POINT('Ctrl Pts',(-1.65615576691353,-0.790973320458416,
17.4420961699749));
#278442=CARTESIAN_POINT('Ctrl Pts',(-0.233373138809018,-1.82044719570678,
17.5532519557504));
#278443=CARTESIAN_POINT('Ctrl Pts',(1.40308183362072,-1.18315363838809,
17.6644077415259));
#278444=CARTESIAN_POINT('Ctrl Pts',(1.75490085728126,0.537413028835761,
17.7755635273015));
#278445=CARTESIAN_POINT('Ctrl Pts',(0.499966531306351,1.76593475496119,
17.8867193130771));
#278446=CARTESIAN_POINT('Ctrl Pts',(-1.2127296557621,1.37759903842392,17.9978750988526));
#278447=CARTESIAN_POINT('Ctrl Pts',(-1.81506973055227,-0.272039250033519,
18.1090308846281));
#278448=CARTESIAN_POINT('Ctrl Pts',(-0.755572766356513,-1.67260595256776,
18.2201866704037));
#278449=CARTESIAN_POINT('Ctrl Pts',(0.995725379371007,-1.54176132508072,
18.3313424561792));
#278450=CARTESIAN_POINT('Ctrl Pts',(1.83533145130754,0.000682196077548512,
18.4424982419548));
#278451=CARTESIAN_POINT('Ctrl Pts',(0.994589208429304,1.54251800818852,
18.5536540277304));
#278452=CARTESIAN_POINT('Ctrl Pts',(-0.756869254017628,1.67202109132145,
18.6648098135059));
#278453=CARTESIAN_POINT('Ctrl Pts',(-1.81518310367551,0.27071417263847,
18.7759655992815));
#278454=CARTESIAN_POINT('Ctrl Pts',(-1.21187150681834,-1.37856996990797,
18.887121385057));
#278455=CARTESIAN_POINT('Ctrl Pts',(0.501620277758415,-1.76543975111565,
18.9982771708326));
#278456=CARTESIAN_POINT('Ctrl Pts',(1.75466810626107,-0.536327979791566,
19.1094329566081));
#278457=CARTESIAN_POINT('Ctrl Pts',(1.40342470040972,1.18464272774391,19.2205887423837));
#278458=CARTESIAN_POINT('Ctrl Pts',(-0.237431411965544,1.81947273062068,
19.3317564093966));
#278459=CARTESIAN_POINT('Ctrl Pts',(-1.17973169467503,1.13405785918806,
19.4058721478177));
#278460=CARTESIAN_POINT('Ctrl Pts',(-1.40184687339747,0.667677681709342,
19.4429359576469));
#278461=CARTESIAN_POINT('Ctrl Pts',(-0.74373075200652,1.51458090132225,
-0.153976802596129));
#278462=CARTESIAN_POINT('Ctrl Pts',(-1.24752359518877,1.26720196942433,
-0.116919470141557));
#278463=CARTESIAN_POINT('Ctrl Pts',(-1.98006238519882,0.234582603216642,
-0.0428102090951364));
#278464=CARTESIAN_POINT('Ctrl Pts',(-1.26926790758847,-1.54015585248706,
0.0683509805431339));
#278465=CARTESIAN_POINT('Ctrl Pts',(0.605260444971807,-1.89977336184568,
0.179506766318684));
#278466=CARTESIAN_POINT('Ctrl Pts',(1.92477550955777,-0.522449202466397,
0.290662552094231));
#278467=CARTESIAN_POINT('Ctrl Pts',(1.48244575045285,1.33449621452525,0.40181833786978));
#278468=CARTESIAN_POINT('Ctrl Pts',(-0.317416417613436,1.96893259775306,
0.51297412364533));
#278469=CARTESIAN_POINT('Ctrl Pts',(-1.82653570741519,0.801002775628761,
0.624129909420876));
#278470=CARTESIAN_POINT('Ctrl Pts',(-1.66337743803531,-1.1004949325196,
0.735285695196427));
#278471=CARTESIAN_POINT('Ctrl Pts',(0.0227718338178408,-1.99430300624619,
0.846441480971973));
#278472=CARTESIAN_POINT('Ctrl Pts',(1.68805388015145,-1.06221565574388,
0.957597266747523));
#278473=CARTESIAN_POINT('Ctrl Pts',(1.80779476543365,0.842443261991487,
1.06875305252307));
#278474=CARTESIAN_POINT('Ctrl Pts',(0.272347738542586,1.97576282189037,
1.17990883829862));
#278475=CARTESIAN_POINT('Ctrl Pts',(-1.51245319508847,1.30011837945816,
1.29106462407417));
#278476=CARTESIAN_POINT('Ctrl Pts',(-1.91248168429486,-0.565893978410986,
1.40222040984972));
#278477=CARTESIAN_POINT('Ctrl Pts',(-0.561477074211649,-1.91378236910807,
1.51337619562527));
#278478=CARTESIAN_POINT('Ctrl Pts',(1.30360504770008,-1.50944856556618,
1.62453198140082));
#278479=CARTESIAN_POINT('Ctrl Pts',(1.97513101637244,0.276908620286904,
1.73568776717636));
#278480=CARTESIAN_POINT('Ctrl Pts',(0.838263940274534,1.80973316606173,
1.84684355295191));
#278481=CARTESIAN_POINT('Ctrl Pts',(-1.06610183475038,1.68560009850343,
1.95799933872746));
#278482=CARTESIAN_POINT('Ctrl Pts',(-1.99436477894357,0.0181630896254633,
2.06915512450301));
#278483=CARTESIAN_POINT('Ctrl Pts',(-1.09662469421168,-1.66590366058159,
2.18031091027856));
#278484=CARTESIAN_POINT('Ctrl Pts',(0.805164400096429,-1.82470026360773,
2.2914666960541));
#278485=CARTESIAN_POINT('Ctrl Pts',(1.96976006393103,-0.312835491254928,
2.40262248182966));
#278486=CARTESIAN_POINT('Ctrl Pts',(1.33088032760376,1.48545558757719,2.5137782676052));
#278487=CARTESIAN_POINT('Ctrl Pts',(-0.526528492639934,1.92369137360171,
2.62493405338075));
#278488=CARTESIAN_POINT('Ctrl Pts',(-1.90185769363675,0.600631389376298,
2.7360898391563));
#278489=CARTESIAN_POINT('Ctrl Pts',(-1.53588163397336,-1.27235543723032,
2.84724562493185));
#278490=CARTESIAN_POINT('Ctrl Pts',(0.236318864634813,-1.98039747202593,
2.9584014107074));
#278491=CARTESIAN_POINT('Ctrl Pts',(1.79215023987601,-0.875224697098474,
3.06955719648295));
#278492=CARTESIAN_POINT('Ctrl Pts',(1.70712244329213,1.03128740720606,3.1807129822585));
#278493=CARTESIAN_POINT('Ctrl Pts',(0.0590853319442645,1.99357208956899,
3.29186876803404));
#278494=CARTESIAN_POINT('Ctrl Pts',(-1.64304920198787,1.13057952951509,
3.4030245538096));
#278495=CARTESIAN_POINT('Ctrl Pts',(-1.84083868002521,-0.767550458818608,
3.51418033958514));
#278496=CARTESIAN_POINT('Ctrl Pts',(-0.353190762987942,-1.96292563222959,
3.6253361253607));
#278497=CARTESIAN_POINT('Ctrl Pts',(1.45783199726549,-1.3610828852297,3.73649191113624));
#278498=CARTESIAN_POINT('Ctrl Pts',(1.93409110299773,0.486941842545606,
3.84764769691179));
#278499=CARTESIAN_POINT('Ctrl Pts',(0.63953264288294,1.88913174538087,3.95880348268734));
#278500=CARTESIAN_POINT('Ctrl Pts',(-1.24056991915922,1.56166802758931,
4.06995926846289));
#278501=CARTESIAN_POINT('Ctrl Pts',(-1.98482991354544,-0.195629668028096,
4.18111505423843));
#278502=CARTESIAN_POINT('Ctrl Pts',(-0.911816838075705,-1.77381250602182,
4.29227084001398));
#278503=CARTESIAN_POINT('Ctrl Pts',(0.996038645384761,-1.72792585767379,
4.40342662578953));
#278504=CARTESIAN_POINT('Ctrl Pts',(1.99193981253791,-0.0999826782201581,
4.51458241156508));
#278505=CARTESIAN_POINT('Ctrl Pts',(1.16405821956878,1.61950276757159,4.62573819734063));
#278506=CARTESIAN_POINT('Ctrl Pts',(-0.729613262866601,1.85620183152771,
4.73689398311618));
#278507=CARTESIAN_POINT('Ctrl Pts',(-1.95526451597723,0.393397286820842,
4.84804976889172));
#278508=CARTESIAN_POINT('Ctrl Pts',(-1.39071222314098,-1.4295944407852,
4.95920555466728));
#278509=CARTESIAN_POINT('Ctrl Pts',(0.447150116962367,-1.94367629136597,
5.07036134044282));
#278510=CARTESIAN_POINT('Ctrl Pts',(1.87561019030566,-0.678164557271505,
5.18151712621837));
#278511=CARTESIAN_POINT('Ctrl Pts',(1.58679672543352,1.20826193553845,5.29267291199392));
#278512=CARTESIAN_POINT('Ctrl Pts',(-0.154858082057787,1.98842644499087,
5.40382869776946));
#278513=CARTESIAN_POINT('Ctrl Pts',(-1.75472773191285,0.948024967800771,
5.51498448354502));
#278514=CARTESIAN_POINT('Ctrl Pts',(-1.7480015569203,-0.960370402356234,
5.62614026932056));
#278515=CARTESIAN_POINT('Ctrl Pts',(-0.1408379168437,-1.98946863104116,
5.73729605509613));
#278516=CARTESIAN_POINT('Ctrl Pts',(1.59527428036014,-1.1970466670682,5.84845184087166));
#278517=CARTESIAN_POINT('Ctrl Pts',(1.87078324453736,0.691368790643559,
5.95960762664722));
#278518=CARTESIAN_POINT('Ctrl Pts',(0.433438131579671,1.94677994103349,
6.07076341242275));
#278519=CARTESIAN_POINT('Ctrl Pts',(-1.40075481130689,1.4197558632801,6.18191919819832));
#278520=CARTESIAN_POINT('Ctrl Pts',(-1.95244290141633,-0.40717007432604,
6.29307498397385));
#278521=CARTESIAN_POINT('Ctrl Pts',(-0.716510862989133,-1.86129872291801,
6.40423076974941));
#278522=CARTESIAN_POINT('Ctrl Pts',(1.17544509299558,-1.61125714461419,
6.51538655552495));
#278523=CARTESIAN_POINT('Ctrl Pts',(1.99118555161327,0.114021277682033,
6.62654234130051));
#278524=CARTESIAN_POINT('Ctrl Pts',(0.983833837275154,1.7349039550794,6.73769812707605));
#278525=CARTESIAN_POINT('Ctrl Pts',(-0.924297699803332,1.76734108616756,
6.8488539128516));
#278526=CARTESIAN_POINT('Ctrl Pts',(-1.98615958580523,0.181633841647562,
6.96000969862716));
#278527=CARTESIAN_POINT('Ctrl Pts',(-1.2295309789503,-1.57037394416718,
7.07116548440269));
#278528=CARTESIAN_POINT('Ctrl Pts',(0.652833148793089,-1.88457677810021,
7.18232127017825));
#278529=CARTESIAN_POINT('Ctrl Pts',(1.93747548067146,-0.473296434081779,
7.29347705595379));
#278530=CARTESIAN_POINT('Ctrl Pts',(1.44820157393307,1.37132525462613,7.40463284172934));
#278531=CARTESIAN_POINT('Ctrl Pts',(-0.367018552212401,1.96038724109538,
7.5157886275049));
#278532=CARTESIAN_POINT('Ctrl Pts',(-1.84620337048521,0.754555410507891,
7.62694441328044));
#278533=CARTESIAN_POINT('Ctrl Pts',(-1.63503898363787,-1.14213321232776,
7.738100199056));
#278534=CARTESIAN_POINT('Ctrl Pts',(0.0731364533010753,-1.99310607141621,
7.84925598483153));
#278535=CARTESIAN_POINT('Ctrl Pts',(1.71434952429531,-1.01922836561103,
7.96041177060709));
#278536=CARTESIAN_POINT('Ctrl Pts',(1.78593630058235,0.887835729727017,
8.07156755638263));
#278537=CARTESIAN_POINT('Ctrl Pts',(0.222353271448042,1.98201407043291,
8.18272334215819));
#278538=CARTESIAN_POINT('Ctrl Pts',(-1.54481224575705,1.26149747446308,
8.29387912793374));
#278539=CARTESIAN_POINT('Ctrl Pts',(-1.89757662307636,-0.614022566581862,
8.40503491370928));
#278540=CARTESIAN_POINT('Ctrl Pts',(-0.512955408022568,-1.92735505346007,
8.51619069948484));
#278541=CARTESIAN_POINT('Ctrl Pts',(1.34131816498633,-1.47603737520274,
8.62734648526037));
#278542=CARTESIAN_POINT('Ctrl Pts',(1.96750596464839,0.326712460415384,
8.73850227103594));
#278543=CARTESIAN_POINT('Ctrl Pts',(0.792282177385192,1.83033049040752,
8.84965805681147));
#278544=CARTESIAN_POINT('Ctrl Pts',(-1.10834032281716,1.65813222679472,
8.96081384258703));
#278545=CARTESIAN_POINT('Ctrl Pts',(-1.99418719557377,-0.0322208275386075,
9.07196962836257));
#278546=CARTESIAN_POINT('Ctrl Pts',(-1.05419364642014,-1.69307309604904,
9.18312541413812));
#278547=CARTESIAN_POINT('Ctrl Pts',(0.85099984806814,-1.80377936879921,
9.29428119991367));
#278548=CARTESIAN_POINT('Ctrl Pts',(1.97703383080595,-0.262979057277202,
9.40543698568922));
#278549=CARTESIAN_POINT('Ctrl Pts',(1.29293269093258,1.51859995042656,9.51659277146476));
#278550=CARTESIAN_POINT('Ctrl Pts',(-0.574953389067615,1.90977730458746,
9.62774855724032));
#278551=CARTESIAN_POINT('Ctrl Pts',(-1.91642292161226,0.552398351044574,
9.73890434301587));
#278552=CARTESIAN_POINT('Ctrl Pts',(-1.50325154405505,-1.31074617985853,
9.85006012879141));
#278553=CARTESIAN_POINT('Ctrl Pts',(0.286268773825686,-1.97379607402841,
9.96121591456697));
#278554=CARTESIAN_POINT('Ctrl Pts',(1.81368676754059,-0.829675275011727,
10.0723717003426));
#278555=CARTESIAN_POINT('Ctrl Pts',(1.68052714837671,1.07408065632265,10.183527486118));
#278556=CARTESIAN_POINT('Ctrl Pts',(0.00870836800959076,1.99442846877101,
10.2946832718936));
#278557=CARTESIAN_POINT('Ctrl Pts',(-1.67108363089793,1.08871495409159,
10.4058390576691));
#278558=CARTESIAN_POINT('Ctrl Pts',(-1.8208627762187,-0.813805568240236,
10.5169948434447));
#278559=CARTESIAN_POINT('Ctrl Pts',(-0.303494089605198,-1.97122096434986,
10.6281506292202));
#278560=CARTESIAN_POINT('Ctrl Pts',(1.49174809747102,-1.32382338943276,
10.7393064149959));
#278561=CARTESIAN_POINT('Ctrl Pts',(1.92117368432247,0.535642070215246,
10.8504622007714));
#278562=CARTESIAN_POINT('Ctrl Pts',(0.591608651771739,1.90468368919001,
10.9616179865469));
#278563=CARTESIAN_POINT('Ctrl Pts',(-1.27962217461932,1.52983261925617,
11.0727737723225));
#278564=CARTESIAN_POINT('Ctrl Pts',(-1.97925492015898,-0.245704525282156,
11.183929558098));
#278565=CARTESIAN_POINT('Ctrl Pts',(-0.866718955302711,-1.79627921138019,
11.2950853438736));
#278566=CARTESIAN_POINT('Ctrl Pts',(1.03936864128602,-1.70221431677358,
11.4062411296491));
#278567=CARTESIAN_POINT('Ctrl Pts',(1.99382978939585,-0.0496338960328293,
11.5173969154247));
#278568=CARTESIAN_POINT('Ctrl Pts',(1.12277774999351,1.64839038969449,11.6285527012001));
#278569=CARTESIAN_POINT('Ctrl Pts',(-0.776268554596024,1.83717932817215,
11.7397084869758));
#278570=CARTESIAN_POINT('Ctrl Pts',(-1.96457791915047,0.343881305546085,
11.8508642727512));
#278571=CARTESIAN_POINT('Ctrl Pts',(-1.35415656036116,-1.46426799553513,
11.9620200585268));
#278572=CARTESIAN_POINT('Ctrl Pts',(0.496105165967445,-1.93176096270167,
12.0731758443023));
#278573=CARTESIAN_POINT('Ctrl Pts',(1.8921423001653,-0.630569796805081,
12.184331630078));
#278574=CARTESIAN_POINT('Ctrl Pts',(1.55576940619927,1.24795925712822,12.2954874158536));
#278575=CARTESIAN_POINT('Ctrl Pts',(-0.205036798398212,1.98388020404971,
12.406643201629));
#278576=CARTESIAN_POINT('Ctrl Pts',(-1.77811515311006,0.903397617330303,
12.5177989874045));
#278577=CARTESIAN_POINT('Ctrl Pts',(-1.72318459844495,-1.00421889665539,
12.6289547731801));
#278578=CARTESIAN_POINT('Ctrl Pts',(-0.0905385207650955,-1.99239140958179,
12.7401105589556));
#278579=CARTESIAN_POINT('Ctrl Pts',(1.62500292968607,-1.1563676885962,12.8512663447312));
#278580=CARTESIAN_POINT('Ctrl Pts',(1.85272215295172,0.738404615830361,
12.9624221305067));
#278581=CARTESIAN_POINT('Ctrl Pts',(0.384123696043651,1.95710749292302,
13.0735779162823));
#278582=CARTESIAN_POINT('Ctrl Pts',(-1.43617121785037,1.38391942891767,
13.1847337020578));
#278583=CARTESIAN_POINT('Ctrl Pts',(-1.94153468089794,-0.456359327272094,
13.2958894878334));
#278584=CARTESIAN_POINT('Ctrl Pts',(-0.66926537767743,-1.87880403633801,
13.4070452736089));
#278585=CARTESIAN_POINT('Ctrl Pts',(1.21577076220752,-1.58105098161919,
13.5182010593846));
#278586=CARTESIAN_POINT('Ctrl Pts',(1.98766997776453,0.164282720367103,
13.62935684516));
#278587=CARTESIAN_POINT('Ctrl Pts',(0.939695813894015,1.7592022425144,13.7405126309357));
#278588=CARTESIAN_POINT('Ctrl Pts',(-0.968646225728449,1.74342916176703,
13.8516684167111));
#278589=CARTESIAN_POINT('Ctrl Pts',(-1.99011393510182,0.131405015243721,
13.9628242024868));
#278590=CARTESIAN_POINT('Ctrl Pts',(-1.18947062351344,-1.60093110049002,
14.0739799882622));
#278591=CARTESIAN_POINT('Ctrl Pts',(0.700229698322543,-1.86748470470437,
14.1851357740379));
#278592=CARTESIAN_POINT('Ctrl Pts',(1.94881283183385,-0.424204313034841,
14.2962915598133));
#278593=CARTESIAN_POINT('Ctrl Pts',(1.41309946048478,1.40746959736092,14.407447345589));
#278594=CARTESIAN_POINT('Ctrl Pts',(-0.416421293069648,1.95049072271464,
14.5186031313644));
#278595=CARTESIAN_POINT('Ctrl Pts',(-1.86467451511134,0.707679097763931,
14.6297589171399));
#278596=CARTESIAN_POINT('Ctrl Pts',(-1.60566669819292,-1.18307024602596,
14.7409147029155));
#278597=CARTESIAN_POINT('Ctrl Pts',(0.123459454748778,-1.99062264524212,
14.852070488691));
#278598=CARTESIAN_POINT('Ctrl Pts',(1.73954844475626,-0.975598258026157,
14.9632262744666));
#278599=CARTESIAN_POINT('Ctrl Pts',(1.7629394807519,0.93266560991816,15.0743820602423));
#278600=CARTESIAN_POINT('Ctrl Pts',(0.172216168564502,1.98699832511316,
15.1855378460178));
#278601=CARTESIAN_POINT('Ctrl Pts',(-1.5761850399453,1.22207261346044,15.2966936317933));
#278602=CARTESIAN_POINT('Ctrl Pts',(-1.88146076618887,-0.661759879420467,
15.4078494175689));
#278603=CARTESIAN_POINT('Ctrl Pts',(-0.464106276586993,-1.9396974291753,
15.5190052033444));
#278604=CARTESIAN_POINT('Ctrl Pts',(1.37817522173939,-1.44168436590672,
15.63016098912));
#278605=CARTESIAN_POINT('Ctrl Pts',(1.95862531632066,0.376307883244237,
15.7413167748956));
#278606=CARTESIAN_POINT('Ctrl Pts',(0.745794779142275,1.84975968712525,
15.852472560671));
#278607=CARTESIAN_POINT('Ctrl Pts',(-1.14987148038453,1.62960618902539,
15.9636283464467));
#278608=CARTESIAN_POINT('Ctrl Pts',(-1.99273696297838,-0.0825841942452913,
16.0747841322222));
#278609=CARTESIAN_POINT('Ctrl Pts',(-1.01108982941028,-1.71916203701588,
16.1859399179978));
#278610=CARTESIAN_POINT('Ctrl Pts',(0.896292202405808,-1.7817073386517,
16.2970957037733));
#278611=CARTESIAN_POINT('Ctrl Pts',(1.98304589182469,-0.212954793104663,
16.4082514895487));
#278612=CARTESIAN_POINT('Ctrl Pts',(1.25415992798953,1.55077516979464,16.5194072753243));
#278613=CARTESIAN_POINT('Ctrl Pts',(-0.623011360411622,1.8946444514862,
16.6305630610998));
#278614=CARTESIAN_POINT('Ctrl Pts',(-1.92976512438537,0.503812781831874,
16.7417188468755));
#278615=CARTESIAN_POINT('Ctrl Pts',(-1.46966210573103,-1.34830042796301,
16.8528746326509));
#278616=CARTESIAN_POINT('Ctrl Pts',(0.336035989762217,-1.96593503647267,
16.9640304184265));
#278617=CARTESIAN_POINT('Ctrl Pts',(1.83406583713234,-0.783596368200354,
17.075186204202));
#278618=CARTESIAN_POINT('Ctrl Pts',(1.6528593655804,1.11618844462176,17.1863419899777));
#278619=CARTESIAN_POINT('Ctrl Pts',(-0.0416741412155506,1.99401204491582,
17.2974977757531));
#278620=CARTESIAN_POINT('Ctrl Pts',(-1.69805162830248,1.04615557244237,
17.4086535615287));
#278621=CARTESIAN_POINT('Ctrl Pts',(-1.7997247870903,-0.859541305954033,
17.5198093473042));
#278622=CARTESIAN_POINT('Ctrl Pts',(-0.253603816106239,-1.97825833001708,
17.6309651330799));
#278623=CARTESIAN_POINT('Ctrl Pts',(1.52471235177915,-1.28571899605279,
17.7421209188553));
#278624=CARTESIAN_POINT('Ctrl Pts',(1.90702990312385,0.584000350826615,
17.853276704631));
#278625=CARTESIAN_POINT('Ctrl Pts',(0.543307687044726,1.91902030858541,
17.9644324904065));
#278626=CARTESIAN_POINT('Ctrl Pts',(-1.31785890259713,1.49702050112338,
18.075588276182));
#278627=CARTESIAN_POINT('Ctrl Pts',(-1.97241470254942,-0.295621819594443,
18.1867440619575));
#278628=CARTESIAN_POINT('Ctrl Pts',(-0.821071944577047,-1.81760100831636,
18.2978998477332));
#278629=CARTESIAN_POINT('Ctrl Pts',(1.08204293472263,-1.67541370682546,
18.4090556335087));
#278630=CARTESIAN_POINT('Ctrl Pts',(1.99443287366644,0.000741334369009545,
18.5202114192842));
#278631=CARTESIAN_POINT('Ctrl Pts',(1.08080827126461,1.67623598536489,18.6313672050597));
#278632=CARTESIAN_POINT('Ctrl Pts',(-0.822480822308558,1.81696544655156,
18.7425229908353));
#278633=CARTESIAN_POINT('Ctrl Pts',(-1.97253790377489,0.294181873738879,
18.8536787766108));
#278634=CARTESIAN_POINT('Ctrl Pts',(-1.31692636233974,-1.49807560082679,
18.9648345623864));
#278635=CARTESIAN_POINT('Ctrl Pts',(0.545104793658038,-1.91848239378999,
19.0759903481619));
#278636=CARTESIAN_POINT('Ctrl Pts',(1.90677697535665,-0.582821240926985,
19.1871461339374));
#278637=CARTESIAN_POINT('Ctrl Pts',(1.52508494104348,1.2873371717567,19.298301919713));
#278638=CARTESIAN_POINT('Ctrl Pts',(-0.258013893309452,1.97719939039036,
19.409469586726));
#278639=CARTESIAN_POINT('Ctrl Pts',(-1.28200041049253,1.23236719634106,
19.4835853251471));
#278640=CARTESIAN_POINT('Ctrl Pts',(-1.5233703351831,0.725557400798528,
19.5206491349764));
#278641=CARTESIAN_POINT('Ctrl Pts',(-0.803060209547395,1.63540320567737,
-0.0762636252666968));
#278642=CARTESIAN_POINT('Ctrl Pts',(-1.3470420001657,1.36829017269927,-0.0392062928121253));
#278643=CARTESIAN_POINT('Ctrl Pts',(-2.13801743397685,0.253295905792618,
0.0349029682342957));
#278644=CARTESIAN_POINT('Ctrl Pts',(-1.3705209164604,-1.66301834137826,
0.146064157872566));
#278645=CARTESIAN_POINT('Ctrl Pts',(0.653543743429279,-2.05132353333556,
0.257219943648115));
#278646=CARTESIAN_POINT('Ctrl Pts',(2.07832017146924,-0.564126419243238,
0.368375729423662));
#278647=CARTESIAN_POINT('Ctrl Pts',(1.60070454501101,1.44095266571342,0.479531515199212));
#278648=CARTESIAN_POINT('Ctrl Pts',(-0.342737602492205,2.12599979262709,
0.59068730097476));
#278649=CARTESIAN_POINT('Ctrl Pts',(-1.9722435088038,0.864900980777003,
0.70184308675031));
#278650=CARTESIAN_POINT('Ctrl Pts',(-1.79606965335395,-1.18828445473139,
0.812998872525858));
#278651=CARTESIAN_POINT('Ctrl Pts',(0.0245884059361645,-2.15339406872207,
0.924154658301406));
#278652=CARTESIAN_POINT('Ctrl Pts',(1.82271460345614,-1.14695153425457,
1.03531044407696));
#278653=CARTESIAN_POINT('Ctrl Pts',(1.95200755008591,0.90964728926624,1.14646622985251));
#278654=CARTESIAN_POINT('Ctrl Pts',(0.294073670335253,2.13337488262056,
1.25762201562806));
#278655=CARTESIAN_POINT('Ctrl Pts',(-1.63310576643698,1.40383241573278,
1.3687778014036));
#278656=CARTESIAN_POINT('Ctrl Pts',(-2.06504563378859,-0.61103690503355,
1.47993358717915));
#278657=CARTESIAN_POINT('Ctrl Pts',(-0.606267652179178,-2.06645007782405,
1.5910893729547));
#278658=CARTESIAN_POINT('Ctrl Pts',(1.4075972251365,-1.62986144931378,1.70224515873025));
#278659=CARTESIAN_POINT('Ctrl Pts',(2.13269267623034,0.29899838622128,1.8134009445058));
#278660=CARTESIAN_POINT('Ctrl Pts',(0.905134571505482,1.95410058228929,
1.92455673028135));
#278661=CARTESIAN_POINT('Ctrl Pts',(-1.1511477245007,1.82006507686451,2.0357125160569));
#278662=CARTESIAN_POINT('Ctrl Pts',(-2.15346076919824,0.0196120094823153,
2.14686830183245));
#278663=CARTESIAN_POINT('Ctrl Pts',(-1.18410547681742,-1.79879739965449,
2.25802408760799));
#278664=CARTESIAN_POINT('Ctrl Pts',(0.869394589529993,-1.97026164657118,
2.36917987338354));
#278665=CARTESIAN_POINT('Ctrl Pts',(2.12689326806894,-0.33779124297771,
2.48033565915909));
#278666=CARTESIAN_POINT('Ctrl Pts',(1.43704832949894,1.60395448516108,2.59149144493464));
#278667=CARTESIAN_POINT('Ctrl Pts',(-0.568531125667906,2.07714955099172,
2.70264723071019));
#278668=CARTESIAN_POINT('Ctrl Pts',(-2.05357413803409,0.648545415275535,
2.81380301648574));
#278669=CARTESIAN_POINT('Ctrl Pts',(-1.65840315664103,-1.37385474687483,
2.92495880226128));
#278670=CARTESIAN_POINT('Ctrl Pts',(0.255170673582664,-2.13837925160624,
3.03611458803684));
#278671=CARTESIAN_POINT('Ctrl Pts',(1.93511501748769,-0.945043790049941,
3.14727037381238));
#278672=CARTESIAN_POINT('Ctrl Pts',(1.84330431857845,1.11355605385433,3.25842615958794));
#278673=CARTESIAN_POINT('Ctrl Pts',(0.0637987321679423,2.15260484480149,
3.36958194536347));
#278674=CARTESIAN_POINT('Ctrl Pts',(-1.77411977773575,1.22076898317417,
3.48073773113904));
#278675=CARTESIAN_POINT('Ctrl Pts',(-1.98768746906812,-0.828780080202557,
3.59189351691457));
#278676=CARTESIAN_POINT('Ctrl Pts',(-0.381365766266981,-2.11951363486232,
3.70304930269013));
#278677=CARTESIAN_POINT('Ctrl Pts',(1.57412728470673,-1.46966022861769,
3.81420508846568));
#278678=CARTESIAN_POINT('Ctrl Pts',(2.08837889554347,0.525786539089682,
3.92536087424122));
#278679=CARTESIAN_POINT('Ctrl Pts',(0.690549929286038,2.03983300571505,
4.03651666001678));
#278680=CARTESIAN_POINT('Ctrl Pts',(-1.33953361018136,1.68624660214174,
4.14767244579232));
#278681=CARTESIAN_POINT('Ctrl Pts',(-2.14316528123572,-0.211235587309644,
4.25882823156787));
#278682=CARTESIAN_POINT('Ctrl Pts',(-0.984554987242856,-1.91531443192384,
4.36998401734341));
#278683=CARTESIAN_POINT('Ctrl Pts',(1.07549540088531,-1.86576727881985,
4.48113980311897));
#278684=CARTESIAN_POINT('Ctrl Pts',(2.15084235652051,-0.107958572784515,
4.59229558889452));
#278685=CARTESIAN_POINT('Ctrl Pts',(1.25691836085871,1.74869497917066,4.70345137467006));
#278686=CARTESIAN_POINT('Ctrl Pts',(-0.787816529282194,2.0042761816252,
4.81460716044562));
#278687=CARTESIAN_POINT('Ctrl Pts',(-2.11124137019343,0.424779675625053,
4.92576294622115));
#278688=CARTESIAN_POINT('Ctrl Pts',(-1.50165318070095,-1.54363714030569,
5.03691873199672));
#278689=CARTESIAN_POINT('Ctrl Pts',(0.482820517584028,-2.09872872087849,
5.14807451777225));
#278690=CARTESIAN_POINT('Ctrl Pts',(2.02523279882188,-0.73226361825264,
5.25923030354781));
#278691=CARTESIAN_POINT('Ctrl Pts',(1.71337988566132,1.30464832941739,5.37038608932336));
#278692=CARTESIAN_POINT('Ctrl Pts',(-0.167211539245795,2.14704871793432,
5.48154187509889));
#278693=CARTESIAN_POINT('Ctrl Pts',(-1.89470721263948,1.02365153954472,
5.59269766087446));
#278694=CARTESIAN_POINT('Ctrl Pts',(-1.8874444720786,-1.03698180353386,
5.70385344665));
#278695=CARTESIAN_POINT('Ctrl Pts',(-0.152072946704935,-2.14817404204614,
5.81500923242555));
#278696=CARTESIAN_POINT('Ctrl Pts',(1.72253371857393,-1.29253838798554,
5.9261650182011));
#278697=CARTESIAN_POINT('Ctrl Pts',(2.02002079424938,0.746521189813437,
6.03732080397665));
#278698=CARTESIAN_POINT('Ctrl Pts',(0.468014689231428,2.10207995725757,
6.1484765897522));
#278699=CARTESIAN_POINT('Ctrl Pts',(-1.51249689387964,1.53301371228206,
6.25963237552774));
#278700=CARTESIAN_POINT('Ctrl Pts',(-2.10819466764088,-0.439651156453509,
6.37078816130329));
#278701=CARTESIAN_POINT('Ctrl Pts',(-0.773668914755293,-2.00977966612803,
6.48194394707884));
#278702=CARTESIAN_POINT('Ctrl Pts',(1.26921359664876,-1.73979158008144,
6.59309973285439));
#278703=CARTESIAN_POINT('Ctrl Pts',(2.15002792611735,0.12311707012406,6.70425551862994));
#278704=CARTESIAN_POINT('Ctrl Pts',(1.06231698150227,1.87330203834093,6.81541130440548));
#278705=CARTESIAN_POINT('Ctrl Pts',(-0.998031481803957,1.90832676902269,
6.92656709018103));
#278706=CARTESIAN_POINT('Ctrl Pts',(-2.14460102512651,0.19612327517835,
7.03772287595658));
#278707=CARTESIAN_POINT('Ctrl Pts',(-1.32761406320357,-1.69564701374563,
7.14887866173214));
#278708=CARTESIAN_POINT('Ctrl Pts',(0.704911453311359,-2.03491467610582,
7.26003444750767));
#278709=CARTESIAN_POINT('Ctrl Pts',(2.09203325437767,-0.511052598680766,
7.37119023328324));
#278710=CARTESIAN_POINT('Ctrl Pts',(1.56372861588939,1.4807196601278,7.48234601905876));
#278711=CARTESIAN_POINT('Ctrl Pts',(-0.396296636453853,2.11677274925197,
7.59350180483433));
#278712=CARTESIAN_POINT('Ctrl Pts',(-1.99348011571256,0.814748380973568,
7.70465759060988));
#278713=CARTESIAN_POINT('Ctrl Pts',(-1.76547056213006,-1.23324433519582,
7.81581337638541));
#278714=CARTESIAN_POINT('Ctrl Pts',(0.0789707503085854,-2.15210165109273,
7.92696916216099));
#278715=CARTESIAN_POINT('Ctrl Pts',(1.85110792380678,-1.10053502918357,
8.0381249479365));
#278716=CARTESIAN_POINT('Ctrl Pts',(1.92840537508305,0.95866083960448,8.14928073371208));
#278717=CARTESIAN_POINT('Ctrl Pts',(0.240091006430557,2.14012481053595,
8.26043651948761));
#278718=CARTESIAN_POINT('Ctrl Pts',(-1.6680461880083,1.3621306144094,8.37159230526317));
#278719=CARTESIAN_POINT('Ctrl Pts',(-2.04895155464346,-0.663004843696095,
8.48274809103872));
#278720=CARTESIAN_POINT('Ctrl Pts',(-0.553875278578563,-2.08110549271774,
8.59390387681425));
#278721=CARTESIAN_POINT('Ctrl Pts',(1.44831882201665,-1.59378495595632,
8.70505966258983));
#278722=CARTESIAN_POINT('Ctrl Pts',(2.12445935305686,0.352775216319991,
8.81621544836534));
#278723=CARTESIAN_POINT('Ctrl Pts',(0.855484716310372,1.97634101212309,
8.92737123414092));
#278724=CARTESIAN_POINT('Ctrl Pts',(-1.19675569349533,1.79040601711647,
9.03852701991645));
#278725=CARTESIAN_POINT('Ctrl Pts',(-2.15326901951224,-0.0347911720002775,
9.149682805692));
#278726=CARTESIAN_POINT('Ctrl Pts',(-1.13828958707659,-1.82813421607752,
9.26083859146756));
#278727=CARTESIAN_POINT('Ctrl Pts',(0.918886457862119,-1.94767183416457,
9.37199437724309));
#278728=CARTESIAN_POINT('Ctrl Pts',(2.13474728343003,-0.283957623473044,
9.48315016301865));
#278729=CARTESIAN_POINT('Ctrl Pts',(1.39607350497437,1.63974286543622,9.5943059487942));
#278730=CARTESIAN_POINT('Ctrl Pts',(-0.620819009915808,2.0621255182378,
9.70546173456975));
#278731=CARTESIAN_POINT('Ctrl Pts',(-2.06930127449923,0.596464694174142,
9.81661752034531));
#278732=CARTESIAN_POINT('Ctrl Pts',(-1.62317007426996,-1.41530802514323,
9.92777330612084));
#278733=CARTESIAN_POINT('Ctrl Pts',(0.309105225076564,-2.13125124184614,
10.0389290918964));
#278734=CARTESIAN_POINT('Ctrl Pts',(1.95836957348472,-0.895860764678115,
10.1500848776719));
#278735=CARTESIAN_POINT('Ctrl Pts',(1.81458744348604,1.15976303872091,10.2612406634475));
#278736=CARTESIAN_POINT('Ctrl Pts',(0.00940305859307401,2.15352953973923,
10.372396449223));
#278737=CARTESIAN_POINT('Ctrl Pts',(-1.80439059051889,1.17556475486775,
10.4835522349986));
#278738=CARTESIAN_POINT('Ctrl Pts',(-1.96611803220744,-0.87872508753828,
10.5947080207741));
#278739=CARTESIAN_POINT('Ctrl Pts',(-0.327704651901493,-2.12847070855169,
10.7058638065496));
#278740=CARTESIAN_POINT('Ctrl Pts',(1.61074896595979,-1.42942843986673,
10.8170195923252));
#278741=CARTESIAN_POINT('Ctrl Pts',(2.07443101868052,0.578371718513652,
10.9281753781008));
#278742=CARTESIAN_POINT('Ctrl Pts',(0.638802908956066,2.05662557106286,
11.0393311638763));
#278743=CARTESIAN_POINT('Ctrl Pts',(-1.38170117198847,1.65187159530215,
11.1504869496518));
#278744=CARTESIAN_POINT('Ctrl Pts',(-2.13714555521918,-0.265305054319054,
11.2616427354274));
#278745=CARTESIAN_POINT('Ctrl Pts',(-0.93585952172376,-1.93957336846002,
11.3727985212029));
#278746=CARTESIAN_POINT('Ctrl Pts',(1.122281950311,-1.83800465724289,11.4839543069785));
#278747=CARTESIAN_POINT('Ctrl Pts',(2.15288310205574,-0.0535933290928604,
11.595110092754));
#278748=CARTESIAN_POINT('Ctrl Pts',(1.21234483413833,1.7798870467472,11.7062658785296));
#278749=CARTESIAN_POINT('Ctrl Pts',(-0.838193642574392,1.98373620060436,
11.8174216643051));
#278750=CARTESIAN_POINT('Ctrl Pts',(-2.12129772927731,0.371313667676383,
11.9285774500807));
#278751=CARTESIAN_POINT('Ctrl Pts',(-1.46218137167207,-1.58107670034554,
12.0397332358562));
#278752=CARTESIAN_POINT('Ctrl Pts',(0.535680846145613,-2.08586287351616,
12.1508890216318));
#278753=CARTESIAN_POINT('Ctrl Pts',(2.04308372077493,-0.680872092205875,
12.2620448074073));
#278754=CARTESIAN_POINT('Ctrl Pts',(1.67987743142135,1.34751241606212,12.3732005931829));
#278755=CARTESIAN_POINT('Ctrl Pts',(-0.221393150467926,2.14213981078881,
12.4843563789585));
#278756=CARTESIAN_POINT('Ctrl Pts',(-1.91996031306156,0.975464141990338,
12.595512164734));
#278757=CARTESIAN_POINT('Ctrl Pts',(-1.86064779623888,-1.08432821340761,
12.7066679505095));
#278758=CARTESIAN_POINT('Ctrl Pts',(-0.0977610287883846,-2.15132997870865,
12.8178237362851));
#278759=CARTESIAN_POINT('Ctrl Pts',(1.75463390441784,-1.24861433497609,
12.9289795220606));
#278760=CARTESIAN_POINT('Ctrl Pts',(2.00051891947241,0.797309192768591,
13.0401353078362));
#278761=CARTESIAN_POINT('Ctrl Pts',(0.414766304882087,2.11323136650364,
13.1512910936117));
#278762=CARTESIAN_POINT('Ctrl Pts',(-1.55073856505364,1.49431850650915,
13.2624468793873));
#278763=CARTESIAN_POINT('Ctrl Pts',(-2.09641626822463,-0.492764372051713,
13.3736026651628));
#278764=CARTESIAN_POINT('Ctrl Pts',(-0.72265452650763,-2.02868142677909,
13.4847584509384));
#278765=CARTESIAN_POINT('Ctrl Pts',(1.31275615594204,-1.70717578798336,
13.5959142367139));
#278766=CARTESIAN_POINT('Ctrl Pts',(2.14623190522668,0.177388006999977,
13.7070700224895));
#278767=CARTESIAN_POINT('Ctrl Pts',(1.01465794601149,1.89953866731797,13.818225808265));
#278768=CARTESIAN_POINT('Ctrl Pts',(-1.04591781220841,1.88250732432719,
13.9293815940406));
#278769=CARTESIAN_POINT('Ctrl Pts',(-2.14887082379515,0.141887556474556,
14.0405373798161));
#278770=CARTESIAN_POINT('Ctrl Pts',(-1.28435798249845,-1.72864179887936,
14.1516931655917));
#278771=CARTESIAN_POINT('Ctrl Pts',(0.756088956586916,-2.01645912077772,
14.2628489513672));
#278772=CARTESIAN_POINT('Ctrl Pts',(2.10427501737539,-0.458044263461713,
14.3740047371428));
#278773=CARTESIAN_POINT('Ctrl Pts',(1.52582630983939,1.51974733697488,14.4851605229183));
#278774=CARTESIAN_POINT('Ctrl Pts',(-0.449640370483944,2.10608675824893,
14.5963163086939));
#278775=CARTESIAN_POINT('Ctrl Pts',(-2.01342475459432,0.764132615209665,
14.7074720944694));
#278776=CARTESIAN_POINT('Ctrl Pts',(-1.73375516829879,-1.27744702921006,
14.818627880245));
#278777=CARTESIAN_POINT('Ctrl Pts',(0.133308156659764,-2.14942011514928,
14.9297836660205));
#278778=CARTESIAN_POINT('Ctrl Pts',(1.87831703179533,-1.05342442733586,
15.0409394517961));
#278779=CARTESIAN_POINT('Ctrl Pts',(1.90357403537827,1.00706692323509,15.1520952375716));
#278780=CARTESIAN_POINT('Ctrl Pts',(0.185954328285773,2.14550667298706,
15.2632510233471));
#278781=CARTESIAN_POINT('Ctrl Pts',(-1.70192167669414,1.31956072328585,
15.3744068091227));
#278782=CARTESIAN_POINT('Ctrl Pts',(-2.03155009131257,-0.714550293911744,
15.4855625948982));
#278783=CARTESIAN_POINT('Ctrl Pts',(-0.501129316923725,-2.09443245385447,
15.5967183806738));
#278784=CARTESIAN_POINT('Ctrl Pts',(1.48811606804899,-1.55669151216713,
15.7078741664493));
#278785=CARTESIAN_POINT('Ctrl Pts',(2.11487027086851,0.40632700309508,15.8190299522249));
#278786=CARTESIAN_POINT('Ctrl Pts',(0.805288889832107,1.99732012955959,
15.9301857380004));
#278787=CARTESIAN_POINT('Ctrl Pts',(-1.24159990628178,1.75960437847669,
16.041341523776));
#278788=CARTESIAN_POINT('Ctrl Pts',(-2.1517030978547,-0.0891721636587039,
16.1524973095515));
#278789=CARTESIAN_POINT('Ctrl Pts',(-1.09174725945757,-1.85630434396745,
16.2636530953271));
#278790=CARTESIAN_POINT('Ctrl Pts',(0.967791908480065,-1.92383905717159,
16.3748088811027));
#278791=CARTESIAN_POINT('Ctrl Pts',(2.1412389431718,-0.229942785495091,
16.4859646668782));
#278792=CARTESIAN_POINT('Ctrl Pts',(1.35420773157483,1.67448479097614,16.5971204526538));
#278793=CARTESIAN_POINT('Ctrl Pts',(-0.672710698452041,2.0457854756219,
16.7082762384293));
#278794=CARTESIAN_POINT('Ctrl Pts',(-2.08370782166148,0.544003319829105,
16.8194320242048));
#278795=CARTESIAN_POINT('Ctrl Pts',(-1.58690111361948,-1.45585807940792,
16.9305878099804));
#278796=CARTESIAN_POINT('Ctrl Pts',(0.362842509370316,-2.12276310759897,
17.0417435957559));
#278797=CARTESIAN_POINT('Ctrl Pts',(1.98037433777956,-0.846106016121839,
17.1528993815315));
#278798=CARTESIAN_POINT('Ctrl Pts',(1.78471252519044,1.2052298816662,17.264055167307));
#278799=CARTESIAN_POINT('Ctrl Pts',(-0.0449986026354138,2.15307989660224,
17.3752109530826));
#278800=CARTESIAN_POINT('Ctrl Pts',(-1.83350989960801,1.12961029372276,
17.4863667388581));
#278801=CARTESIAN_POINT('Ctrl Pts',(-1.94329380726708,-0.928109291449652,
17.5975225246337));
#278802=CARTESIAN_POINT('Ctrl Pts',(-0.273834493403462,-2.1360694643274,
17.7086783104092));
#278803=CARTESIAN_POINT('Ctrl Pts',(1.64634286993759,-1.3882843537175,17.8198340961848));
#278804=CARTESIAN_POINT('Ctrl Pts',(2.05915894896643,0.630587672817468,
17.9309898819603));
#278805=CARTESIAN_POINT('Ctrl Pts',(0.586648842783101,2.07210586220963,
18.0421456677359));
#278806=CARTESIAN_POINT('Ctrl Pts',(-1.42298814943216,1.61644196382285,
18.1533014535114));
#278807=CARTESIAN_POINT('Ctrl Pts',(-2.12975967454656,-0.31920438915537,
18.264457239287));
#278808=CARTESIAN_POINT('Ctrl Pts',(-0.886571122797581,-1.96259606406497,
18.3756130250625));
#278809=CARTESIAN_POINT('Ctrl Pts',(1.16836049007425,-1.8090660885702,18.4867688108381));
#278810=CARTESIAN_POINT('Ctrl Pts',(2.15353429602535,0.000800472660472174,
18.5979245966136));
#278811=CARTESIAN_POINT('Ctrl Pts',(1.16702733409992,1.80995396254128,18.7090803823892));
#278812=CARTESIAN_POINT('Ctrl Pts',(-0.888092390599487,1.96190980178168,
18.8202361681647));
#278813=CARTESIAN_POINT('Ctrl Pts',(-2.12989270387429,0.317649574839287,
18.9313919539403));
#278814=CARTESIAN_POINT('Ctrl Pts',(-1.42198121786115,-1.6175812317456,
19.0425477397158));
#278815=CARTESIAN_POINT('Ctrl Pts',(0.588589309557662,-2.07152503646434,
19.1537035254914));
#278816=CARTESIAN_POINT('Ctrl Pts',(2.05888584445224,-0.629314502062404,
19.2648593112669));
#278817=CARTESIAN_POINT('Ctrl Pts',(1.64674518167725,1.39003161576949,19.3760150970424));
#278818=CARTESIAN_POINT('Ctrl Pts',(-0.278596374653366,2.13492605016005,
19.4871827640554));
#278819=CARTESIAN_POINT('Ctrl Pts',(-1.38426912631003,1.33067653349406,
19.5612985024766));
#278820=CARTESIAN_POINT('Ctrl Pts',(-1.64489379696873,0.783437119887715,
19.5983623123059));
#278821=CARTESIAN_POINT('Ctrl Pts',(-0.86238966708827,1.75622551003249,
0.00144955206273537));
#278822=CARTESIAN_POINT('Ctrl Pts',(-1.44656040514264,1.46937837597419,
0.0385068845173068));
#278823=CARTESIAN_POINT('Ctrl Pts',(-2.2959724827549,0.272009208368595,
0.112616145563727));
#278824=CARTESIAN_POINT('Ctrl Pts',(-1.47177392533232,-1.78588083026947,
0.223777335201998));
#278825=CARTESIAN_POINT('Ctrl Pts',(0.701827041886748,-2.20287370482543,
0.334933120977547));
#278826=CARTESIAN_POINT('Ctrl Pts',(2.23186483338071,-0.605803636020076,
0.446088906753094));
#278827=CARTESIAN_POINT('Ctrl Pts',(1.71896333956916,1.5474091169016,0.557244692528645));
#278828=CARTESIAN_POINT('Ctrl Pts',(-0.36805878737097,2.2830669875011,0.668400478304191));
#278829=CARTESIAN_POINT('Ctrl Pts',(-2.1179513101924,0.928799185925246,
0.779556264079742));
#278830=CARTESIAN_POINT('Ctrl Pts',(-1.92876186867258,-1.27607397694317,
0.89071204985529));
#278831=CARTESIAN_POINT('Ctrl Pts',(0.0264049780544867,-2.31248513119795,
1.00186783563084));
#278832=CARTESIAN_POINT('Ctrl Pts',(1.95737532676084,-1.23168741276525,
1.11302362140639));
#278833=CARTESIAN_POINT('Ctrl Pts',(2.09622033473819,0.976851316540996,
1.22417940718193));
#278834=CARTESIAN_POINT('Ctrl Pts',(0.31579960212792,2.29098694335075,1.33533519295748));
#278835=CARTESIAN_POINT('Ctrl Pts',(-1.75375833778551,1.50754645200738,
1.44649097873303));
#278836=CARTESIAN_POINT('Ctrl Pts',(-2.2176095832823,-0.656179831656115,
1.55764676450858));
#278837=CARTESIAN_POINT('Ctrl Pts',(-0.65105823014671,-2.21911778654004,
1.66880255028413));
#278838=CARTESIAN_POINT('Ctrl Pts',(1.51158940257292,-1.75027433306136,
1.77995833605968));
#278839=CARTESIAN_POINT('Ctrl Pts',(2.29025433608824,0.321088152155656,
1.89111412183523));
#278840=CARTESIAN_POINT('Ctrl Pts',(0.972005202736432,2.09846799851684,
2.00226990761077));
#278841=CARTESIAN_POINT('Ctrl Pts',(-1.23619361425102,1.9545300552256,2.11342569338632));
#278842=CARTESIAN_POINT('Ctrl Pts',(-2.31255675945291,0.0210609293391671,
2.22458147916187));
#278843=CARTESIAN_POINT('Ctrl Pts',(-1.27158625942316,-1.9316911387274,
2.33573726493742));
#278844=CARTESIAN_POINT('Ctrl Pts',(0.933624778963557,-2.11582302953462,
2.44689305071297));
#278845=CARTESIAN_POINT('Ctrl Pts',(2.28402647220686,-0.362746994700493,
2.55804883648852));
#278846=CARTESIAN_POINT('Ctrl Pts',(1.54321633139411,1.72245338274497,2.66920462226407));
#278847=CARTESIAN_POINT('Ctrl Pts',(-0.610533758695877,2.23060772838173,
2.78036040803961));
#278848=CARTESIAN_POINT('Ctrl Pts',(-2.20529058243143,0.696459441174774,
2.89151619381516));
#278849=CARTESIAN_POINT('Ctrl Pts',(-1.78092467930869,-1.47535405651934,
3.00267197959071));
#278850=CARTESIAN_POINT('Ctrl Pts',(0.274022482530514,-2.29636103118655,
3.11382776536626));
#278851=CARTESIAN_POINT('Ctrl Pts',(2.07807979509936,-1.01486288300141,
3.22498355114181));
#278852=CARTESIAN_POINT('Ctrl Pts',(1.97948619386476,1.19582470050258,3.33613933691736));
#278853=CARTESIAN_POINT('Ctrl Pts',(0.0685121323916199,2.31163760003399,
3.44729512269291));
#278854=CARTESIAN_POINT('Ctrl Pts',(-1.90519035348363,1.31095843683326,
3.55845090846846));
#278855=CARTESIAN_POINT('Ctrl Pts',(-2.13453625811103,-0.890009701586508,
3.669606694244));
#278856=CARTESIAN_POINT('Ctrl Pts',(-0.409540769546024,-2.27610163749505,
3.78076248001955));
#278857=CARTESIAN_POINT('Ctrl Pts',(1.69042257214797,-1.57823757200569,
3.8919182657951));
#278858=CARTESIAN_POINT('Ctrl Pts',(2.24266668808919,0.564631235633758,
4.00307405157065));
#278859=CARTESIAN_POINT('Ctrl Pts',(0.74156721568914,2.19053426604923,4.1142298373462));
#278860=CARTESIAN_POINT('Ctrl Pts',(-1.43849730120351,1.81082517669416,
4.22538562312174));
#278861=CARTESIAN_POINT('Ctrl Pts',(-2.30150064892601,-0.226841506591189,
4.33654140889729));
#278862=CARTESIAN_POINT('Ctrl Pts',(-1.05729313641001,-2.05681635782586,
4.44769719467285));
#278863=CARTESIAN_POINT('Ctrl Pts',(1.15495215638586,-2.00360869996592,
4.55885298044839));
#278864=CARTESIAN_POINT('Ctrl Pts',(2.3097449005031,-0.115934467348872,
4.67000876622394));
#278865=CARTESIAN_POINT('Ctrl Pts',(1.34977850214863,1.87788719076972,4.78116455199949));
#278866=CARTESIAN_POINT('Ctrl Pts',(-0.846019795697788,2.15235053172271,
4.89232033777504));
#278867=CARTESIAN_POINT('Ctrl Pts',(-2.26721822440964,0.456162064429264,
5.00347612355059));
#278868=CARTESIAN_POINT('Ctrl Pts',(-1.6125941382609,-1.65767983982618,
5.11463190932614));
#278869=CARTESIAN_POINT('Ctrl Pts',(0.51849091820569,-2.253781150391,5.22578769510168));
#278870=CARTESIAN_POINT('Ctrl Pts',(2.17485540733811,-0.786362679233778,
5.33694348087723));
#278871=CARTESIAN_POINT('Ctrl Pts',(1.83996304588912,1.40103472329633,5.44809926665279));
#278872=CARTESIAN_POINT('Ctrl Pts',(-0.179564996433804,2.30567099087778,
5.55925505242832));
#278873=CARTESIAN_POINT('Ctrl Pts',(-2.03468669336613,1.09927811128868,
5.67041083820389));
#278874=CARTESIAN_POINT('Ctrl Pts',(-2.02688738723689,-1.11359320471147,
5.78156662397941));
#278875=CARTESIAN_POINT('Ctrl Pts',(-0.163307976566169,-2.30687945305112,
5.89272240975499));
#278876=CARTESIAN_POINT('Ctrl Pts',(1.84979315678771,-1.38803010890287,
6.00387819553052));
#278877=CARTESIAN_POINT('Ctrl Pts',(2.1692583439614,0.801673588983312,6.11503398130608));
#278878=CARTESIAN_POINT('Ctrl Pts',(0.502591246883182,2.25737997348164,
6.22618976708162));
#278879=CARTESIAN_POINT('Ctrl Pts',(-1.62423897645238,1.646271561284,6.33734555285718));
#278880=CARTESIAN_POINT('Ctrl Pts',(-2.26394643386545,-0.472132238580979,
6.44850133863271));
#278881=CARTESIAN_POINT('Ctrl Pts',(-0.830826966521448,-2.15826060933807,
6.55965712440827));
#278882=CARTESIAN_POINT('Ctrl Pts',(1.36298210030195,-1.8683260155487,6.67081291018381));
#278883=CARTESIAN_POINT('Ctrl Pts',(2.30887030062143,0.132212862566083,
6.78196869595937));
#278884=CARTESIAN_POINT('Ctrl Pts',(1.14080012572939,2.01170012160247,6.89312448173491));
#278885=CARTESIAN_POINT('Ctrl Pts',(-1.07176526380458,2.04931245187782,
7.00428026751046));
#278886=CARTESIAN_POINT('Ctrl Pts',(-2.30304246444779,0.210612708709141,
7.11543605328602));
#278887=CARTESIAN_POINT('Ctrl Pts',(-1.42569714745683,-1.82092008332409,
7.22659183906156));
#278888=CARTESIAN_POINT('Ctrl Pts',(0.756989757829629,-2.18525257411142,
7.33774762483711));
#278889=CARTESIAN_POINT('Ctrl Pts',(2.24659102808386,-0.548808763279752,
7.44890341061265));
#278890=CARTESIAN_POINT('Ctrl Pts',(1.67925565784572,1.59011406562948,7.5600591963882));
#278891=CARTESIAN_POINT('Ctrl Pts',(-0.425574720695307,2.27315825740855,
7.67121498216375));
#278892=CARTESIAN_POINT('Ctrl Pts',(-2.1407568609399,0.87494135143925,7.78237076793931));
#278893=CARTESIAN_POINT('Ctrl Pts',(-1.89590214062225,-1.32435545806388,
7.89352655371484));
#278894=CARTESIAN_POINT('Ctrl Pts',(0.0848050473160995,-2.31109723076924,
8.00468233949041));
#278895=CARTESIAN_POINT('Ctrl Pts',(1.98786632331827,-1.18184169275612,
8.11583812526594));
#278896=CARTESIAN_POINT('Ctrl Pts',(2.07087444958375,1.02948594948194,8.2269939110415));
#278897=CARTESIAN_POINT('Ctrl Pts',(0.25782874141307,2.29823555063899,8.33814969681704));
#278898=CARTESIAN_POINT('Ctrl Pts',(-1.79128013025956,1.46276375435572,
8.4493054825926));
#278899=CARTESIAN_POINT('Ctrl Pts',(-2.20032648621057,-0.711987120810329,
8.56046126836814));
#278900=CARTESIAN_POINT('Ctrl Pts',(-0.594795149134557,-2.23485593197539,
8.67161705414369));
#278901=CARTESIAN_POINT('Ctrl Pts',(1.55531947904698,-1.71153253670991,
8.78277283991924));
#278902=CARTESIAN_POINT('Ctrl Pts',(2.28141274146532,0.378837972224598,
8.89392862569479));
#278903=CARTESIAN_POINT('Ctrl Pts',(0.918687255235554,2.12235153383867,
9.00508441147033));
#278904=CARTESIAN_POINT('Ctrl Pts',(-1.28517106417351,1.92267980743821,
9.11624019724589));
#278905=CARTESIAN_POINT('Ctrl Pts',(-2.31235084345071,-0.0373615164619474,
9.22739598302143));
#278906=CARTESIAN_POINT('Ctrl Pts',(-1.22238552773304,-1.963195336106,9.33855176879698));
#278907=CARTESIAN_POINT('Ctrl Pts',(0.986773067656097,-2.09156429952993,
9.44970755457253));
#278908=CARTESIAN_POINT('Ctrl Pts',(2.29246073605411,-0.304936189668887,
9.56086334034808));
#278909=CARTESIAN_POINT('Ctrl Pts',(1.49921431901616,1.76088578044588,9.67201912612363));
#278910=CARTESIAN_POINT('Ctrl Pts',(-0.666684630764002,2.21447373188816,
9.78317491189918));
#278911=CARTESIAN_POINT('Ctrl Pts',(-2.22217962738618,0.640531037303711,
9.89433069767472));
#278912=CARTESIAN_POINT('Ctrl Pts',(-1.74308860448485,-1.51986987042792,
10.0054864834503));
#278913=CARTESIAN_POINT('Ctrl Pts',(0.331941676327445,-2.28870640966387,
10.1166422692258));
#278914=CARTESIAN_POINT('Ctrl Pts',(2.10305237942883,-0.962046254344501,
10.2277980550014));
#278915=CARTESIAN_POINT('Ctrl Pts',(1.94864773859537,1.24544542111916,10.3389538407769));
#278916=CARTESIAN_POINT('Ctrl Pts',(0.0100977491765532,2.31263061070744,
10.4501096265525));
#278917=CARTESIAN_POINT('Ctrl Pts',(-1.93769755013984,1.26241455564391,
10.561265412328));
#278918=CARTESIAN_POINT('Ctrl Pts',(-2.11137328819618,-0.943644606836327,
10.6724211981036));
#278919=CARTESIAN_POINT('Ctrl Pts',(-0.351915214197786,-2.28572045275351,
10.7835769838791));
#278920=CARTESIAN_POINT('Ctrl Pts',(1.72974983444855,-1.5350334903007,10.8947327696547));
#278921=CARTESIAN_POINT('Ctrl Pts',(2.22768835303858,0.621101366812054,
11.0058885554302));
#278922=CARTESIAN_POINT('Ctrl Pts',(0.685997166140391,2.2085674529357,11.1170443412058));
#278923=CARTESIAN_POINT('Ctrl Pts',(-1.48378016935762,1.77391057134812,
11.2282001269813));
#278924=CARTESIAN_POINT('Ctrl Pts',(-2.29503619027939,-0.284905583355947,
11.3393559127569));
#278925=CARTESIAN_POINT('Ctrl Pts',(-1.00500008814481,-2.08286752553985,
11.4505116985324));
#278926=CARTESIAN_POINT('Ctrl Pts',(1.20519525933597,-1.9737949977122,11.561667484308));
#278927=CARTESIAN_POINT('Ctrl Pts',(2.31193641471564,-0.057552762152893,
11.6728232700835));
#278928=CARTESIAN_POINT('Ctrl Pts',(1.30191191828315,1.9113837037999,11.783979055859));
#278929=CARTESIAN_POINT('Ctrl Pts',(-0.900118730552761,2.13029307303659,
11.8951348416346));
#278930=CARTESIAN_POINT('Ctrl Pts',(-2.27801753940416,0.398746029806683,
12.0062906274101));
#278931=CARTESIAN_POINT('Ctrl Pts',(-1.57020618298296,-1.69788540515596,
12.1174464131857));
#278932=CARTESIAN_POINT('Ctrl Pts',(0.575256526323781,-2.23996478433065,
12.2286021989612));
#278933=CARTESIAN_POINT('Ctrl Pts',(2.19402514138456,-0.731174387606673,
12.3397579847368));
#278934=CARTESIAN_POINT('Ctrl Pts',(1.80398545664344,1.44706557499601,12.4509137705123));
#278935=CARTESIAN_POINT('Ctrl Pts',(-0.237749502537639,2.30039941752791,
12.5620695562879));
#278936=CARTESIAN_POINT('Ctrl Pts',(-2.06180547301307,1.04753066665038,
12.6732253420634));
#278937=CARTESIAN_POINT('Ctrl Pts',(-1.99811099403281,-1.16443753015984,
12.784381127839));
#278938=CARTESIAN_POINT('Ctrl Pts',(-0.104983536811676,-2.31026854783552,
12.8955369136145));
#278939=CARTESIAN_POINT('Ctrl Pts',(1.88426487914961,-1.34086098135597,
13.0066926993901));
#278940=CARTESIAN_POINT('Ctrl Pts',(2.14831568599309,0.856213769706821,
13.1178484851656));
#278941=CARTESIAN_POINT('Ctrl Pts',(0.445408913720521,2.26935524008425,
13.2290042709412));
#278942=CARTESIAN_POINT('Ctrl Pts',(-1.6653059122569,1.60471758410063,13.3401600567167));
#278943=CARTESIAN_POINT('Ctrl Pts',(-2.25129785555133,-0.529169416831332,
13.4513158424923));
#278944=CARTESIAN_POINT('Ctrl Pts',(-0.77604367533783,-2.17855881722017,
13.5624716282678));
#278945=CARTESIAN_POINT('Ctrl Pts',(1.40974154967657,-1.83330059434755,
13.6736274140434));
#278946=CARTESIAN_POINT('Ctrl Pts',(2.30479383268882,0.190493293632852,
13.7847831998189));
#278947=CARTESIAN_POINT('Ctrl Pts',(1.08962007812897,2.03987509212151,13.8959389855945));
#278948=CARTESIAN_POINT('Ctrl Pts',(-1.12318939868838,2.02158548688735,
14.00709477137));
#278949=CARTESIAN_POINT('Ctrl Pts',(-2.30762771248847,0.152370097705391,
14.1182505571456));
#278950=CARTESIAN_POINT('Ctrl Pts',(-1.37924534148346,-1.85635249726869,
14.2294063429211));
#278951=CARTESIAN_POINT('Ctrl Pts',(0.811948214851289,-2.16543353685108,
14.3405621286967));
#278952=CARTESIAN_POINT('Ctrl Pts',(2.25973720291691,-0.491884213888585,
14.4517179144722));
#278953=CARTESIAN_POINT('Ctrl Pts',(1.63855315919402,1.63202507658885,14.5628737002478));
#278954=CARTESIAN_POINT('Ctrl Pts',(-0.482859447898242,2.2616827937832,
14.6740294860233));
#278955=CARTESIAN_POINT('Ctrl Pts',(-2.16217499407731,0.820586132655404,
14.7851852717988));
#278956=CARTESIAN_POINT('Ctrl Pts',(-1.86184363840467,-1.37182381239417,
14.8963410575744));
#278957=CARTESIAN_POINT('Ctrl Pts',(0.143156858570753,-2.30821758505642,
15.0074968433499));
#278958=CARTESIAN_POINT('Ctrl Pts',(2.0170856188344,-1.13125059664556,15.1186526291255));
#278959=CARTESIAN_POINT('Ctrl Pts',(2.04420859000465,1.08146823655202,15.229808414901));
#278960=CARTESIAN_POINT('Ctrl Pts',(0.199692488007044,2.30401502086096,
15.3409642006766));
#278961=CARTESIAN_POINT('Ctrl Pts',(-1.82765831344299,1.41704883311125,
15.4521199864521));
#278962=CARTESIAN_POINT('Ctrl Pts',(-2.18163941643627,-0.767340708403025,
15.5632757722277));
#278963=CARTESIAN_POINT('Ctrl Pts',(-0.538152357260458,-2.24916747853362,
15.6744315580032));
#278964=CARTESIAN_POINT('Ctrl Pts',(1.59805691435858,-1.67169865842755,
15.7855873437788));
#278965=CARTESIAN_POINT('Ctrl Pts',(2.27111522541637,0.436346122945927,
15.8967431295543));
#278966=CARTESIAN_POINT('Ctrl Pts',(0.86478300052194,2.14488057199392,16.0078989153299));
#278967=CARTESIAN_POINT('Ctrl Pts',(-1.33332833217902,1.88960256792799,
16.1190547011054));
#278968=CARTESIAN_POINT('Ctrl Pts',(-2.31066923273102,-0.0957601330721178,
16.230210486881));
#278969=CARTESIAN_POINT('Ctrl Pts',(-1.17240468950486,-1.99344665091902,
16.3413662726565));
#278970=CARTESIAN_POINT('Ctrl Pts',(1.03929161455433,-2.06597077569147,
16.4525220584321));
#278971=CARTESIAN_POINT('Ctrl Pts',(2.29943199451892,-0.246930777885519,
16.5636778442076));
#278972=CARTESIAN_POINT('Ctrl Pts',(1.45425553516014,1.79819441215764,16.6748336299832));
#278973=CARTESIAN_POINT('Ctrl Pts',(-0.722410036492459,2.19692649975759,
16.7859894157587));
#278974=CARTESIAN_POINT('Ctrl Pts',(-2.23765051893758,0.584193857826336,
16.8971452015343));
#278975=CARTESIAN_POINT('Ctrl Pts',(-1.70414012150793,-1.56341573085281,
17.0083009873098));
#278976=CARTESIAN_POINT('Ctrl Pts',(0.389649028978418,-2.27959117872528,
17.1194567730854));
#278977=CARTESIAN_POINT('Ctrl Pts',(2.12668283842677,-0.908615664043321,
17.2306125588609));
#278978=CARTESIAN_POINT('Ctrl Pts',(1.91656568480049,1.29427131871064,17.3417683446365));
#278979=CARTESIAN_POINT('Ctrl Pts',(-0.0483230640552768,2.31214774828866,
17.452924130412));
#278980=CARTESIAN_POINT('Ctrl Pts',(-1.96896817091355,1.21306501500312,
17.5640799161876));
#278981=CARTESIAN_POINT('Ctrl Pts',(-2.08686282744385,-0.99667727694527,
17.6752357019631));
#278982=CARTESIAN_POINT('Ctrl Pts',(-0.294065170700686,-2.29388059863771,
17.7863914877387));
#278983=CARTESIAN_POINT('Ctrl Pts',(1.76797338809603,-1.4908497113822,17.8975472735142));
#278984=CARTESIAN_POINT('Ctrl Pts',(2.21128799480902,0.677174994808322,
18.0087030592898));
#278985=CARTESIAN_POINT('Ctrl Pts',(0.629989998521478,2.22519141583385,
18.1198588450653));
#278986=CARTESIAN_POINT('Ctrl Pts',(-1.52811739626718,1.73586342652233,
18.2310146308409));
#278987=CARTESIAN_POINT('Ctrl Pts',(-2.2871046465437,-0.342786958716292,
18.3421704166164));
#278988=CARTESIAN_POINT('Ctrl Pts',(-0.95207030101812,-2.10759111981359,
18.453326202392));
#278989=CARTESIAN_POINT('Ctrl Pts',(1.25467804542587,-1.94271847031493,
18.5644819881675));
#278990=CARTESIAN_POINT('Ctrl Pts',(2.31263571838425,0.000859610951930963,
18.6756377739431));
#278991=CARTESIAN_POINT('Ctrl Pts',(1.25324639693522,1.94367193971766,18.7867935597186));
#278992=CARTESIAN_POINT('Ctrl Pts',(-0.953703958890417,2.10685415701179,
18.8979493454942));
#278993=CARTESIAN_POINT('Ctrl Pts',(-2.28724750397368,0.341117275939698,
19.0091051312697));
#278994=CARTESIAN_POINT('Ctrl Pts',(-1.52703607338255,-1.73708686266442,
19.1202609170453));
#278995=CARTESIAN_POINT('Ctrl Pts',(0.632073825457285,-2.22456767913867,
19.2314167028208));
#278996=CARTESIAN_POINT('Ctrl Pts',(2.21099471354783,-0.675807763197824,
19.3425724885964));
#278997=CARTESIAN_POINT('Ctrl Pts',(1.768405422311,1.49272605978228,19.4537282743719));
#278998=CARTESIAN_POINT('Ctrl Pts',(-0.299178855997274,2.29265270992973,
19.5648959413849));
#278999=CARTESIAN_POINT('Ctrl Pts',(-1.48653784212754,1.42898587064706,
19.639011679806));
#279000=CARTESIAN_POINT('Ctrl Pts',(-1.76641725875435,0.841316838976901,
19.6760754896353));
#279001=CARTESIAN_POINT('Ctrl Pts',(-0.905547729029968,-1.26791219016627,
3.38487918249974E-16));
#279002=CARTESIAN_POINT('Ctrl Pts',(-0.93771513294814,-1.25071447123035,
-1.97792095906261E-15));
#279003=CARTESIAN_POINT('Ctrl Pts',(-0.96917675062485,-1.23233980165227,
-2.13242252659455E-16));
#279004=CARTESIAN_POINT('Ctrl Pts',(-0.999860368201583,-1.21280268753011,
-9.61036805691151E-16));
#279005=CARTESIAN_POINT('Ctrl Pts',(-1.05019035785126,-1.1807561809833,
-2.25512455836343E-15));
#279006=CARTESIAN_POINT('Ctrl Pts',(-1.09842841594666,-1.1455850368464,
-2.75096923024122E-15));
#279007=CARTESIAN_POINT('Ctrl Pts',(-1.14449463040455,-1.10761563373825,
-2.31065167000111E-15));
#279008=CARTESIAN_POINT('Ctrl Pts',(-1.17053805883182,-1.08614971899119,
-2.06171914970765E-15));
#279009=CARTESIAN_POINT('Ctrl Pts',(-1.19588705872478,-1.063788463934,-8.1926151363717E-16));
#279010=CARTESIAN_POINT('Ctrl Pts',(-1.22052445577263,-1.0405840768243,
-2.02268757298896E-15));
#279011=CARTESIAN_POINT('Ctrl Pts',(-1.23356026960347,-1.0283064782682,
-2.5965085128221E-15));
#279012=CARTESIAN_POINT('Ctrl Pts',(-1.24640012070248,-1.01578919396326,
-1.89951844817313E-15));
#279013=CARTESIAN_POINT('Ctrl Pts',(-1.25902027597637,-1.00306131550636,
-1.97758476261356E-15));
#279014=CARTESIAN_POINT('Ctrl Pts',(-1.30242662502562,-0.959284458330949,
-1.88174753472955E-15));
#279015=CARTESIAN_POINT('Ctrl Pts',(-1.34328094576712,-0.912979946993025,
-1.27617630927406E-15));
#279016=CARTESIAN_POINT('Ctrl Pts',(-1.38149779807473,-0.864485899841547,
-1.29063426612674E-15));
#279017=CARTESIAN_POINT('Ctrl Pts',(-1.42075956301071,-0.81466594437451,
-1.30548752768883E-15));
#279018=CARTESIAN_POINT('Ctrl Pts',(-1.45723839042144,-0.762534493232605,
-3.150204436215E-15));
#279019=CARTESIAN_POINT('Ctrl Pts',(-1.49081464423019,-0.70841114099212,
-2.56739074444567E-15));
#279020=CARTESIAN_POINT('Ctrl Pts',(-1.49552688682915,-0.700815226108965,
-2.48559604747741E-15));
#279021=CARTESIAN_POINT('Ctrl Pts',(-1.50018190566982,-0.693180012726265,
-2.45505863419059E-15));
#279022=CARTESIAN_POINT('Ctrl Pts',(-1.50477931581713,-0.685506323835288,
-2.18575157973078E-15));
#279023=CARTESIAN_POINT('Ctrl Pts',(-1.51106438534805,-0.675015707011237,
-1.67622061700782E-15));
#279024=CARTESIAN_POINT('Ctrl Pts',(-1.5172370080675,-0.664461134174755,
-5.50282080994333E-16));
#279025=CARTESIAN_POINT('Ctrl Pts',(-1.5232955325984,-0.653847043301167,
-4.71844785465692E-16));
#279026=CARTESIAN_POINT('Ctrl Pts',(-1.55549299934074,-0.597439441721034,
2.74586708188979E-16));
#279027=CARTESIAN_POINT('Ctrl Pts',(-1.58448057296325,-0.539337269758026,
-2.67852813923984E-16));
#279028=CARTESIAN_POINT('Ctrl Pts',(-1.61016391944946,-0.47989642590738,
-1.16573417585641E-15));
#279029=CARTESIAN_POINT('Ctrl Pts',(-1.63628474196843,-0.419443099335088,
-2.07890955628107E-15));
#279030=CARTESIAN_POINT('Ctrl Pts',(-1.65898855606191,-0.357604293189553,
-7.61811381027507E-16));
#279031=CARTESIAN_POINT('Ctrl Pts',(-1.67814164180346,-0.294713444473936,
-7.63278329429795E-16));
#279032=CARTESIAN_POINT('Ctrl Pts',(-1.69045739883456,-0.254273568481462,
-7.64221601983552E-16));
#279033=CARTESIAN_POINT('Ctrl Pts',(-1.70130430670316,-0.213397904158502,
1.6222274639253E-16));
#279034=CARTESIAN_POINT('Ctrl Pts',(-1.71063726747206,-0.172168887794852,
-1.92901250528621E-15));
#279035=CARTESIAN_POINT('Ctrl Pts',(-1.71589881203146,-0.148925641400778,
-3.06462610868884E-15));
#279036=CARTESIAN_POINT('Ctrl Pts',(-1.7206790422679,-0.125570016898669,
-7.50804587875827E-17));
#279037=CARTESIAN_POINT('Ctrl Pts',(-1.72496866549233,-0.102116340889781,
-9.57567358739198E-16));
#279038=CARTESIAN_POINT('Ctrl Pts',(-1.72707108291268,-0.0906212947207782,
-1.44338884350977E-15));
#279039=CARTESIAN_POINT('Ctrl Pts',(-1.72905591297498,-0.0791009626866409,
-1.97430438624691E-15));
#279040=CARTESIAN_POINT('Ctrl Pts',(-1.73092110454086,-0.0675624532590521,
-1.83186799063151E-15));
#279041=CARTESIAN_POINT('Ctrl Pts',(-1.74174234252042,-0.000619754863062469,
-5.07256798513496E-16));
#279042=CARTESIAN_POINT('Ctrl Pts',(-1.74849833894868,0.0666674919201606,
7.85842007761142E-16));
#279043=CARTESIAN_POINT('Ctrl Pts',(-1.7510698873627,0.13394129902393,8.74300631892311E-16));
#279044=CARTESIAN_POINT('Ctrl Pts',(-1.75198203547585,0.157803838760529,
1.06041694804641E-15));
#279045=CARTESIAN_POINT('Ctrl Pts',(-1.75236732825439,0.181664982389618,
-3.03227639702671E-16));
#279046=CARTESIAN_POINT('Ctrl Pts',(-1.75221911350936,0.205509592721547,
-4.57966997657877E-16));
#279047=CARTESIAN_POINT('Ctrl Pts',(-1.75181220987844,0.270971760604655,
-1.03286705753963E-15));
#279048=CARTESIAN_POINT('Ctrl Pts',(-1.74738828583053,0.336308629139333,
1.51075324298343E-15));
#279049=CARTESIAN_POINT('Ctrl Pts',(-1.73917033238596,0.401277976570864,
8.32667268468867E-16));
#279050=CARTESIAN_POINT('Ctrl Pts',(-1.73175672467545,0.459888342072993,
2.20950075987451E-16));
#279051=CARTESIAN_POINT('Ctrl Pts',(-1.72125458542747,0.518200223470177,
4.69347102986873E-16));
#279052=CARTESIAN_POINT('Ctrl Pts',(-1.70779140168744,0.576038554497463,
-6.10622663543836E-16));
#279053=CARTESIAN_POINT('Ctrl Pts',(-1.70537963519586,0.586399591782088,
-6.30492532896913E-16));
#279054=CARTESIAN_POINT('Ctrl Pts',(-1.70287252597029,0.596746365633996,
1.79996086398271E-15));
#279055=CARTESIAN_POINT('Ctrl Pts',(-1.70027142920407,0.607074958677167,
1.9151347174784E-15));
#279056=CARTESIAN_POINT('Ctrl Pts',(-1.68381517035749,0.672420470942285,
1.83985930547722E-15));
#279057=CARTESIAN_POINT('Ctrl Pts',(-1.66367353779973,0.736753172822899,
2.48254355522872E-15));
#279058=CARTESIAN_POINT('Ctrl Pts',(-1.64010460098311,0.799821324003097,
2.83106871279415E-15));
#279059=CARTESIAN_POINT('Ctrl Pts',(-1.61575949880483,0.864966417166323,
3.19107139932377E-15));
#279060=CARTESIAN_POINT('Ctrl Pts',(-1.58775758055669,0.928763170627653,
7.18035494846759E-16));
#279061=CARTESIAN_POINT('Ctrl Pts',(-1.556326723057,0.990938813102449,1.0547118733939E-15));
#279062=CARTESIAN_POINT('Ctrl Pts',(-1.5248958655573,1.05311445557725,1.39138825194104E-15));
#279063=CARTESIAN_POINT('Ctrl Pts',(-1.49003568291284,1.11366995051747,
1.65653319858449E-15));
#279064=CARTESIAN_POINT('Ctrl Pts',(-1.45192228062725,1.17232315389904,
2.60902410786912E-15));
#279065=CARTESIAN_POINT('Ctrl Pts',(-1.43661514216392,1.19587950551396,
2.98313285321639E-15));
#279066=CARTESIAN_POINT('Ctrl Pts',(-1.42078271004317,1.21912883273614,
-3.24800180492398E-18));
#279067=CARTESIAN_POINT('Ctrl Pts',(-1.4044342596313,1.24205188600702,1.02695629777827E-15));
#279068=CARTESIAN_POINT('Ctrl Pts',(-1.39840915285019,1.2505000165776,1.16179888517215E-15));
#279069=CARTESIAN_POINT('Ctrl Pts',(-1.39231500560742,1.25890225569876,
-1.49405468388659E-17));
#279070=CARTESIAN_POINT('Ctrl Pts',(-1.38615790425663,1.26725033866967,
1.94289029309402E-16));
#279071=CARTESIAN_POINT('Ctrl Pts',(-1.34330654088438,1.32535020035255,
2.16119872575111E-15));
#279072=CARTESIAN_POINT('Ctrl Pts',(-1.29733814342063,1.38092917463918,
1.37308607647262E-15));
#279073=CARTESIAN_POINT('Ctrl Pts',(-1.2484938594593,1.43370660660493,2.05391259555654E-15));
#279074=CARTESIAN_POINT('Ctrl Pts',(-1.19953661080933,1.48660609965309,
3.06915354955197E-15));
#279075=CARTESIAN_POINT('Ctrl Pts',(-1.14768972594085,1.5366920862558,1.38515409442575E-15));
#279076=CARTESIAN_POINT('Ctrl Pts',(-1.09314642559825,1.58366574341901,
1.85962356624714E-15));
#279077=CARTESIAN_POINT('Ctrl Pts',(-1.03976854854967,1.62963571738155,
2.22260353012378E-15));
#279078=CARTESIAN_POINT('Ctrl Pts',(-0.983807683858392,1.67262579927252,
2.03200015230422E-15));
#279079=CARTESIAN_POINT('Ctrl Pts',(-0.925405164442978,1.71232676209298,
1.55431223447522E-15));
#279080=CARTESIAN_POINT('Ctrl Pts',(-0.904425650494227,1.72658825135077,
1.88961112987798E-15));
#279081=CARTESIAN_POINT('Ctrl Pts',(-0.883130725037691,1.74042497017167,
1.29805087082181E-15));
#279082=CARTESIAN_POINT('Ctrl Pts',(-0.861525859670521,1.75382131162754,
-2.22044604925031E-16));
#279083=CARTESIAN_POINT('Origin',(-0.866025403784439,-1.5,-4.));
#279084=CARTESIAN_POINT('',(-0.866025403784439,-1.5,-4.));
#279085=CARTESIAN_POINT('',(0.866025403784439,-1.5,-4.));
#279086=CARTESIAN_POINT('',(-0.43301270189222,-1.5,-4.));
#279087=CARTESIAN_POINT('',(-0.866025403784439,-1.5,-2.));
#279088=CARTESIAN_POINT('',(-0.866025403784439,-1.5,-4.));
#279089=CARTESIAN_POINT('',(0.866025403784439,-1.5,-2.));
#279090=CARTESIAN_POINT('',(-0.866025403784439,-1.5,-2.));
#279091=CARTESIAN_POINT('',(0.866025403784439,-1.5,-4.));
#279092=CARTESIAN_POINT('Origin',(-1.73205080756888,2.12115047744981E-16,
-4.));
#279093=CARTESIAN_POINT('',(-1.73205080756888,2.12115047744981E-16,-4.));
#279094=CARTESIAN_POINT('',(-1.51554445662277,-0.375,-4.));
#279095=CARTESIAN_POINT('',(-1.73205080756888,2.77555756156289E-16,-2.));
#279096=CARTESIAN_POINT('',(-1.73205080756888,2.12115047744981E-16,-4.));
#279097=CARTESIAN_POINT('',(-1.73205080756888,2.12115047744981E-16,-2.));
#279098=CARTESIAN_POINT('Origin',(-0.866025403784438,1.5,-4.));
#279099=CARTESIAN_POINT('',(-0.866025403784438,1.5,-4.));
#279100=CARTESIAN_POINT('',(-1.08253175473055,1.125,-4.));
#279101=CARTESIAN_POINT('',(-0.866025403784438,1.5,-2.));
#279102=CARTESIAN_POINT('',(-0.866025403784438,1.5,-4.));
#279103=CARTESIAN_POINT('',(-0.866025403784438,1.5,-2.));
#279104=CARTESIAN_POINT('Origin',(0.866025403784439,1.5,-4.));
#279105=CARTESIAN_POINT('',(0.866025403784439,1.5,-4.));
#279106=CARTESIAN_POINT('',(0.43301270189222,1.5,-4.));
#279107=CARTESIAN_POINT('',(0.866025403784439,1.5,-2.));
#279108=CARTESIAN_POINT('',(0.866025403784439,1.5,-4.));
#279109=CARTESIAN_POINT('',(0.866025403784439,1.5,-2.));
#279110=CARTESIAN_POINT('Origin',(1.73205080756888,0.,-4.));
#279111=CARTESIAN_POINT('',(1.73205080756888,0.,-4.));
#279112=CARTESIAN_POINT('',(1.51554445662277,0.375,-4.));
#279113=CARTESIAN_POINT('',(1.73205080756888,0.,-2.));
#279114=CARTESIAN_POINT('',(1.73205080756888,0.,-4.));
#279115=CARTESIAN_POINT('',(1.73205080756888,0.,-2.));
#279116=CARTESIAN_POINT('Origin',(0.866025403784439,-1.5,-4.));
#279117=CARTESIAN_POINT('',(1.08253175473055,-1.125,-4.));
#279118=CARTESIAN_POINT('',(0.866025403784439,-1.5,-2.));
#279119=CARTESIAN_POINT('Origin',(0.,2.77555756156289E-16,-2.));
#279120=CARTESIAN_POINT('Origin',(0.,0.,0.));
#279121=CARTESIAN_POINT('',(-3.5,-4.28626379701574E-16,0.));
#279122=CARTESIAN_POINT('Origin',(0.,0.,0.));
#279123=CARTESIAN_POINT('Origin',(0.,0.,-4.));
#279124=CARTESIAN_POINT('',(-3.5,-4.28626379701574E-16,-4.));
#279125=CARTESIAN_POINT('',(-3.5,-4.28626379701574E-16,-4.));
#279126=CARTESIAN_POINT('Origin',(0.,0.,-4.));
#279127=CARTESIAN_POINT('Origin',(0.,0.,-4.));
#279128=CARTESIAN_POINT('Origin',(0.,0.,20.));
#289366=UNCERTAINTY_MEASURE_WITH_UNIT(LENGTH_MEASURE(0.01),#289388,
'DISTANCE_ACCURACY_VALUE',
'Maximum model space distance between geometric entities at asserted c
onnectivities');
#289368=UNCERTAINTY_MEASURE_WITH_UNIT(LENGTH_MEASURE(0.01),#289388,
'DISTANCE_ACCURACY_VALUE',
'Maximum model space distance between geometric entities at asserted c
onnectivities');
#289385=(
GEOMETRIC_REPRESENTATION_CONTEXT(3)
GLOBAL_UNCERTAINTY_ASSIGNED_CONTEXT((#289366))
GLOBAL_UNIT_ASSIGNED_CONTEXT((#289388,#289390,#289391))
REPRESENTATION_CONTEXT('','3D')
);
#289387=(
GEOMETRIC_REPRESENTATION_CONTEXT(3)
GLOBAL_UNCERTAINTY_ASSIGNED_CONTEXT((#289368))
GLOBAL_UNIT_ASSIGNED_CONTEXT((#289388,#289390,#289391))
REPRESENTATION_CONTEXT('','3D')
);
#289388=(
LENGTH_UNIT()
NAMED_UNIT(*)
SI_UNIT(.MILLI.,.METRE.)
);
#289390=(
NAMED_UNIT(*)
PLANE_ANGLE_UNIT()
SI_UNIT($,.RADIAN.)
);
#289391=(
NAMED_UNIT(*)
SI_UNIT($,.STERADIAN.)
SOLID_ANGLE_UNIT()
);
#289408=SHAPE_DEFINITION_REPRESENTATION(#289426,#289469);
#289426=PRODUCT_DEFINITION_SHAPE('',$,#289488);
#289469=SHAPE_REPRESENTATION('',(#17788),#289385);
#289471=PRODUCT_DEFINITION_CONTEXT('part definition',#289527,'design');
#289488=PRODUCT_DEFINITION('Socket head cap screw M4x20',
'Socket head cap screw M4x20',#289506,#289471);
#289506=PRODUCT_DEFINITION_FORMATION('',$,#289545);
#289527=APPLICATION_CONTEXT(
'Core Data for Automotive Mechanical Design Process');
#289528=PRODUCT_CONTEXT('part definition',#289527,'mechanical');
#289545=PRODUCT('Socket head cap screw M4x20',
'Socket head cap screw M4x20',$,(#289528));
#289553=PRESENTATION_STYLE_ASSIGNMENT((#289560));
#289560=SURFACE_STYLE_USAGE(.BOTH.,#289567);
#289567=SURFACE_SIDE_STYLE('',(#289574));
#289574=SURFACE_STYLE_FILL_AREA(#289581);
#289581=FILL_AREA_STYLE('Opaque(64,72,82)',(#289588));
#289588=FILL_AREA_STYLE_COLOUR('Opaque(64,72,82)',#289595);
#289595=COLOUR_RGB('Opaque(64,72,82)',0.250980392156863,0.282352941176471,
0.32156862745098);
ENDSEC;
END-ISO-10303-21;
